ISO-10303-21;
HEADER;
FILE_DESCRIPTION (('STEP AP214'),
    '1' );
FILE_NAME ('Ruler Clamping Screw.step',
    '2026-10-24T22:54:28',
    ( '' ),
    ( '' ),
    'SwSTEP 2.0',
    'SolidWorks 2025',
    '' );
FILE_SCHEMA (( 'AUTOMOTIVE_DESIGN' ));
ENDSEC;

DATA;
#1=ORIENTED_EDGE ( 'NONE', *, *, #34988, .F. ) ;
#4=EDGE_LOOP ( 'NONE', ( #11290, #35593, #8233, #19286 ) ) ;
#10=( BOUNDED_CURVE ( )  B_SPLINE_CURVE ( 3, ( #30460, #11695, #20771, #8817 ),
 .UNSPECIFIED., .F., .T. ) 
 B_SPLINE_CURVE_WITH_KNOTS ( ( 4, 4 ),
 ( 1.347909859412855349, 1.534781240595300522 ),
 .UNSPECIFIED. ) 
 CURVE ( )  GEOMETRIC_REPRESENTATION_ITEM ( )  RATIONAL_B_SPLINE_CURVE ( ( 1.000000000000000000, 0.9970920404276226723, 0.9970920404276226723, 1.000000000000000000 ) ) 
 REPRESENTATION_ITEM ( '' )  );
#17=EDGE_CURVE ( 'NONE', #19674, #35253, #14622, .T. ) ;
#23=CARTESIAN_POINT ( 'NONE',  ( 3.455257086698204194, -26.54807830652391587, 7.773839561854632763 ) ) ;
#25=ORIENTED_EDGE ( 'NONE', *, *, #12233, .F. ) ;
#26=CARTESIAN_POINT ( 'NONE',  ( 1.060267149064800352, -26.12896262584469298, 7.720710062488891801 ) ) ;
#31=CARTESIAN_POINT ( 'NONE',  ( 0.5348300231373435132, -32.76390415370035214, 7.769368695748487319 ) ) ;
#36=CARTESIAN_POINT ( 'NONE',  ( 5.099449461929271621, -29.65043611971386639, 7.782034975670477195 ) ) ;
#39=CARTESIAN_POINT ( 'NONE',  ( -1.226608418644374421, -31.29986830985462376, 7.712764235869104645 ) ) ;
#40=EDGE_CURVE ( 'NONE', #7218, #20784, #16731, .T. ) ;
#47=ORIENTED_EDGE ( 'NONE', *, *, #36430, .F. ) ;
#53=CARTESIAN_POINT ( 'NONE',  ( 3.926249267005272436, -32.27095793936597090, 6.894806418505347700 ) ) ;
#59=CARTESIAN_POINT ( 'NONE',  ( 2.829405163535268386, -26.36285597610873310, 7.703977250142849620 ) ) ;
#67=ORIENTED_EDGE ( 'NONE', *, *, #17962, .F. ) ;
#68=VECTOR ( 'NONE', #23704, 1000.000000000000114 ) ;
#70=CARTESIAN_POINT ( 'NONE',  ( 1.700390093233090871, -29.56993018339339940, 7.800000000000000711 ) ) ;
#73=CARTESIAN_POINT ( 'NONE',  ( -1.583170569706177977, -30.78163712919650052, 7.638132480492516585 ) ) ;
#77=CARTESIAN_POINT ( 'NONE',  ( -1.419381273142192645, -31.15644416743037937, 6.921725064902950031 ) ) ;
#83=CARTESIAN_POINT ( 'NONE',  ( -0.6417018516168193631, -32.03460162637909292, 6.959317978105162616 ) ) ;
#85=PLANE ( 'NONE',  #11053 ) ;
#87=CARTESIAN_POINT ( 'NONE',  ( -0.8882241849766865371, -31.77426936318072848, 7.740055089680403455 ) ) ;
#88=CARTESIAN_POINT ( 'NONE',  ( 0.4809511200452799562, -32.83872382006634894, 7.781480525794716385 ) ) ;
#97=CARTESIAN_POINT ( 'NONE',  ( 2.985793545108982983, -26.31449737714283543, 6.863805608295730387 ) ) ;
#100=CARTESIAN_POINT ( 'NONE',  ( 5.698101969243359655, -32.85371976261941285, 7.695279973900954751 ) ) ;
#102=CARTESIAN_POINT ( 'NONE',  ( 1.179471205431445346, -26.21005746276246029, 7.784476445165072533 ) ) ;
#103=CARTESIAN_POINT ( 'NONE',  ( 5.054793046568992310, -30.12489038615697012, 7.703977250142847844 ) ) ;
#104=ORIENTED_EDGE ( 'NONE', *, *, #1781, .F. ) ;
#106=CARTESIAN_POINT ( 'NONE',  ( 1.651639975615219580, -32.96958066925694908, 6.894806418505345036 ) ) ;
#108=CARTESIAN_POINT ( 'NONE',  ( -1.333134932519906446, -31.10541900397473825, 7.013842709614101167 ) ) ;
#109=VERTEX_POINT ( 'NONE', #17965 ) ;
#113=B_SPLINE_CURVE_WITH_KNOTS ( 'NONE', 3,
 ( #29364, #35364, #7331, #3877, #28763, #574, #25671, #10213, #29561, #28964 ),
 .UNSPECIFIED., .F., .F.,
 ( 4, 3, 3, 4 ),
 ( 8.388765757908052086E-05, 0.0001053129305727058042, 0.0001360598016347105499, 0.0001612931755702039531 ),
 .UNSPECIFIED. ) ;
#119=CARTESIAN_POINT ( 'NONE',  ( 2.752162513012757827, -32.80316080117250266, 7.759451378593094084 ) ) ;
#124=ORIENTED_EDGE ( 'NONE', *, *, #26461, .T. ) ;
#126=CARTESIAN_POINT ( 'NONE',  ( -1.313163417236760111, -31.34995842213618999, 7.678495282201405203 ) ) ;
#133=CARTESIAN_POINT ( 'NONE',  ( -1.740904132959085304, -28.93157757802832819, 6.894806418505347700 ) ) ;
#136=DIRECTION ( 'NONE',  ( -1.000000000000000000, 0.000000000000000000, 0.000000000000000000 ) ) ;
#145=DIRECTION ( 'NONE',  ( 0.7055275666422168301, -0.2567910337120241637, -0.6605219282605403475 ) ) ;
#149=ORIENTED_EDGE ( 'NONE', *, *, #27849, .F. ) ;
#152=CARTESIAN_POINT ( 'NONE',  ( -1.531573891984414848, -33.61112889622174293, 7.754798119455333705 ) ) ;
#154=CARTESIAN_POINT ( 'NONE',  ( 3.979840844262043209, -26.93328804621895145, 7.785344483711591934 ) ) ;
#155=ORIENTED_EDGE ( 'NONE', *, *, #18670, .T. ) ;
#157=CARTESIAN_POINT ( 'NONE',  ( 4.045228995182856835, -26.97152095390259063, 7.750000000000000888 ) ) ;
#159=CARTESIAN_POINT ( 'NONE',  ( -1.333134932519906446, -31.10541900397473825, 7.013842709614101167 ) ) ;
#164=CARTESIAN_POINT ( 'NONE',  ( 5.401390093233090717, -29.58343279012807159, 7.635761828346577573 ) ) ;
#166=ORIENTED_EDGE ( 'NONE', *, *, #31920, .F. ) ;
#171=CARTESIAN_POINT ( 'NONE',  ( -1.621161547238496814, -30.32835594263312018, 7.139196562012270597 ) ) ;
#174=DIRECTION ( 'NONE',  ( 0.1736481776669273336, 0.9848077530122085754, -0.000000000000000000 ) ) ;
#177=CARTESIAN_POINT ( 'NONE',  ( -0.5626977249550375593, -26.90001753928526540, 7.750000000000002665 ) ) ;
#180=CARTESIAN_POINT ( 'NONE',  ( -2.184219888937934950, -32.98850935093154391, 7.754798119455333705 ) ) ;
#181=CARTESIAN_POINT ( 'NONE',  ( 4.091040325523227494, -27.01360636453728503, 6.980586498568968956 ) ) ;
#183=CARTESIAN_POINT ( 'NONE',  ( 4.697270888919727660, -27.96407818295915249, 7.768425012602590662 ) ) ;
#186=CARTESIAN_POINT ( 'NONE',  ( 4.308434419475116961, -31.75125399145456484, 7.763628509615286610 ) ) ;
#204=CARTESIAN_POINT ( 'NONE',  ( 4.710286264421988278, -27.98859379816425985, 6.865312560952602894 ) ) ;
#225=CARTESIAN_POINT ( 'NONE',  ( 0.9702812410957980527, -32.99293223504097483, 7.751599049952198506 ) ) ;
#226=CARTESIAN_POINT ( 'NONE',  ( 4.404516770028685357, -31.79202354683301834, 7.697032948437507294 ) ) ;
#235=DIRECTION ( 'NONE',  ( 1.000000000000000000, -1.982541115402065307E-15, 0.000000000000000000 ) ) ;
#238=CARTESIAN_POINT ( 'NONE',  ( -0.4939712552137372481, -26.86236983215355778, 7.785593909369612931 ) ) ;
#241=CARTESIAN_POINT ( 'NONE',  ( -0.9807834779648342272, -31.66069757387703731, 7.754798119455333705 ) ) ;
#242=CARTESIAN_POINT ( 'NONE',  ( 4.950332314942309964, -28.57099297037561314, 6.882085323592685988 ) ) ;
#243=CARTESIAN_POINT ( 'NONE',  ( -0.8662471634088840799, -27.19035536265291242, 7.009310105710486738 ) ) ;
#244=( BOUNDED_CURVE ( )  B_SPLINE_CURVE ( 3, ( #39857, #2200, #21130, #40056 ),
 .UNSPECIFIED., .F., .T. ) 
 B_SPLINE_CURVE_WITH_KNOTS ( ( 4, 4 ),
 ( 4.708531083176466403, 4.895802057644187855 ),
 .UNSPECIFIED. ) 
 CURVE ( )  GEOMETRIC_REPRESENTATION_ITEM ( )  RATIONAL_B_SPLINE_CURVE ( ( 1.000000000000000000, 0.9970795998553221295, 0.9970795998553221295, 1.000000000000000000 ) ) 
 REPRESENTATION_ITEM ( '' )  );
#252=CARTESIAN_POINT ( 'NONE',  ( 2.835692379953925535, -26.36507494999243306, 7.730758795053811028 ) ) ;
#260=ORIENTED_EDGE ( 'NONE', *, *, #6620, .T. ) ;
#266=CARTESIAN_POINT ( 'NONE',  ( 4.319862405889217882, -31.89123791683478970, 6.863805608295729499 ) ) ;
#270=DIRECTION ( 'NONE',  ( -0.000000000000000000, -0.000000000000000000, -1.000000000000000000 ) ) ;
#274=CARTESIAN_POINT ( 'NONE',  ( -0.6367654070295342139, -32.03928316901375695, 6.988553391373221402 ) ) ;
#279=DIRECTION ( 'NONE',  ( -0.3420201433256601642, -0.9396926207859115365, -0.000000000000000000 ) ) ;
#281=CARTESIAN_POINT ( 'NONE',  ( -0.6411629333918610341, -32.17099039281331585, 7.754798119455333705 ) ) ;
#282=CARTESIAN_POINT ( 'NONE',  ( 2.085863669803346365, -32.94801029878254184, 6.979335674598006634 ) ) ;
#283=CYLINDRICAL_SURFACE ( 'NONE', #22172, 0.09010775117052897965 ) ;
#284=ADVANCED_FACE ( 'NONE', ( #25588 ), #38132, .T. ) ;
#285=CARTESIAN_POINT ( 'NONE',  ( -1.450854365928797352, -28.29334945402236556, 7.754798119455333705 ) ) ;
#293=AXIS2_PLACEMENT_3D ( 'NONE', #5150, #36441, #8215 ) ;
#294=CARTESIAN_POINT ( 'NONE',  ( -0.9541984736338051665, -27.30603911067314726, 7.781480525794718162 ) ) ;
#298=ADVANCED_FACE ( 'NONE', ( #28261 ), #85, .F. ) ;
#299=CARTESIAN_POINT ( 'NONE',  ( 3.540652623597135840, -26.59276059082981547, 6.863784140767622333 ) ) ;
#300=CARTESIAN_POINT ( 'NONE',  ( -1.499157785959173594, -28.41975916621540321, 7.635761828346577573 ) ) ;
#302=EDGE_CURVE ( 'NONE', #31037, #37836, #19719, .T. ) ;
#304=CARTESIAN_POINT ( 'NONE',  ( 2.778259044425222868, -32.89982485500929954, 7.750000000000000888 ) ) ;
#309=VERTEX_POINT ( 'NONE', #39328 ) ;
#312=CARTESIAN_POINT ( 'NONE',  ( -1.482088180267139066, -30.76652202637871625, 7.693875151218754205 ) ) ;
#317=CARTESIAN_POINT ( 'NONE',  ( 4.666500650180242182, -31.42793668606411117, 7.750000000000000888 ) ) ;
#319=CARTESIAN_POINT ( 'NONE',  ( 5.100040579096636328, -29.61868030101130245, 6.894806418505348589 ) ) ;
#320=VERTEX_POINT ( 'NONE', #7642 ) ;
#326=CARTESIAN_POINT ( 'NONE',  ( 1.679836435472961131, -32.96988196360472756, 7.779495906702013741 ) ) ;
#329=CYLINDRICAL_SURFACE ( 'NONE', #3480, 2.500000000000000444 ) ;
#330=CARTESIAN_POINT ( 'NONE',  ( 3.410240285952196970, -32.62386096090719434, 6.880608371227951992 ) ) ;
#331=DIRECTION ( 'NONE',  ( -0.7660444431189813441, 0.6427876096865353661, -0.000000000000000000 ) ) ;
#332=CARTESIAN_POINT ( 'NONE',  ( 5.195448342531864050, -29.75585445294578690, 6.921725064902942925 ) ) ;
#336=EDGE_CURVE ( 'NONE', #19965, #16079, #3389, .T. ) ;
#345=EDGE_CURVE ( 'NONE', #17688, #33823, #20191, .T. ) ;
#346=CARTESIAN_POINT ( 'NONE',  ( 2.121967401070180337, -33.04444778638764291, 6.980586498568968068 ) ) ;
#347=VERTEX_POINT ( 'NONE', #17486 ) ;
#352=CARTESIAN_POINT ( 'NONE',  ( 0.02261628322158271143, -32.52713990352308571, 7.652160403243382980 ) ) ;
#353=ORIENTED_EDGE ( 'NONE', *, *, #28391, .T. ) ;
#357=VERTEX_POINT ( 'NONE', #8227 ) ;
#358=ORIENTED_EDGE ( 'NONE', *, *, #26602, .T. ) ;
#360=AXIS2_PLACEMENT_3D ( 'NONE', #5847, #22109, #33859 ) ;
#361=CARTESIAN_POINT ( 'NONE',  ( -1.698669275463088990, -29.48942424707293242, 7.782034975670477195 ) ) ;
#363=CARTESIAN_POINT ( 'NONE',  ( -1.688708477085993920, -29.88419193628291382, 7.576089344240128476 ) ) ;
#368=CARTESIAN_POINT ( 'NONE',  ( -0.5359795030213230227, -32.26226207767182785, 7.750000000000001776 ) ) ;
#369=CARTESIAN_POINT ( 'NONE',  ( 3.424610526961022305, -26.52410162464354215, 7.660770905198775793 ) ) ;
#373=DIRECTION ( 'NONE',  ( 0.3420201433256662704, 0.9396926207859093161, -0.000000000000000000 ) ) ;
#374=EDGE_LOOP ( 'NONE', ( #7724, #13238, #35896, #104 ) ) ;
#376=CARTESIAN_POINT ( 'NONE',  ( 4.296241352401964697, -27.37412594797728715, 7.635761828346577573 ) ) ;
#382=CARTESIAN_POINT ( 'NONE',  ( -0.01842261143103093163, -32.61881242066402820, 7.698786668945016842 ) ) ;
#383=ORIENTED_EDGE ( 'NONE', *, *, #7114, .F. ) ;
#384=CARTESIAN_POINT ( 'NONE',  ( 4.025803068412391106, -27.08951600530382464, 7.013842709614101167 ) ) ;
#389=CARTESIAN_POINT ( 'NONE',  ( 1.750706304578934613, -26.17028763529686941, 7.785868773668302545 ) ) ;
#400=CARTESIAN_POINT ( 'NONE',  ( 5.197301300333582397, -29.56993018336890700, 7.767301406056524193 ) ) ;
#401=CARTESIAN_POINT ( 'NONE',  ( 4.298799322723926508, -31.91476908534313850, 7.750000000000000888 ) ) ;
#415=CARTESIAN_POINT ( 'NONE',  ( 4.749297472835599443, -31.28869828601962766, 7.697032948437507294 ) ) ;
#416=CARTESIAN_POINT ( 'NONE',  ( 4.612110029931828059, -31.32547828874780649, 6.880147297696984410 ) ) ;
#418=CARTESIAN_POINT ( 'NONE',  ( 4.390205000165592786, -31.80932647847912875, 7.635761828346570468 ) ) ;
#419=CARTESIAN_POINT ( 'NONE',  ( 0.6185823884176052667, -26.24155567332487493, 7.754798119455333705 ) ) ;
#422=VERTEX_POINT ( 'NONE', #38922 ) ;
#424=EDGE_LOOP ( 'NONE', ( #10663, #22952, #33559, #23632 ) ) ;
#426=CARTESIAN_POINT ( 'NONE',  ( 3.444423122666314896, -26.53698764147170408, 7.762796336881262249 ) ) ;
#435=CARTESIAN_POINT ( 'NONE',  ( -1.345091088867315765, -27.84509849030786555, 7.730015791551950954 ) ) ;
#437=EDGE_LOOP ( 'NONE', ( #28811, #8609, #22831, #13291, #24960 ) ) ;
#453=CARTESIAN_POINT ( 'NONE',  ( 4.960875347057841722, -28.60596118244303199, 6.969307238440507035 ) ) ;
#455=ORIENTED_EDGE ( 'NONE', *, *, #8758, .F. ) ;
#461=CARTESIAN_POINT ( 'NONE',  ( -1.749742372765484610, -28.98121160874161006, 7.747520101777647383 ) ) ;
#463=VERTEX_POINT ( 'NONE', #26182 ) ;
#465=CARTESIAN_POINT ( 'NONE',  ( 2.480201502389029589, -26.15790714162507413, 7.006248344249653037 ) ) ;
#466=CARTESIAN_POINT ( 'NONE',  ( 1.123253381486050140, -26.11784194350818211, 6.894806418505347700 ) ) ;
#471=ORIENTED_EDGE ( 'NONE', *, *, #26054, .F. ) ;
#476=CARTESIAN_POINT ( 'NONE',  ( -0.1957518678886271957, -32.51180877674722325, 7.011627023500184741 ) ) ;
#481=CARTESIAN_POINT ( 'NONE',  ( -1.421733872515562824, -31.15181216911474493, 6.971170733404102648 ) ) ;
#483=CARTESIAN_POINT ( 'NONE',  ( 3.559755418260376114, -26.72339534466646427, 7.013842709614101167 ) ) ;
#486=VERTEX_POINT ( 'NONE', #10706 ) ;
#487=CARTESIAN_POINT ( 'NONE',  ( -0.6086181687031891885, -32.06563633890338139, 6.876076431790004939 ) ) ;
#491=CARTESIAN_POINT ( 'NONE',  ( 2.850561110411099275, -26.37038230420113649, 7.635761828346577573 ) ) ;
#493=DIRECTION ( 'NONE',  ( -0.000000000000000000, -0.000000000000000000, -1.000000000000000000 ) ) ;
#494=CARTESIAN_POINT ( 'NONE',  ( 1.123253381486050140, -26.11784194350818211, 6.894806418505347700 ) ) ;
#498=ORIENTED_EDGE ( 'NONE', *, *, #29293, .F. ) ;
#500=CARTESIAN_POINT ( 'NONE',  ( 3.037211893591657219, -26.44376520468768632, 7.013842709614101167 ) ) ;
#502=CARTESIAN_POINT ( 'NONE',  ( 2.926619159346142141, -26.29176571567377607, 6.894806418505347700 ) ) ;
#503=VECTOR ( 'NONE', #9003, 1000.000000000000000 ) ;
#505=CARTESIAN_POINT ( 'NONE',  ( -0.9006701161811203615, -27.22837715677322379, 7.754798119455333705 ) ) ;
#507=EDGE_CURVE ( 'NONE', #30375, #12399, #25450, .T. ) ;
#509=CARTESIAN_POINT ( 'NONE',  ( 3.531565352711682149, -26.58716268337259336, 6.863805608295729499 ) ) ;
#515=FACE_OUTER_BOUND ( 'NONE', #22231, .T. ) ;
#517=CARTESIAN_POINT ( 'NONE',  ( 1.105923466014343548, -33.01907637181788147, 7.635761828346575797 ) ) ;
#521=CARTESIAN_POINT ( 'NONE',  ( -1.668836025287037783, -30.02645519570809185, 6.865312560952603782 ) ) ;
#524=CARTESIAN_POINT ( 'NONE',  ( -1.629071066768614129, -30.64913839573838317, 7.751599049952198506 ) ) ;
#535=VECTOR ( 'NONE', #9009, 1000.000000000000114 ) ;
#536=CARTESIAN_POINT ( 'NONE',  ( -0.3903772972505400451, -26.88875661219547553, 7.754798119455333705 ) ) ;
#539=PLANE ( 'NONE',  #36059 ) ;
#542=CARTESIAN_POINT ( 'NONE',  ( 5.123097946374971734, -30.30141562551846235, 7.750000000000000888 ) ) ;
#545=VECTOR ( 'NONE', #23483, 1000.000000000000114 ) ;
#549=CARTESIAN_POINT ( 'NONE',  ( 3.364053381479577443, -33.98248085747043490, 7.695279973900954751 ) ) ;
#552=CARTESIAN_POINT ( 'NONE',  ( 2.274693159464038050, -26.11736939636621813, 7.714178352335855138 ) ) ;
#560=CARTESIAN_POINT ( 'NONE',  ( 1.187115290808829382, -26.11501310037670009, 7.776484688137383472 ) ) ;
#566=CARTESIAN_POINT ( 'NONE',  ( -0.9271279775035500270, -27.41211907304282036, 7.695279973900954751 ) ) ;
#568=ORIENTED_EDGE ( 'NONE', *, *, #13622, .T. ) ;
#569=ORIENTED_EDGE ( 'NONE', *, *, #7114, .T. ) ;
#573=CARTESIAN_POINT ( 'NONE',  ( 1.043287501142265317, -33.00769343636290643, 6.878641987404677138 ) ) ;
#574=CARTESIAN_POINT ( 'NONE',  ( -1.791168270219405168, -29.47546713279042052, 7.776484688137385248 ) ) ;
#577=ORIENTED_EDGE ( 'NONE', *, *, #16277, .T. ) ;
#579=VERTEX_POINT ( 'NONE', #22497 ) ;
#580=CARTESIAN_POINT ( 'NONE',  ( 2.910139986571841586, -32.85421171754464353, 7.635761828346577573 ) ) ;
#581=CARTESIAN_POINT ( 'NONE',  ( -0.5918003806487183160, -32.19643581148406497, 7.784725160561907664 ) ) ;
#583=DIRECTION ( 'NONE',  ( -0.7541618601367610086, 0.000000000000000000, -0.6566885781822769941 ) ) ;
#587=CARTESIAN_POINT ( 'NONE',  ( -0.5766758124320290335, -26.91192889271322031, 7.700536657684223130 ) ) ;
#588=CARTESIAN_POINT ( 'NONE',  ( 2.931185808669444448, -32.84638282411071941, 7.695279973900954751 ) ) ;
#589=CARTESIAN_POINT ( 'NONE',  ( 4.585610243088643401, -31.36868105187616607, 7.761597726988854085 ) ) ;
#591=EDGE_CURVE ( 'NONE', #40022, #24258, #30271, .T. ) ;
#593=CARTESIAN_POINT ( 'NONE',  ( -0.3224798742589583544, -26.83716377573245637, 6.979335674598003969 ) ) ;
#598=B_SPLINE_CURVE_WITH_KNOTS ( 'NONE', 3,
 ( #2240, #37206, #5108, #40291 ),
 .UNSPECIFIED., .F., .F.,
 ( 4, 4 ),
 ( 0.000000000000000000, 6.391136169993505180E-06 ),
 .UNSPECIFIED. ) ;
#604=CARTESIAN_POINT ( 'NONE',  ( -1.625093378867604521, -28.86200076037926721, 7.757178535559534183 ) ) ;
#612=B_SPLINE_CURVE_WITH_KNOTS ( 'NONE', 3,
 ( #9768, #21164, #13060, #34714, #9561, #5509, #17845, #2236, #31810, #18829, #11664, #30427, #25622, #3019, #6493, #15941, #14757, #38165, #28506 ),
 .UNSPECIFIED., .F., .F.,
 ( 4, 3, 3, 3, 3, 3, 4 ),
 ( 0.000000000000000000, 2.546128104244683795E-05, 5.711050680483705015E-05, 8.113074941675759084E-05, 0.0001053129305727034461, 0.0001360598016347089778, 0.0001612931755702011070 ),
 .UNSPECIFIED. ) ;
#614=VERTEX_POINT ( 'NONE', #36444 ) ;
#616=CARTESIAN_POINT ( 'NONE',  ( 4.734418770087374106, -28.03542604781803504, 6.895222827070020877 ) ) ;
#626=VECTOR ( 'NONE', #14878, 1000.000000000000114 ) ;
#631=CARTESIAN_POINT ( 'NONE',  ( 2.338742698598151204, -26.12863595720122234, 6.894806418505347700 ) ) ;
#634=ORIENTED_EDGE ( 'NONE', *, *, #35348, .T. ) ;
#635=EDGE_CURVE ( 'NONE', #4065, #23718, #31879, .T. ) ;
#636=CARTESIAN_POINT ( 'NONE',  ( 0.5000100785294406824, -32.75099641114868376, 7.784838882742140420 ) ) ;
#637=VERTEX_POINT ( 'NONE', #15225 ) ;
#640=CYLINDRICAL_SURFACE ( 'NONE', #18375, 0.09010775117052950700 ) ;
#645=CARTESIAN_POINT ( 'NONE',  ( -0.7996099067669091287, -29.56993018339339940, -8.199999999999999289 ) ) ;
#648=CARTESIAN_POINT ( 'NONE',  ( -1.263904303455110734, -31.23517888999192138, 7.784838882742139532 ) ) ;
#651=VERTEX_POINT ( 'NONE', #34201 ) ;
#655=AXIS2_PLACEMENT_3D ( 'NONE', #39482, #36815, #24042 ) ;
#657=CARTESIAN_POINT ( 'NONE',  ( 3.012471863950764828, -26.32525666483178384, 7.753200566781599079 ) ) ;
#658=CARTESIAN_POINT ( 'NONE',  ( 2.277726599503935745, -26.11787535206076427, 7.665454363767879364 ) ) ;
#660=LINE ( 'NONE', #26374, #16175 ) ;
#664=VECTOR ( 'NONE', #23686, 999.9999999999998863 ) ;
#666=ORIENTED_EDGE ( 'NONE', *, *, #24110, .T. ) ;
#669=CARTESIAN_POINT ( 'NONE',  ( 4.435798653882254250, -27.39796262386320080, 7.776484688137385248 ) ) ;
#673=CARTESIAN_POINT ( 'NONE',  ( 4.431287826448039979, -27.54454009300915018, 6.920489980334473934 ) ) ;
#674=CARTESIAN_POINT ( 'NONE',  ( 1.751749777469023384, -26.08494242606548141, 7.785344483711591934 ) ) ;
#677=CARTESIAN_POINT ( 'NONE',  ( -0.9615818451583477700, -31.84235468436096639, 7.660770905198781122 ) ) ;
#680=CARTESIAN_POINT ( 'NONE',  ( 2.278142440318064565, -26.21937241936939245, 7.756377446753164762 ) ) ;
#681=CARTESIAN_POINT ( 'NONE',  ( -1.149815663681586608, -27.52689394563671854, 7.501983001166817822 ) ) ;
#685=CARTESIAN_POINT ( 'NONE',  ( 0.5325725529551263993, -26.27050565893173228, 6.894806418505347700 ) ) ;
#686=CARTESIAN_POINT ( 'NONE',  ( -0.5871382310426926932, -32.08534543543891004, 6.865312560952603782 ) ) ;
#688=ADVANCED_FACE ( 'NONE', ( #37252 ), #40049, .T. ) ;
#690=DIRECTION ( 'NONE',  ( -0.8660254037844344888, -0.5000000000000069944, -0.000000000000000000 ) ) ;
#691=CARTESIAN_POINT ( 'NONE',  ( 4.360293939584222400, -27.29508367342402408, 7.720710062488894465 ) ) ;
#693=CARTESIAN_POINT ( 'NONE',  ( 2.086269118658516497, -32.94796176668813104, 6.929923840112066635 ) ) ;
#694=B_SPLINE_CURVE_WITH_KNOTS ( 'NONE', 3,
 ( #33425, #8670, #33002, #32808, #27015, #17125, #17517, #39773, #29697, #14043 ),
 .UNSPECIFIED., .F., .F.,
 ( 4, 3, 3, 4 ),
 ( 0.0001477827378591783816, 0.0001512763324577387676, 0.0001815301820994196414, 0.0002056071264154448830 ),
 .UNSPECIFIED. ) ;
#695=DIRECTION ( 'NONE',  ( -0.9848077530122067991, -0.1736481776669374644, -0.000000000000000000 ) ) ;
#702=ORIENTED_EDGE ( 'NONE', *, *, #27883, .T. ) ;
#703=CARTESIAN_POINT ( 'NONE',  ( -0.9362520439413681839, -27.29047943236446372, 7.785344483711591934 ) ) ;
#704=DIRECTION ( 'NONE',  ( -0.6427876096865430267, 0.7660444431189749048, -0.000000000000000000 ) ) ;
#708=CARTESIAN_POINT ( 'NONE',  ( -1.771784689607549979, -30.01038707958819174, 7.013842709614101167 ) ) ;
#712=CARTESIAN_POINT ( 'NONE',  ( 0.4869470754961160996, -26.28701135364670805, 7.750000000000001776 ) ) ;
#716=CARTESIAN_POINT ( 'NONE',  ( -1.708141087249497758, -28.77499324473749809, 6.936703618422972006 ) ) ;
#723=CARTESIAN_POINT ( 'NONE',  ( 1.700390093233090871, -29.56993018339339940, 7.750000000000000888 ) ) ;
#726=CARTESIAN_POINT ( 'NONE',  ( 4.668540769505296950, -31.42424039273510061, 7.754798119455333705 ) ) ;
#727=B_SPLINE_CURVE_WITH_KNOTS ( 'NONE', 3,
 ( #13029, #25593, #38137, #22519, #282, #22110, #34687, #2990, #28884, #693, #38330, #6050, #15509, #6252, #28066, #12421, #18799, #3197, #6462, #19014, #31575, #38534, #7052, #26000, #32193, #10340, #29287, #13636, #29493, #1696, #16912 ),
 .UNSPECIFIED., .F., .F.,
 ( 4, 3, 3, 3, 3, 3, 3, 3, 3, 3, 4 ),
 ( 0.000000000000000000, 2.999644130997628625E-05, 6.002588995694725670E-05, 8.960886084587959242E-05, 0.0001190604700446492963, 0.0001489538463052720186, 0.0001796139255493969062, 0.0002109707048517083796, 0.0002426195318110367931, 0.0002740640997890067261, 0.0002849778069099888106 ),
 .UNSPECIFIED. ) ;
#728=LINE ( 'NONE', #13680, #33363 ) ;
#733=CARTESIAN_POINT ( 'NONE',  ( 3.376940742481379321, -32.64225469758540044, 6.865554069792297653 ) ) ;
#735=DIRECTION ( 'NONE',  ( 0.1736481776669273613, 0.9848077530122086864, -0.000000000000000000 ) ) ;
#751=CARTESIAN_POINT ( 'NONE',  ( 2.117690421663379841, -33.04496407602081121, 6.961115707816238007 ) ) ;
#757=DIRECTION ( 'NONE',  ( 0.8660254037844450359, -0.4999999999999888978, -0.000000000000000000 ) ) ;
#760=ORIENTED_EDGE ( 'NONE', *, *, #18864, .T. ) ;
#762=CARTESIAN_POINT ( 'NONE',  ( -1.723126226492296853, -28.85479948634039360, 7.766640943994350010 ) ) ;
#767=CARTESIAN_POINT ( 'NONE',  ( 1.531218635892081847, -33.06583936671340496, 7.013842709614101167 ) ) ;
#768=CARTESIAN_POINT ( 'NONE',  ( 0.9171018672454774867, -32.98115864172326184, 6.906857269533146493 ) ) ;
#769=CARTESIAN_POINT ( 'NONE',  ( 3.015109609237833332, -26.32624206733842698, 7.750000000000000888 ) ) ;
#772=EDGE_LOOP ( 'NONE', ( #34997, #39847, #32312, #40232, #11861 ) ) ;
#773=CARTESIAN_POINT ( 'NONE',  ( 5.200265217546576224, -29.54023460135108436, 7.660770905198780234 ) ) ;
#774=VERTEX_POINT ( 'NONE', #22842 ) ;
#775=CARTESIAN_POINT ( 'NONE',  ( -0.9509358128338576410, -31.69844278021870210, 6.874555630061443878 ) ) ;
#776=LINE ( 'NONE', #7142, #14906 ) ;
#781=DIRECTION ( 'NONE',  ( 0.4999999999999979461, 0.8660254037844397068, -0.000000000000000000 ) ) ;
#785=CARTESIAN_POINT ( 'NONE',  ( -1.272073826050460932, -27.72701560212543725, 7.766640943994650215 ) ) ;
#789=CARTESIAN_POINT ( 'NONE',  ( -0.3256050783848223329, -26.83948268077026711, 6.988553391373221402 ) ) ;
#791=CARTESIAN_POINT ( 'NONE',  ( 0.6185823884176052667, -26.24155567332487493, 7.754798119455333705 ) ) ;
#798=CARTESIAN_POINT ( 'NONE',  ( 4.821723147117300989, -30.91800106084867394, 6.997764925645181044 ) ) ;
#799=B_SPLINE_CURVE_WITH_KNOTS ( 'NONE', 3,
 ( #35004, #6778, #10055, #6976, #15414, #27973, #40522, #31289, #24905, #37438 ),
 .UNSPECIFIED., .F., .F.,
 ( 4, 3, 3, 4 ),
 ( 8.940560153363745023E-19, 3.025570593003111997E-05, 6.051145698344058784E-05, 6.468151674593778733E-05 ),
 .UNSPECIFIED. ) ;
#803=ORIENTED_EDGE ( 'NONE', *, *, #28324, .T. ) ;
#807=ORIENTED_EDGE ( 'NONE', *, *, #15906, .F. ) ;
#811=EDGE_CURVE ( 'NONE', #38080, #11405, #6983, .T. ) ;
#814=ORIENTED_EDGE ( 'NONE', *, *, #31306, .F. ) ;
#815=ORIENTED_EDGE ( 'NONE', *, *, #10557, .T. ) ;
#816=EDGE_CURVE ( 'NONE', #10909, #29634, #27831, .T. ) ;
#818=CARTESIAN_POINT ( 'NONE',  ( 0.03162470699431383508, -32.53223031769636009, 7.703977250142849620 ) ) ;
#819=CARTESIAN_POINT ( 'NONE',  ( 4.580489648044480333, -31.37689880320810332, 6.863904403958575706 ) ) ;
#820=CARTESIAN_POINT ( 'NONE',  ( 3.962066057316325551, -32.24103972498801340, 7.638132480492515697 ) ) ;
#830=CARTESIAN_POINT ( 'NONE',  ( 0.4404571835168948346, -32.72788522653752352, 6.864651958020304257 ) ) ;
#834=CARTESIAN_POINT ( 'NONE',  ( 0.5495968526122669839, -32.76925980410539552, 7.756377446753163873 ) ) ;
#835=EDGE_LOOP ( 'NONE', ( #34028, #35440, #19587, #33373, #11686 ) ) ;
#838=CARTESIAN_POINT ( 'NONE',  ( 5.072211240599806104, -29.13298902044168415, 6.871394612369934762 ) ) ;
#842=CARTESIAN_POINT ( 'NONE',  ( 4.402564028851855937, -31.79440116261879368, 7.720710062488891801 ) ) ;
#843=ORIENTED_EDGE ( 'NONE', *, *, #8264, .F. ) ;
#862=CARTESIAN_POINT ( 'NONE',  ( 3.884973724021333119, -32.30444921973087702, 6.865554069792297653 ) ) ;
#867=CARTESIAN_POINT ( 'NONE',  ( 4.459949229015542471, -27.41706340682027232, 7.751599049952173637 ) ) ;
#871=CARTESIAN_POINT ( 'NONE',  ( 4.398191130436243768, -27.36279617112402462, 7.785096263473211486 ) ) ;
#872=DIRECTION ( 'NONE',  ( 0.000000000000000000, 0.7126435865141270698, -0.7015262779114420644 ) ) ;
#880=CARTESIAN_POINT ( 'NONE',  ( -0.1940712780794633940, -32.51289061680132875, 7.013842709614101167 ) ) ;
#881=B_SPLINE_CURVE_WITH_KNOTS ( 'NONE', 3,
 ( #6575, #34996, #12940, #40517, #31896, #12730, #25309, #34187, #9231, #37841, #3102, #21809, #9644, #28803, #22229, #38052, #9852, #28594, #34389, #6773, #37631, #3308, #5092, #604, #13146 ),
 .UNSPECIFIED., .F., .F.,
 ( 4, 3, 3, 3, 3, 3, 3, 3, 4 ),
 ( 6.468151674593807193E-05, 9.076621574721745937E-05, 0.0001210204262067965164, 0.0001512763324577425352, 0.0001815301820994146811, 0.0002117781465860671007, 0.0002420274594459666966, 0.0002722905548971137285, 0.0002816827545175591132 ),
 .UNSPECIFIED. ) ;
#883=CARTESIAN_POINT ( 'NONE',  ( 2.396593935003837661, -26.24196453429818732, 7.768425012602593327 ) ) ;
#885=DIRECTION ( 'NONE',  ( -1.000000000000000000, 0.000000000000000000, 0.000000000000000000 ) ) ;
#886=CARTESIAN_POINT ( 'NONE',  ( -0.5483518474143298516, -32.12005952999000868, 6.870716933885664623 ) ) ;
#888=CARTESIAN_POINT ( 'NONE',  ( 1.122637746148142490, -32.92048794741741347, 7.756377446753163873 ) ) ;
#889=PLANE ( 'NONE',  #1673 ) ;
#892=CARTESIAN_POINT ( 'NONE',  ( -1.466146261265031558, -28.33173257664969213, 7.782034975670477195 ) ) ;
#894=ORIENTED_EDGE ( 'NONE', *, *, #2902, .T. ) ;
#904=CARTESIAN_POINT ( 'NONE',  ( 5.049772904672250817, -28.55423167660719841, 6.971170733404099984 ) ) ;
#905=CARTESIAN_POINT ( 'NONE',  ( 1.120974760640235823, -26.21965457890690132, 7.775108481317163367 ) ) ;
#906=CARTESIAN_POINT ( 'NONE',  ( 1.226940962756493336, -26.10208781839716252, 6.870724624169668004 ) ) ;
#908=VERTEX_POINT ( 'NONE', #17636 ) ;
#914=VECTOR ( 'NONE', #6048, 1000.000000000000000 ) ;
#924=ORIENTED_EDGE ( 'NONE', *, *, #32559, .T. ) ;
#933=CARTESIAN_POINT ( 'NONE',  ( -0.1271964900342822669, -32.54647689963780977, 7.776484688137386136 ) ) ;
#934=DIRECTION ( 'NONE',  ( -0.000000000000000000, -0.000000000000000000, -1.000000000000000000 ) ) ;
#939=CARTESIAN_POINT ( 'NONE',  ( 5.119051991949654656, -30.32009737959945284, 6.875780273367530171 ) ) ;
#944=LINE ( 'NONE', #37986, #7913 ) ;
#952=VECTOR ( 'NONE', #26317, 999.9999999999998863 ) ;
#953=CYLINDRICAL_SURFACE ( 'NONE', #22759, 0.09010775117052971517 ) ;
#960=CARTESIAN_POINT ( 'NONE',  ( -2.628911188892000261, -29.52345495559962885, 6.954324564059724878 ) ) ;
#961=CARTESIAN_POINT ( 'NONE',  ( 1.086859017207900235, -26.12551858065138077, 7.762796336881262249 ) ) ;
#963=CARTESIAN_POINT ( 'NONE',  ( -1.748913751257205051, -28.97637829014552580, 7.636816916992232862 ) ) ;
#969=CARTESIAN_POINT ( 'NONE',  ( -1.268168650321787716, -31.22753658603060956, 6.894806418505346812 ) ) ;
#973=CARTESIAN_POINT ( 'NONE',  ( 1.005809635450030548, -33.00033240446269645, 6.864368109219936009 ) ) ;
#974=CARTESIAN_POINT ( 'NONE',  ( 3.235878913814441038, -32.60345520914638939, 7.013842709614101167 ) ) ;
#976=CARTESIAN_POINT ( 'NONE',  ( 3.501122161660540577, -26.68594518542784044, 7.759451378593094084 ) ) ;
#979=CARTESIAN_POINT ( 'NONE',  ( 5.172564876073734830, -29.12947328719863194, 7.013842709614101167 ) ) ;
#981=VECTOR ( 'NONE', #27050, 1000.000000000000114 ) ;
#982=CARTESIAN_POINT ( 'NONE',  ( -1.034439892636894731, -31.59000574243066950, 6.949473656533220023 ) ) ;
#983=CARTESIAN_POINT ( 'NONE',  ( -0.5790606577958476997, -32.20657232056785091, 7.785344483711592822 ) ) ;
#985=DIRECTION ( 'NONE',  ( 1.000000000000000000, 6.938893903907229167E-15, 0.000000000000000000 ) ) ;
#989=CARTESIAN_POINT ( 'NONE',  ( -0.5767923600352571345, -26.91202874155497682, 7.697032948437509958 ) ) ;
#990=CARTESIAN_POINT ( 'NONE',  ( 2.931185808669443116, -32.84638282411072652, 7.697032948437507294 ) ) ;
#991=CARTESIAN_POINT ( 'NONE',  ( -1.643416196941662077, -30.18553864676747622, 7.652160403243382980 ) ) ;
#995=CARTESIAN_POINT ( 'NONE',  ( 4.912218266805315814, -28.45446572434498478, 7.785868773668302545 ) ) ;
#997=ORIENTED_EDGE ( 'NONE', *, *, #14340, .F. ) ;
#1006=CARTESIAN_POINT ( 'NONE',  ( 4.817698917275965442, -30.92727803983277113, 6.939395833800437785 ) ) ;
#1007=VECTOR ( 'NONE', #40210, 1000.000000000000000 ) ;
#1008=CARTESIAN_POINT ( 'NONE',  ( -1.276779499330499945, -27.72966765302937020, 6.863784140767622333 ) ) ;
#1015=VERTEX_POINT ( 'NONE', #14154 ) ;
#1022=CARTESIAN_POINT ( 'NONE',  ( 5.026281758278582146, -30.27593629695115496, 6.864216812889196717 ) ) ;
#1023=CARTESIAN_POINT ( 'NONE',  ( 4.550261139223147566, -31.42419555005044529, 6.887945620086119547 ) ) ;
#1025=CARTESIAN_POINT ( 'NONE',  ( -1.256369394170508080, -27.89135685030788281, 7.740055089680399014 ) ) ;
#1030=CARTESIAN_POINT ( 'NONE',  ( 2.340513037401407814, -33.01089774094209872, 7.720710062488891801 ) ) ;
#1031=ORIENTED_EDGE ( 'NONE', *, *, #32756, .T. ) ;
#1032=EDGE_CURVE ( 'NONE', #11431, #579, #22616, .T. ) ;
#1036=B_SPLINE_CURVE_WITH_KNOTS ( 'NONE', 3,
 ( #712, #38554, #16533, #12844, #26023, #25214, #25413, #37743, #22941, #22131 ),
 .UNSPECIFIED., .F., .F.,
 ( 4, 3, 3, 4 ),
 ( 0.0001585009270395677274, 0.0001815657551981830287, 0.0002118214035944111502, 0.0002170292169044726665 ),
 .UNSPECIFIED. ) ;
#1038=CARTESIAN_POINT ( 'NONE',  ( 4.043087352902885456, -26.96969281642315863, 7.753200566781576875 ) ) ;
#1041=ORIENTED_EDGE ( 'NONE', *, *, #23793, .F. ) ;
#1048=ADVANCED_FACE ( 'NONE', ( #36597 ), #30425, .F. ) ;
#1050=CARTESIAN_POINT ( 'NONE',  ( 4.395707693226862389, -31.80270533321202819, 7.743886751744248897 ) ) ;
#1051=B_SPLINE_CURVE_WITH_KNOTS ( 'NONE', 3,
 ( #27385, #22205, #6549, #12707, #11927, #24087, #39946, #8228, #25281, #11722 ),
 .UNSPECIFIED., .F., .F.,
 ( 4, 3, 3, 4 ),
 ( 1.748223473168675632E-18, 3.025570593002983587E-05, 6.051145698343930035E-05, 6.468151674593807193E-05 ),
 .UNSPECIFIED. ) ;
#1055=ORIENTED_EDGE ( 'NONE', *, *, #816, .T. ) ;
#1058=CARTESIAN_POINT ( 'NONE',  ( 1.706484455665669753, -33.06855198763274473, 7.762796336881262249 ) ) ;
#1059=ORIENTED_EDGE ( 'NONE', *, *, #32997, .F. ) ;
#1060=CARTESIAN_POINT ( 'NONE',  ( 2.185047844817765483, -33.03621188651298723, 7.751599049952199394 ) ) ;
#1063=ORIENTED_EDGE ( 'NONE', *, *, #31441, .T. ) ;
#1068=ORIENTED_EDGE ( 'NONE', *, *, #28555, .F. ) ;
#1072=VECTOR ( 'NONE', #38963, 1000.000000000000000 ) ;
#1075=ORIENTED_EDGE ( 'NONE', *, *, #31430, .F. ) ;
#1077=CARTESIAN_POINT ( 'NONE',  ( 2.463123297529182132, -26.15404171320399485, 6.883550009118462931 ) ) ;
#1079=DIRECTION ( 'NONE',  ( -1.000000000000000000, -0.000000000000000000, -0.000000000000000000 ) ) ;
#1081=ORIENTED_EDGE ( 'NONE', *, *, #31234, .T. ) ;
#1083=EDGE_CURVE ( 'NONE', #19523, #19287, #35465, .T. ) ;
#1084=CARTESIAN_POINT ( 'NONE',  ( 4.315404545797473013, -33.85565925846036350, 7.754798119455333705 ) ) ;
#1085=CARTESIAN_POINT ( 'NONE',  ( 1.217126534916886937, -26.10345411493373291, 7.750000000000000888 ) ) ;
#1088=CARTESIAN_POINT ( 'NONE',  ( -0.9694501004374326270, -31.83310420932945206, 7.640616322432100205 ) ) ;
#1094=CARTESIAN_POINT ( 'NONE',  ( -0.5792506522025446802, -32.09249774648650089, 6.863904403958575706 ) ) ;
#1098=CARTESIAN_POINT ( 'NONE',  ( 1.012709997867073053, -32.89967220964104655, 7.774064877406528851 ) ) ;
#1099=CARTESIAN_POINT ( 'NONE',  ( 4.979285396424428356, -28.34565668833202778, 7.730015791551950954 ) ) ;
#1100=( BOUNDED_CURVE ( )  B_SPLINE_CURVE ( 3, ( #29336, #4230, #16755, #22564 ),
 .UNSPECIFIED., .F., .T. ) 
 B_SPLINE_CURVE_WITH_KNOTS ( ( 4, 4 ),
 ( 1.381924640371168467, 1.574767692156076482 ),
 .UNSPECIFIED. ) 
 CURVE ( )  GEOMETRIC_REPRESENTATION_ITEM ( )  RATIONAL_B_SPLINE_CURVE ( ( 1.000000000000000000, 0.9969033633783032089, 0.9969033633783032089, 1.000000000000000000 ) ) 
 REPRESENTATION_ITEM ( '' )  );
#1101=CARTESIAN_POINT ( 'NONE',  ( 3.295664264696410495, -32.57244657952615086, 7.757178535559533294 ) ) ;
#1102=CARTESIAN_POINT ( 'NONE',  ( -1.585292354492739975, -28.37344205933749208, 7.767720160662274331 ) ) ;
#1113=CARTESIAN_POINT ( 'NONE',  ( 3.075873696215302378, -26.35153850715824575, 6.941203072598471913 ) ) ;
#1118=CARTESIAN_POINT ( 'NONE',  ( 0.9577497276855772013, -32.88784831336140968, 6.871394612369935651 ) ) ;
#1121=CARTESIAN_POINT ( 'NONE',  ( 0.4628871221125078761, -32.84386297521798070, 6.883108633650832253 ) ) ;
#1123=VERTEX_POINT ( 'NONE', #40087 ) ;
#1128=VERTEX_POINT ( 'NONE', #31251 ) ;
#1131=CARTESIAN_POINT ( 'NONE',  ( -1.709556888978058131, -28.78108823880591416, 6.917411966759697606 ) ) ;
#1136=ADVANCED_FACE ( 'NONE', ( #21366 ), #40284, .T. ) ;
#1146=CARTESIAN_POINT ( 'NONE',  ( -0.07982934255991593064, -32.56666002521691183, 7.785096263473210598 ) ) ;
#1147=CARTESIAN_POINT ( 'NONE',  ( -0.9728551256764975674, -31.82908634522761560, 7.756742906098587298 ) ) ;
#1153=CARTESIAN_POINT ( 'NONE',  ( -1.097841762937593613, -31.67228564313648320, 6.980586498568973397 ) ) ;
#1154=CARTESIAN_POINT ( 'NONE',  ( 5.195112791980205813, -29.76205841885524350, 6.951256099901581997 ) ) ;
#1155=CARTESIAN_POINT ( 'NONE',  ( -0.5686205303572778869, -26.90504279848119040, 7.651421919295151142 ) ) ;
#1156=DIRECTION ( 'NONE',  ( -0.4826092789263672911, 0.5751513419797894544, 0.6605219282605377940 ) ) ;
#1159=CARTESIAN_POINT ( 'NONE',  ( 4.296241352401964697, -27.37412594797728715, 7.635761828346577573 ) ) ;
#1167=DIRECTION ( 'NONE',  ( 0.4999999999999980016, 0.8660254037844398178, -0.000000000000000000 ) ) ;
#1169=ORIENTED_EDGE ( 'NONE', *, *, #23859, .F. ) ;
#1171=B_SPLINE_CURVE_WITH_KNOTS ( 'NONE', 3,
 ( #13418, #35872, #19809, #10123, #22712, #32187, #32584, #32384, #3985, #4178, #16695, #16504, #29081, #29485, #7651, #29281, #20202, #26200, #38731, #23106, #8441, #27599, #11935, #39537, #15037, #8039, #17298, #36263, #1691, #20596, #11323 ),
 .UNSPECIFIED., .F., .F.,
 ( 4, 3, 3, 3, 3, 3, 3, 3, 3, 3, 4 ),
 ( 1.022834283856302764E-18, 2.999644130997711973E-05, 6.002588995694830702E-05, 8.960886084587982281E-05, 0.0001190604700446476022, 0.0001489538463052710970, 0.0001796139255493959305, 0.0002109707048517047475, 0.0002426195318110325918, 0.0002740640997890037445, 0.0002849778069099849075 ),
 .UNSPECIFIED. ) ;
#1172=CARTESIAN_POINT ( 'NONE',  ( 2.963766215430877260, -26.31911081783852779, 7.782861076432730840 ) ) ;
#1175=CARTESIAN_POINT ( 'NONE',  ( 5.052185455143900938, -30.14046697283304255, 7.643333865083955736 ) ) ;
#1177=VERTEX_POINT ( 'NONE', #12903 ) ;
#1182=DIRECTION ( 'NONE',  ( 1.000000000000000000, 0.000000000000000000, 0.000000000000000000 ) ) ;
#1188=CYLINDRICAL_SURFACE ( 'NONE', #2503, 0.09010775117052992333 ) ;
#1191=CARTESIAN_POINT ( 'NONE',  ( -1.766059499949450773, -30.05349463170571767, 6.867199677474202346 ) ) ;
#1192=CARTESIAN_POINT ( 'NONE',  ( 4.281682929012584182, -27.35702998321412593, 7.695279973900954751 ) ) ;
#1194=FACE_OUTER_BOUND ( 'NONE', #38012, .T. ) ;
#1198=DIRECTION ( 'NONE',  ( 0.7660444431189857850, -0.6427876096865299260, -0.000000000000000000 ) ) ;
#1199=CARTESIAN_POINT ( 'NONE',  ( 2.931042139431549565, -32.84643678970255110, 7.700536657684216912 ) ) ;
#1200=FACE_OUTER_BOUND ( 'NONE', #32712, .T. ) ;
#1201=ADVANCED_FACE ( 'NONE', ( #35560 ), #30903, .T. ) ;
#1202=CARTESIAN_POINT ( 'NONE',  ( 1.671100228160198764, -26.17005511905719217, 7.730758795053807475 ) ) ;
#1203=CARTESIAN_POINT ( 'NONE',  ( -0.3331733235464042209, -26.84510637993277271, 7.006423389747791219 ) ) ;
#1204=EDGE_CURVE ( 'NONE', #22060, #24466, #16197, .T. ) ;
#1205=CARTESIAN_POINT ( 'NONE',  ( 4.918762182065622213, -28.47348944886545397, 7.784476445165072533 ) ) ;
#1206=CARTESIAN_POINT ( 'NONE',  ( -1.577774374486538678, -28.34370111728035013, 6.894806418505347700 ) ) ;
#1208=DIRECTION ( 'NONE',  ( 0.6427876096865379196, 0.7660444431189793457, -0.000000000000000000 ) ) ;
#1214=CARTESIAN_POINT ( 'NONE',  ( -0.4597662833393237336, -26.81607390015101799, 6.865482280155367434 ) ) ;
#1215=CARTESIAN_POINT ( 'NONE',  ( -1.302730225678609965, -27.77235727801802057, 6.875671892026061549 ) ) ;
#1218=ORIENTED_EDGE ( 'NONE', *, *, #19193, .T. ) ;
#1219=CARTESIAN_POINT ( 'NONE',  ( 6.396068641104377228, -30.45570603157191769, 7.013842709614101167 ) ) ;
#1221=EDGE_LOOP ( 'NONE', ( #16790, #18819, #34634, #35996, #28546 ) ) ;
#1222=CARTESIAN_POINT ( 'NONE',  ( -0.9146243593313261311, -25.28420110832643886, 7.754798119455333705 ) ) ;
#1229=CARTESIAN_POINT ( 'NONE',  ( 5.035164781800626876, -30.23278213633238209, 6.874555630061440326 ) ) ;
#1233=CARTESIAN_POINT ( 'NONE',  ( -1.694464052375517671, -29.38293999636734810, 7.013842709614101167 ) ) ;
#1241=CARTESIAN_POINT ( 'NONE',  ( 0.3419956299568869262, -32.68678192801872484, 6.949473656533215582 ) ) ;
#1246=PLANE ( 'NONE',  #30331 ) ;
#1253=CARTESIAN_POINT ( 'NONE',  ( -2.735299443412492426, -31.17001996922091678, 7.635761828346577573 ) ) ;
#1254=ORIENTED_EDGE ( 'NONE', *, *, #35907, .T. ) ;
#1256=CARTESIAN_POINT ( 'NONE',  ( -1.644646209780476820, -30.17880794741612505, 7.748216051605118615 ) ) ;
#1257=CARTESIAN_POINT ( 'NONE',  ( 4.990378111456791999, -28.41860493638662888, 7.785096263473211486 ) ) ;
#1258=ORIENTED_EDGE ( 'NONE', *, *, #18494, .T. ) ;
#1265=CARTESIAN_POINT ( 'NONE',  ( 2.406735030961865363, -33.78287863190474383, 7.695279973900954751 ) ) ;
#1268=CARTESIAN_POINT ( 'NONE',  ( 3.799857242690032777, -32.37032976418250740, 6.941203072598476354 ) ) ;
#1272=CARTESIAN_POINT ( 'NONE',  ( 5.885943586549580608, -28.70822073431874344, 7.754798119455333705 ) ) ;
#1274=CARTESIAN_POINT ( 'NONE',  ( -1.627984416835427162, -30.65173788820889200, 7.754798119455333705 ) ) ;
#1275=ORIENTED_EDGE ( 'NONE', *, *, #39239, .T. ) ;
#1276=CARTESIAN_POINT ( 'NONE',  ( -1.593127767899503722, -28.38555688987459291, 7.635761828346575797 ) ) ;
#1277=CARTESIAN_POINT ( 'NONE',  ( 4.419915592368481860, -27.38632609080736557, 7.782861076432731728 ) ) ;
#1279=EDGE_CURVE ( 'NONE', #38902, #32411, #11629, .T. ) ;
#1283=EDGE_CURVE ( 'NONE', #1015, #486, #19030, .T. ) ;
#1289=CARTESIAN_POINT ( 'NONE',  ( -0.1048951552736917536, -32.56843413746527460, 6.870737987065012042 ) ) ;
#1294=CARTESIAN_POINT ( 'NONE',  ( -0.5714818571711197670, -32.09947517033602793, 6.864276522220859711 ) ) ;
#1295=CARTESIAN_POINT ( 'NONE',  ( 3.925174318192090617, -26.86801694415465747, 7.670465701733752972 ) ) ;
#1300=CARTESIAN_POINT ( 'NONE',  ( 4.998117124696596747, -33.55594714837163650, 7.695279973900954751 ) ) ;
#1301=CARTESIAN_POINT ( 'NONE',  ( -1.544665293549569052, -28.25920506871950622, 7.754798119455333705 ) ) ;
#1302=CARTESIAN_POINT ( 'NONE',  ( -0.4574464213436950089, -32.19742739189324254, 7.692469944509193525 ) ) ;
#1308=EDGE_CURVE ( 'NONE', #14269, #28383, #9170, .T. ) ;
#1309=CARTESIAN_POINT ( 'NONE',  ( 3.066970013825967900, -26.34774553824737708, 6.912143950357344302 ) ) ;
#1312=DIRECTION ( 'NONE',  ( -0.7508067542896625923, -2.621427771679738966E-15, -0.6605219282605402364 ) ) ;
#1313=FACE_OUTER_BOUND ( 'NONE', #22762, .T. ) ;
#1315=CARTESIAN_POINT ( 'NONE',  ( 0.9049691096044686356, -32.87557774234537789, 6.969307238440506147 ) ) ;
#1323=VERTEX_POINT ( 'NONE', #39007 ) ;
#1328=EDGE_CURVE ( 'NONE', #24028, #6532, #20952, .T. ) ;
#1332=AXIS2_PLACEMENT_3D ( 'NONE', #24016, #5096, #8576 ) ;
#1333=CARTESIAN_POINT ( 'NONE',  ( -1.628563930502259671, -30.65045316922430985, 7.753200566781576875 ) ) ;
#1335=( BOUNDED_CURVE ( )  B_SPLINE_CURVE ( 3, ( #4532, #4336, #38084, #3943 ),
 .UNSPECIFIED., .F., .T. ) 
 B_SPLINE_CURVE_WITH_KNOTS ( ( 4, 4 ),
 ( 4.748221474220560623, 4.941946782021396700 ),
 .UNSPECIFIED. ) 
 CURVE ( )  GEOMETRIC_REPRESENTATION_ITEM ( )  RATIONAL_B_SPLINE_CURVE ( ( 1.000000000000000000, 0.9968749865767494445, 0.9968749865767494445, 1.000000000000000000 ) ) 
 REPRESENTATION_ITEM ( '' )  );
#1339=ORIENTED_EDGE ( 'NONE', *, *, #33464, .T. ) ;
#1342=CARTESIAN_POINT ( 'NONE',  ( -2.689021718275399042, -31.29716697405881476, 7.754798119455333705 ) ) ;
#1348=CARTESIAN_POINT ( 'NONE',  ( -2.617163280481567433, -29.45682925621299475, 6.894806418505347700 ) ) ;
#1350=CARTESIAN_POINT ( 'NONE',  ( -1.066124925935248546, -31.71387034028391838, 6.870724624169668893 ) ) ;
#1353=CARTESIAN_POINT ( 'NONE',  ( 1.295029243323604806, -26.19418099523372945, 7.013842709614101167 ) ) ;
#1356=CARTESIAN_POINT ( 'NONE',  ( 1.845516155340734654, -26.07294027404319792, 6.875780273367530171 ) ) ;
#1357=APPLICATION_CONTEXT ( 'automotive_design' ) ;
#1370=CARTESIAN_POINT ( 'NONE',  ( 5.098140652402787687, -29.31764686638471318, 7.505001789837626447 ) ) ;
#1381=CARTESIAN_POINT ( 'NONE',  ( 3.922988059513587089, -26.99698279172644177, 6.894806418505345924 ) ) ;
#1383=CARTESIAN_POINT ( 'NONE',  ( 5.200294581628556401, -29.54390383290751387, 7.737115613922530777 ) ) ;
#1384=AXIS2_PLACEMENT_3D ( 'NONE', #17559, #13890, #30147 ) ;
#1386=B_SPLINE_CURVE_WITH_KNOTS ( 'NONE', 3,
 ( #30871, #40309, #7660, #17112, #27556, #32794, #14029, #4772, #186, #40504, #34378, #28793, #25697, #9018, #34178, #31071, #40719, #37622, #35189, #26309, #10836, #19723, #26111, #23413, #38240 ),
 .UNSPECIFIED., .F., .F.,
 ( 4, 3, 3, 3, 3, 3, 3, 3, 4 ),
 ( 6.468151674594278821E-05, 9.076621574722433050E-05, 0.0001210204262068000672, 0.0001512763324577483628, 0.0001815301820994212134, 0.0002117781465860742022, 0.0002420274594459714671, 0.0002722905548971123733, 0.0002816827545175610106 ),
 .UNSPECIFIED. ) ;
#1388=CARTESIAN_POINT ( 'NONE',  ( 5.141009602703632275, -28.92794678622675875, 7.678495282201402539 ) ) ;
#1391=CARTESIAN_POINT ( 'NONE',  ( -1.483415766250580470, -30.76298519013761279, 7.721096864323905073 ) ) ;
#1392=CARTESIAN_POINT ( 'NONE',  ( 3.858201203583684791, -26.94241211265676839, 7.703977250142846955 ) ) ;
#1394=CARTESIAN_POINT ( 'NONE',  ( -1.645585159361036220, -30.17362680341680203, 7.635761828346577573 ) ) ;
#1395=CARTESIAN_POINT ( 'NONE',  ( 4.422352071802834850, -27.36970206379270820, 6.870737987065012042 ) ) ;
#1397=CARTESIAN_POINT ( 'NONE',  ( 5.098207581826219581, -29.69173459304409946, 7.754798119455333705 ) ) ;
#1398=CARTESIAN_POINT ( 'NONE',  ( 4.172240291830656034, -31.90445124331759530, 6.911401339314958925 ) ) ;
#1399=CARTESIAN_POINT ( 'NONE',  ( 2.493334271959621873, -32.98593869321148730, 7.139344958878412584 ) ) ;
#1402=ORIENTED_EDGE ( 'NONE', *, *, #10684, .T. ) ;
#1407=CARTESIAN_POINT ( 'NONE',  ( -1.265893590836503213, -27.71217119381226368, 6.867199677474202346 ) ) ;
#1410=VECTOR ( 'NONE', #12265, 1000.000000000000000 ) ;
#1411=CARTESIAN_POINT ( 'NONE',  ( 4.826899123084856136, -31.15826764627123424, 7.139344958878409919 ) ) ;
#1413=ORIENTED_EDGE ( 'NONE', *, *, #26461, .F. ) ;
#1419=ORIENTED_EDGE ( 'NONE', *, *, #7107, .T. ) ;
#1420=EDGE_CURVE ( 'NONE', #637, #12025, #9690, .T. ) ;
#1421=EDGE_CURVE ( 'NONE', #24859, #27482, #2904, .T. ) ;
#1423=CARTESIAN_POINT ( 'NONE',  ( 5.038442556635803982, -30.21599964681902506, 6.887041543973312585 ) ) ;
#1430=ORIENTED_EDGE ( 'NONE', *, *, #39262, .F. ) ;
#1438=CARTESIAN_POINT ( 'NONE',  ( -0.5120772278873689798, -26.98826626735417378, 7.680992449362115337 ) ) ;
#1441=CARTESIAN_POINT ( 'NONE',  ( 1.578585683582427235, -32.96774767198657941, 7.754798119455333705 ) ) ;
#1442=CARTESIAN_POINT ( 'NONE',  ( 1.145429890469515932, -32.92433313672930240, 7.695279973900954751 ) ) ;
#1446=CARTESIAN_POINT ( 'NONE',  ( -0.1040043641139408170, -32.45162424111279620, 7.754798119455333705 ) ) ;
#1447=DIRECTION ( 'NONE',  ( -0.2567910337120311026, 0.7055275666422143876, -0.6605219282605403475 ) ) ;
#1449=VECTOR ( 'NONE', #20329, 1000.000000000000114 ) ;
#1451=ORIENTED_EDGE ( 'NONE', *, *, #23533, .F. ) ;
#1452=ORIENTED_EDGE ( 'NONE', *, *, #25717, .T. ) ;
#1454=CARTESIAN_POINT ( 'NONE',  ( -1.649286765102148777, -30.58465425659426629, 6.951256099901588215 ) ) ;
#1459=DIRECTION ( 'NONE',  ( 0.4999999999999979461, 0.8660254037844397068, -0.000000000000000000 ) ) ;
#1460=( NAMED_UNIT ( * ) SI_UNIT ( $, .STERADIAN. ) SOLID_ANGLE_UNIT ( ) );
#1462=CARTESIAN_POINT ( 'NONE',  ( 4.820161459608385712, -27.98341619935644076, 6.921725064902950919 ) ) ;
#1467=CARTESIAN_POINT ( 'NONE',  ( -1.312937918266134707, -31.35033874361411321, 7.710604733652628440 ) ) ;
#1476=DIRECTION ( 'NONE',  ( 1.000000000000000000, 1.486905836551549118E-14, 0.000000000000000000 ) ) ;
#1479=CARTESIAN_POINT ( 'NONE',  ( -1.057258846844102873, -31.72486802769777725, 7.754798119455333705 ) ) ;
#1483=PLANE ( 'NONE',  #5669 ) ;
#1488=CARTESIAN_POINT ( 'NONE',  ( 0.06942149629988161874, -26.47315344242070267, 6.870724624169668893 ) ) ;
#1491=CARTESIAN_POINT ( 'NONE',  ( 1.099000663213878015, -32.91633116162691408, 7.775108481317161591 ) ) ;
#1492=CARTESIAN_POINT ( 'NONE',  ( 1.700390093233090871, -29.56993018339339940, 6.850000000000000533 ) ) ;
#1496=CARTESIAN_POINT ( 'NONE',  ( -1.799609906766908685, -29.56993018339339940, 6.850000000000000533 ) ) ;
#1499=CARTESIAN_POINT ( 'NONE',  ( 5.015318072754217482, -33.54151383920058294, 7.635761828346577573 ) ) ;
#1501=CARTESIAN_POINT ( 'NONE',  ( -1.346804739101824966, -27.84812774008250003, 7.670465701733752972 ) ) ;
#1502=ADVANCED_FACE ( 'NONE', ( #24970 ), #34457, .T. ) ;
#1503=EDGE_LOOP ( 'NONE', ( #28736, #3473, #31108, #47 ) ) ;
#1504=CARTESIAN_POINT ( 'NONE',  ( 0.9053063435450576790, -25.37262878166647084, 7.695279973900954751 ) ) ;
#1505=CARTESIAN_POINT ( 'NONE',  ( 3.883672655497297121, -32.17632179888655486, 7.769368695748489095 ) ) ;
#1507=CARTESIAN_POINT ( 'NONE',  ( 5.050166971101031521, -28.55553628183517034, 6.961115707816237119 ) ) ;
#1510=CARTESIAN_POINT ( 'NONE',  ( 1.267242271181500568, -26.09682929696383269, 6.903112506833892326 ) ) ;
#1511=VERTEX_POINT ( 'NONE', #22897 ) ;
#1517=ORIENTED_EDGE ( 'NONE', *, *, #33017, .T. ) ;
#1520=CARTESIAN_POINT ( 'NONE',  ( -0.6429675508017466123, -32.04310423402981201, 7.386948897581452123 ) ) ;
#1523=CARTESIAN_POINT ( 'NONE',  ( -0.9161852239640245754, -27.39886279396606739, 7.748216051605112398 ) ) ;
#1529=AXIS2_PLACEMENT_3D ( 'NONE', #27491, #14703, #26872 ) ;
#1533=B_SPLINE_CURVE_WITH_KNOTS ( 'NONE', 3,
 ( #20835, #8882, #2747, #15270, #5200, #37095, #28034, #27218, #37297, #6017, #27821, #36493, #9094, #8472, #24538, #5610, #18149, #21464, #5813, #40579, #14646, #17731, #18354, #23917, #11553, #21668, #18553, #12179, #8263, #34246, #21055 ),
 .UNSPECIFIED., .F., .F.,
 ( 4, 3, 3, 3, 3, 3, 3, 3, 3, 3, 4 ),
 ( 9.171767249593720258E-19, 2.999644130998047059E-05, 6.002588995695312495E-05, 8.960886084588529804E-05, 0.0001190604700446542971, 0.0001489538463052789846, 0.0001796139255494059864, 0.0002109707048517130417, 0.0002426195318110442199, 0.0002740640997890140445, 0.0002849778069099921174 ),
 .UNSPECIFIED. ) ;
#1538=CARTESIAN_POINT ( 'NONE',  ( 3.323202191371804393, -32.67097531272231947, 6.875780273367528395 ) ) ;
#1539=CARTESIAN_POINT ( 'NONE',  ( -1.100427372579028340, -31.66883981513531054, 6.961115707816243336 ) ) ;
#1541=CARTESIAN_POINT ( 'NONE',  ( 2.691619168861421052, -32.82224166115583586, 6.887945620086118659 ) ) ;
#1543=B_SPLINE_CURVE_WITH_KNOTS ( 'NONE', 3,
 ( #23430, #35995, #27318, #8159, #7776, #4889, #39878, #23812, #30209, #11655, #1614, #1823, #32906, #2026, #14345, #11247, #36387, #20731, #33316, #28552, #34762, #40690, #18457, #30839, #37596, #12495, #9605, #15583, #40279, #21769, #11860 ),
 .UNSPECIFIED., .F., .F.,
 ( 4, 3, 3, 3, 3, 3, 3, 3, 3, 3, 4 ),
 ( 1.852685484479510593E-18, 2.999644130997725525E-05, 6.002588995694735157E-05, 8.960886084588132715E-05, 0.0001190604700446500145, 0.0001489538463052724794, 0.0001796139255493986139, 0.0002109707048517102228, 0.0002426195318110376876, 0.0002740640997890085692, 0.0002849778069099863169 ),
 .UNSPECIFIED. ) ;
#1544=CYLINDRICAL_SURFACE ( 'NONE', #1384, 0.09010775117053103356 ) ;
#1549=ADVANCED_FACE ( 'NONE', ( #16893 ), #29473, .F. ) ;
#1557=CARTESIAN_POINT ( 'NONE',  ( 2.296140040222784950, -32.91733974362343673, 7.763628509615286610 ) ) ;
#1565=( BOUNDED_CURVE ( )  B_SPLINE_CURVE ( 3, ( #2291, #14607, #30485, #27179 ),
 .UNSPECIFIED., .F., .T. ) 
 B_SPLINE_CURVE_WITH_KNOTS ( ( 4, 4 ),
 ( 4.708531083176467291, 4.895802057644188743 ),
 .UNSPECIFIED. ) 
 CURVE ( )  GEOMETRIC_REPRESENTATION_ITEM ( )  RATIONAL_B_SPLINE_CURVE ( ( 1.000000000000000000, 0.9970795998553221295, 0.9970795998553221295, 1.000000000000000000 ) ) 
 REPRESENTATION_ITEM ( '' )  );
#1573=CARTESIAN_POINT ( 'NONE',  ( 1.700390093233090871, -29.56993018339339940, 7.800000000000000711 ) ) ;
#1576=EDGE_CURVE ( 'NONE', #32349, #32411, #25781, .T. ) ;
#1580=DIRECTION ( 'NONE',  ( -0.3420201433256706003, 0.9396926207859077618, 0.000000000000000000 ) ) ;
#1584=DIRECTION ( 'NONE',  ( 0.8660254037844380415, 0.5000000000000009992, -0.000000000000000000 ) ) ;
#1585=CARTESIAN_POINT ( 'NONE',  ( -1.642727701737825896, -30.18925514571027335, 7.661510568013096822 ) ) ;
#1586=CARTESIAN_POINT ( 'NONE',  ( 0.6319492117650733487, -26.23698571484616693, 6.870724624169667116 ) ) ;
#1589=CARTESIAN_POINT ( 'NONE',  ( 4.497269860293852339, -27.46577629914297702, 6.921725064902955360 ) ) ;
#1590=EDGE_CURVE ( 'NONE', #33368, #22465, #31032, .T. ) ;
#1592=CARTESIAN_POINT ( 'NONE',  ( 4.176219800253964998, -31.90023320913972782, 7.006423389747793884 ) ) ;
#1594=DIRECTION ( 'NONE',  ( -0.000000000000000000, -0.000000000000000000, -1.000000000000000000 ) ) ;
#1601=CARTESIAN_POINT ( 'NONE',  ( -0.4841935375551393306, -26.83541114705590758, 6.865554069792297653 ) ) ;
#1602=CARTESIAN_POINT ( 'NONE',  ( 4.365277478145313417, -27.30091955980304874, 7.651421919295146701 ) ) ;
#1603=ORIENTED_EDGE ( 'NONE', *, *, #23697, .T. ) ;
#1604=CARTESIAN_POINT ( 'NONE',  ( 1.076698322469717750, -26.22039822960329403, 7.257242401810562349 ) ) ;
#1614=CARTESIAN_POINT ( 'NONE',  ( -0.7684451854189515707, -27.23222622129974724, 6.920489980334480151 ) ) ;
#1617=CARTESIAN_POINT ( 'NONE',  ( -0.1022282953655194032, -32.45273633994818141, 7.757178535559533294 ) ) ;
#1621=CARTESIAN_POINT ( 'NONE',  ( 4.659461314909612462, -31.24441443385555672, 7.661510568013094158 ) ) ;
#1624=CARTESIAN_POINT ( 'NONE',  ( 5.128111633932078917, -30.21023550748081377, 7.783750581861600182 ) ) ;
#1628=CARTESIAN_POINT ( 'NONE',  ( 0.3430422367937097095, -32.68723900743627553, 6.939395833800439561 ) ) ;
#1637=CARTESIAN_POINT ( 'NONE',  ( 4.634605404468733703, -27.83824422985297531, 7.257242401810564125 ) ) ;
#1650=CARTESIAN_POINT ( 'NONE',  ( 4.992773418886902626, -28.42625648742630773, 7.785344483711591934 ) ) ;
#1652=VERTEX_POINT ( 'NONE', #8029 ) ;
#1654=CARTESIAN_POINT ( 'NONE',  ( -1.642705848810893210, -30.60612974056809676, 6.895394898881666457 ) ) ;
#1659=CARTESIAN_POINT ( 'NONE',  ( 3.070800210251708684, -33.66578602384694108, 6.894806418505347700 ) ) ;
#1661=B_SPLINE_CURVE_WITH_KNOTS ( 'NONE', 3,
 ( #18220, #12034, #5678, #9164, #15136, #8953, #12251, #24823, #6090, #18623, #38179, #29133, #28313, #38375, #22561, #31414, #16163, #9782, #37768, #25637, #6707, #34518, #10177, #9362, #19255, #21946, #7101, #19664, #3241, #9982, #22766 ),
 .UNSPECIFIED., .F., .F.,
 ( 4, 3, 3, 3, 3, 3, 3, 3, 3, 3, 4 ),
 ( 9.697399036122160616E-19, 2.999644130997348087E-05, 6.002588995694365173E-05, 8.960886084587883348E-05, 0.0001190604700446476428, 0.0001489538463052722083, 0.0001796139255493953341, 0.0002109707048517089488, 0.0002426195318110391512, 0.0002740640997890091655, 0.0002849778069099856122 ),
 .UNSPECIFIED. ) ;
#1665=CARTESIAN_POINT ( 'NONE',  ( 4.296671084470158775, -27.37462607708720341, 7.756377446753165650 ) ) ;
#1673=AXIS2_PLACEMENT_3D ( 'NONE', #10532, #29286, #19619 ) ;
#1674=CARTESIAN_POINT ( 'NONE',  ( 0.01821419288840892339, -26.61520874120817837, 7.779495906702012853 ) ) ;
#1681=AXIS2_PLACEMENT_3D ( 'NONE', #30370, #39405, #20676 ) ;
#1685=CARTESIAN_POINT ( 'NONE',  ( 1.700390093233090871, -29.56993018339339940, 7.800000000000000711 ) ) ;
#1691=CARTESIAN_POINT ( 'NONE',  ( 0.5882562476373008886, -26.35696177504351212, 6.889465824494256374 ) ) ;
#1696=CARTESIAN_POINT ( 'NONE',  ( 2.240298271943185870, -32.92678960775148056, 6.892063359921933419 ) ) ;
#1700=CIRCLE ( 'NONE', #31296, 2.500000000000000444 ) ;
#1702=ORIENTED_EDGE ( 'NONE', *, *, #12600, .T. ) ;
#1707=CARTESIAN_POINT ( 'NONE',  ( 3.058617350509197585, -26.34421757184894020, 7.009310105710484962 ) ) ;
#1708=VERTEX_POINT ( 'NONE', #39529 ) ;
#1710=DIRECTION ( 'NONE',  ( 1.000000000000000000, -6.938893903907229167E-15, 0.000000000000000000 ) ) ;
#1713=CARTESIAN_POINT ( 'NONE',  ( 0.3374848729783252455, -32.79366859719224436, 7.002103980607166989 ) ) ;
#1717=CARTESIAN_POINT ( 'NONE',  ( 0.9730757925788008356, -32.99329091482906762, 7.754798119455333705 ) ) ;
#1736=CARTESIAN_POINT ( 'NONE',  ( -2.672839399606415256, -26.73366507310607076, 6.894806418505347700 ) ) ;
#1740=CARTESIAN_POINT ( 'NONE',  ( -1.799609906766908685, -29.56993018339339940, 7.202408869016148074 ) ) ;
#1744=LINE ( 'NONE', #1348, #22039 ) ;
#1748=CARTESIAN_POINT ( 'NONE',  ( 2.716203735777188211, -32.81465175439641513, 6.871394612369935651 ) ) ;
#1750=CARTESIAN_POINT ( 'NONE',  ( 1.805519397879190135, -26.07149441967674974, 6.863784140767622333 ) ) ;
#1756=ORIENTED_EDGE ( 'NONE', *, *, #13156, .F. ) ;
#1758=CARTESIAN_POINT ( 'NONE',  ( -0.5390062018526512455, -32.25974509032589310, 7.635761828346574021 ) ) ;
#1762=VECTOR ( 'NONE', #8028, 1000.000000000000000 ) ;
#1764=DIRECTION ( 'NONE',  ( 0.9396926207859126468, -0.3420201433256568335, -0.000000000000000000 ) ) ;
#1767=ORIENTED_EDGE ( 'NONE', *, *, #38842, .T. ) ;
#1772=CARTESIAN_POINT ( 'NONE',  ( 0.2199985751287987512, -32.63861014186149845, 7.505001789837627335 ) ) ;
#1774=CARTESIAN_POINT ( 'NONE',  ( 0.9235138160669791318, -32.98262327366389712, 7.010186378901970272 ) ) ;
#1780=EDGE_CURVE ( 'NONE', #6329, #6673, #5162, .T. ) ;
#1781=EDGE_CURVE ( 'NONE', #32844, #18906, #1565, .T. ) ;
#1785=CARTESIAN_POINT ( 'NONE',  ( 4.643350526641022213, -31.46439155470594073, 7.013842709614101167 ) ) ;
#1790=LINE ( 'NONE', #17203, #33947 ) ;
#1791=CARTESIAN_POINT ( 'NONE',  ( 0.5390211770124229140, -26.26822319535999384, 6.887161170156906209 ) ) ;
#1795=CARTESIAN_POINT ( 'NONE',  ( 4.499507836142066175, -27.46875105750827117, 6.931070083220562061 ) ) ;
#1798=ADVANCED_FACE ( 'NONE', ( #14817 ), #24295, .F. ) ;
#1799=CYLINDRICAL_SURFACE ( 'NONE', #31361, 0.09010775117052916006 ) ;
#1803=CARTESIAN_POINT ( 'NONE',  ( 2.246982590450817163, -33.01192690407003028, 7.785593909369613819 ) ) ;
#1806=CYLINDRICAL_SURFACE ( 'NONE', #13869, 0.09010775117052903516 ) ;
#1807=( BOUNDED_CURVE ( )  B_SPLINE_CURVE ( 3, ( #16042, #25522, #21824, #38067 ),
 .UNSPECIFIED., .F., .T. ) 
 B_SPLINE_CURVE_WITH_KNOTS ( ( 4, 4 ),
 ( 4.708531083176466403, 4.895802057644187855 ),
 .UNSPECIFIED. ) 
 CURVE ( )  GEOMETRIC_REPRESENTATION_ITEM ( )  RATIONAL_B_SPLINE_CURVE ( ( 1.000000000000000000, 0.9970795998553221295, 0.9970795998553221295, 1.000000000000000000 ) ) 
 REPRESENTATION_ITEM ( '' )  );
#1808=CARTESIAN_POINT ( 'NONE',  ( -1.639146693691649892, -28.93157757802832819, 6.894806418505346812 ) ) ;
#1811=CARTESIAN_POINT ( 'NONE',  ( -0.5730865926811068434, -32.23100210249002373, 6.894806418505347700 ) ) ;
#1812=ADVANCED_FACE ( 'NONE', ( #3333 ), #9456, .T. ) ;
#1815=B_SPLINE_CURVE_WITH_KNOTS ( 'NONE', 3,
 ( #35736, #25649, #16764, #28743, #6915, #16972, #552, #7510, #13088, #13896 ),
 .UNSPECIFIED., .F., .F.,
 ( 4, 3, 3, 4 ),
 ( 0.0005050348086185292486, 0.0005143352185143279303, 0.0005445898203825193500, 0.0005634294782181697644 ),
 .UNSPECIFIED. ) ;
#1819=CARTESIAN_POINT ( 'NONE',  ( -1.525553370913913076, -28.21224846644693685, 7.010186378901971160 ) ) ;
#1823=CARTESIAN_POINT ( 'NONE',  ( -0.7714601053644620787, -27.23540912346919285, 6.911401339314957148 ) ) ;
#1832=EDGE_CURVE ( 'NONE', #20740, #908, #20462, .T. ) ;
#1833=CARTESIAN_POINT ( 'NONE',  ( -2.489212967774009577, -31.84613700427082250, 6.954324564059724878 ) ) ;
#1840=CARTESIAN_POINT ( 'NONE',  ( 1.092632081715625203, -33.01346371419235481, 7.767720160662275219 ) ) ;
#1843=CARTESIAN_POINT ( 'NONE',  ( 2.782197798051136317, -32.89830469346890141, 7.754798119455333705 ) ) ;
#1844=ORIENTED_EDGE ( 'NONE', *, *, #4047, .F. ) ;
#1857=CARTESIAN_POINT ( 'NONE',  ( 5.022807544912395450, -28.47749337420469828, 7.766640943994347346 ) ) ;
#1861=CARTESIAN_POINT ( 'NONE',  ( -1.632554375314136275, -30.63837106486143114, 6.870724624169666228 ) ) ;
#1872=ORIENTED_EDGE ( 'NONE', *, *, #31070, .T. ) ;
#1873=CARTESIAN_POINT ( 'NONE',  ( 4.809580840142714031, -27.96276457679604377, 6.887547729233689076 ) ) ;
#1880=EDGE_LOOP ( 'NONE', ( #32919, #33955, #32628, #37606, #11902 ) ) ;
#1882=CARTESIAN_POINT ( 'NONE',  ( 1.075169146119493879, -26.22790998750958025, 7.680992449362119778 ) ) ;
#1883=CARTESIAN_POINT ( 'NONE',  ( -1.796218690686571584, -29.41562043804214710, 6.880828092187096345 ) ) ;
#1899=CARTESIAN_POINT ( 'NONE',  ( 4.198225232297463805, -33.92331276665304785, 7.635761828346577573 ) ) ;
#1900=CARTESIAN_POINT ( 'NONE',  ( 4.647595270087047759, -31.26523263687563770, 7.763628509615284834 ) ) ;
#1903=CARTESIAN_POINT ( 'NONE',  ( 0.04221685988047467475, -26.48763128618372065, 6.863784140767622333 ) ) ;
#1906=DIRECTION ( 'NONE',  ( -0.2567910337120262732, -0.7055275666422161640, -0.6605219282605403475 ) ) ;
#1907=CARTESIAN_POINT ( 'NONE',  ( 4.433004015503416717, -25.10972701691773779, 7.013842709614101167 ) ) ;
#1909=CARTESIAN_POINT ( 'NONE',  ( -0.4624923041496786791, -32.19327532559099581, 7.661510568013091493 ) ) ;
#1916=EDGE_CURVE ( 'NONE', #32358, #40685, #13785, .T. ) ;
#1917=CARTESIAN_POINT ( 'NONE',  ( -0.5737835481674327109, -32.09740712681197294, 7.759451378593101190 ) ) ;
#1918=CARTESIAN_POINT ( 'NONE',  ( 1.822194502883781375, -26.17211269480022295, 7.754798119455333705 ) ) ;
#1920=CARTESIAN_POINT ( 'NONE',  ( 1.054320629807504295, -32.90798264679612117, 6.887041543973314361 ) ) ;
#1921=CARTESIAN_POINT ( 'NONE',  ( 0.3819031147581120056, -32.81210268184693746, 6.868546646838340486 ) ) ;
#1928=LINE ( 'NONE', #26624, #39013 ) ;
#1931=B_SPLINE_CURVE_WITH_KNOTS ( 'NONE', 3,
 ( #31893, #12728, #28170, #3501, #6769, #9642, #12524, #31280, #25502, #35196 ),
 .UNSPECIFIED., .F., .F.,
 ( 4, 3, 3, 4 ),
 ( 0.0002170292169044773015, 0.0002420761345915959295, 0.0002723302478206993896, 0.0002816811360866744701 ),
 .UNSPECIFIED. ) ;
#1934=CARTESIAN_POINT ( 'NONE',  ( 2.277491769660097365, -26.21926552469281191, 7.635761828346577573 ) ) ;
#1940=EDGE_CURVE ( 'NONE', #309, #774, #8122, .T. ) ;
#1942=CARTESIAN_POINT ( 'NONE',  ( 4.361462012329716309, -31.84340686930758935, 6.894806418505347700 ) ) ;
#1946=CARTESIAN_POINT ( 'NONE',  ( 4.582084150952498547, -31.37432464074042215, 7.754798119455333705 ) ) ;
#1953=CARTESIAN_POINT ( 'NONE',  ( 5.159329814365638534, -29.03529183849990147, 6.867280401193707640 ) ) ;
#1956=CARTESIAN_POINT ( 'NONE',  ( 3.388683086819756163, -26.61871572696936994, 7.635761828346577573 ) ) ;
#1959=CARTESIAN_POINT ( 'NONE',  ( 5.000279045638660769, -30.73643474909027518, 7.670465701733750308 ) ) ;
#1960=CARTESIAN_POINT ( 'NONE',  ( 2.664359094183485599, -32.83041543721814293, 6.969307238440505259 ) ) ;
#1961=CARTESIAN_POINT ( 'NONE',  ( 1.686887486498408029, -26.16995699532097319, 7.635761828346577573 ) ) ;
#1964=CARTESIAN_POINT ( 'NONE',  ( 2.183954541545420458, -33.03637977657594149, 6.867199677474202346 ) ) ;
#1969=CARTESIAN_POINT ( 'NONE',  ( 4.289323970621365056, -27.35503128888597146, 7.257242401810561461 ) ) ;
#1970=ORIENTED_EDGE ( 'NONE', *, *, #27641, .F. ) ;
#1972=CARTESIAN_POINT ( 'NONE',  ( -0.5254690805390769270, -26.86890242742082080, 6.894806418505347700 ) ) ;
#1973=CARTESIAN_POINT ( 'NONE',  ( 3.058784556509318797, -26.45307843876808462, 6.949473656533219135 ) ) ;
#1975=CARTESIAN_POINT ( 'NONE',  ( -0.9695225508750403565, -31.83301800158153227, 7.749999999999998224 ) ) ;
#1976=PLANE ( 'NONE',  #31756 ) ;
#1984=CARTESIAN_POINT ( 'NONE',  ( 0.5660192589948234154, -26.36474644288341551, 7.782167645815905033 ) ) ;
#1986=AXIS2_PLACEMENT_3D ( 'NONE', #22368, #9786, #6511 ) ;
#1991=EDGE_LOOP ( 'NONE', ( #13209, #16071, #3495, #40369 ) ) ;
#1993=ORIENTED_EDGE ( 'NONE', *, *, #28989, .F. ) ;
#1996=CARTESIAN_POINT ( 'NONE',  ( 1.554942410987211865, -32.96681772520712883, 6.868387053540520704 ) ) ;
#1997=CARTESIAN_POINT ( 'NONE',  ( 2.346459556658704315, -26.23187771999068119, 6.887041543973313473 ) ) ;
#2005=CARTESIAN_POINT ( 'NONE',  ( 4.172416336262816827, -31.90426121769112555, 6.997764925645185485 ) ) ;
#2006=VERTEX_POINT ( 'NONE', #36843 ) ;
#2010=CARTESIAN_POINT ( 'NONE',  ( 2.222359783566090208, -33.02043838110294871, 7.780491323090172884 ) ) ;
#2015=CARTESIAN_POINT ( 'NONE',  ( -1.621787578243040651, -28.84658016871684794, 6.865312560952603782 ) ) ;
#2016=CARTESIAN_POINT ( 'NONE',  ( 2.363993368752974167, -26.14856561996513662, 7.785593909369613819 ) ) ;
#2017=CARTESIAN_POINT ( 'NONE',  ( -0.6924112550790449960, -32.12424229857576563, 6.971170733404098208 ) ) ;
#2018=ORIENTED_EDGE ( 'NONE', *, *, #8403, .T. ) ;
#2023=CARTESIAN_POINT ( 'NONE',  ( 4.200390093233091093, -29.56993018339339940, 6.800000000000000711 ) ) ;
#2026=CARTESIAN_POINT ( 'NONE',  ( -0.7792710424444403428, -27.24370714888392442, 6.895222827070024429 ) ) ;
#2028=VECTOR ( 'NONE', #21034, 1000.000000000000000 ) ;
#2034=CARTESIAN_POINT ( 'NONE',  ( -1.203028700869076095, -27.80068031303635223, 7.782034975670476307 ) ) ;
#2035=DIRECTION ( 'NONE',  ( -0.7660444431189725734, -0.6427876096865456912, -0.000000000000000000 ) ) ;
#2036=CARTESIAN_POINT ( 'NONE',  ( 1.700390093233090871, -29.56993018339339940, 7.800000000000000711 ) ) ;
#2042=CARTESIAN_POINT ( 'NONE',  ( -0.9575446616272440536, -31.84707375580262578, 7.698786668945011513 ) ) ;
#2043=CARTESIAN_POINT ( 'NONE',  ( 4.979040433996382298, -28.34499767243864810, 7.660770905198782899 ) ) ;
#2047=EDGE_LOOP ( 'NONE', ( #3058, #8960, #20319, #1430, #12735 ) ) ;
#2048=PLANE ( 'NONE',  #33916 ) ;
#2050=B_SPLINE_CURVE_WITH_KNOTS ( 'NONE', 3,
 ( #483, #38322, #7244, #13626, #13019, #22709, #22904, #38127, #31977, #29279, #9929, #26197, #22511, #10525, #19405, #10119, #32378, #21378, #5937, #32977, #15188, #18476, #32783, #37417, #36260, #33957, #31061, #4762, #9213, #27548, #17099 ),
 .UNSPECIFIED., .F., .F.,
 ( 4, 3, 3, 3, 3, 3, 3, 3, 3, 3, 4 ),
 ( 9.697399036122160616E-19, 2.999644130997572721E-05, 6.002588995694706019E-05, 8.960886084587848111E-05, 0.0001190604700446479952, 0.0001489538463052703923, 0.0001796139255493973670, 0.0002109707048517048017, 0.0002426195318110344079, 0.0002740640997890034193, 0.0002849778069099790528 ),
 .UNSPECIFIED. ) ;
#2056=CARTESIAN_POINT ( 'NONE',  ( -0.4463135599462602632, -26.93331026361374470, 7.785868773668302545 ) ) ;
#2057=VERTEX_POINT ( 'NONE', #34806 ) ;
#2067=EDGE_CURVE ( 'NONE', #21810, #21380, #35663, .T. ) ;
#2074=VECTOR ( 'NONE', #40514, 999.9999999999998863 ) ;
#2075=VERTEX_POINT ( 'NONE', #4254 ) ;
#2076=CARTESIAN_POINT ( 'NONE',  ( 0.1069670619869697303, -26.56643171602332032, 7.754798119455333705 ) ) ;
#2080=CARTESIAN_POINT ( 'NONE',  ( 4.746899557684813864, -27.84691535960167030, 6.894806418505347700 ) ) ;
#2081=ORIENTED_EDGE ( 'NONE', *, *, #25583, .F. ) ;
#2084=CARTESIAN_POINT ( 'NONE',  ( -1.718189074305093600, -25.68532020122240311, 7.754798119455333705 ) ) ;
#2085=ORIENTED_EDGE ( 'NONE', *, *, #29510, .T. ) ;
#2086=CARTESIAN_POINT ( 'NONE',  ( 0.02667858525708081963, -26.61042181407449192, 7.782167645815904145 ) ) ;
#2098=CARTESIAN_POINT ( 'NONE',  ( 3.913290293412393872, -32.15122301917286762, 7.695279973900954751 ) ) ;
#2100=DIRECTION ( 'NONE',  ( -0.9848077530122091305, 0.1736481776669241417, -0.000000000000000000 ) ) ;
#2103=CARTESIAN_POINT ( 'NONE',  ( 4.738207753463742122, -31.30822356001046458, 7.635761828346574021 ) ) ;
#2104=CARTESIAN_POINT ( 'NONE',  ( 5.191948456685583579, -29.66439323399636407, 7.776484688137390577 ) ) ;
#2105=LINE ( 'NONE', #4974, #34272 ) ;
#2110=VERTEX_POINT ( 'NONE', #17790 ) ;
#2116=VERTEX_POINT ( 'NONE', #5666 ) ;
#2118=CARTESIAN_POINT ( 'NONE',  ( 3.794562874143936781, -32.24844578246045046, 7.759451378593092308 ) ) ;
#2123=CARTESIAN_POINT ( 'NONE',  ( 1.276579259530898458, -26.09568431166286828, 6.921725064902952695 ) ) ;
#2135=AXIS2_PLACEMENT_3D ( 'NONE', #31784, #38746, #31994 ) ;
#2137=CARTESIAN_POINT ( 'NONE',  ( -0.8845957367844016206, -27.36134505743407530, 7.782167645815903256 ) ) ;
#2140=CARTESIAN_POINT ( 'NONE',  ( 5.150390093233091271, -29.56993018339339940, 6.800000000000000711 ) ) ;
#2145=ORIENTED_EDGE ( 'NONE', *, *, #16317, .F. ) ;
#2146=CARTESIAN_POINT ( 'NONE',  ( -1.722970638209900596, -28.84261588273779964, 7.754798119455333705 ) ) ;
#2149=CARTESIAN_POINT ( 'NONE',  ( -1.699609906766908818, -29.56993018339339940, 7.800000000000000711 ) ) ;
#2150=CARTESIAN_POINT ( 'NONE',  ( -0.8980191362577285563, -27.22509128144364610, 7.750000000000000888 ) ) ;
#2151=CARTESIAN_POINT ( 'NONE',  ( 5.175086729718587186, -29.14981455392978660, 6.931070083220560285 ) ) ;
#2154=CARTESIAN_POINT ( 'NONE',  ( 3.369155479471896530, -26.60763004909045293, 7.693875151218755981 ) ) ;
#2155=DIRECTION ( 'NONE',  ( 0.000000000000000000, 0.000000000000000000, 1.000000000000000000 ) ) ;
#2156=LINE ( 'NONE', #30142, #981 ) ;
#2159=CARTESIAN_POINT ( 'NONE',  ( 4.893494088014897159, -28.40195944670255912, 7.763628509615286610 ) ) ;
#2160=CARTESIAN_POINT ( 'NONE',  ( 2.829405163535268386, -26.36285597610873310, 7.693875151218754205 ) ) ;
#2162=CARTESIAN_POINT ( 'NONE',  ( 2.173839223709712609, -33.03777254838963273, 6.870724624169667116 ) ) ;
#2166=EDGE_CURVE ( 'NONE', #15412, #463, #32244, .T. ) ;
#2171=CARTESIAN_POINT ( 'NONE',  ( 0.1649012726517564975, -26.53640515764040231, 7.013842709614101167 ) ) ;
#2173=CARTESIAN_POINT ( 'NONE',  ( 4.703888560603170177, -27.97650715214728123, 7.754798119455333705 ) ) ;
#2176=CARTESIAN_POINT ( 'NONE',  ( -1.799591427079094030, -29.58235858030848675, 7.756555456908253987 ) ) ;
#2179=VERTEX_POINT ( 'NONE', #28708 ) ;
#2184=B_SPLINE_CURVE_WITH_KNOTS ( 'NONE', 3,
 ( #9126, #30772, #2574, #39599, #36720, #15096, #8503, #21086, #37125, #8913 ),
 .UNSPECIFIED., .F., .F.,
 ( 4, 3, 3, 4 ),
 ( 0.000000000000000000, 3.025570593003320367E-05, 6.051145698344263427E-05, 6.468151674593523946E-05 ),
 .UNSPECIFIED. ) ;
#2186=CARTESIAN_POINT ( 'NONE',  ( 4.042068651234693277, -27.10486591319729754, 6.969307238440507923 ) ) ;
#2194=CARTESIAN_POINT ( 'NONE',  ( 1.564919489175762735, -32.96724492301107290, 6.865312560952603782 ) ) ;
#2195=CARTESIAN_POINT ( 'NONE',  ( 2.363242046172057353, -26.23515549482586096, 6.874555630061442102 ) ) ;
#2196=CARTESIAN_POINT ( 'NONE',  ( 4.899937972425366439, -30.72010120057137073, 7.635761828346577573 ) ) ;
#2199=CARTESIAN_POINT ( 'NONE',  ( 0.03162470699431464694, -32.53223031769636009, 7.695279973900954751 ) ) ;
#2200=CARTESIAN_POINT ( 'NONE',  ( -0.2278126045957919732, -32.49907834724773892, 7.387053503561885393 ) ) ;
#2204=CARTESIAN_POINT ( 'NONE',  ( 4.169225371885145748, -31.90763414548703736, 6.920489980334481928 ) ) ;
#2208=EDGE_CURVE ( 'NONE', #39394, #6683, #34217, .T. ) ;
#2211=ADVANCED_FACE ( 'NONE', ( #12236 ), #15533, .T. ) ;
#2213=CARTESIAN_POINT ( 'NONE',  ( 4.858345136377215212, -30.82986309310958717, 6.864651958020304257 ) ) ;
#2216=CARTESIAN_POINT ( 'NONE',  ( -0.5981535632466232766, -32.20939563122895777, 6.870737987065014707 ) ) ;
#2217=EDGE_LOOP ( 'NONE', ( #7470, #10552, #37349, #36551, #15075 ) ) ;
#2222=FACE_OUTER_BOUND ( 'NONE', #18144, .T. ) ;
#2225=CARTESIAN_POINT ( 'NONE',  ( 4.757778760719634903, -27.89174059054909094, 7.782861076432730840 ) ) ;
#2231=CARTESIAN_POINT ( 'NONE',  ( 3.215891561669039778, -32.61348987959953405, 6.969307238440507923 ) ) ;
#2232=CARTESIAN_POINT ( 'NONE',  ( -0.5122432252254431884, -25.35718825981775382, 6.894806418505347700 ) ) ;
#2234=CARTESIAN_POINT ( 'NONE',  ( -0.7036529332303063100, -33.97746366811107777, 7.754798119455333705 ) ) ;
#2236=CARTESIAN_POINT ( 'NONE',  ( -1.588256500155083240, -30.72927027690474588, 7.783750581861600182 ) ) ;
#2237=EDGE_CURVE ( 'NONE', #3709, #38484, #12067, .T. ) ;
#2240=CARTESIAN_POINT ( 'NONE',  ( 2.427704393887406109, -26.14656945195773119, 7.754798119455333705 ) ) ;
#2243=CARTESIAN_POINT ( 'NONE',  ( 4.980612442748399538, -28.34920280925516067, 7.651421919295148477 ) ) ;
#2247=EDGE_LOOP ( 'NONE', ( #37637, #20979, #7092, #5383, #24729, #13471, #35158, #1970, #9566, #30476, #35986, #38208, #17257, #8671, #568, #8414, #19701, #30000, #31642, #34439, #8412, #35612, #36565, #19976, #32199, #12550, #28388, #10697, #37997, #5132, #17816, #36421, #21136, #15271, #2911, #28020, #38944, #3852, #29067, #5595, #31313, #9348, #8981, #14811, #37671, #32166, #16658, #29257, #924, #20770, #38872, #1452, #22742, #11385, #4690, #10496, #28593, #17131, #6628, #24887, #28531, #27213, #5335, #2550, #31484, #14702, #634, #33370, #38957, #20583, #11954, #15069, #22955, #12057, #39174, #26267, #2677, #11741, #28224, #11570, #8617, #27262, #2085, #2493, #20124, #6337, #12944, #29023, #30223, #40017, #20313, #23227, #21014, #31960, #30017, #9656, #11589, #6267, #13165, #35393, #25301, #32133, #3515, #4497, #8922, #22876, #34969, #23283, #26326, #5836 ) ) ;
#2249=EDGE_CURVE ( 'NONE', #14798, #25728, #39563, .T. ) ;
#2250=CARTESIAN_POINT ( 'NONE',  ( 5.062217907964971175, -29.06188122502908300, 6.870716933885666400 ) ) ;
#2254=CARTESIAN_POINT ( 'NONE',  ( -0.4228120283973959559, -26.91435142379919299, 7.782034975670478083 ) ) ;
#2256=CARTESIAN_POINT ( 'NONE',  ( 2.828915453401516622, -32.86827817813306751, 7.784725160561909441 ) ) ;
#2260=ORIENTED_EDGE ( 'NONE', *, *, #9898, .F. ) ;
#2263=CARTESIAN_POINT ( 'NONE',  ( -1.328168952220487586, -31.31782122304711180, 7.767720160662272555 ) ) ;
#2266=CARTESIAN_POINT ( 'NONE',  ( -1.697427395360086244, -29.44812577374269580, 7.754798119455333705 ) ) ;
#2276=CARTESIAN_POINT ( 'NONE',  ( 4.812521983982041895, -27.96848237138598137, 7.013842709614101167 ) ) ;
#2277=CARTESIAN_POINT ( 'NONE',  ( 4.330482794039245853, -27.41523602638843826, 7.784838882742139532 ) ) ;
#2280=EDGE_CURVE ( 'NONE', #33469, #30519, #10206, .T. ) ;
#2285=CARTESIAN_POINT ( 'NONE',  ( 1.700390093233090871, -29.56993018339339940, 7.750000000000000888 ) ) ;
#2289=CARTESIAN_POINT ( 'NONE',  ( -0.2130774203410400469, -26.63113507583277695, 7.139344958878410807 ) ) ;
#2290=CIRCLE ( 'NONE', #12098, 3.499999999999999556 ) ;
#2291=CARTESIAN_POINT ( 'NONE',  ( 1.079328522417935421, -26.12547340107537863, 7.635761828346579350 ) ) ;
#2297=EDGE_CURVE ( 'NONE', #38669, #22132, #38337, .T. ) ;
#2301=CARTESIAN_POINT ( 'NONE',  ( 2.721058752466466224, -32.91780047479638682, 6.921725064902950919 ) ) ;
#2302=ORIENTED_EDGE ( 'NONE', *, *, #7859, .F. ) ;
#2304=CARTESIAN_POINT ( 'NONE',  ( -0.01667042123058508352, -26.52005313930425601, 6.887161170156905321 ) ) ;
#2306=DIRECTION ( 'NONE',  ( -1.000000000000000000, -0.000000000000000000, -0.000000000000000000 ) ) ;
#2308=CYLINDRICAL_SURFACE ( 'NONE', #36846, 0.09010775117053060335 ) ;
#2309=CARTESIAN_POINT ( 'NONE',  ( 4.307676847859603697, -31.90100969392960906, 7.766640943994648438 ) ) ;
#2310=CARTESIAN_POINT ( 'NONE',  ( 1.723121472978328406, -33.06985636609709900, 7.742274884880762542 ) ) ;
#2316=CARTESIAN_POINT ( 'NONE',  ( 4.298799322723926508, -31.91476908534313850, 7.750000000000000888 ) ) ;
#2317=CARTESIAN_POINT ( 'NONE',  ( -1.337427566997555717, -27.83163680677632001, 7.635761828346574021 ) ) ;
#2321=DIRECTION ( 'NONE',  ( 0.3420201433256790380, -0.9396926207859046531, -0.000000000000000000 ) ) ;
#2327=CARTESIAN_POINT ( 'NONE',  ( 0.4918310210129015481, -32.74788313599579936, 6.894806418505344148 ) ) ;
#2328=CARTESIAN_POINT ( 'NONE',  ( 2.976970822604137368, -26.41868572423151207, 7.754798119455333705 ) ) ;
#2333=EDGE_CURVE ( 'NONE', #3701, #1652, #26316, .T. ) ;
#2340=CARTESIAN_POINT ( 'NONE',  ( -1.086373026989221113, -31.68746443619045650, 7.013842709614101167 ) ) ;
#2342=VERTEX_POINT ( 'NONE', #5204 ) ;
#2346=ORIENTED_EDGE ( 'NONE', *, *, #32057, .F. ) ;
#2348=DIRECTION ( 'NONE',  ( -0.4999999999999918954, -0.8660254037844432595, -0.000000000000000000 ) ) ;
#2352=CARTESIAN_POINT ( 'NONE',  ( -1.771784689607549979, -30.01038707958819174, 7.013842709614101167 ) ) ;
#2357=CARTESIAN_POINT ( 'NONE',  ( 1.578585683582427235, -32.96774767198657941, 7.754798119455333705 ) ) ;
#2361=CARTESIAN_POINT ( 'NONE',  ( 0.5360542692519894015, -32.87058578193457237, 7.678495282201401650 ) ) ;
#2367=CARTESIAN_POINT ( 'NONE',  ( 0.5039019691771889908, -32.85561263111923580, 7.767720160662273443 ) ) ;
#2371=CARTESIAN_POINT ( 'NONE',  ( 4.902329457098593579, -28.42639230875254341, 7.779495906702013741 ) ) ;
#2374=CARTESIAN_POINT ( 'NONE',  ( -0.5254690805390769270, -26.86890242742082080, 6.894806418505347700 ) ) ;
#2375=ORIENTED_EDGE ( 'NONE', *, *, #4167, .F. ) ;
#2376=CARTESIAN_POINT ( 'NONE',  ( 0.09894228122565373873, -26.45779829264445482, 7.013842709614101167 ) ) ;
#2380=CARTESIAN_POINT ( 'NONE',  ( 0.1190537080039397733, -26.56003401220450755, 6.865312560952603782 ) ) ;
#2382=CARTESIAN_POINT ( 'NONE',  ( -0.8913790868336790574, -27.21773604496269527, 6.870724624169666228 ) ) ;
#2383=CARTESIAN_POINT ( 'NONE',  ( 1.212546478539324957, -26.20509443716330722, 6.864651958020304257 ) ) ;
#2390=VECTOR ( 'NONE', #23325, 1000.000000000000114 ) ;
#2397=VECTOR ( 'NONE', #32821, 1000.000000000000000 ) ;
#2398=FACE_OUTER_BOUND ( 'NONE', #17268, .T. ) ;
#2403=ORIENTED_EDGE ( 'NONE', *, *, #33054, .F. ) ;
#2407=CARTESIAN_POINT ( 'NONE',  ( -0.1576164094376339420, -32.53604074034053895, 7.750000000000000888 ) ) ;
#2411=CARTESIAN_POINT ( 'NONE',  ( 2.486219537498463694, -26.26198458709621164, 6.911401339314955372 ) ) ;
#2412=CARTESIAN_POINT ( 'NONE',  ( -1.761252033055642707, -30.06883868682544758, 7.766640943994345569 ) ) ;
#2414=DIRECTION ( 'NONE',  ( 0.9848077530122080203, 0.1736481776669307198, -0.000000000000000000 ) ) ;
#2417=CARTESIAN_POINT ( 'NONE',  ( 3.905425806387133214, -32.15794714433188517, 7.652160403243384756 ) ) ;
#2421=( BOUNDED_CURVE ( )  B_SPLINE_CURVE ( 3, ( #4834, #24177, #33044, #1972 ),
 .UNSPECIFIED., .F., .T. ) 
 B_SPLINE_CURVE_WITH_KNOTS ( ( 4, 4 ),
 ( 4.708531083176467291, 4.895802057644187855 ),
 .UNSPECIFIED. ) 
 CURVE ( )  GEOMETRIC_REPRESENTATION_ITEM ( )  RATIONAL_B_SPLINE_CURVE ( ( 1.000000000000000000, 0.9970795998553221295, 0.9970795998553221295, 1.000000000000000000 ) ) 
 REPRESENTATION_ITEM ( '' )  );
#2422=CARTESIAN_POINT ( 'NONE',  ( 0.5045334820826082867, -26.37958808575769609, 7.257242401810563237 ) ) ;
#2426=CARTESIAN_POINT ( 'NONE',  ( -1.666358850447297923, -30.04427921204255014, 7.759451378593096749 ) ) ;
#2430=CARTESIAN_POINT ( 'NONE',  ( 4.846488009122917440, -30.85918098452591707, 6.865312560952602894 ) ) ;
#2431=VERTEX_POINT ( 'NONE', #31142 ) ;
#2432=CARTESIAN_POINT ( 'NONE',  ( 1.578585683582428345, -33.06757917596850405, 7.754798119455333705 ) ) ;
#2441=CARTESIAN_POINT ( 'NONE',  ( -1.534565338722829964, -28.23383362140880948, 6.877402575842993748 ) ) ;
#2445=ORIENTED_EDGE ( 'NONE', *, *, #4755, .F. ) ;
#2447=CARTESIAN_POINT ( 'NONE',  ( 3.355851366112005518, -32.53968674081319534, 6.892063359921934307 ) ) ;
#2448=CARTESIAN_POINT ( 'NONE',  ( 4.959554532356096779, -30.84580132059966573, 6.865554069792298542 ) ) ;
#2460=CARTESIAN_POINT ( 'NONE',  ( 2.868207633511080434, -32.86935470785505231, 6.894806418505347700 ) ) ;
#2461=CARTESIAN_POINT ( 'NONE',  ( 3.848298546108438245, -32.20554951821143419, 6.894806418505343260 ) ) ;
#2470=CYLINDRICAL_SURFACE ( 'NONE', #25330, 0.09010775117053081151 ) ;
#2473=CARTESIAN_POINT ( 'NONE',  ( 2.805807153542528187, -32.88323007867923309, 7.776484688137380807 ) ) ;
#2475=EDGE_LOOP ( 'NONE', ( #24880, #22470, #13430, #38232 ) ) ;
#2480=CARTESIAN_POINT ( 'NONE',  ( 3.481437286441587453, -32.58288071328335178, 7.686927408461905031 ) ) ;
#2481=VECTOR ( 'NONE', #30760, 1000.000000000000000 ) ;
#2482=CARTESIAN_POINT ( 'NONE',  ( 4.667181775993622495, -31.24519220632647887, 7.257242401810564125 ) ) ;
#2483=VECTOR ( 'NONE', #26320, 1000.000000000000000 ) ;
#2487=ORIENTED_EDGE ( 'NONE', *, *, #24774, .T. ) ;
#2488=PLANE ( 'NONE',  #30568 ) ;
#2493=ORIENTED_EDGE ( 'NONE', *, *, #16858, .T. ) ;
#2495=CARTESIAN_POINT ( 'NONE',  ( 5.401390093233090717, -29.51577928193538369, 7.695279973900954751 ) ) ;
#2499=CARTESIAN_POINT ( 'NONE',  ( -1.795329325813683541, -29.39687274210862711, 7.009310105710486738 ) ) ;
#2502=ORIENTED_EDGE ( 'NONE', *, *, #20115, .F. ) ;
#2503=AXIS2_PLACEMENT_3D ( 'NONE', #38822, #35761, #7535 ) ;
#2506=EDGE_CURVE ( 'NONE', #6019, #35491, #30780, .T. ) ;
#2507=VERTEX_POINT ( 'NONE', #466 ) ;
#2508=DIRECTION ( 'NONE',  ( -0.9396926207859007674, 0.3420201433256899737, 0.000000000000000000 ) ) ;
#2511=CARTESIAN_POINT ( 'NONE',  ( 5.135506051709807451, -30.24079465769465358, 6.870737987065013819 ) ) ;
#2513=CARTESIAN_POINT ( 'NONE',  ( 2.716088600019323618, -32.91931299483255202, 6.971170733404099984 ) ) ;
#2518=CARTESIAN_POINT ( 'NONE',  ( 5.197301300333582397, -29.56993018336890700, 7.767301406056524193 ) ) ;
#2521=CARTESIAN_POINT ( 'NONE',  ( 1.728381123661779206, -33.06982220562891683, 7.733670252284492008 ) ) ;
#2522=ORIENTED_EDGE ( 'NONE', *, *, #25016, .F. ) ;
#2528=CARTESIAN_POINT ( 'NONE',  ( 1.700390093233090871, -29.56993018339339940, 7.750000000000000888 ) ) ;
#2532=CARTESIAN_POINT ( 'NONE',  ( -0.5234024681467984719, -32.14186482873412842, 7.785868773668302545 ) ) ;
#2536=CARTESIAN_POINT ( 'NONE',  ( 5.029344116975409840, -28.48940719755995588, 7.753200566781599079 ) ) ;
#2548=CARTESIAN_POINT ( 'NONE',  ( 5.051054751933684805, -30.14703185982037681, 7.635761828346577573 ) ) ;
#2550=ORIENTED_EDGE ( 'NONE', *, *, #23247, .T. ) ;
#2560=CARTESIAN_POINT ( 'NONE',  ( -1.333134932519906446, -31.10541900397473825, 7.013842709614101167 ) ) ;
#2565=DIRECTION ( 'NONE',  ( 0.6427876096865369204, 0.7660444431189800119, 0.000000000000000000 ) ) ;
#2567=CARTESIAN_POINT ( 'NONE',  ( 5.153279172109078488, -30.14225614731512337, 7.695279973900954751 ) ) ;
#2571=CARTESIAN_POINT ( 'NONE',  ( -0.08061302505832330934, -26.55695359817150347, 7.698786668945011513 ) ) ;
#2572=DIRECTION ( 'NONE',  ( 0.5000000000000101030, -0.8660254037844328234, -0.000000000000000000 ) ) ;
#2574=CARTESIAN_POINT ( 'NONE',  ( 4.631989694572121508, -27.84779834644859875, 7.652160403243386533 ) ) ;
#2575=CARTESIAN_POINT ( 'NONE',  ( 4.999814617694763541, -28.40211264311544070, 6.894806418505347700 ) ) ;
#2577=ADVANCED_FACE ( 'NONE', ( #3172 ), #15687, .T. ) ;
#2589=CARTESIAN_POINT ( 'NONE',  ( 4.999814617694763541, -28.40211264311544070, 6.894806418505347700 ) ) ;
#2590=ADVANCED_FACE ( 'NONE', ( #9502 ), #22085, .T. ) ;
#2591=ADVANCED_FACE ( 'NONE', ( #15889 ), #28448, .F. ) ;
#2595=VERTEX_POINT ( 'NONE', #28110 ) ;
#2601=VERTEX_POINT ( 'NONE', #5892 ) ;
#2607=CARTESIAN_POINT ( 'NONE',  ( 4.370501521683438639, -27.46502734687952341, 6.864651958020305145 ) ) ;
#2612=CYLINDRICAL_SURFACE ( 'NONE', #25913, 0.09010775117053089478 ) ;
#2629=CARTESIAN_POINT ( 'NONE',  ( -1.661009635141104557, -30.08088777829730986, 7.782034975670476307 ) ) ;
#2630=EDGE_CURVE ( 'NONE', #2431, #25345, #244, .T. ) ;
#2632=CARTESIAN_POINT ( 'NONE',  ( -0.7779991009897547771, -25.20532047864482905, 7.695279973900954751 ) ) ;
#2638=ORIENTED_EDGE ( 'NONE', *, *, #3054, .F. ) ;
#2641=EDGE_CURVE ( 'NONE', #20325, #9389, #7639, .T. ) ;
#2645=ORIENTED_EDGE ( 'NONE', *, *, #17327, .T. ) ;
#2647=CARTESIAN_POINT ( 'NONE',  ( -1.517898193795411688, -28.19420277047165513, 6.965379264086543287 ) ) ;
#2649=CARTESIAN_POINT ( 'NONE',  ( -1.799609906766908463, -29.35564777783850232, 7.376841543590335171 ) ) ;
#2650=ORIENTED_EDGE ( 'NONE', *, *, #1328, .T. ) ;
#2652=CARTESIAN_POINT ( 'NONE',  ( 3.221468612762000028, -32.61070642268291664, 6.988553391373222290 ) ) ;
#2653=CARTESIAN_POINT ( 'NONE',  ( 4.924757601813157137, -30.93136360911756455, 6.903112506833882556 ) ) ;
#2655=CARTESIAN_POINT ( 'NONE',  ( 3.435168117181346847, -26.53010312597114506, 7.640616322432100205 ) ) ;
#2658=VERTEX_POINT ( 'NONE', #30607 ) ;
#2659=CARTESIAN_POINT ( 'NONE',  ( 4.262268152916126596, -27.17521612592422287, 7.139344958878409919 ) ) ;
#2662=CARTESIAN_POINT ( 'NONE',  ( -0.9575113486053222767, -31.84711263666175540, 7.695279973900954751 ) ) ;
#2667=CARTESIAN_POINT ( 'NONE',  ( -2.585338981833881000, -32.18494463595775557, 7.754798119455333705 ) ) ;
#2668=ORIENTED_EDGE ( 'NONE', *, *, #302, .F. ) ;
#2672=TOROIDAL_SURFACE ( 'NONE', #9877, 3.449999999999999289, 0.05000000000000000278 ) ;
#2676=CARTESIAN_POINT ( 'NONE',  ( -0.3920297796076317454, -26.89004521068930487, 7.757178535559532406 ) ) ;
#2677=ORIENTED_EDGE ( 'NONE', *, *, #39884, .T. ) ;
#2680=ORIENTED_EDGE ( 'NONE', *, *, #21939, .F. ) ;
#2691=CARTESIAN_POINT ( 'NONE',  ( 0.09894228122565373873, -26.45779829264445482, 7.013842709614101167 ) ) ;
#2694=ADVANCED_FACE ( 'NONE', ( #40446 ), #2672, .T. ) ;
#2695=ORIENTED_EDGE ( 'NONE', *, *, #15247, .F. ) ;
#2706=CARTESIAN_POINT ( 'NONE',  ( 0.8146142450545547087, -34.26560873126469176, 7.013842709614101167 ) ) ;
#2719=CARTESIAN_POINT ( 'NONE',  ( -0.9253594976165760988, -27.40996412519702830, 7.670860738520320687 ) ) ;
#2723=CARTESIAN_POINT ( 'NONE',  ( 5.100370998373280784, -29.55708692423313622, 7.756377446753162097 ) ) ;
#2724=CARTESIAN_POINT ( 'NONE',  ( 4.639361780851547934, -31.47058591824991680, 6.903112506833880779 ) ) ;
#2726=CARTESIAN_POINT ( 'NONE',  ( 4.200390093233091093, -29.56993018339339940, -8.199999999999999289 ) ) ;
#2733=CARTESIAN_POINT ( 'NONE',  ( -0.4535387154642924190, -26.81129727883429581, 7.753200566781576875 ) ) ;
#2740=VERTEX_POINT ( 'NONE', #32927 ) ;
#2741=CYLINDRICAL_SURFACE ( 'NONE', #12887, 3.399999999999999911 ) ;
#2747=CARTESIAN_POINT ( 'NONE',  ( -0.1692143551933917855, -32.40975312335586267, 6.997764925645182821 ) ) ;
#2750=CARTESIAN_POINT ( 'NONE',  ( 2.340111981911837002, -33.01097012869268355, 7.670465701733748531 ) ) ;
#2751=CARTESIAN_POINT ( 'NONE',  ( 1.823599949180766178, -26.07217602587316563, 7.753200566781576875 ) ) ;
#2752=CARTESIAN_POINT ( 'NONE',  ( 0.5849256341846700291, -26.35810200982117735, 7.785868773668302545 ) ) ;
#2755=CARTESIAN_POINT ( 'NONE',  ( 1.694295730800539301, -26.07130837915405053, 7.762796336881262249 ) ) ;
#2760=CARTESIAN_POINT ( 'NONE',  ( -1.693160655833844785, -29.36061310642847033, 6.969307238440506147 ) ) ;
#2763=CARTESIAN_POINT ( 'NONE',  ( -1.349486950856045642, -31.28699069785708531, 6.887161170156906209 ) ) ;
#2764=CARTESIAN_POINT ( 'NONE',  ( -1.266467741383816348, -27.71311663036093620, 7.751599049952198506 ) ) ;
#2770=CARTESIAN_POINT ( 'NONE',  ( 2.474049714983521664, -26.15650803111381606, 7.013842709614101167 ) ) ;
#2792=CARTESIAN_POINT ( 'NONE',  ( 2.960323002949313054, -26.41197514024928950, 6.864651958020303368 ) ) ;
#2793=CARTESIAN_POINT ( 'NONE',  ( 1.263448930281367844, -26.19810903602668617, 6.871394612369934762 ) ) ;
#2801=CARTESIAN_POINT ( 'NONE',  ( -0.9949275067606662137, -27.33715503357474930, 7.743886751744253338 ) ) ;
#2805=ADVANCED_FACE ( 'NONE', ( #6299 ), #37457, .T. ) ;
#2808=VERTEX_POINT ( 'NONE', #34933 ) ;
#2813=CARTESIAN_POINT ( 'NONE',  ( -1.315742883474435132, -31.34558487397897508, 7.660770905198780234 ) ) ;
#2817=CARTESIAN_POINT ( 'NONE',  ( -1.739541145475530959, -30.13246378897379429, 7.785096263473211486 ) ) ;
#2823=CARTESIAN_POINT ( 'NONE',  ( 5.057121750476042621, -29.02914024523307646, 7.785868773668302545 ) ) ;
#2825=EDGE_CURVE ( 'NONE', #17549, #39112, #30931, .T. ) ;
#2833=CARTESIAN_POINT ( 'NONE',  ( -1.656341564009858214, -30.11072012155374367, 7.785868773668302545 ) ) ;
#2834=DIRECTION ( 'NONE',  ( -0.1736481776669340227, 0.9848077530122074652, -0.000000000000000000 ) ) ;
#2839=B_SPLINE_CURVE_WITH_KNOTS ( 'NONE', 3,
 ( #25557, #657, #10300, #22480 ),
 .UNSPECIFIED., .F., .F.,
 ( 4, 4 ),
 ( 9.697399036122160616E-19, 6.391136169900461152E-06 ),
 .UNSPECIFIED. ) ;
#2842=CARTESIAN_POINT ( 'NONE',  ( 0.3635682928745467835, -32.69609516209911959, 7.013842709614101167 ) ) ;
#2848=CARTESIAN_POINT ( 'NONE',  ( -1.699073845469069255, -29.50955693216743114, 7.785172627573962778 ) ) ;
#2851=CARTESIAN_POINT ( 'NONE',  ( -1.338764679050899131, -31.09425634719163867, 6.911401339314953596 ) ) ;
#2855=CARTESIAN_POINT ( 'NONE',  ( 4.926836536535178723, -30.92641363086458384, 7.011627023500182965 ) ) ;
#2856=DIRECTION ( 'NONE',  ( 1.000000000000000000, 1.486905836551549118E-14, 0.000000000000000000 ) ) ;
#2857=PLANE ( 'NONE',  #34746 ) ;
#2864=EDGE_CURVE ( 'NONE', #14158, #12025, #25641, .T. ) ;
#2878=CARTESIAN_POINT ( 'NONE',  ( 1.804255514706574859, -26.17150069821536462, 6.864651958020304257 ) ) ;
#2885=CARTESIAN_POINT ( 'NONE',  ( -1.324540874619418718, -31.33056052611255637, 7.756742906098587298 ) ) ;
#2888=CARTESIAN_POINT ( 'NONE',  ( 1.686887486498432676, -33.27093018339341768, 7.635761828346577573 ) ) ;
#2889=PLANE ( 'NONE',  #3419 ) ;
#2902=EDGE_CURVE ( 'NONE', #30637, #7963, #23317, .T. ) ;
#2903=CARTESIAN_POINT ( 'NONE',  ( 4.747787266833422670, -31.29137887042594812, 7.720710062488892689 ) ) ;
#2904=( BOUNDED_CURVE ( )  B_SPLINE_CURVE ( 3, ( #18996, #40389, #3380, #3180 ),
 .UNSPECIFIED., .F., .T. ) 
 B_SPLINE_CURVE_WITH_KNOTS ( ( 4, 4 ),
 ( 4.708531083176465515, 4.895802057644187855 ),
 .UNSPECIFIED. ) 
 CURVE ( )  GEOMETRIC_REPRESENTATION_ITEM ( )  RATIONAL_B_SPLINE_CURVE ( ( 1.000000000000000000, 0.9970795998553221295, 0.9970795998553221295, 1.000000000000000000 ) ) 
 REPRESENTATION_ITEM ( '' )  );
#2907=CARTESIAN_POINT ( 'NONE',  ( 0.5786059417041748976, -26.26757555510396713, 7.782861076432730840 ) ) ;
#2911=ORIENTED_EDGE ( 'NONE', *, *, #27478, .T. ) ;
#2916=ORIENTED_EDGE ( 'NONE', *, *, #7749, .T. ) ;
#2917=CARTESIAN_POINT ( 'NONE',  ( 1.057242960569752199, -26.12952878737186424, 7.695279973900954751 ) ) ;
#2922=CARTESIAN_POINT ( 'NONE',  ( 2.853954305276058090, -32.87437726030070451, 6.880608371227949327 ) ) ;
#2929=CARTESIAN_POINT ( 'NONE',  ( 5.142386813909727294, -29.02333768617571508, 7.785593909369613819 ) ) ;
#2930=CARTESIAN_POINT ( 'NONE',  ( -1.347007080367232490, -27.84848149636083647, 7.720710062488895353 ) ) ;
#2935=ORIENTED_EDGE ( 'NONE', *, *, #27522, .T. ) ;
#2943=B_SPLINE_CURVE_WITH_KNOTS ( 'NONE', 3,
 ( #8887, #21469, #10802, #7928, #24543, #21673, #27827, #4846, #20683, #12184, #29958, #26869, #1984, #39004, #2752, #24754, #39415, #6024, #8114, #33060, #9098, #37302, #14504, #11206, #14301 ),
 .UNSPECIFIED., .F., .F.,
 ( 4, 3, 3, 3, 3, 3, 3, 3, 4 ),
 ( 6.468151674593461604E-05, 9.076621574722018343E-05, 0.0001210204262067970314, 0.0001512763324577426978, 0.0001815301820994211321, 0.0002117781465860719796, 0.0002420274594459745029, 0.0002722905548971148127, 0.0002816827545175550475 ),
 .UNSPECIFIED. ) ;
#2949=DIRECTION ( 'NONE',  ( -0.000000000000000000, -0.000000000000000000, -1.000000000000000000 ) ) ;
#2956=DIRECTION ( 'NONE',  ( 0.8660254037844449249, -0.4999999999999888423, -0.000000000000000000 ) ) ;
#2959=DIRECTION ( 'NONE',  ( 0.3420201433256790380, -0.9396926207859046531, -0.000000000000000000 ) ) ;
#2964=ORIENTED_EDGE ( 'NONE', *, *, #5617, .T. ) ;
#2965=VECTOR ( 'NONE', #35031, 1000.000000000000000 ) ;
#2966=CYLINDRICAL_SURFACE ( 'NONE', #10935, 3.399999999999999911 ) ;
#2969=CARTESIAN_POINT ( 'NONE',  ( 4.285954546368581752, -31.92892498175183746, 6.875780273367530171 ) ) ;
#2970=CARTESIAN_POINT ( 'NONE',  ( -1.698585778792500500, -29.48648546284218597, 6.870716933885664623 ) ) ;
#2972=CARTESIAN_POINT ( 'NONE',  ( -1.422033770034941691, -31.15121742542976335, 6.941203072598476354 ) ) ;
#2973=CARTESIAN_POINT ( 'NONE',  ( -1.784526601892259201, -29.51671012356495893, 7.785387725071483800 ) ) ;
#2976=EDGE_CURVE ( 'NONE', #8430, #5452, #25174, .T. ) ;
#2977=DIRECTION ( 'NONE',  ( 0.9396926207859001012, 0.3420201433256914170, 0.000000000000000000 ) ) ;
#2978=ORIENTED_EDGE ( 'NONE', *, *, #30502, .F. ) ;
#2980=CARTESIAN_POINT ( 'NONE',  ( 0.5338855275361950037, -32.86981913579896286, 7.670465701733744979 ) ) ;
#2982=CARTESIAN_POINT ( 'NONE',  ( 1.700390093233090871, -29.56993018339339940, 7.800000000000000711 ) ) ;
#2986=DIRECTION ( 'NONE',  ( -1.000000000000000000, 0.000000000000000000, 0.000000000000000000 ) ) ;
#2987=CARTESIAN_POINT ( 'NONE',  ( -0.9235197406764784622, -31.73212748787619120, 7.782167645815905921 ) ) ;
#2990=CARTESIAN_POINT ( 'NONE',  ( 2.082411851988426932, -32.94840020570687500, 6.949473656533219135 ) ) ;
#2995=VECTOR ( 'NONE', #37718, 1000.000000000000000 ) ;
#3001=ORIENTED_EDGE ( 'NONE', *, *, #18169, .T. ) ;
#3002=LINE ( 'NONE', #37943, #39012 ) ;
#3004=CARTESIAN_POINT ( 'NONE',  ( -1.423076598144291882, -28.22681595598903215, 6.903372536218456368 ) ) ;
#3006=CARTESIAN_POINT ( 'NONE',  ( 5.049684637985137670, -30.15498985193316983, 7.763628509615285722 ) ) ;
#3010=EDGE_CURVE ( 'NONE', #3356, #17087, #33242, .T. ) ;
#3013=CARTESIAN_POINT ( 'NONE',  ( -0.9919418010453353585, -27.33356058713898307, 7.750000000000000888 ) ) ;
#3019=CARTESIAN_POINT ( 'NONE',  ( -1.607058046179752786, -30.68314444182777478, 7.780491323090173772 ) ) ;
#3023=VERTEX_POINT ( 'NONE', #33034 ) ;
#3027=B_SPLINE_CURVE_WITH_KNOTS ( 'NONE', 3,
 ( #5222, #11777, #8288, #21076 ),
 .UNSPECIFIED., .F., .F.,
 ( 4, 4 ),
 ( 1.084202172485504434E-18, 6.391136169897158570E-06 ),
 .UNSPECIFIED. ) ;
#3028=CARTESIAN_POINT ( 'NONE',  ( -1.318021224226250565, -31.34171659909466001, 7.651421919295144036 ) ) ;
#3030=ADVANCED_FACE ( 'NONE', ( #29337 ), #13887, .F. ) ;
#3035=CARTESIAN_POINT ( 'NONE',  ( 1.700390093233090871, -29.56993018339339940, -8.199999999999999289 ) ) ;
#3037=CARTESIAN_POINT ( 'NONE',  ( 5.053861318879985021, -29.00936730667186936, 7.782167645815905033 ) ) ;
#3045=CARTESIAN_POINT ( 'NONE',  ( 4.990103580310159437, -30.76080248691535957, 7.762796336881261361 ) ) ;
#3046=CIRCLE ( 'NONE', #18788, 3.499999999999999556 ) ;
#3054=EDGE_CURVE ( 'NONE', #37103, #6285, #28374, .T. ) ;
#3058=ORIENTED_EDGE ( 'NONE', *, *, #31222, .F. ) ;
#3064=EDGE_CURVE ( 'NONE', #19164, #31083, #15949, .T. ) ;
#3071=CARTESIAN_POINT ( 'NONE',  ( 4.930099663604494253, -30.91864233902528980, 6.887547729233684635 ) ) ;
#3073=DIRECTION ( 'NONE',  ( 1.000000000000000000, 0.000000000000000000, 0.000000000000000000 ) ) ;
#3078=EDGE_CURVE ( 'NONE', #32722, #20830, #19948, .T. ) ;
#3083=ORIENTED_EDGE ( 'NONE', *, *, #35411, .T. ) ;
#3089=CARTESIAN_POINT ( 'NONE',  ( 4.093676667351576093, -27.01607437347052354, 6.941203072598475465 ) ) ;
#3091=CARTESIAN_POINT ( 'NONE',  ( -1.771784689607549979, -30.01038707958819174, 7.013842709614101167 ) ) ;
#3102=CARTESIAN_POINT ( 'NONE',  ( -1.646010885000422919, -28.96854075337417100, 7.775108481317160702 ) ) ;
#3103=ORIENTED_EDGE ( 'NONE', *, *, #31523, .T. ) ;
#3107=EDGE_CURVE ( 'NONE', #23038, #25920, #2184, .T. ) ;
#3108=VECTOR ( 'NONE', #34384, 1000.000000000000000 ) ;
#3111=ORIENTED_EDGE ( 'NONE', *, *, #5354, .F. ) ;
#3115=ORIENTED_EDGE ( 'NONE', *, *, #17962, .T. ) ;
#3117=EDGE_CURVE ( 'NONE', #20830, #6937, #38043, .T. ) ;
#3123=CARTESIAN_POINT ( 'NONE',  ( 0.6225211420409756391, -26.24003551177748861, 7.750000000000000888 ) ) ;
#3124=CARTESIAN_POINT ( 'NONE',  ( 0.4980641348985772043, -26.28438548574166234, 7.762796336881262249 ) ) ;
#3127=EDGE_CURVE ( 'NONE', #38408, #2507, #39654, .T. ) ;
#3130=CARTESIAN_POINT ( 'NONE',  ( 3.549680971525970286, -26.59936163035850498, 7.761113333117554802 ) ) ;
#3134=B_SPLINE_CURVE_WITH_KNOTS ( 'NONE', 3,
 ( #14995, #40109, #8603, #8803, #6148, #30869, #18689, #11483, #33554, #30446, #33749, #5529, #18073, #11889, #24886, #37424, #15400, #24672, #21388, #5738, #18480, #31068, #2878, #27957, #40501, #12311, #22064, #9696, #16074, #24271, #31646 ),
 .UNSPECIFIED., .F., .F.,
 ( 4, 3, 3, 3, 3, 3, 3, 3, 3, 3, 4 ),
 ( 2.168404344971008627E-19, 2.999644130997765844E-05, 6.002588995694966905E-05, 8.960886084588222161E-05, 0.0001190604700446502449, 0.0001489538463052725336, 0.0001796139255493988849, 0.0002109707048517092470, 0.0002426195318110382839, 0.0002740640997890069971, 0.0002849778069099863169 ),
 .UNSPECIFIED. ) ;
#3137=CARTESIAN_POINT ( 'NONE',  ( 0.5678122933612703704, -32.77574794603017949, 7.721096864323903297 ) ) ;
#3141=CARTESIAN_POINT ( 'NONE',  ( 5.100196023652643795, -29.53360033513232352, 7.701140543647732706 ) ) ;
#3142=CYLINDRICAL_SURFACE ( 'NONE', #4266, 0.09010775117052743921 ) ;
#3144=ORIENTED_EDGE ( 'NONE', *, *, #28255, .F. ) ;
#3146=VECTOR ( 'NONE', #27938, 999.9999999999998863 ) ;
#3149=B_SPLINE_CURVE_WITH_KNOTS ( 'NONE', 3,
 ( #24103, #33803, #37069, #5791, #33190, #11733, #39546, #11329, #38794, #35729, #24519, #11532, #4975, #10588, #34019, #36466, #2309, #8655, #7505 ),
 .UNSPECIFIED., .F., .F.,
 ( 4, 3, 3, 3, 3, 3, 4 ),
 ( 1.939479807224432123E-18, 2.546128104244549286E-05, 5.711050680484235597E-05, 8.113074941676337777E-05, 0.0001053129305727048827, 0.0001360598016347113902, 0.0001612931755702018660 ),
 .UNSPECIFIED. ) ;
#3152=EDGE_CURVE ( 'NONE', #5452, #37103, #727, .T. ) ;
#3155=EDGE_CURVE ( 'NONE', #24578, #14209, #12519, .T. ) ;
#3171=CARTESIAN_POINT ( 'NONE',  ( 2.327231899816259997, -33.01333973636840824, 7.643192810543819604 ) ) ;
#3172=FACE_OUTER_BOUND ( 'NONE', #19431, .T. ) ;
#3179=CARTESIAN_POINT ( 'NONE',  ( 4.746218651982971437, -31.29415061712129287, 7.660770905198780234 ) ) ;
#3180=CARTESIAN_POINT ( 'NONE',  ( 3.973866779147308570, -26.90885826429679284, 6.894806418505347700 ) ) ;
#3182=CARTESIAN_POINT ( 'NONE',  ( 4.312771555195475059, -31.89921506522781058, 6.863784140767622333 ) ) ;
#3183=CARTESIAN_POINT ( 'NONE',  ( -1.696924646384579738, -29.43445957933605683, 6.865312560952603782 ) ) ;
#3189=CARTESIAN_POINT ( 'NONE',  ( -0.6373138688605560764, -32.03876546204544695, 6.920489980334476599 ) ) ;
#3195=CARTESIAN_POINT ( 'NONE',  ( 0.5197218266442334977, -32.86477804699348582, 7.750000000000000888 ) ) ;
#3197=CARTESIAN_POINT ( 'NONE',  ( 2.137331256184830330, -32.94175133076011264, 6.871394612369936539 ) ) ;
#3202=VERTEX_POINT ( 'NONE', #39340 ) ;
#3205=CARTESIAN_POINT ( 'NONE',  ( 2.949167456357904893, -26.30028875085877971, 6.875671892026063325 ) ) ;
#3209=CARTESIAN_POINT ( 'NONE',  ( 5.041426625178103471, -28.52708634086149431, 6.887547729233689964 ) ) ;
#3210=LINE ( 'NONE', #35497, #6955 ) ;
#3211=CARTESIAN_POINT ( 'NONE',  ( 5.026336154413283630, -30.27568385775391491, 7.759451378593097637 ) ) ;
#3219=CARTESIAN_POINT ( 'NONE',  ( 1.700390093233090871, -29.56993018339339940, 7.800000000000000711 ) ) ;
#3222=AXIS2_PLACEMENT_3D ( 'NONE', #8894, #9305, #21477 ) ;
#3224=CARTESIAN_POINT ( 'NONE',  ( -1.676831472725793137, -29.96287608038002759, 6.911401339314957148 ) ) ;
#3228=CARTESIAN_POINT ( 'NONE',  ( 2.769712674093031790, -32.79741141385554215, 7.774064877406527962 ) ) ;
#3231=ORIENTED_EDGE ( 'NONE', *, *, #15623, .F. ) ;
#3234=ORIENTED_EDGE ( 'NONE', *, *, #28324, .F. ) ;
#3236=CARTESIAN_POINT ( 'NONE',  ( -1.321885274144181555, -31.33510862625826121, 7.640616322432100205 ) ) ;
#3237=EDGE_LOOP ( 'NONE', ( #16370, #19178, #33564, #34234 ) ) ;
#3241=CARTESIAN_POINT ( 'NONE',  ( 3.844353976790406247, -32.20876071027002041, 6.889465824494255486 ) ) ;
#3244=CARTESIAN_POINT ( 'NONE',  ( 4.326139684082770387, -31.72989624158975630, 7.670860738520324240 ) ) ;
#3245=CARTESIAN_POINT ( 'NONE',  ( 3.346956565312060761, -25.15115677713068365, 7.695279973900954751 ) ) ;
#3246=DIRECTION ( 'NONE',  ( -0.1736481776669207000, -0.9848077530122097967, -0.000000000000000000 ) ) ;
#3251=ORIENTED_EDGE ( 'NONE', *, *, #28369, .T. ) ;
#3254=CARTESIAN_POINT ( 'NONE',  ( 3.926249267005272436, -32.27095793936597090, 6.894806418505347700 ) ) ;
#3260=DIRECTION ( 'NONE',  ( -0.000000000000000000, -0.000000000000000000, -1.000000000000000000 ) ) ;
#3267=CARTESIAN_POINT ( 'NONE',  ( -1.724485732198442367, -28.92201308620781930, 7.785096263473211486 ) ) ;
#3274=AXIS2_PLACEMENT_3D ( 'NONE', #21161, #28351, #30847 ) ;
#3275=( BOUNDED_CURVE ( )  B_SPLINE_CURVE ( 3, ( #2328, #14444, #8060, #14849 ),
 .UNSPECIFIED., .F., .T. ) 
 B_SPLINE_CURVE_WITH_KNOTS ( ( 4, 4 ),
 ( 4.748221474220560623, 4.941946782021394924 ),
 .UNSPECIFIED. ) 
 CURVE ( )  GEOMETRIC_REPRESENTATION_ITEM ( )  RATIONAL_B_SPLINE_CURVE ( ( 1.000000000000000000, 0.9968749865767494445, 0.9968749865767494445, 1.000000000000000000 ) ) 
 REPRESENTATION_ITEM ( '' )  );
#3280=ORIENTED_EDGE ( 'NONE', *, *, #23460, .F. ) ;
#3281=ORIENTED_EDGE ( 'NONE', *, *, #24500, .T. ) ;
#3282=LINE ( 'NONE', #28358, #12863 ) ;
#3285=CARTESIAN_POINT ( 'NONE',  ( 5.014391224573804706, -30.32979629098898400, 6.882085323592686876 ) ) ;
#3290=CARTESIAN_POINT ( 'NONE',  ( 2.863609035986291573, -26.26888160889163615, 7.695279973900954751 ) ) ;
#3293=VECTOR ( 'NONE', #19856, 1000.000000000000000 ) ;
#3295=CARTESIAN_POINT ( 'NONE',  ( 0.1003003074055170557, -25.13424064674780922, 7.635761828346577573 ) ) ;
#3296=CARTESIAN_POINT ( 'NONE',  ( 4.650447641269607857, -27.87959612855872393, 7.775108481317163367 ) ) ;
#3305=DIRECTION ( 'NONE',  ( -0.8660254037844344888, -0.5000000000000069944, -0.000000000000000000 ) ) ;
#3308=CARTESIAN_POINT ( 'NONE',  ( -1.626039020774626032, -28.86646067482757871, 7.761597726988852308 ) ) ;
#3313=EDGE_CURVE ( 'NONE', #17660, #27165, #39960, .T. ) ;
#3324=DIRECTION ( 'NONE',  ( 0.6427876096865481337, -0.7660444431189707970, -0.000000000000000000 ) ) ;
#3327=ORIENTED_EDGE ( 'NONE', *, *, #28017, .F. ) ;
#3333=FACE_OUTER_BOUND ( 'NONE', #15770, .T. ) ;
#3337=ORIENTED_EDGE ( 'NONE', *, *, #14439, .T. ) ;
#3341=CARTESIAN_POINT ( 'NONE',  ( 5.100265157569299213, -29.54064031832051995, 7.730758795053803922 ) ) ;
#3344=ADVANCED_FACE ( 'NONE', ( #8045 ), #2308, .F. ) ;
#3345=CARTESIAN_POINT ( 'NONE',  ( 0.3101223678018852903, -32.78940688952906157, 7.387053503561888057 ) ) ;
#3348=CARTESIAN_POINT ( 'NONE',  ( -1.231676799035886338, -31.29127234582281147, 7.740055089680402567 ) ) ;
#3350=ORIENTED_EDGE ( 'NONE', *, *, #12600, .F. ) ;
#3354=ORIENTED_EDGE ( 'NONE', *, *, #9205, .T. ) ;
#3356=VERTEX_POINT ( 'NONE', #18327 ) ;
#3360=CARTESIAN_POINT ( 'NONE',  ( 4.956441579199191594, -28.59108968528456884, 6.903372536218457256 ) ) ;
#3366=ORIENTED_EDGE ( 'NONE', *, *, #22486, .F. ) ;
#3369=CARTESIAN_POINT ( 'NONE',  ( 2.900770107936768039, -26.38886395563813281, 7.784838882742139532 ) ) ;
#3370=ORIENTED_EDGE ( 'NONE', *, *, #30891, .F. ) ;
#3372=CARTESIAN_POINT ( 'NONE',  ( 2.342373490399764613, -33.01054969286393259, 7.678495282201403427 ) ) ;
#3373=DIRECTION ( 'NONE',  ( -1.000000000000000000, 0.000000000000000000, 0.000000000000000000 ) ) ;
#3380=CARTESIAN_POINT ( 'NONE',  ( 3.807509736567908032, -26.76673175688157968, 7.139344958878409919 ) ) ;
#3387=CARTESIAN_POINT ( 'NONE',  ( 1.525564357956455730, -33.06556116538863677, 7.006908160621414972 ) ) ;
#3388=EDGE_CURVE ( 'NONE', #36741, #20650, #2105, .T. ) ;
#3389=B_SPLINE_CURVE_WITH_KNOTS ( 'NONE', 3,
 ( #17700, #30277, #26789, #11118, #39739, #10920, #32777, #36062, #3828, #23878 ),
 .UNSPECIFIED., .F., .F.,
 ( 4, 3, 3, 4 ),
 ( 2.168404344971008868E-19, 3.025570593003233292E-05, 6.051145698344455873E-05, 6.468151674593992863E-05 ),
 .UNSPECIFIED. ) ;
#3390=DIRECTION ( 'NONE',  ( -0.8660254037844271613, 0.5000000000000200950, 0.000000000000000000 ) ) ;
#3397=CARTESIAN_POINT ( 'NONE',  ( -0.8852381447421843186, -31.77776508760973684, 7.730758795053809251 ) ) ;
#3399=CARTESIAN_POINT ( 'NONE',  ( 3.390724148067801202, -32.51998773142989307, 7.775108481317163367 ) ) ;
#3400=CARTESIAN_POINT ( 'NONE',  ( 1.667220786302370916, -26.17008988074897857, 7.670860738520328681 ) ) ;
#3401=B_SPLINE_CURVE_WITH_KNOTS ( 'NONE', 3,
 ( #1843, #20965, #33126, #17651 ),
 .UNSPECIFIED., .F., .F.,
 ( 4, 4 ),
 ( 0.000000000000000000, 6.391136169898815367E-06 ),
 .UNSPECIFIED. ) ;
#3404=CARTESIAN_POINT ( 'NONE',  ( -1.452474534483126467, -28.29735402062384253, 7.759451378593095860 ) ) ;
#3419=AXIS2_PLACEMENT_3D ( 'NONE', #21807, #34994, #19321 ) ;
#3429=B_SPLINE_CURVE_WITH_KNOTS ( 'NONE', 3,
 ( #3195, #18385, #21897, #2367, #28265, #18797, #88, #40209, #15711, #11992, #14886, #27455, #12210, #24572, #37123, #8911, #24782, #30970, #6460 ),
 .UNSPECIFIED., .F., .F.,
 ( 4, 3, 3, 3, 3, 3, 4 ),
 ( 2.453269466693398698E-18, 2.546128104244655335E-05, 5.711050680483562714E-05, 8.113074941675540888E-05, 0.0001053129305727054790, 0.0001360598016347109565, 0.0001612931755702008360 ),
 .UNSPECIFIED. ) ;
#3438=CARTESIAN_POINT ( 'NONE',  ( 1.601361038683358107, -32.96850034175079003, 7.774064877406528851 ) ) ;
#3441=CARTESIAN_POINT ( 'NONE',  ( -1.557213004826014435, -30.54360219153006284, 6.997764925645186374 ) ) ;
#3442=DIRECTION ( 'NONE',  ( 0.6834397476448847986, 0.000000000000000000, 0.7300069255418719649 ) ) ;
#3444=CARTESIAN_POINT ( 'NONE',  ( 5.200191349065117485, -29.60785068007726650, 6.887161170156909762 ) ) ;
#3446=CARTESIAN_POINT ( 'NONE',  ( 3.481437286441587453, -32.58288071328335178, 7.697032948437506406 ) ) ;
#3456=FACE_OUTER_BOUND ( 'NONE', #12785, .T. ) ;
#3459=ORIENTED_EDGE ( 'NONE', *, *, #39750, .T. ) ;
#3461=DIRECTION ( 'NONE',  ( -0.1736481776669268062, 0.9848077530122086864, 0.000000000000000000 ) ) ;
#3467=ORIENTED_EDGE ( 'NONE', *, *, #10335, .T. ) ;
#3473=ORIENTED_EDGE ( 'NONE', *, *, #26327, .F. ) ;
#3480=AXIS2_PLACEMENT_3D ( 'NONE', #28312, #12661, #22155 ) ;
#3487=CARTESIAN_POINT ( 'NONE',  ( -2.503969810797764151, -28.81487718949574983, 7.635761828346577573 ) ) ;
#3490=CARTESIAN_POINT ( 'NONE',  ( 1.822194502883781375, -26.17211269480022295, 7.754798119455333705 ) ) ;
#3491=CARTESIAN_POINT ( 'NONE',  ( -0.7974450458313169232, -25.21654760013375451, 7.635761828346577573 ) ) ;
#3495=ORIENTED_EDGE ( 'NONE', *, *, #811, .T. ) ;
#3501=CARTESIAN_POINT ( 'NONE',  ( 2.927923484755866834, -32.84760645976612636, 7.670465701733751196 ) ) ;
#3503=ORIENTED_EDGE ( 'NONE', *, *, #2976, .T. ) ;
#3509=( BOUNDED_CURVE ( )  B_SPLINE_CURVE ( 3, ( #29605, #26523, #39058, #13348 ),
 .UNSPECIFIED., .F., .T. ) 
 B_SPLINE_CURVE_WITH_KNOTS ( ( 4, 4 ),
 ( 4.748221474220560623, 4.941946782021394924 ),
 .UNSPECIFIED. ) 
 CURVE ( )  GEOMETRIC_REPRESENTATION_ITEM ( )  RATIONAL_B_SPLINE_CURVE ( ( 1.000000000000000000, 0.9968749865767494445, 0.9968749865767494445, 1.000000000000000000 ) ) 
 REPRESENTATION_ITEM ( '' )  );
#3511=ADVANCED_FACE ( 'NONE', ( #40553 ), #31521, .T. ) ;
#3514=VERTEX_POINT ( 'NONE', #19366 ) ;
#3515=ORIENTED_EDGE ( 'NONE', *, *, #21679, .T. ) ;
#3517=CARTESIAN_POINT ( 'NONE',  ( 4.743949789439241727, -28.05442871495747781, 6.969307238440504371 ) ) ;
#3518=CARTESIAN_POINT ( 'NONE',  ( 4.546323995280799224, -31.43022402557198092, 6.895222827070023541 ) ) ;
#3526=B_SPLINE_CURVE_WITH_KNOTS ( 'NONE', 3,
 ( #11962, #59, #31341, #22081, #252, #35256, #7025, #25770, #25564, #37689, #12791, #21867, #38307, #3369, #9912, #19387, #10103, #32168, #6222, #28654, #28233, #13000, #22691, #12588, #29060 ),
 .UNSPECIFIED., .F., .F.,
 ( 4, 3, 3, 3, 3, 3, 3, 3, 4 ),
 ( 6.468151674593313881E-05, 9.076621574722140316E-05, 0.0001210204262067985899, 0.0001512763324577444867, 0.0001815301820994240866, 0.0002117781465860715459, 0.0002420274594459770508, 0.0002722905548971173064, 0.0002816827545175549933 ),
 .UNSPECIFIED. ) ;
#3536=CARTESIAN_POINT ( 'NONE',  ( 5.099204911771554549, -29.65969559590484650, 7.778050822775633755 ) ) ;
#3537=CARTESIAN_POINT ( 'NONE',  ( -1.343629279779518182, -27.84251741988426687, 7.737115613922535218 ) ) ;
#3540=CARTESIAN_POINT ( 'NONE',  ( 3.852146645688039328, -32.33035474113215457, 7.750000000000000888 ) ) ;
#3551=LINE ( 'NONE', #1219, #16039 ) ;
#3552=CARTESIAN_POINT ( 'NONE',  ( 4.958069736096009095, -28.59650564702042885, 6.911401339314955372 ) ) ;
#3553=DIRECTION ( 'NONE',  ( 1.000000000000000000, 0.000000000000000000, 0.000000000000000000 ) ) ;
#3554=VERTEX_POINT ( 'NONE', #34224 ) ;
#3561=VERTEX_POINT ( 'NONE', #9687 ) ;
#3570=EDGE_LOOP ( 'NONE', ( #27467, #36982, #29080, #9143, #27593 ) ) ;
#3572=VECTOR ( 'NONE', #28694, 1000.000000000000000 ) ;
#3573=CARTESIAN_POINT ( 'NONE',  ( 1.728294629719529185, -26.08119623175329593, 7.781480525794719050 ) ) ;
#3577=CARTESIAN_POINT ( 'NONE',  ( -0.1307851662454839470, -32.55269768341421610, 6.863805608295729499 ) ) ;
#3580=CARTESIAN_POINT ( 'NONE',  ( -1.415111900810474443, -31.16482645844592625, 6.903112506833888773 ) ) ;
#3585=CARTESIAN_POINT ( 'NONE',  ( 1.665108719337590415, -26.07010776075642511, 7.707984471951055738 ) ) ;
#3588=EDGE_CURVE ( 'NONE', #32059, #27620, #29230, .T. ) ;
#3591=CARTESIAN_POINT ( 'NONE',  ( 4.944078209288079506, -30.88464969939810345, 7.750000000000000888 ) ) ;
#3592=CARTESIAN_POINT ( 'NONE',  ( -0.9721080757342911438, -31.67178857246723211, 7.768425012602590662 ) ) ;
#3593=CARTESIAN_POINT ( 'NONE',  ( 1.713892699967800581, -32.96990337146582561, 7.635761828346577573 ) ) ;
#3594=CARTESIAN_POINT ( 'NONE',  ( 1.664433243520564876, -26.17012032033359148, 7.693875151218753317 ) ) ;
#3599=DIRECTION ( 'NONE',  ( 0.000000000000000000, -0.7126435865141248494, 0.7015262779114442848 ) ) ;
#3604=CARTESIAN_POINT ( 'NONE',  ( 1.700390093233090871, -29.56993018339339940, 7.800000000000000711 ) ) ;
#3607=DIRECTION ( 'NONE',  ( 1.000000000000000000, 3.965082230804130614E-15, 0.000000000000000000 ) ) ;
#3610=CARTESIAN_POINT ( 'NONE',  ( -1.635225080001443621, -33.52415522258557701, 7.635761828346577573 ) ) ;
#3618=CARTESIAN_POINT ( 'NONE',  ( -1.659981793545334039, -30.08761321148581658, 6.874555630061442102 ) ) ;
#3632=CARTESIAN_POINT ( 'NONE',  ( -0.03896179826184579392, -32.60714627078814942, 7.756742906098588186 ) ) ;
#3635=CARTESIAN_POINT ( 'NONE',  ( -1.013064772776306688, -31.75849859061222347, 7.784725160561910329 ) ) ;
#3655=CARTESIAN_POINT ( 'NONE',  ( 5.671973749040267521, -26.25500220387225170, 7.635761828346577573 ) ) ;
#3667=VERTEX_POINT ( 'NONE', #22671 ) ;
#3678=CARTESIAN_POINT ( 'NONE',  ( -1.757012188144002840, -30.11440263980361465, 6.870737987065013819 ) ) ;
#3679=CARTESIAN_POINT ( 'NONE',  ( 4.285952550363297142, -27.36202013534370181, 7.661510568013097711 ) ) ;
#3681=PLANE ( 'NONE',  #7034 ) ;
#3686=CARTESIAN_POINT ( 'NONE',  ( -1.327607472881008110, -27.82106663299630611, 7.767720160662274331 ) ) ;
#3690=AXIS2_PLACEMENT_3D ( 'NONE', #12089, #6350, #21792 ) ;
#3693=FACE_OUTER_BOUND ( 'NONE', #16574, .T. ) ;
#3694=CARTESIAN_POINT ( 'NONE',  ( 4.630123336105056886, -27.84462688399876029, 7.730758795053809251 ) ) ;
#3701=VERTEX_POINT ( 'NONE', #23459 ) ;
#3709=VERTEX_POINT ( 'NONE', #7805 ) ;
#3712=B_SPLINE_CURVE_WITH_KNOTS ( 'NONE', 3,
 ( #24367, #35582, #10632, #38639, #24162, #7352, #21087, #23208, #2159, #5643, #32482, #2371, #36930, #33658, #995, #14889, #1205, #30354, #10828, #35973, #14680, #36721, #40013, #8709, #19909 ),
 .UNSPECIFIED., .F., .F.,
 ( 4, 3, 3, 3, 3, 3, 3, 3, 4 ),
 ( 6.468151674593633721E-05, 9.076621574722126763E-05, 0.0001210204262067980478, 0.0001512763324577447036, 0.0001815301820994257400, 0.0002117781465860766417, 0.0002420274594459822007, 0.0002722905548971199627, 0.0002816827545175661063 ),
 .UNSPECIFIED. ) ;
#3716=EDGE_CURVE ( 'NONE', #40022, #6547, #39412, .T. ) ;
#3718=CARTESIAN_POINT ( 'NONE',  ( 4.723729895314598082, -28.01446086209832842, 6.876076431790004051 ) ) ;
#3719=EDGE_CURVE ( 'NONE', #33808, #40124, #11473, .T. ) ;
#3720=CARTESIAN_POINT ( 'NONE',  ( 4.574815660364650149, -31.38590853778189782, 6.865312560952602894 ) ) ;
#3722=PLANE ( 'NONE',  #13917 ) ;
#3745=ORIENTED_EDGE ( 'NONE', *, *, #27944, .T. ) ;
#3748=( BOUNDED_CURVE ( )  B_SPLINE_CURVE ( 3, ( #27503, #40054, #24411, #8747 ),
 .UNSPECIFIED., .F., .T. ) 
 B_SPLINE_CURVE_WITH_KNOTS ( ( 4, 4 ),
 ( 4.708531083176467291, 4.895802057644189631 ),
 .UNSPECIFIED. ) 
 CURVE ( )  GEOMETRIC_REPRESENTATION_ITEM ( )  RATIONAL_B_SPLINE_CURVE ( ( 1.000000000000000000, 0.9970795998553221295, 0.9970795998553221295, 1.000000000000000000 ) ) 
 REPRESENTATION_ITEM ( '' )  );
#3754=ORIENTED_EDGE ( 'NONE', *, *, #10665, .F. ) ;
#3765=CARTESIAN_POINT ( 'NONE',  ( -1.697427395360086244, -29.44812577374269580, 7.754798119455333705 ) ) ;
#3770=ADVANCED_FACE ( 'NONE', ( #29831 ), #33751, .F. ) ;
#3773=CARTESIAN_POINT ( 'NONE',  ( 4.432911746439800460, -27.54673335294005199, 6.929923840112061306 ) ) ;
#3775=DIRECTION ( 'NONE',  ( 0.4999999999999855116, 0.8660254037844470343, 0.000000000000000000 ) ) ;
#3776=CARTESIAN_POINT ( 'NONE',  ( 0.5371228601270917613, -32.87096174259440318, 7.698786668945009737 ) ) ;
#3778=CARTESIAN_POINT ( 'NONE',  ( -0.9575113486053227208, -31.84711263666175540, 7.686927408461905920 ) ) ;
#3783=DIRECTION ( 'NONE',  ( 0.9848077530122103518, -0.1736481776669172583, -0.000000000000000000 ) ) ;
#3785=CARTESIAN_POINT ( 'NONE',  ( 1.681055494462310618, -26.06998307431192075, 7.747520101777647383 ) ) ;
#3790=CYLINDRICAL_SURFACE ( 'NONE', #39746, 0.09010775117052950700 ) ;
#3791=CARTESIAN_POINT ( 'NONE',  ( 1.736248384610752149, -32.96974108739077991, 7.691066658568946224 ) ) ;
#3792=CARTESIAN_POINT ( 'NONE',  ( 1.664466114274210318, -26.17011997221232278, 7.692469944509197965 ) ) ;
#3798=CARTESIAN_POINT ( 'NONE',  ( 2.625420455124711339, -26.29080307942845351, 7.505001789837626447 ) ) ;
#3803=CARTESIAN_POINT ( 'NONE',  ( -0.9222807936984492860, -27.27089925875410259, 7.782861076432730840 ) ) ;
#3807=CARTESIAN_POINT ( 'NONE',  ( 1.074608721727911664, -26.22801491291194864, 7.703977250142849620 ) ) ;
#3810=CARTESIAN_POINT ( 'NONE',  ( 4.404516770028684469, -31.79202354683301834, 7.695279973900954751 ) ) ;
#3816=CARTESIAN_POINT ( 'NONE',  ( 1.700390093233090871, -29.56993018339339940, 6.800000000000000711 ) ) ;
#3822=CARTESIAN_POINT ( 'NONE',  ( -1.708395779829353645, -28.77608428252948158, 6.976682809038451616 ) ) ;
#3825=ORIENTED_EDGE ( 'NONE', *, *, #28655, .F. ) ;
#3828=CARTESIAN_POINT ( 'NONE',  ( -1.261910041069867372, -27.90116479715461750, 7.693875151218753317 ) ) ;
#3836=ORIENTED_EDGE ( 'NONE', *, *, #2506, .T. ) ;
#3838=CARTESIAN_POINT ( 'NONE',  ( -0.9757923178187628555, -31.82346948261344366, 7.762796336881261361 ) ) ;
#3841=CARTESIAN_POINT ( 'NONE',  ( 3.417450607696787657, -32.61980722748252504, 6.887161170156907097 ) ) ;
#3843=FACE_OUTER_BOUND ( 'NONE', #13102, .T. ) ;
#3844=CARTESIAN_POINT ( 'NONE',  ( -0.5612858708501290428, -26.89882064179876409, 7.638132480492516585 ) ) ;
#3845=ORIENTED_EDGE ( 'NONE', *, *, #21407, .F. ) ;
#3847=AXIS2_PLACEMENT_3D ( 'NONE', #1253, #1447, #39291 ) ;
#3848=FACE_OUTER_BOUND ( 'NONE', #8797, .T. ) ;
#3851=FACE_OUTER_BOUND ( 'NONE', #25626, .T. ) ;
#3852=ORIENTED_EDGE ( 'NONE', *, *, #19159, .T. ) ;
#3862=CARTESIAN_POINT ( 'NONE',  ( 2.241180031393448235, -32.92666184063634205, 7.785868773668302545 ) ) ;
#3864=ORIENTED_EDGE ( 'NONE', *, *, #36921, .F. ) ;
#3869=CARTESIAN_POINT ( 'NONE',  ( -1.722734353762952475, -28.91418899491404915, 7.785344483711591934 ) ) ;
#3871=CARTESIAN_POINT ( 'NONE',  ( -1.280268548403576290, -31.20570797914146155, 6.874555630061442990 ) ) ;
#3876=CARTESIAN_POINT ( 'NONE',  ( 1.062037487868057184, -33.01122440958558002, 6.894806418505347700 ) ) ;
#3877=CARTESIAN_POINT ( 'NONE',  ( -1.786480958475062719, -29.49459066941995644, 7.782861076432731728 ) ) ;
#3880=CARTESIAN_POINT ( 'NONE',  ( 5.200206962362909913, -29.53412679592301870, 7.700536657684215136 ) ) ;
#3883=CARTESIAN_POINT ( 'NONE',  ( -0.9720661970843325062, -31.83001367219261013, 7.635761828346575797 ) ) ;
#3887=CYLINDRICAL_SURFACE ( 'NONE', #39222, 3.399999999999999911 ) ;
#3891=CARTESIAN_POINT ( 'NONE',  ( -0.5744564167362967710, -26.91002633704227875, 7.720710062488898906 ) ) ;
#3892=CARTESIAN_POINT ( 'NONE',  ( -1.292017994372690159, -27.78295751345079623, 7.785344483711591934 ) ) ;
#3899=CARTESIAN_POINT ( 'NONE',  ( -0.3376550272357887184, -26.84845906633096746, 6.895222827070021765 ) ) ;
#3900=CARTESIAN_POINT ( 'NONE',  ( 4.669725009344072753, -27.91368402659282921, 7.785868773668303433 ) ) ;
#3904=B_SPLINE_CURVE_WITH_KNOTS ( 'NONE', 3,
 ( #7597, #20149, #32729, #4525, #17046, #1438, #10873, #29819, #13971, #26539 ),
 .UNSPECIFIED., .F., .F.,
 ( 4, 3, 3, 4 ),
 ( 1.022834283856302764E-18, 3.025570593003180098E-05, 6.051145698344018127E-05, 6.468151674593884443E-05 ),
 .UNSPECIFIED. ) ;
#3907=CARTESIAN_POINT ( 'NONE',  ( 1.109803157764845061, -33.01974279738480789, 7.750000000000000888 ) ) ;
#3911=CARTESIAN_POINT ( 'NONE',  ( -0.3996106877581342420, -26.76992922016355436, 6.971170733404096431 ) ) ;
#3912=CARTESIAN_POINT ( 'NONE',  ( -1.543298022821887328, -28.25521066738867049, 7.750000000000000888 ) ) ;
#3915=ORIENTED_EDGE ( 'NONE', *, *, #8014, .T. ) ;
#3916=CARTESIAN_POINT ( 'NONE',  ( -1.722317759908783996, -28.83844474126830804, 7.750000000000000888 ) ) ;
#3922=ORIENTED_EDGE ( 'NONE', *, *, #30549, .T. ) ;
#3923=EDGE_LOOP ( 'NONE', ( #27975, #36477, #33008, #33198, #7175 ) ) ;
#3924=CARTESIAN_POINT ( 'NONE',  ( -0.002090259858060845594, -32.51298313013740682, 7.769368695748488207 ) ) ;
#3941=CARTESIAN_POINT ( 'NONE',  ( 5.076275776509211468, -29.16566689353966169, 6.895222827070021765 ) ) ;
#3943=CARTESIAN_POINT ( 'NONE',  ( 5.011198270955363299, -30.34358980514384285, 7.013842709614101167 ) ) ;
#3944=CARTESIAN_POINT ( 'NONE',  ( -1.765891609886502511, -30.05458793497804137, 7.751599049952173637 ) ) ;
#3947=EDGE_CURVE ( 'NONE', #2740, #7424, #22013, .T. ) ;
#3950=EDGE_CURVE ( 'NONE', #34664, #4150, #32091, .T. ) ;
#3958=ORIENTED_EDGE ( 'NONE', *, *, #11545, .T. ) ;
#3960=CARTESIAN_POINT ( 'NONE',  ( 4.954463893073100422, -28.58453498085037836, 7.013842709614101167 ) ) ;
#3961=CARTESIAN_POINT ( 'NONE',  ( 2.272716057154847924, -26.11704110451741556, 7.695279973900954751 ) ) ;
#3980=CARTESIAN_POINT ( 'NONE',  ( 2.255350295996689347, -26.21552723005750352, 7.703977250142848732 ) ) ;
#3983=CARTESIAN_POINT ( 'NONE',  ( 2.338742698598151204, -26.12863595720122234, 6.894806418505347700 ) ) ;
#3985=CARTESIAN_POINT ( 'NONE',  ( 0.7364113883766857382, -26.30944669709577610, 6.939395833800442226 ) ) ;
#3988=CARTESIAN_POINT ( 'NONE',  ( 1.144161204942605092, -32.92412392164827395, 7.712764235869103757 ) ) ;
#3989=CARTESIAN_POINT ( 'NONE',  ( -1.797340250851707344, -29.44390463015740522, 7.750000000000000888 ) ) ;
#3992=CARTESIAN_POINT ( 'NONE',  ( 3.397908533250484364, -32.51584789198624037, 7.769368695748488207 ) ) ;
#3993=CARTESIAN_POINT ( 'NONE',  ( -1.580282519025539401, -28.36646263432153248, 7.773839561854630986 ) ) ;
#3996=VECTOR ( 'NONE', #20602, 999.9999999999998863 ) ;
#3997=EDGE_CURVE ( 'NONE', #4296, #17900, #13329, .T. ) ;
#3999=ORIENTED_EDGE ( 'NONE', *, *, #21548, .F. ) ;
#4004=CARTESIAN_POINT ( 'NONE',  ( 1.700390093233090871, -29.56993018339339940, 7.750000000000000888 ) ) ;
#4009=CARTESIAN_POINT ( 'NONE',  ( 1.228243814321680949, -26.20287178139112072, 7.757178535559533294 ) ) ;
#4010=CARTESIAN_POINT ( 'NONE',  ( 4.390205000165592786, -31.80932647847912875, 7.635761828346570468 ) ) ;
#4012=VECTOR ( 'NONE', #16704, 1000.000000000000227 ) ;
#4013=LINE ( 'NONE', #26621, #39888 ) ;
#4015=DIRECTION ( 'NONE',  ( -1.000000000000000000, 0.000000000000000000, 0.000000000000000000 ) ) ;
#4019=CARTESIAN_POINT ( 'NONE',  ( -0.7969451277773216269, -31.88752197801528965, 7.139196562012274150 ) ) ;
#4021=EDGE_CURVE ( 'NONE', #14780, #4065, #28124, .T. ) ;
#4032=CARTESIAN_POINT ( 'NONE',  ( -1.544665293549569052, -28.25920506871950622, 7.754798119455333705 ) ) ;
#4035=VERTEX_POINT ( 'NONE', #32106 ) ;
#4038=CARTESIAN_POINT ( 'NONE',  ( 1.700390093233090871, -29.56993018339339940, 7.800000000000000711 ) ) ;
#4040=DIRECTION ( 'NONE',  ( -0.6427876096865235978, 0.7660444431189911141, 0.000000000000000000 ) ) ;
#4043=AXIS2_PLACEMENT_3D ( 'NONE', #30127, #39795, #38619 ) ;
#4044=CARTESIAN_POINT ( 'NONE',  ( 1.746865321026883189, -25.24062890126829828, 6.954324564059724878 ) ) ;
#4047=EDGE_CURVE ( 'NONE', #32530, #357, #22320, .T. ) ;
#4048=EDGE_LOOP ( 'NONE', ( #39370, #38765, #30452, #36692, #14431 ) ) ;
#4053=ORIENTED_EDGE ( 'NONE', *, *, #19621, .F. ) ;
#4056=CARTESIAN_POINT ( 'NONE',  ( 2.903857642304979336, -26.28925757113477957, 7.773839561854631874 ) ) ;
#4059=ORIENTED_EDGE ( 'NONE', *, *, #14400, .F. ) ;
#4060=CARTESIAN_POINT ( 'NONE',  ( 3.992580567114907719, -26.94342455530274449, 7.784725160561908552 ) ) ;
#4061=ORIENTED_EDGE ( 'NONE', *, *, #23923, .F. ) ;
#4064=CARTESIAN_POINT ( 'NONE',  ( -1.314124652899413048, -31.14241256655375523, 6.868387053540519815 ) ) ;
#4065=VERTEX_POINT ( 'NONE', #17823 ) ;
#4070=EDGE_CURVE ( 'NONE', #9920, #10407, #32597, .T. ) ;
#4074=CARTESIAN_POINT ( 'NONE',  ( 5.200212981237024579, -29.53471514687662136, 7.710604733652628440 ) ) ;
#4075=ADVANCED_FACE ( 'NONE', ( #14732 ), #1806, .F. ) ;
#4077=CARTESIAN_POINT ( 'NONE',  ( -0.5575963939758998844, -32.23273358912542363, 7.778495531946298058 ) ) ;
#4078=AXIS2_PLACEMENT_3D ( 'NONE', #2528, #22476, #35043 ) ;
#4080=CARTESIAN_POINT ( 'NONE',  ( 5.143799646208105258, -28.94308837681026247, 7.643192810543818716 ) ) ;
#4081=DIRECTION ( 'NONE',  ( -0.1736481776669333843, 0.9848077530122075762, 0.000000000000000000 ) ) ;
#4086=B_SPLINE_CURVE_WITH_KNOTS ( 'NONE', 3,
 ( #21493, #36518, #39811, #27852, #36925, #8499, #40404, #17968, #12208, #33458 ),
 .UNSPECIFIED., .F., .F.,
 ( 4, 3, 3, 4 ),
 ( 8.940560153363745023E-19, 3.025570593003112336E-05, 6.051145698344056074E-05, 6.468151674593758404E-05 ),
 .UNSPECIFIED. ) ;
#4087=CARTESIAN_POINT ( 'NONE',  ( 3.922602026865150471, -26.86590094501167059, 7.700536657684220465 ) ) ;
#4089=CARTESIAN_POINT ( 'NONE',  ( -0.3795852241544983574, -26.88035727981826994, 6.865312560952602894 ) ) ;
#4090=CARTESIAN_POINT ( 'NONE',  ( 4.700764115346282246, -27.97063167234916392, 7.761597726988848756 ) ) ;
#4116=CARTESIAN_POINT ( 'NONE',  ( 1.074608721727911442, -26.22801491291194864, 7.695279973900954751 ) ) ;
#4122=VERTEX_POINT ( 'NONE', #28332 ) ;
#4130=VERTEX_POINT ( 'NONE', #6109 ) ;
#4132=CARTESIAN_POINT ( 'NONE',  ( 5.068171392735082215, -29.10285614499638740, 6.863904403958576594 ) ) ;
#4137=CARTESIAN_POINT ( 'NONE',  ( 0.1120526303552441955, -32.69643921324515645, 7.139344958878412584 ) ) ;
#4143=ORIENTED_EDGE ( 'NONE', *, *, #24636, .T. ) ;
#4146=CARTESIAN_POINT ( 'NONE',  ( 2.186430707228644188, -33.03594076280592162, 7.753200566781576875 ) ) ;
#4148=ORIENTED_EDGE ( 'NONE', *, *, #23205, .T. ) ;
#4149=ADVANCED_FACE ( 'NONE', ( #33648 ), #24150, .F. ) ;
#4150=VERTEX_POINT ( 'NONE', #40004 ) ;
#4161=CARTESIAN_POINT ( 'NONE',  ( 2.394970551016177840, -26.13952796232410591, 6.864368109219935121 ) ) ;
#4162=CARTESIAN_POINT ( 'NONE',  ( 4.382959869488853855, -27.33051813421351994, 7.773839561854632763 ) ) ;
#4163=CARTESIAN_POINT ( 'NONE',  ( 6.040270069758088667, -32.09115252335679003, 7.635761828346577573 ) ) ;
#4166=CARTESIAN_POINT ( 'NONE',  ( 1.700390093233090871, -29.56993018339339940, 7.800000000000000711 ) ) ;
#4167=EDGE_CURVE ( 'NONE', #14186, #7610, #11775, .T. ) ;
#4169=ADVANCED_FACE ( 'NONE', ( #18377 ), #14877, .F. ) ;
#4170=CARTESIAN_POINT ( 'NONE',  ( 1.869561550574128761, -26.07402100007339740, 7.013842709614101167 ) ) ;
#4171=CARTESIAN_POINT ( 'NONE',  ( 1.686887486498407140, -26.06995622926011436, 7.635761828346576685 ) ) ;
#4173=CARTESIAN_POINT ( 'NONE',  ( -0.9644972916791141326, -31.83894080698376783, 7.651421919295144924 ) ) ;
#4176=LINE ( 'NONE', #38729, #9050 ) ;
#4177=CARTESIAN_POINT ( 'NONE',  ( 4.728387659347194294, -31.31879373379047848, 7.767720160662276996 ) ) ;
#4178=CARTESIAN_POINT ( 'NONE',  ( 0.7337844087288916128, -26.31022567980965121, 6.929923840112065747 ) ) ;
#4182=CARTESIAN_POINT ( 'NONE',  ( 1.050623329351162871, -32.90726492125749303, 7.785172627573962778 ) ) ;
#4184=CARTESIAN_POINT ( 'NONE',  ( 3.297628331390787260, -32.57140239904362033, 7.759451378593095860 ) ) ;
#4187=LINE ( 'NONE', #14232, #68 ) ;
#4190=DIRECTION ( 'NONE',  ( -0.7660444431189800119, -0.6427876096865369204, 0.000000000000000000 ) ) ;
#4192=CARTESIAN_POINT ( 'NONE',  ( 3.041304459685018724, -26.33696975259048756, 6.880828092187095457 ) ) ;
#4195=CARTESIAN_POINT ( 'NONE',  ( -1.600607472504411488, -28.40656649520510157, 7.700536657684219577 ) ) ;
#4197=CARTESIAN_POINT ( 'NONE',  ( 0.9148132382037100774, -32.87793322582781030, 6.997764925645181933 ) ) ;
#4198=CARTESIAN_POINT ( 'NONE',  ( 0.3249534634392911014, -32.78834191550933497, 6.945385021654666424 ) ) ;
#4199=CARTESIAN_POINT ( 'NONE',  ( -0.5626977249550375593, -26.90001753928526540, 7.750000000000002665 ) ) ;
#4200=ORIENTED_EDGE ( 'NONE', *, *, #10963, .T. ) ;
#4204=AXIS2_PLACEMENT_3D ( 'NONE', #11892, #27756, #18694 ) ;
#4205=CARTESIAN_POINT ( 'NONE',  ( -0.03438793071513444183, -32.60975724081566796, 7.640616322432101981 ) ) ;
#4209=CARTESIAN_POINT ( 'NONE',  ( -1.713501025485110407, -28.79831591363838683, 6.891695036779140970 ) ) ;
#4216=( BOUNDED_CURVE ( )  B_SPLINE_CURVE ( 3, ( #2691, #5342, #24688, #39922 ),
 .UNSPECIFIED., .F., .T. ) 
 B_SPLINE_CURVE_WITH_KNOTS ( ( 4, 4 ),
 ( 1.347909859412855127, 1.534781240595299634 ),
 .UNSPECIFIED. ) 
 CURVE ( )  GEOMETRIC_REPRESENTATION_ITEM ( )  RATIONAL_B_SPLINE_CURVE ( ( 1.000000000000000000, 0.9970920404276226723, 0.9970920404276226723, 1.000000000000000000 ) ) 
 REPRESENTATION_ITEM ( '' )  );
#4223=CARTESIAN_POINT ( 'NONE',  ( -0.09336860625537750369, -32.55799552926065843, 7.785593909369614707 ) ) ;
#4226=CARTESIAN_POINT ( 'NONE',  ( -1.337427566997555717, -27.83163680677632001, 7.635761828346574021 ) ) ;
#4227=CARTESIAN_POINT ( 'NONE',  ( 5.127407220394881726, -30.28097170179577091, 6.864216812889599062 ) ) ;
#4228=CARTESIAN_POINT ( 'NONE',  ( 5.198146613259219784, -29.69565482044479410, 6.867199677474200570 ) ) ;
#4230=CARTESIAN_POINT ( 'NONE',  ( -0.6172017013887949322, -27.07259496238298269, 7.139196562012275038 ) ) ;
#4235=CARTESIAN_POINT ( 'NONE',  ( 5.200390093233090205, -29.56993018339339940, 6.929570838012950595 ) ) ;
#4246=CARTESIAN_POINT ( 'NONE',  ( 2.896878217289016622, -26.28424773566757722, 7.767720160662274331 ) ) ;
#4247=CARTESIAN_POINT ( 'NONE',  ( 1.153797596015393667, -26.12793346271676498, 7.785593909369613819 ) ) ;
#4249=CARTESIAN_POINT ( 'NONE',  ( -1.750280548689878701, -28.98434346021053543, 7.646866513072558824 ) ) ;
#4254=CARTESIAN_POINT ( 'NONE',  ( 4.983308922979784228, -28.35648716565642857, 7.750000000000000000 ) ) ;
#4256=CARTESIAN_POINT ( 'NONE',  ( -1.269366464186706844, -31.22539145627230184, 6.892063359921934307 ) ) ;
#4258=ADVANCED_FACE ( 'NONE', ( #11984 ), #15087, .F. ) ;
#4260=CARTESIAN_POINT ( 'NONE',  ( 5.986119168300054305, -26.95491573082899706, 7.754798119455333705 ) ) ;
#4262=CARTESIAN_POINT ( 'NONE',  ( 4.163022776446456241, -25.19622345277205966, 7.695279973900954751 ) ) ;
#4266=AXIS2_PLACEMENT_3D ( 'NONE', #6609, #16263, #22463 ) ;
#4267=CARTESIAN_POINT ( 'NONE',  ( -1.773217931840104900, -29.99897723786583015, 6.998987538705435441 ) ) ;
#4268=CARTESIAN_POINT ( 'NONE',  ( 4.281704324602110923, -27.35705493990426262, 7.692469944509198854 ) ) ;
#4270=CARTESIAN_POINT ( 'NONE',  ( 4.720365337249898374, -27.80081420075986287, 7.743886751744251562 ) ) ;
#4274=CARTESIAN_POINT ( 'NONE',  ( 3.881713901294285396, -26.96188585715140107, 7.763628509615284834 ) ) ;
#4275=CARTESIAN_POINT ( 'NONE',  ( -1.576116513076069259, -30.80058222959184633, 7.700536657684210695 ) ) ;
#4280=CARTESIAN_POINT ( 'NONE',  ( 1.700390093233090871, -29.56993018339339940, 7.750000000000000888 ) ) ;
#4290=CARTESIAN_POINT ( 'NONE',  ( -0.4761956913552217729, -26.82902173683139679, 6.863805608295729499 ) ) ;
#4291=CARTESIAN_POINT ( 'NONE',  ( -1.381852710791847461, -31.22270215869128762, 7.766640943994346458 ) ) ;
#4292=AXIS2_PLACEMENT_3D ( 'NONE', #31777, #493, #19413 ) ;
#4293=EDGE_CURVE ( 'NONE', #40685, #23776, #35087, .T. ) ;
#4296=VERTEX_POINT ( 'NONE', #36513 ) ;
#4299=VECTOR ( 'NONE', #29453, 1000.000000000000000 ) ;
#4300=ORIENTED_EDGE ( 'NONE', *, *, #28965, .T. ) ;
#4302=ORIENTED_EDGE ( 'NONE', *, *, #10002, .F. ) ;
#4303=VERTEX_POINT ( 'NONE', #33453 ) ;
#4309=CARTESIAN_POINT ( 'NONE',  ( -0.06885977712395061068, -32.47334897749556859, 7.782034975670476307 ) ) ;
#4310=EDGE_CURVE ( 'NONE', #19528, #21404, #30343, .T. ) ;
#4331=ADVANCED_FACE ( 'NONE', ( #11574 ), #22513, .F. ) ;
#4333=CARTESIAN_POINT ( 'NONE',  ( 5.078111950526700724, -29.18133977915486099, 6.920489980334476599 ) ) ;
#4336=CARTESIAN_POINT ( 'NONE',  ( 5.090329724959301139, -29.91149280961422008, 7.505001789837621118 ) ) ;
#4338=CARTESIAN_POINT ( 'NONE',  ( -0.5096406291778409203, -26.98618015562372108, 7.721096864323899744 ) ) ;
#4340=CARTESIAN_POINT ( 'NONE',  ( 5.018694563533798281, -28.47163790933613825, 7.771081512783701406 ) ) ;
#4346=EDGE_CURVE ( 'NONE', #13345, #28759, #33084, .T. ) ;
#4352=CARTESIAN_POINT ( 'NONE',  ( -1.799609906766908685, -29.56993018339339940, 7.800000000000000711 ) ) ;
#4353=ORIENTED_EDGE ( 'NONE', *, *, #507, .T. ) ;
#4355=CARTESIAN_POINT ( 'NONE',  ( 3.799575776136275174, -32.37054073623617256, 6.951256099901591767 ) ) ;
#4361=CARTESIAN_POINT ( 'NONE',  ( 3.852146645688039328, -32.33035474113215457, 7.750000000000000888 ) ) ;
#4364=CARTESIAN_POINT ( 'NONE',  ( 2.477266370399229256, -26.15723709312290524, 7.010186378901970272 ) ) ;
#4366=PLANE ( 'NONE',  #9959 ) ;
#4374=CARTESIAN_POINT ( 'NONE',  ( -0.08235064813525205807, -32.58188673079869346, 6.887161170156905321 ) ) ;
#4376=CARTESIAN_POINT ( 'NONE',  ( 2.285449761772891719, -26.22063563864136171, 7.763628509615287498 ) ) ;
#4382=DIRECTION ( 'NONE',  ( -0.7541618601367555685, 0.000000000000000000, -0.6566885781822833223 ) ) ;
#4384=CARTESIAN_POINT ( 'NONE',  ( 1.004186251462368507, -32.89789583248860794, 7.768425012602594215 ) ) ;
#4385=CARTESIAN_POINT ( 'NONE',  ( 4.698894047304983168, -31.37521543190015905, 6.870737987065013819 ) ) ;
#4386=CARTESIAN_POINT ( 'NONE',  ( -1.799548180193444757, -29.59071677051289839, 7.745317755893211142 ) ) ;
#4388=CARTESIAN_POINT ( 'NONE',  ( -1.548293269840338660, -28.28698065990691646, 7.776484688137388801 ) ) ;
#4392=ADVANCED_FACE ( 'NONE', ( #9117 ), #40399, .F. ) ;
#4399=ORIENTED_EDGE ( 'NONE', *, *, #14362, .F. ) ;
#4403=CARTESIAN_POINT ( 'NONE',  ( 0.9110305502213149609, -32.87703034998288842, 6.988553391373221402 ) ) ;
#4404=CARTESIAN_POINT ( 'NONE',  ( 0.3731043410590647036, -32.80849661502264780, 6.872971584836694348 ) ) ;
#4408=CARTESIAN_POINT ( 'NONE',  ( -1.741823553407790603, -30.20331317155271478, 7.737115613922535218 ) ) ;
#4410=CARTESIAN_POINT ( 'NONE',  ( -0.03609309492223993637, -32.60878366570602083, 7.638132480492516585 ) ) ;
#4414=CARTESIAN_POINT ( 'NONE',  ( -1.712708766155947249, -28.79484523504865479, 7.012192614029402193 ) ) ;
#4420=CARTESIAN_POINT ( 'NONE',  ( -0.7622425899803056959, -33.94363691401473915, 7.695279973900954751 ) ) ;
#4430=EDGE_LOOP ( 'NONE', ( #38174, #23858, #21182, #37088, #18242 ) ) ;
#4434=CARTESIAN_POINT ( 'NONE',  ( -1.100220459609689394, -31.66911586629656838, 6.951256099901595320 ) ) ;
#4436=DIRECTION ( 'NONE',  ( -0.7660444431189813441, 0.6427876096865353661, -0.000000000000000000 ) ) ;
#4437=CARTESIAN_POINT ( 'NONE',  ( -2.726063116431162392, -27.94446379774605660, 7.635761828346577573 ) ) ;
#4439=CARTESIAN_POINT ( 'NONE',  ( 1.869561550574128761, -26.07402100007339740, 7.013842709614101167 ) ) ;
#4442=ORIENTED_EDGE ( 'NONE', *, *, #21963, .F. ) ;
#4450=EDGE_CURVE ( 'NONE', #21747, #35504, #7053, .T. ) ;
#4453=CARTESIAN_POINT ( 'NONE',  ( 2.992014398447776724, -26.32199281776421884, 7.771081512783698741 ) ) ;
#4454=CARTESIAN_POINT ( 'NONE',  ( 1.102287257230225581, -26.12705058514163525, 7.773839561854632763 ) ) ;
#4455=VERTEX_POINT ( 'NONE', #16310 ) ;
#4456=CARTESIAN_POINT ( 'NONE',  ( 5.054787681455045423, -30.12492281798062521, 7.692469944509195301 ) ) ;
#4457=B_SPLINE_CURVE_WITH_KNOTS ( 'NONE', 3,
 ( #18767, #461, #25155, #15885, #28857, #9290, #18984, #35056, #28444, #37902 ),
 .UNSPECIFIED., .F., .F.,
 ( 4, 3, 3, 4 ),
 ( 0.0005050348086185383559, 0.0005143352185143338934, 0.0005445898203825257468, 0.0005634294782181790886 ),
 .UNSPECIFIED. ) ;
#4466=CARTESIAN_POINT ( 'NONE',  ( 3.964423987650910419, -27.03334556693910429, 6.864651958020303368 ) ) ;
#4467=DIRECTION ( 'NONE',  ( -0.5000000000000036637, 0.8660254037844367092, 0.000000000000000000 ) ) ;
#4477=CARTESIAN_POINT ( 'NONE',  ( -1.501549270632406063, -30.71346805803427316, 7.779495906702013741 ) ) ;
#4478=DIRECTION ( 'NONE',  ( -0.8660254037844415942, 0.4999999999999950040, -0.000000000000000000 ) ) ;
#4479=CARTESIAN_POINT ( 'NONE',  ( -1.576062547484236243, -30.80072589882973944, 7.697032948437506406 ) ) ;
#4481=CARTESIAN_POINT ( 'NONE',  ( 3.972279103913426201, -32.23235770788113541, 7.730015791551950954 ) ) ;
#4484=CARTESIAN_POINT ( 'NONE',  ( 5.030284764849001000, -28.49206123220129783, 7.750000000000000888 ) ) ;
#4486=CARTESIAN_POINT ( 'NONE',  ( 2.704822964097302052, -32.92983929193388093, 7.387053503561887169 ) ) ;
#4489=AXIS2_PLACEMENT_3D ( 'NONE', #14466, #8081, #5217 ) ;
#4494=CARTESIAN_POINT ( 'NONE',  ( 1.096693473209699121, -26.22395493079927320, 7.635761828346577573 ) ) ;
#4495=CARTESIAN_POINT ( 'NONE',  ( -1.240463007521606764, -27.67219833340346113, 7.009310105710485850 ) ) ;
#4497=ORIENTED_EDGE ( 'NONE', *, *, #31027, .T. ) ;
#4502=EDGE_LOOP ( 'NONE', ( #16669, #5606, #37962, #29719 ) ) ;
#4508=CARTESIAN_POINT ( 'NONE',  ( 5.026513843668968917, -30.27484297658092061, 6.864216812889196717 ) ) ;
#4513=CARTESIAN_POINT ( 'NONE',  ( 4.662690227536056220, -31.23869556963216709, 7.693875151218752428 ) ) ;
#4516=ORIENTED_EDGE ( 'NONE', *, *, #16317, .T. ) ;
#4522=CARTESIAN_POINT ( 'NONE',  ( 0.4771275691783791184, -32.74226228095595559, 6.880147297696982633 ) ) ;
#4525=CARTESIAN_POINT ( 'NONE',  ( -0.5075199548166184904, -26.98436772626320490, 7.661510568013095046 ) ) ;
#4527=CARTESIAN_POINT ( 'NONE',  ( -1.639146693691649892, -28.93157757802832819, 6.894806418505346812 ) ) ;
#4532=CARTESIAN_POINT ( 'NONE',  ( 5.098207581826219581, -29.69173459304409946, 7.754798119455333705 ) ) ;
#4533=DIRECTION ( 'NONE',  ( 0.7660444431189771253, 0.6427876096865405842, -0.000000000000000000 ) ) ;
#4535=CARTESIAN_POINT ( 'NONE',  ( 3.870387127636869540, -26.95245864641162825, 7.643333865083954848 ) ) ;
#4537=CARTESIAN_POINT ( 'NONE',  ( -1.153862800135780464, -27.72243446737795125, 6.882085323592686876 ) ) ;
#4549=CARTESIAN_POINT ( 'NONE',  ( 4.772714607425114330, -27.89337953414514359, 6.865554069792297653 ) ) ;
#4554=EDGE_CURVE ( 'NONE', #16283, #19590, #26400, .T. ) ;
#4555=CARTESIAN_POINT ( 'NONE',  ( -1.226243465414398548, -31.30048392015029890, 7.680992449362119778 ) ) ;
#4556=ORIENTED_EDGE ( 'NONE', *, *, #12160, .F. ) ;
#4557=CARTESIAN_POINT ( 'NONE',  ( 2.497040581740529674, -26.16180034221845219, 6.955226052476382925 ) ) ;
#4558=CARTESIAN_POINT ( 'NONE',  ( 4.386463650923984048, -27.33967598338160343, 7.778495531946297170 ) ) ;
#4573=CARTESIAN_POINT ( 'NONE',  ( 4.639185200793720654, -27.65646266981928036, 7.139344958878412584 ) ) ;
#4575=ADVANCED_FACE ( 'NONE', ( #35474 ), #16905, .F. ) ;
#4576=DIRECTION ( 'NONE',  ( -1.000000000000000000, 0.000000000000000000, 0.000000000000000000 ) ) ;
#4578=CARTESIAN_POINT ( 'NONE',  ( 0.1132627511917800867, -26.45046942404118440, 6.989977667959447416 ) ) ;
#4580=CARTESIAN_POINT ( 'NONE',  ( 0.9946364188725682620, -32.89587624457358572, 7.759451378593097637 ) ) ;
#4581=CARTESIAN_POINT ( 'NONE',  ( 1.700390093233090871, -29.56993018339339940, 7.750000000000000888 ) ) ;
#4584=EDGE_CURVE ( 'NONE', #2595, #24834, #1171, .T. ) ;
#4587=CARTESIAN_POINT ( 'NONE',  ( 1.700390093233090871, -29.56993018339339940, 7.800000000000000711 ) ) ;
#4589=CARTESIAN_POINT ( 'NONE',  ( 3.070482080713194950, -26.34923958263044597, 6.921725064902947366 ) ) ;
#4594=CARTESIAN_POINT ( 'NONE',  ( 2.310642412388812961, -32.91472262586214015, 7.643333865083956624 ) ) ;
#4597=EDGE_LOOP ( 'NONE', ( #20473, #17904, #34990, #38022, #18712 ) ) ;
#4611=CARTESIAN_POINT ( 'NONE',  ( -1.629504578382812818, -30.64779913458552230, 7.750000000000000888 ) ) ;
#4612=ADVANCED_FACE ( 'NONE', ( #33599 ), #23695, .F. ) ;
#4629=CARTESIAN_POINT ( 'NONE',  ( 5.112556415631599904, -30.34910987273946148, 7.006908160621412307 ) ) ;
#4631=CARTESIAN_POINT ( 'NONE',  ( 2.679230591341950962, -32.82598166935948569, 6.903372536218455480 ) ) ;
#4633=CARTESIAN_POINT ( 'NONE',  ( 4.668948836787977896, -27.91232378075620701, 6.894806418505348589 ) ) ;
#4634=ORIENTED_EDGE ( 'NONE', *, *, #38564, .T. ) ;
#4637=ORIENTED_EDGE ( 'NONE', *, *, #8585, .T. ) ;
#4639=CARTESIAN_POINT ( 'NONE',  ( 0.1824275742476695050, -26.52759723137196701, 6.929923840112064859 ) ) ;
#4640=CARTESIAN_POINT ( 'NONE',  ( 2.876659513533784018, -26.27350604724992067, 7.743886751744251562 ) ) ;
#4641=PRODUCT_CONTEXT ( 'NONE', #11045, 'mechanical' ) ;
#4642=CARTESIAN_POINT ( 'NONE',  ( 2.287972448046889706, -32.91877281575333569, 7.769368695748486431 ) ) ;
#4643=CARTESIAN_POINT ( 'NONE',  ( -2.772340841568255776, -28.07161080258395103, 7.754798119455333705 ) ) ;
#4644=CARTESIAN_POINT ( 'NONE',  ( 5.141684319425215755, -30.20828278875847062, 6.894806418505347700 ) ) ;
#4647=EDGE_LOOP ( 'NONE', ( #28907, #11112, #23141, #1339, #24209 ) ) ;
#4651=FACE_OUTER_BOUND ( 'NONE', #11592, .T. ) ;
#4652=CYLINDRICAL_SURFACE ( 'NONE', #37650, 3.399999999999999911 ) ;
#4657=VECTOR ( 'NONE', #6665, 1000.000000000000114 ) ;
#4658=ADVANCED_FACE ( 'NONE', ( #29432 ), #26351, .F. ) ;
#4662=CARTESIAN_POINT ( 'NONE',  ( 1.490503839106549266, -32.96344572930279071, 6.959317978105165281 ) ) ;
#4663=CARTESIAN_POINT ( 'NONE',  ( 2.493137266801881413, -26.26364043220722877, 6.929923840112065747 ) ) ;
#4665=CARTESIAN_POINT ( 'NONE',  ( -1.529814622690701009, -30.63098279475522290, 7.768425012602592439 ) ) ;
#4666=CARTESIAN_POINT ( 'NONE',  ( 3.946934465176325624, -27.01784786054519216, 7.782034975670478083 ) ) ;
#4667=CARTESIAN_POINT ( 'NONE',  ( 1.700390093233090871, -29.56993018339339940, 7.750000000000000888 ) ) ;
#4669=CARTESIAN_POINT ( 'NONE',  ( 0.6026438237153681765, -26.24651957209255926, 6.863784140767622333 ) ) ;
#4670=CARTESIAN_POINT ( 'NONE',  ( 4.483263867588910934, -27.44727572642202063, 6.887547729233693516 ) ) ;
#4671=AXIS2_PLACEMENT_3D ( 'NONE', #17550, #39380, #21487 ) ;
#4672=CARTESIAN_POINT ( 'NONE',  ( 1.123053586962270423, -33.02198501472603454, 7.665454363767879364 ) ) ;
#4673=CARTESIAN_POINT ( 'NONE',  ( 4.271731398765316712, -31.79438740411119468, 6.892063359921928978 ) ) ;
#4674=CARTESIAN_POINT ( 'NONE',  ( -1.583399485992929234, -33.56764205940365997, 7.695279973900954751 ) ) ;
#4682=CARTESIAN_POINT ( 'NONE',  ( -1.255528973988210284, -27.69575237218189301, 6.875780273367530171 ) ) ;
#4683=CARTESIAN_POINT ( 'NONE',  ( 2.415520790285624386, -26.14641386366805520, 7.766640943994648438 ) ) ;
#4687=ORIENTED_EDGE ( 'NONE', *, *, #5684, .T. ) ;
#4689=ORIENTED_EDGE ( 'NONE', *, *, #21764, .F. ) ;
#4690=ORIENTED_EDGE ( 'NONE', *, *, #30724, .T. ) ;
#4696=CARTESIAN_POINT ( 'NONE',  ( 4.771399860080459909, -27.90595840320830234, 7.776484688137385248 ) ) ;
#4698=CARTESIAN_POINT ( 'NONE',  ( 0.02581832829155081277, -32.52895329133826863, 7.730758795053807475 ) ) ;
#4701=CARTESIAN_POINT ( 'NONE',  ( -1.242662853510920540, -27.86744983030224176, 7.769368695748485543 ) ) ;
#4705=CARTESIAN_POINT ( 'NONE',  ( 5.121754656661359206, -30.23353345891325006, 7.785593909369613819 ) ) ;
#4706=EDGE_LOOP ( 'NONE', ( #30056, #10455, #15653, #11096, #39480 ) ) ;
#4707=ADVANCED_FACE ( 'NONE', ( #25942 ), #1246, .F. ) ;
#4710=VERTEX_POINT ( 'NONE', #4527 ) ;
#4711=CARTESIAN_POINT ( 'NONE',  ( 1.128064129311358244, -33.02281926226938680, 7.701614758090453705 ) ) ;
#4714=CARTESIAN_POINT ( 'NONE',  ( 4.487153213455422396, -27.45239593059636363, 7.013842709614101167 ) ) ;
#4715=ORIENTED_EDGE ( 'NONE', *, *, #3010, .T. ) ;
#4716=FACE_OUTER_BOUND ( 'NONE', #4647, .T. ) ;
#4723=VERTEX_POINT ( 'NONE', #1441 ) ;
#4725=CARTESIAN_POINT ( 'NONE',  ( 3.425778817581328628, -32.49961169336884126, 7.661510568013098599 ) ) ;
#4726=AXIS2_PLACEMENT_3D ( 'NONE', #2234, #14755, #7975 ) ;
#4727=CARTESIAN_POINT ( 'NONE',  ( -1.206564353649571819, -27.80649297760044902, 6.874555630061442102 ) ) ;
#4729=ORIENTED_EDGE ( 'NONE', *, *, #29201, .T. ) ;
#4731=CARTESIAN_POINT ( 'NONE',  ( -1.609939828903696135, -30.70650248539039850, 6.870737987065014707 ) ) ;
#4737=CARTESIAN_POINT ( 'NONE',  ( 4.922922413687589760, -28.48582435662824963, 6.870716933885665512 ) ) ;
#4745=CARTESIAN_POINT ( 'NONE',  ( -1.225953191357326499, -31.30097466021442187, 7.693875151218753317 ) ) ;
#4755=EDGE_CURVE ( 'NONE', #19731, #33546, #12962, .T. ) ;
#4757=CARTESIAN_POINT ( 'NONE',  ( 1.664433243520564654, -26.07011488755866679, 7.685194954629195330 ) ) ;
#4762=CARTESIAN_POINT ( 'NONE',  ( 3.449177982490851502, -26.65415568621681075, 6.887041543973315250 ) ) ;
#4763=AXIS2_PLACEMENT_3D ( 'NONE', #31582, #10540, #3599 ) ;
#4764=CARTESIAN_POINT ( 'NONE',  ( 4.672854012516526545, -31.41284476466181630, 7.766640943994350010 ) ) ;
#4771=LINE ( 'NONE', #36081, #4012 ) ;
#4772=CARTESIAN_POINT ( 'NONE',  ( 4.313182060182604083, -31.74555727507705072, 7.756377446753161209 ) ) ;
#4776=EDGE_CURVE ( 'NONE', #12173, #26219, #17717, .T. ) ;
#4779=CARTESIAN_POINT ( 'NONE',  ( 3.076514354118595751, -26.35181238915100010, 6.961115707816235343 ) ) ;
#4782=DIRECTION ( 'NONE',  ( -0.000000000000000000, -0.000000000000000000, -1.000000000000000000 ) ) ;
#4784=CARTESIAN_POINT ( 'NONE',  ( 0.9102967148584886203, -32.87685623351212882, 6.920489980334477487 ) ) ;
#4785=CARTESIAN_POINT ( 'NONE',  ( -1.453630635037690411, -28.30022421521090337, 6.864276522220859711 ) ) ;
#4787=CARTESIAN_POINT ( 'NONE',  ( 0.3915459956710288236, -32.81601029087934052, 6.865706122441729065 ) ) ;
#4788=AXIS2_PLACEMENT_3D ( 'NONE', #10745, #7672, #20226 ) ;
#4791=ADVANCED_FACE ( 'NONE', ( #21239 ), #33811, .F. ) ;
#4793=EDGE_CURVE ( 'NONE', #34797, #22022, #12931, .T. ) ;
#4795=CARTESIAN_POINT ( 'NONE',  ( -0.03280221984780769956, -32.61066108333789515, 7.643192810543824933 ) ) ;
#4796=ORIENTED_EDGE ( 'NONE', *, *, #32659, .F. ) ;
#4806=EDGE_CURVE ( 'NONE', #13346, #38041, #12569, .T. ) ;
#4812=ORIENTED_EDGE ( 'NONE', *, *, #38697, .F. ) ;
#4816=CARTESIAN_POINT ( 'NONE',  ( 5.153606329123710417, -28.99954047225407905, 6.887161170156904433 ) ) ;
#4817=EDGE_LOOP ( 'NONE', ( #10398, #36335, #26717, #36229 ) ) ;
#4820=DIRECTION ( 'NONE',  ( 0.7660444431189740166, 0.6427876096865440259, 0.000000000000000000 ) ) ;
#4824=CARTESIAN_POINT ( 'NONE',  ( 2.458815852472819419, -32.89148182386498576, 7.139196562012271485 ) ) ;
#4827=CARTESIAN_POINT ( 'NONE',  ( 1.784616897348816789, -26.07094378080929431, 6.865554069792297653 ) ) ;
#4834=CARTESIAN_POINT ( 'NONE',  ( -0.9894248136993964993, -27.33053388830764874, 7.635761828346571356 ) ) ;
#4836=CARTESIAN_POINT ( 'NONE',  ( -0.8549290955373274326, -27.17820325474436771, 6.931070083220554068 ) ) ;
#4838=LINE ( 'NONE', #29947, #35065 ) ;
#4841=CARTESIAN_POINT ( 'NONE',  ( 5.054793046568992310, -30.12489038615697012, 7.695279973900954751 ) ) ;
#4846=CARTESIAN_POINT ( 'NONE',  ( 0.5254594208927613197, -26.37938586935893071, 7.756377446753165650 ) ) ;
#4851=VERTEX_POINT ( 'NONE', #2266 ) ;
#4860=CARTESIAN_POINT ( 'NONE',  ( 3.859195309938889817, -26.94322764099525003, 7.712764235869101093 ) ) ;
#4861=LINE ( 'NONE', #26495, #12202 ) ;
#4862=CARTESIAN_POINT ( 'NONE',  ( 0.6856660200322349796, -26.22025332505815598, 6.951256099901589991 ) ) ;
#4865=CARTESIAN_POINT ( 'NONE',  ( 1.108594127457504630, -33.01953560066821325, 7.638991368224661294 ) ) ;
#4870=FACE_OUTER_BOUND ( 'NONE', #12919, .T. ) ;
#4875=CARTESIAN_POINT ( 'NONE',  ( -1.626196100676897238, -28.86720385366933428, 6.864276522220859711 ) ) ;
#4877=ORIENTED_EDGE ( 'NONE', *, *, #28030, .T. ) ;
#4886=CARTESIAN_POINT ( 'NONE',  ( -1.518811278079208238, -28.19634271586866703, 6.974994249511789590 ) ) ;
#4889=CARTESIAN_POINT ( 'NONE',  ( -0.7646741769630207575, -27.22825162539180610, 6.969307238440508812 ) ) ;
#4894=CARTESIAN_POINT ( 'NONE',  ( -1.337427566997555717, -27.83163680677632001, 7.635761828346574021 ) ) ;
#4896=CYLINDRICAL_SURFACE ( 'NONE', #7430, 3.399999999999999911 ) ;
#4898=ORIENTED_EDGE ( 'NONE', *, *, #21253, .F. ) ;
#4899=CARTESIAN_POINT ( 'NONE',  ( 5.146918245836023864, -30.17145770867207588, 7.762796336881260473 ) ) ;
#4908=CARTESIAN_POINT ( 'NONE',  ( -1.512235554918550662, -28.43529712411073263, 7.257242401810563237 ) ) ;
#4918=CARTESIAN_POINT ( 'NONE',  ( -0.4994316697168441066, -26.97748265041383320, 7.748216051605117727 ) ) ;
#4921=DIRECTION ( 'NONE',  ( -1.000000000000000000, 0.000000000000000000, 0.000000000000000000 ) ) ;
#4926=CARTESIAN_POINT ( 'NONE',  ( -1.647480198169903431, -30.59059884262676121, 6.921725064902949143 ) ) ;
#4931=CARTESIAN_POINT ( 'NONE',  ( -1.744066689084928345, -30.19099175420856440, 7.635761828346576685 ) ) ;
#4936=CARTESIAN_POINT ( 'NONE',  ( 5.056857618328627346, -29.02759656560906976, 6.894806418505346812 ) ) ;
#4938=ORIENTED_EDGE ( 'NONE', *, *, #21078, .F. ) ;
#4941=CARTESIAN_POINT ( 'NONE',  ( 4.792398414354069658, -27.92993265294842331, 6.867199677474202346 ) ) ;
#4942=CARTESIAN_POINT ( 'NONE',  ( 4.312106210101242176, -27.39300398378253476, 7.775108481317161591 ) ) ;
#4950=CARTESIAN_POINT ( 'NONE',  ( 0.09453809279883360062, -26.57304938770676728, 7.768425012602595991 ) ) ;
#4951=CARTESIAN_POINT ( 'NONE',  ( 1.084781629859024710, -26.22612389321864512, 7.652160403243385645 ) ) ;
#4952=CARTESIAN_POINT ( 'NONE',  ( -1.794705841495275900, -29.38469240096594604, 6.989977667959445640 ) ) ;
#4965=CARTESIAN_POINT ( 'NONE',  ( -1.788417373966595170, -29.89300939100614940, 7.566278858797844897 ) ) ;
#4966=B_SPLINE_CURVE_WITH_KNOTS ( 'NONE', 3,
 ( #28927, #3632, #35327, #38175, #10168, #25430, #10578, #29329, #1146, #28722, #4223, #34721, #6501, #25836, #933, #35522, #25630, #9978, #19855 ),
 .UNSPECIFIED., .F., .F.,
 ( 4, 3, 3, 3, 3, 3, 4 ),
 ( 2.176562864887236392E-18, 2.546128104244634667E-05, 5.711050680483281499E-05, 8.113074941675401297E-05, 0.0001053129305727108458, 0.0001360598016347140465, 0.0001612931755702068262 ),
 .UNSPECIFIED. ) ;
#4967=FACE_OUTER_BOUND ( 'NONE', #29900, .T. ) ;
#4968=DIRECTION ( 'NONE',  ( -0.9396926207859058744, -0.3420201433256757628, -0.000000000000000000 ) ) ;
#4970=CARTESIAN_POINT ( 'NONE',  ( 0.07757799509440113650, -26.46888505406446512, 6.875780273367532835 ) ) ;
#4972=LINE ( 'NONE', #33602, #28616 ) ;
#4974=CARTESIAN_POINT ( 'NONE',  ( -1.032223829037264728, -34.03013334986905392, 7.013842709614101167 ) ) ;
#4975=CARTESIAN_POINT ( 'NONE',  ( 4.323060980164646239, -31.86896110803267490, 7.782861076432731728 ) ) ;
#4976=AXIS2_PLACEMENT_3D ( 'NONE', #25692, #19517, #29388 ) ;
#4981=DIRECTION ( 'NONE',  ( -0.5751513419797895654, -0.4826092789263638494, -0.6605219282605402364 ) ) ;
#4986=FACE_OUTER_BOUND ( 'NONE', #4597, .T. ) ;
#4988=EDGE_CURVE ( 'NONE', #9291, #14078, #36465, .T. ) ;
#4991=CARTESIAN_POINT ( 'NONE',  ( 0.4563090418891334044, -32.84136142028145144, 6.878641987404678027 ) ) ;
#4997=CARTESIAN_POINT ( 'NONE',  ( -0.02383034049480821370, -32.61575874214327087, 7.660770905198784675 ) ) ;
#5014=CARTESIAN_POINT ( 'NONE',  ( 1.626267501107426350, -33.06915981226823931, 6.867280401193707640 ) ) ;
#5018=CARTESIAN_POINT ( 'NONE',  ( 5.001438667734867671, -30.73314912614656436, 7.697032948437507294 ) ) ;
#5019=CARTESIAN_POINT ( 'NONE',  ( -1.699609906766909040, -29.50756078821139639, 7.152329793038292749 ) ) ;
#5022=CARTESIAN_POINT ( 'NONE',  ( 3.430329942220429640, -32.60247582573452263, 7.778495531946297170 ) ) ;
#5024=CARTESIAN_POINT ( 'NONE',  ( 5.121025113131824291, -30.31110547187388349, 6.870724624169667116 ) ) ;
#5025=CARTESIAN_POINT ( 'NONE',  ( 5.001438667734867671, -30.73314912614656436, 7.686927408461905920 ) ) ;
#5026=CARTESIAN_POINT ( 'NONE',  ( 2.663812202415797969, -32.83057702712517312, 6.959317978105163505 ) ) ;
#5027=CARTESIAN_POINT ( 'NONE',  ( 5.093942500299159626, -29.77923753713957922, 6.939395833800446667 ) ) ;
#5029=CARTESIAN_POINT ( 'NONE',  ( 1.890031703046834100, -26.07506968295128758, 6.931070083220556732 ) ) ;
#5030=CARTESIAN_POINT ( 'NONE',  ( 2.147225889248687736, -33.04129679599670055, 6.887547729233689964 ) ) ;
#5035=VERTEX_POINT ( 'NONE', #24685 ) ;
#5037=CARTESIAN_POINT ( 'NONE',  ( 0.1522824367581332439, -26.54282551325666617, 6.882085323592685988 ) ) ;
#5039=CARTESIAN_POINT ( 'NONE',  ( 3.048699747109260283, -26.44869756457103094, 6.911401339314957148 ) ) ;
#5040=( BOUNDED_CURVE ( )  B_SPLINE_CURVE ( 3, ( #22178, #8976, #6114, #31842 ),
 .UNSPECIFIED., .F., .T. ) 
 B_SPLINE_CURVE_WITH_KNOTS ( ( 4, 4 ),
 ( 1.381924640371168467, 1.574767692156077148 ),
 .UNSPECIFIED. ) 
 CURVE ( )  GEOMETRIC_REPRESENTATION_ITEM ( )  RATIONAL_B_SPLINE_CURVE ( ( 1.000000000000000000, 0.9969033633783032089, 0.9969033633783032089, 1.000000000000000000 ) ) 
 REPRESENTATION_ITEM ( '' )  );
#5042=CARTESIAN_POINT ( 'NONE',  ( -0.8539220219492742459, -27.17712883508125898, 6.971170733404098208 ) ) ;
#5047=ORIENTED_EDGE ( 'NONE', *, *, #11462, .T. ) ;
#5052=EDGE_CURVE ( 'NONE', #5880, #33546, #23899, .T. ) ;
#5053=CARTESIAN_POINT ( 'NONE',  ( 4.425213896693725779, -27.53636676661391647, 7.006423389747786779 ) ) ;
#5054=CARTESIAN_POINT ( 'NONE',  ( 3.956488544215869485, -27.02628791689333099, 6.866852738645442322 ) ) ;
#5057=ORIENTED_EDGE ( 'NONE', *, *, #635, .F. ) ;
#5062=CARTESIAN_POINT ( 'NONE',  ( 1.512295318426525759, -32.96472816114737725, 6.895222827070022653 ) ) ;
#5063=CARTESIAN_POINT ( 'NONE',  ( 2.423740107909631902, -26.24775251191726611, 6.865312560952602894 ) ) ;
#5065=CARTESIAN_POINT ( 'NONE',  ( -1.527091137229058981, -30.63925276425332811, 7.774064877406527074 ) ) ;
#5068=CARTESIAN_POINT ( 'NONE',  ( 0.6846915864468829938, -26.22054737195424323, 6.971170733404100872 ) ) ;
#5069=ADVANCED_FACE ( 'NONE', ( #36626 ), #27968, .F. ) ;
#5074=CARTESIAN_POINT ( 'NONE',  ( 4.501000646075883793, -27.47074450049024463, 6.951256099901593544 ) ) ;
#5077=ORIENTED_EDGE ( 'NONE', *, *, #19547, .F. ) ;
#5080=CARTESIAN_POINT ( 'NONE',  ( 2.231683959652603022, -33.01691039817721673, 7.782861076432731728 ) ) ;
#5086=CARTESIAN_POINT ( 'NONE',  ( -0.5913600112788022223, -32.21528109744426160, 6.875671892026064214 ) ) ;
#5092=CARTESIAN_POINT ( 'NONE',  ( -1.625555967947097225, -28.86417650903285548, 7.759451378593097637 ) ) ;
#5096=DIRECTION ( 'NONE',  ( -0.1736481776669340227, 0.9848077530122074652, -0.000000000000000000 ) ) ;
#5097=EDGE_LOOP ( 'NONE', ( #16309, #40363, #13808, #17192 ) ) ;
#5104=CARTESIAN_POINT ( 'NONE',  ( 4.749297472835600331, -31.28869828601962766, 7.695279973900954751 ) ) ;
#5108=CARTESIAN_POINT ( 'NONE',  ( 2.430498945370407782, -26.14692813174583108, 7.751599049952198506 ) ) ;
#5111=ADVANCED_FACE ( 'NONE', ( #34185 ), #2889, .F. ) ;
#5112=CARTESIAN_POINT ( 'NONE',  ( 4.976842733950423536, -28.33913446795707358, 7.695279973900954751 ) ) ;
#5119=B_SPLINE_CURVE_WITH_KNOTS ( 'NONE', 3,
 ( #12436, #103, #34089, #28491, #9337, #18600, #31793, #5865, #3006, #27672, #27873, #9546, #21916, #12225, #37344, #40227, #12636, #24804, #18813, #9139, #21713, #34492, #3211, #25207, #37737 ),
 .UNSPECIFIED., .F., .F.,
 ( 4, 3, 3, 3, 3, 3, 3, 3, 4 ),
 ( 6.468151674593740786E-05, 9.076621574721993949E-05, 0.0001210204262067974786, 0.0001512763324577440531, 0.0001815301820994204274, 0.0002117781465860696215, 0.0002420274594459737711, 0.0002722905548971171980, 0.0002816827545175588422 ),
 .UNSPECIFIED. ) ;
#5120=EDGE_CURVE ( 'NONE', #16194, #22132, #16226, .T. ) ;
#5121=CARTESIAN_POINT ( 'NONE',  ( 5.057666307568779551, -29.03261825887476988, 6.889465824494256374 ) ) ;
#5127=EDGE_LOOP ( 'NONE', ( #26350, #8424, #39154, #29092 ) ) ;
#5130=CARTESIAN_POINT ( 'NONE',  ( -1.158355754856540631, -27.72937577116574204, 6.876076431790005827 ) ) ;
#5131=ORIENTED_EDGE ( 'NONE', *, *, #28017, .T. ) ;
#5132=ORIENTED_EDGE ( 'NONE', *, *, #16450, .T. ) ;
#5140=VERTEX_POINT ( 'NONE', #12322 ) ;
#5150=CARTESIAN_POINT ( 'NONE',  ( 1.700390093233090871, -29.56993018339339940, 7.800000000000000711 ) ) ;
#5153=CARTESIAN_POINT ( 'NONE',  ( -0.02954803322811855662, -26.64293167151592456, 7.712764235869101093 ) ) ;
#5161=CARTESIAN_POINT ( 'NONE',  ( 6.019945922396399141, -27.01350538757900210, 7.695279973900954751 ) ) ;
#5162=LINE ( 'NONE', #17699, #664 ) ;
#5172=ORIENTED_EDGE ( 'NONE', *, *, #30683, .F. ) ;
#5174=FACE_OUTER_BOUND ( 'NONE', #15524, .T. ) ;
#5175=EDGE_CURVE ( 'NONE', #5140, #23918, #36779, .T. ) ;
#5178=CARTESIAN_POINT ( 'NONE',  ( 5.194214398482093209, -29.67280000852606392, 7.771081512783709400 ) ) ;
#5180=CARTESIAN_POINT ( 'NONE',  ( 0.05942261555421801678, -26.47845355906757447, 7.751599049952173637 ) ) ;
#5184=CARTESIAN_POINT ( 'NONE',  ( 3.293813124479239018, -32.57342865076346783, 7.754798119455333705 ) ) ;
#5187=CARTESIAN_POINT ( 'NONE',  ( -2.485163400083383323, -30.43163963246801984, 7.754798119455333705 ) ) ;
#5190=CARTESIAN_POINT ( 'NONE',  ( 3.890029461744421102, -32.17099692592865523, 7.763628509615289275 ) ) ;
#5194=CARTESIAN_POINT ( 'NONE',  ( 1.260455253761291861, -26.09768921580216627, 6.895394898881670898 ) ) ;
#5200=CARTESIAN_POINT ( 'NONE',  ( -0.1757080581666877195, -32.40546732307887368, 6.979335674598003969 ) ) ;
#5204=CARTESIAN_POINT ( 'NONE',  ( 1.105923466014343548, -33.01907637181788147, 7.635761828346575797 ) ) ;
#5206=CARTESIAN_POINT ( 'NONE',  ( -0.6444488087166562185, -32.16833941288422238, 7.750000000000000888 ) ) ;
#5215=CARTESIAN_POINT ( 'NONE',  ( -1.534173489221649866, -30.61759350290857284, 7.754798119455333705 ) ) ;
#5217=DIRECTION ( 'NONE',  ( 1.000000000000000000, 0.000000000000000000, 0.000000000000000000 ) ) ;
#5222=CARTESIAN_POINT ( 'NONE',  ( -1.057258846844102873, -31.72486802769777725, 7.754798119455333705 ) ) ;
#5226=CARTESIAN_POINT ( 'NONE',  ( 3.369241353962452390, -26.60767842677951833, 7.691066658568955106 ) ) ;
#5231=CARTESIAN_POINT ( 'NONE',  ( 5.095583499898731716, -29.75083557328108697, 6.887945620086122211 ) ) ;
#5237=VERTEX_POINT ( 'NONE', #32367 ) ;
#5240=CARTESIAN_POINT ( 'NONE',  ( 3.031610088737084041, -26.44136528038649203, 6.887945620086121323 ) ) ;
#5242=ADVANCED_FACE ( 'NONE', ( #32173 ), #32570, .F. ) ;
#5245=DIRECTION ( 'NONE',  ( 1.224646799147353207E-16, 1.000000000000000000, -0.000000000000000000 ) ) ;
#5248=ORIENTED_EDGE ( 'NONE', *, *, #9010, .F. ) ;
#5249=ORIENTED_EDGE ( 'NONE', *, *, #35976, .F. ) ;
#5263=ADVANCED_FACE ( 'NONE', ( #16491 ), #4366, .F. ) ;
#5264=CARTESIAN_POINT ( 'NONE',  ( 1.497294612651186796, -32.96385891360668552, 6.988553391373221402 ) ) ;
#5266=CARTESIAN_POINT ( 'NONE',  ( -1.534173489221649866, -30.61759350290857284, 7.754798119455333705 ) ) ;
#5267=CARTESIAN_POINT ( 'NONE',  ( 3.972827115442711055, -27.04089282105746861, 7.761597726988854973 ) ) ;
#5268=DIRECTION ( 'NONE',  ( 1.000000000000000000, 0.000000000000000000, 0.000000000000000000 ) ) ;
#5269=CARTESIAN_POINT ( 'NONE',  ( 0.6655969032795109319, -26.22639806170147025, 7.011627023500184741 ) ) ;
#5270=DIRECTION ( 'NONE',  ( 1.000000000000000000, 0.000000000000000000, 0.000000000000000000 ) ) ;
#5271=AXIS2_PLACEMENT_3D ( 'NONE', #34935, #6512, #136 ) ;
#5273=CARTESIAN_POINT ( 'NONE',  ( -0.4281225035922071043, -26.91860427732644467, 6.874555630061442102 ) ) ;
#5276=( BOUNDED_CURVE ( )  B_SPLINE_CURVE ( 3, ( #17440, #27341, #39901, #11675 ),
 .UNSPECIFIED., .F., .T. ) 
 B_SPLINE_CURVE_WITH_KNOTS ( ( 4, 4 ),
 ( 1.347909859412854905, 1.534781240595299412 ),
 .UNSPECIFIED. ) 
 CURVE ( )  GEOMETRIC_REPRESENTATION_ITEM ( )  RATIONAL_B_SPLINE_CURVE ( ( 1.000000000000000000, 0.9970920404276226723, 0.9970920404276226723, 1.000000000000000000 ) ) 
 REPRESENTATION_ITEM ( '' )  );
#5282=CYLINDRICAL_SURFACE ( 'NONE', #6961, 0.09010775117052866046 ) ;
#5286=CARTESIAN_POINT ( 'NONE',  ( 4.842674212786914900, -30.86841026102256791, 6.868387053540519815 ) ) ;
#5287=CARTESIAN_POINT ( 'NONE',  ( -1.628373570674043425, -28.87751162402568639, 6.864651958020304257 ) ) ;
#5289=CARTESIAN_POINT ( 'NONE',  ( -0.6209176402083074198, -32.18940249604951731, 6.863805608295729499 ) ) ;
#5294=CARTESIAN_POINT ( 'NONE',  ( -1.524383821632846470, -28.20947427840861366, 7.006248344249653037 ) ) ;
#5298=CARTESIAN_POINT ( 'NONE',  ( 4.777565610504584726, -27.91210591261665641, 7.771081512783700518 ) ) ;
#5303=B_SPLINE_CURVE_WITH_KNOTS ( 'NONE', 3,
 ( #23243, #25931, #4899, #13964, #10664, #26733, #35613, #1624, #26341, #17430, #4705, #14159, #26137, #39270, #20141, #7384, #26530, #11062, #17036 ),
 .UNSPECIFIED., .F., .F.,
 ( 4, 3, 3, 3, 3, 3, 4 ),
 ( 0.000000000000000000, 2.546128104244995842E-05, 5.711050680484009269E-05, 8.113074941675803807E-05, 0.0001053129305727061295, 0.0001360598016347041260, 0.0001612931755702019473 ),
 .UNSPECIFIED. ) ;
#5305=DIRECTION ( 'NONE',  ( -1.000000000000000000, 0.000000000000000000, 0.000000000000000000 ) ) ;
#5307=CARTESIAN_POINT ( 'NONE',  ( -1.084049423045779115, -33.98664651305095674, 6.954324564059724878 ) ) ;
#5308=B_SPLINE_CURVE_WITH_KNOTS ( 'NONE', 3,
 ( #15983, #25060, #28550, #2848, #15581, #361, #6120, #9192, #12898, #38008, #28135, #25266, #18654 ),
 .UNSPECIFIED., .F., .F.,
 ( 4, 3, 3, 3, 4 ),
 ( 0.0002056071264154448830, 0.0002117781465860642546, 0.0002420274594459682145, 0.0002722905548971127528, 0.0002816827545175561317 ),
 .UNSPECIFIED. ) ;
#5309=LINE ( 'NONE', #27326, #11344 ) ;
#5318=CARTESIAN_POINT ( 'NONE',  ( 4.984671627384348547, -28.36018029005467866, 7.635761828346577573 ) ) ;
#5327=FACE_OUTER_BOUND ( 'NONE', #24655, .T. ) ;
#5329=CARTESIAN_POINT ( 'NONE',  ( -0.4693117693055204320, -26.95220437874807118, 7.779495906702012853 ) ) ;
#5335=ORIENTED_EDGE ( 'NONE', *, *, #30710, .T. ) ;
#5342=CARTESIAN_POINT ( 'NONE',  ( -0.09519644969557856939, -26.55769863645182483, 7.255881584735164758 ) ) ;
#5344=EDGE_CURVE ( 'NONE', #21663, #16587, #20465, .T. ) ;
#5347=CARTESIAN_POINT ( 'NONE',  ( 0.03159606602598123704, -32.53221418380139340, 7.692469944509198854 ) ) ;
#5351=CARTESIAN_POINT ( 'NONE',  ( 4.281682929012584182, -27.35702998321412593, 7.695279973900954751 ) ) ;
#5352=ORIENTED_EDGE ( 'NONE', *, *, #4167, .T. ) ;
#5354=EDGE_CURVE ( 'NONE', #20784, #5955, #9486, .T. ) ;
#5357=EDGE_LOOP ( 'NONE', ( #19533, #37436, #32519, #36112 ) ) ;
#5359=CARTESIAN_POINT ( 'NONE',  ( 1.074641032650325734, -26.22800886213295968, 7.692469944509198854 ) ) ;
#5367=CYLINDRICAL_SURFACE ( 'NONE', #17531, 0.09010775117052900740 ) ;
#5370=CARTESIAN_POINT ( 'NONE',  ( 5.138907313317528924, -30.22313780932130456, 6.880608371227949327 ) ) ;
#5371=CARTESIAN_POINT ( 'NONE',  ( 2.817966617839567700, -32.88670914974743198, 6.865554069792297653 ) ) ;
#5372=ORIENTED_EDGE ( 'NONE', *, *, #26630, .F. ) ;
#5374=CARTESIAN_POINT ( 'NONE',  ( 0.09941021755798716553, -26.45755754540749649, 6.895394898881670898 ) ) ;
#5381=EDGE_CURVE ( 'NONE', #5651, #5955, #33386, .T. ) ;
#5383=ORIENTED_EDGE ( 'NONE', *, *, #22574, .F. ) ;
#5387=EDGE_CURVE ( 'NONE', #35810, #38896, #5768, .T. ) ;
#5389=VERTEX_POINT ( 'NONE', #30071 ) ;
#5390=CARTESIAN_POINT ( 'NONE',  ( -0.5758167276443872939, -25.38032712238630495, 6.954324564059724878 ) ) ;
#5396=CARTESIAN_POINT ( 'NONE',  ( 1.282747240999764005, -26.09493745707318269, 6.951256099901592655 ) ) ;
#5404=ORIENTED_EDGE ( 'NONE', *, *, #32196, .T. ) ;
#5415=CARTESIAN_POINT ( 'NONE',  ( 3.477536630118434058, -26.67135291403582187, 7.778050822775628426 ) ) ;
#5418=CARTESIAN_POINT ( 'NONE',  ( -1.772036214352060046, -30.00840427972128666, 7.011627023500184741 ) ) ;
#5420=DIRECTION ( 'NONE',  ( 0.1736481776669333843, -0.9848077530122075762, 0.000000000000000000 ) ) ;
#5422=FACE_OUTER_BOUND ( 'NONE', #22342, .T. ) ;
#5431=DIRECTION ( 'NONE',  ( -0.8660254037844345998, -0.5000000000000071054, -0.000000000000000000 ) ) ;
#5433=CARTESIAN_POINT ( 'NONE',  ( 5.096859737624582998, -29.72513773616743649, 6.871394612369937427 ) ) ;
#5445=CARTESIAN_POINT ( 'NONE',  ( 0.1758335091890310398, -26.53089376604643590, 6.997764925645182821 ) ) ;
#5447=CARTESIAN_POINT ( 'NONE',  ( 2.913702424011483938, -26.39378773199812400, 6.889465824494256374 ) ) ;
#5448=CARTESIAN_POINT ( 'NONE',  ( -0.9508493577463464907, -27.28497717535191214, 6.880608371227950215 ) ) ;
#5449=CARTESIAN_POINT ( 'NONE',  ( 1.272770162583354514, -26.19691824104105748, 6.876076431790004051 ) ) ;
#5452=VERTEX_POINT ( 'NONE', #15426 ) ;
#5456=EDGE_CURVE ( 'NONE', #1177, #23554, #5970, .T. ) ;
#5462=EDGE_LOOP ( 'NONE', ( #30702, #33894, #15950, #21765 ) ) ;
#5471=CARTESIAN_POINT ( 'NONE',  ( 2.480576858534745188, -26.26064724879598344, 7.006423389747790331 ) ) ;
#5474=CARTESIAN_POINT ( 'NONE',  ( -0.03448549664302677509, -32.60970101154014600, 7.750000000000000000 ) ) ;
#5488=CARTESIAN_POINT ( 'NONE',  ( 4.878343045835490166, -30.77848925561357873, 6.894806418505348589 ) ) ;
#5491=CARTESIAN_POINT ( 'NONE',  ( -0.6881146421603261398, -32.12826045096961991, 6.989977667959442975 ) ) ;
#5497=CARTESIAN_POINT ( 'NONE',  ( -1.549564175422862622, -28.27077767054321455, 6.864673517077424236 ) ) ;
#5504=CARTESIAN_POINT ( 'NONE',  ( 3.248497749708064486, -32.59703485353012553, 6.882085323592685988 ) ) ;
#5509=CARTESIAN_POINT ( 'NONE',  ( -1.586485268957895434, -30.74699233443655544, 7.778495531946295394 ) ) ;
#5516=CARTESIAN_POINT ( 'NONE',  ( 1.044648904753755714, -32.99305463038944453, 7.785344483711591934 ) ) ;
#5520=DIRECTION ( 'NONE',  ( 0.5000000000000101030, -0.8660254037844328234, -0.000000000000000000 ) ) ;
#5522=CARTESIAN_POINT ( 'NONE',  ( 2.931185808669444448, -32.84638282411071941, 7.695279973900954751 ) ) ;
#5524=CARTESIAN_POINT ( 'NONE',  ( 4.077110055691020918, -27.00064969655394620, 7.013842709614101167 ) ) ;
#5527=DIRECTION ( 'NONE',  ( 0.9848077530122103518, -0.1736481776669172583, -0.000000000000000000 ) ) ;
#5529=CARTESIAN_POINT ( 'NONE',  ( 1.899862297872551897, -26.17578186266363360, 6.911401339314954484 ) ) ;
#5532=EDGE_CURVE ( 'NONE', #29219, #10909, #6387, .T. ) ;
#5533=CARTESIAN_POINT ( 'NONE',  ( -0.8208322467303189596, -33.90981015991838632, 7.635761828346577573 ) ) ;
#5536=CARTESIAN_POINT ( 'NONE',  ( -1.218159702771259179, -27.82577619805188007, 6.892063359921932530 ) ) ;
#5546=EDGE_LOOP ( 'NONE', ( #23614, #37724, #33149, #7563 ) ) ;
#5547=ORIENTED_EDGE ( 'NONE', *, *, #38564, .F. ) ;
#5548=CARTESIAN_POINT ( 'NONE',  ( 1.700390093233090871, -29.56993018339339940, 7.750000000000000888 ) ) ;
#5549=EDGE_CURVE ( 'NONE', #33766, #32438, #31045, .T. ) ;
#5552=ORIENTED_EDGE ( 'NONE', *, *, #13112, .F. ) ;
#5560=CARTESIAN_POINT ( 'NONE',  ( -1.798045670483560343, -29.46480087874731169, 6.863784140767622333 ) ) ;
#5563=ADVANCED_FACE ( 'NONE', ( #24914 ), #3722, .F. ) ;
#5569=FACE_OUTER_BOUND ( 'NONE', #11977, .T. ) ;
#5575=CARTESIAN_POINT ( 'NONE',  ( 2.808265793782570796, -32.88997780688298178, 6.863805608295730387 ) ) ;
#5577=CARTESIAN_POINT ( 'NONE',  ( 1.077276024005688448, -26.12584348203982643, 7.638132480492517473 ) ) ;
#5580=CARTESIAN_POINT ( 'NONE',  ( 5.194824081808306460, -29.57876364156226856, 7.773839561854631874 ) ) ;
#5589=B_SPLINE_CURVE_WITH_KNOTS ( 'NONE', 3,
 ( #1942, #27439, #14461, #33442, #27034, #39579, #17748, #266, #3182, #12806, #15696, #28046, #2969, #34054, #9304, #22093, #37509, #21882, #21476, #22304, #37916, #24972, #34459, #18779, #9511, #12404, #24553, #12605, #25171, #31356, #6235 ),
 .UNSPECIFIED., .F., .F.,
 ( 4, 3, 3, 3, 3, 3, 3, 3, 3, 3, 4 ),
 ( 0.000000000000000000, 3.077658087705419847E-05, 6.152638666999087351E-05, 9.267501192706417050E-05, 0.0001241882240135146176, 0.0001556618703051724378, 0.0001866161554452211381, 0.0002167966385860937832, 0.0002463805737537747790, 0.0002758761370306506470, 0.0002847094172290062959 ),
 .UNSPECIFIED. ) ;
#5592=CARTESIAN_POINT ( 'NONE',  ( -89.20959394718985891, -29.69173459304409946, 7.754798119455333705 ) ) ;
#5593=CARTESIAN_POINT ( 'NONE',  ( 5.209482458574877128, -25.70382654691659496, 6.954324564059724878 ) ) ;
#5595=ORIENTED_EDGE ( 'NONE', *, *, #7859, .T. ) ;
#5597=CARTESIAN_POINT ( 'NONE',  ( -0.4706772961942385369, -32.18650550059052051, 7.748216051605114174 ) ) ;
#5603=VERTEX_POINT ( 'NONE', #418 ) ;
#5606=ORIENTED_EDGE ( 'NONE', *, *, #31294, .F. ) ;
#5610=CARTESIAN_POINT ( 'NONE',  ( -0.1471056227823456797, -32.42418307676227585, 6.882085323592684212 ) ) ;
#5614=CARTESIAN_POINT ( 'NONE',  ( 2.255350295996689347, -26.21552723005750352, 7.693875151218753317 ) ) ;
#5617=EDGE_CURVE ( 'NONE', #29634, #22430, #1807, .T. ) ;
#5620=CARTESIAN_POINT ( 'NONE',  ( 3.469639963590166687, -26.66651138929124798, 7.782034975670473642 ) ) ;
#5621=CARTESIAN_POINT ( 'NONE',  ( -1.693538636980199907, -29.36683470281148445, 6.988553391373221402 ) ) ;
#5623=CARTESIAN_POINT ( 'NONE',  ( -1.772492569845566246, -30.00477039368643162, 7.006908160621414083 ) ) ;
#5625=LINE ( 'NONE', #39378, #31442 ) ;
#5627=EDGE_CURVE ( 'NONE', #30413, #19523, #5765, .T. ) ;
#5628=CARTESIAN_POINT ( 'NONE',  ( 1.700390093233090871, -29.56993018339339940, -8.199999999999999289 ) ) ;
#5637=CARTESIAN_POINT ( 'NONE',  ( 5.904749997263966321, -30.32498317729107740, 7.635761828346577573 ) ) ;
#5638=CARTESIAN_POINT ( 'NONE',  ( -0.06469087068677582819, -26.54759843608177761, 7.750000000000000888 ) ) ;
#5639=DIRECTION ( 'NONE',  ( 1.047444401652940007E-14, -1.000000000000000000, -0.000000000000000000 ) ) ;
#5641=CARTESIAN_POINT ( 'NONE',  ( 5.099365965258681577, -29.65337490394464481, 6.870716933885662847 ) ) ;
#5643=CARTESIAN_POINT ( 'NONE',  ( 4.896323676056323571, -28.40975410443699900, 7.769368695748486431 ) ) ;
#5646=EDGE_LOOP ( 'NONE', ( #16328, #1258, #15496, #36918, #5372 ) ) ;
#5647=( BOUNDED_CURVE ( )  B_SPLINE_CURVE ( 3, ( #12905, #30850, #12076, #6130 ),
 .UNSPECIFIED., .F., .F. ) 
 B_SPLINE_CURVE_WITH_KNOTS ( ( 4, 4 ),
 ( 1.381924640371166690, 1.574767692156074483 ),
 .UNSPECIFIED. ) 
 CURVE ( )  GEOMETRIC_REPRESENTATION_ITEM ( )  RATIONAL_B_SPLINE_CURVE ( ( 1.000000000000000000, 0.9969033633783033199, 0.9969033633783033199, 1.000000000000000000 ) ) 
 REPRESENTATION_ITEM ( '' )  );
#5649=CARTESIAN_POINT ( 'NONE',  ( 6.372929778535830536, -30.51927953399086846, 6.954324564059724878 ) ) ;
#5651=VERTEX_POINT ( 'NONE', #1233 ) ;
#5655=CARTESIAN_POINT ( 'NONE',  ( 4.806945244714058596, -28.17076227882084183, 7.505001789837628223 ) ) ;
#5656=CARTESIAN_POINT ( 'NONE',  ( 4.856901937812163617, -30.83345229474961613, 7.768425012602592439 ) ) ;
#5658=VERTEX_POINT ( 'NONE', #10464 ) ;
#5664=ORIENTED_EDGE ( 'NONE', *, *, #33915, .T. ) ;
#5666=CARTESIAN_POINT ( 'NONE',  ( -1.576062547484235354, -30.80072589882973944, 7.695279973900954751 ) ) ;
#5669=AXIS2_PLACEMENT_3D ( 'NONE', #14017, #26589, #10925 ) ;
#5672=EDGE_LOOP ( 'NONE', ( #15310, #14150, #29169, #26671, #19624 ) ) ;
#5673=CARTESIAN_POINT ( 'NONE',  ( 2.570535995292712705, -32.96706368601960691, 7.501983001166817822 ) ) ;
#5674=CARTESIAN_POINT ( 'NONE',  ( -1.315039247493585250, -27.79308300620435901, 6.894806418505347700 ) ) ;
#5676=CARTESIAN_POINT ( 'NONE',  ( 3.419158195859356653, -26.52102280379090971, 7.695279973900954751 ) ) ;
#5678=CARTESIAN_POINT ( 'NONE',  ( 3.729508372841241925, -32.29806033631375328, 6.997764925645183709 ) ) ;
#5682=CARTESIAN_POINT ( 'NONE',  ( 5.061789821607289852, -29.05897258848950671, 7.782034975670476307 ) ) ;
#5684=EDGE_CURVE ( 'NONE', #7585, #17512, #7581, .T. ) ;
#5687=ADVANCED_FACE ( 'NONE', ( #7781 ), #26526, .F. ) ;
#5695=CARTESIAN_POINT ( 'NONE',  ( -89.20959394718985891, -29.69173459304409946, 7.754798119455333705 ) ) ;
#5698=CARTESIAN_POINT ( 'NONE',  ( 4.854410821503884144, -30.83963615157586702, 6.864276522220859711 ) ) ;
#5699=ORIENTED_EDGE ( 'NONE', *, *, #34988, .T. ) ;
#5701=CARTESIAN_POINT ( 'NONE',  ( -0.6442351191163634416, -32.16855289001363616, 6.867199677474201458 ) ) ;
#5707=CARTESIAN_POINT ( 'NONE',  ( 2.685785295776140114, -32.82400398323339630, 7.013842709614101167 ) ) ;
#5709=CARTESIAN_POINT ( 'NONE',  ( -1.343169602973049548, -31.08543165182933876, 6.969307238440504371 ) ) ;
#5713=CARTESIAN_POINT ( 'NONE',  ( 3.255859414528191387, -32.59326998547489040, 6.876076431790004939 ) ) ;
#5714=CARTESIAN_POINT ( 'NONE',  ( 4.923146412972194241, -30.93516854733796961, 6.998987538705428335 ) ) ;
#5716=CARTESIAN_POINT ( 'NONE',  ( -1.184830056622453887, -27.77117931491062208, 7.761597726988851420 ) ) ;
#5718=CARTESIAN_POINT ( 'NONE',  ( -1.534173489221649866, -30.61759350290857284, 7.754798119455333705 ) ) ;
#5719=VECTOR ( 'NONE', #1594, 1000.000000000000000 ) ;
#5721=ORIENTED_EDGE ( 'NONE', *, *, #1032, .F. ) ;
#5722=CARTESIAN_POINT ( 'NONE',  ( 5.020414555553945668, -30.30303151990228727, 6.868387053540521592 ) ) ;
#5738=CARTESIAN_POINT ( 'NONE',  ( 1.835860697290446986, -26.17261544377572946, 6.865312560952603782 ) ) ;
#5742=EDGE_LOOP ( 'NONE', ( #16157, #12740, #16436, #9941, #6866 ) ) ;
#5750=AXIS2_PLACEMENT_3D ( 'NONE', #16178, #28745, #25651 ) ;
#5752=CARTESIAN_POINT ( 'NONE',  ( -1.743019459741919519, -30.19677198997656120, 7.643192810543824045 ) ) ;
#5757=CARTESIAN_POINT ( 'NONE',  ( -0.8208322467303189596, -33.90981015991838632, 7.635761828346577573 ) ) ;
#5762=DIRECTION ( 'NONE',  ( 0.000000000000000000, 0.000000000000000000, 1.000000000000000000 ) ) ;
#5765=( BOUNDED_CURVE ( )  B_SPLINE_CURVE ( 3, ( #34405, #6177, #18719, #3123 ),
 .UNSPECIFIED., .F., .T. ) 
 B_SPLINE_CURVE_WITH_KNOTS ( ( 4, 4 ),
 ( 1.347909859412853795, 1.534781240595299190 ),
 .UNSPECIFIED. ) 
 CURVE ( )  GEOMETRIC_REPRESENTATION_ITEM ( )  RATIONAL_B_SPLINE_CURVE ( ( 1.000000000000000000, 0.9970920404276226723, 0.9970920404276226723, 1.000000000000000000 ) ) 
 REPRESENTATION_ITEM ( '' )  );
#5767=CARTESIAN_POINT ( 'NONE',  ( 1.700390093233090871, -29.56993018339339940, 6.850000000000000533 ) ) ;
#5768=LINE ( 'NONE', #2706, #33667 ) ;
#5772=EDGE_LOOP ( 'NONE', ( #32075, #7390, #19563, #24589 ) ) ;
#5774=AXIS2_PLACEMENT_3D ( 'NONE', #14358, #18467, #34159 ) ;
#5776=CARTESIAN_POINT ( 'NONE',  ( 3.468923106531234257, -26.56255022247102104, 7.781480525794718162 ) ) ;
#5781=AXIS2_PLACEMENT_3D ( 'NONE', #2495, #11913, #5762 ) ;
#5782=CARTESIAN_POINT ( 'NONE',  ( 2.798136362750837325, -32.89334079469422534, 6.863784140767622333 ) ) ;
#5787=CARTESIAN_POINT ( 'NONE',  ( 5.100255277763929840, -29.60020768353928133, 7.782167645815905033 ) ) ;
#5788=CARTESIAN_POINT ( 'NONE',  ( 4.634613070157855397, -31.47789877608044051, 6.989977667959441199 ) ) ;
#5791=CARTESIAN_POINT ( 'NONE',  ( 4.378698603929789712, -31.81803082612050915, 7.767720160662272555 ) ) ;
#5792=CARTESIAN_POINT ( 'NONE',  ( 1.732966464757989877, -32.97687815986694204, 7.257242401810562349 ) ) ;
#5799=EDGE_CURVE ( 'NONE', #35245, #25861, #13277, .T. ) ;
#5800=DIRECTION ( 'NONE',  ( -0.000000000000000000, -0.000000000000000000, -1.000000000000000000 ) ) ;
#5801=VECTOR ( 'NONE', #31672, 1000.000000000000114 ) ;
#5802=ORIENTED_EDGE ( 'NONE', *, *, #2902, .F. ) ;
#5803=CARTESIAN_POINT ( 'NONE',  ( -0.4752369984505682154, -32.18272215034290440, 7.756377446753160321 ) ) ;
#5805=VERTEX_POINT ( 'NONE', #20136 ) ;
#5806=DIRECTION ( 'NONE',  ( -0.000000000000000000, -0.000000000000000000, -1.000000000000000000 ) ) ;
#5813=CARTESIAN_POINT ( 'NONE',  ( -0.1240150654202767239, -32.43899724728002099, 6.868387053540519815 ) ) ;
#5814=VERTEX_POINT ( 'NONE', #32514 ) ;
#5828=CARTESIAN_POINT ( 'NONE',  ( -1.576062547484236243, -30.80072589882973944, 7.686927408461904143 ) ) ;
#5831=CARTESIAN_POINT ( 'NONE',  ( -1.391618227887877035, -31.20992771383839681, 6.867199677474202346 ) ) ;
#5833=CARTESIAN_POINT ( 'NONE',  ( 1.508261857771285630, -33.06465288214051412, 6.951256099901591767 ) ) ;
#5835=DIRECTION ( 'NONE',  ( 1.000000000000000000, 0.000000000000000000, 0.000000000000000000 ) ) ;
#5836=ORIENTED_EDGE ( 'NONE', *, *, #30264, .T. ) ;
#5838=CARTESIAN_POINT ( 'NONE',  ( -0.4171441595639596156, -26.78316706317107787, 7.013842709614101167 ) ) ;
#5841=EDGE_CURVE ( 'NONE', #16079, #3202, #36943, .T. ) ;
#5843=CARTESIAN_POINT ( 'NONE',  ( 3.358214364009863839, -32.64710570066487350, 7.771081512783699630 ) ) ;
#5844=CARTESIAN_POINT ( 'NONE',  ( 5.200390093233091093, -29.58029039483751532, 6.917973428066312103 ) ) ;
#5845=CARTESIAN_POINT ( 'NONE',  ( 5.042311414493532595, -28.94418112281064381, 7.692469944509197077 ) ) ;
#5846=CARTESIAN_POINT ( 'NONE',  ( -2.371969930399573379, -31.07359169918526121, 7.013842709614101167 ) ) ;
#5847=CARTESIAN_POINT ( 'NONE',  ( -89.20959394718985891, -29.62408108485141511, 7.695279973900954751 ) ) ;
#5849=CARTESIAN_POINT ( 'NONE',  ( -1.718189074305093600, -25.68532020122240311, 7.754798119455333705 ) ) ;
#5853=CARTESIAN_POINT ( 'NONE',  ( -1.528613082588902161, -30.63465995288272126, 6.864651958020303368 ) ) ;
#5859=ORIENTED_EDGE ( 'NONE', *, *, #1308, .T. ) ;
#5863=CARTESIAN_POINT ( 'NONE',  ( 4.866926447731218630, -30.80812779013709246, 7.782034975670474530 ) ) ;
#5865=CARTESIAN_POINT ( 'NONE',  ( 5.050947857257105156, -30.14768253047834179, 7.756377446753164762 ) ) ;
#5868=CARTESIAN_POINT ( 'NONE',  ( 4.077110055691020918, -27.00064969655394620, 7.013842709614101167 ) ) ;
#5869=ADVANCED_FACE ( 'NONE', ( #14354 ), #39467, .F. ) ;
#5880=VERTEX_POINT ( 'NONE', #17843 ) ;
#5883=CARTESIAN_POINT ( 'NONE',  ( -1.314331979139722328, -31.34797709682064948, 7.670465701733750308 ) ) ;
#5884=DIRECTION ( 'NONE',  ( 0.6605219282605377940, 0.000000000000000000, 0.7508067542896647018 ) ) ;
#5885=VECTOR ( 'NONE', #35608, 999.9999999999998863 ) ;
#5888=CARTESIAN_POINT ( 'NONE',  ( -1.743814956362963020, -30.10855858896023562, 7.784725160561909441 ) ) ;
#5892=CARTESIAN_POINT ( 'NONE',  ( 4.327908163969746980, -31.72774129374395713, 7.695279973900954751 ) ) ;
#5899=CARTESIAN_POINT ( 'NONE',  ( 4.949073456306528840, -30.85287970687986459, 7.776484688137387913 ) ) ;
#5901=ADVANCED_FACE ( 'NONE', ( #24442 ), #37002, .F. ) ;
#5906=ORIENTED_EDGE ( 'NONE', *, *, #11088, .F. ) ;
#5908=CARTESIAN_POINT ( 'NONE',  ( 5.200381411266750575, -29.56092842603204573, 7.630645770930537530 ) ) ;
#5917=CARTESIAN_POINT ( 'NONE',  ( -1.341942858788335524, -31.08789270237882718, 6.929923840112062194 ) ) ;
#5923=CARTESIAN_POINT ( 'NONE',  ( 4.944205726023573888, -30.88437588337916750, 6.867199677474200570 ) ) ;
#5934=DIRECTION ( 'NONE',  ( -0.8660254037844344888, -0.5000000000000069944, -0.000000000000000000 ) ) ;
#5935=ORIENTED_EDGE ( 'NONE', *, *, #4293, .F. ) ;
#5937=CARTESIAN_POINT ( 'NONE',  ( 3.524795251886475800, -26.70086311950679203, 6.868387053540519815 ) ) ;
#5938=CARTESIAN_POINT ( 'NONE',  ( 4.072390683603376083, -26.99628265760808077, 6.887547729233689964 ) ) ;
#5946=ORIENTED_EDGE ( 'NONE', *, *, #21078, .T. ) ;
#5955=VERTEX_POINT ( 'NONE', #14550 ) ;
#5960=CARTESIAN_POINT ( 'NONE',  ( 4.367500526856323617, -27.46123205189602601, 7.774064877406527962 ) ) ;
#5965=DIRECTION ( 'NONE',  ( -0.7541618601367574559, 0.000000000000000000, 0.6566885781822809909 ) ) ;
#5967=VERTEX_POINT ( 'NONE', #33322 ) ;
#5970=LINE ( 'NONE', #28187, #25104 ) ;
#5976=CARTESIAN_POINT ( 'NONE',  ( 4.712621640174670112, -27.77434364046474258, 7.255881584735163869 ) ) ;
#5978=B_SPLINE_CURVE_WITH_KNOTS ( 'NONE', 3,
 ( #32275, #35370, #1383, #10814, #32076, #4074, #3880, #23389, #16397, #35957, #773, #13305, #25878, #38418, #10218, #22798 ),
 .UNSPECIFIED., .F., .F.,
 ( 4, 3, 3, 3, 3, 4 ),
 ( 0.0001585009270395748831, 0.0001815657551981855495, 0.0002118214035944150533, 0.0002420761345915980979, 0.0002723302478207033470, 0.0002816811360866766385 ),
 .UNSPECIFIED. ) ;
#5980=ORIENTED_EDGE ( 'NONE', *, *, #11186, .T. ) ;
#5985=VERTEX_POINT ( 'NONE', #5104 ) ;
#5987=CARTESIAN_POINT ( 'NONE',  ( 2.717497961161612352, -32.91888605690400027, 6.931070083220557621 ) ) ;
#5990=CARTESIAN_POINT ( 'NONE',  ( 1.063398716408742395, -26.12838261010132257, 7.660770905198780234 ) ) ;
#5992=CARTESIAN_POINT ( 'NONE',  ( 5.141725130632948115, -28.98151016813169889, 7.778495531946298058 ) ) ;
#5999=ORIENTED_EDGE ( 'NONE', *, *, #2280, .T. ) ;
#6010=( BOUNDED_CURVE ( )  B_SPLINE_CURVE ( 3, ( #31762, #6648, #23444, #17040 ),
 .UNSPECIFIED., .F., .T. ) 
 B_SPLINE_CURVE_WITH_KNOTS ( ( 4, 4 ),
 ( 1.347909859412853795, 1.534781240595298968 ),
 .UNSPECIFIED. ) 
 CURVE ( )  GEOMETRIC_REPRESENTATION_ITEM ( )  RATIONAL_B_SPLINE_CURVE ( ( 1.000000000000000000, 0.9970920404276226723, 0.9970920404276226723, 1.000000000000000000 ) ) 
 REPRESENTATION_ITEM ( '' )  );
#6017=CARTESIAN_POINT ( 'NONE',  ( -0.1753662704952551610, -32.40569076283811256, 6.929923840112063083 ) ) ;
#6018=ADVANCED_FACE ( 'NONE', ( #31252 ), #40480, .F. ) ;
#6019=VERTEX_POINT ( 'NONE', #34964 ) ;
#6022=CARTESIAN_POINT ( 'NONE',  ( 3.855327937537480487, -32.32757912347058493, 7.754798119455333705 ) ) ;
#6024=CARTESIAN_POINT ( 'NONE',  ( 0.6134941550689647638, -26.34832452513749956, 7.782034975670476307 ) ) ;
#6028=ORIENTED_EDGE ( 'NONE', *, *, #12864, .F. ) ;
#6033=CYLINDRICAL_SURFACE ( 'NONE', #3222, 0.09010775117052929883 ) ;
#6039=CARTESIAN_POINT ( 'NONE',  ( 0.03672680498656953618, -25.15737950931636036, 7.695279973900954751 ) ) ;
#6040=DIRECTION ( 'NONE',  ( -0.7394003126383950075, 0.1303762246624157739, 0.6605219282605377940 ) ) ;
#6041=LINE ( 'NONE', #37712, #22348 ) ;
#6043=CARTESIAN_POINT ( 'NONE',  ( 2.138864189560986340, -33.04235649097854832, 7.011627023500183853 ) ) ;
#6047=CARTESIAN_POINT ( 'NONE',  ( 5.042323503313180133, -28.94424569214364240, 7.691066658568946224 ) ) ;
#6048=DIRECTION ( 'NONE',  ( 0.9848077530122080203, 0.1736481776669307198, -0.000000000000000000 ) ) ;
#6050=CARTESIAN_POINT ( 'NONE',  ( 2.093335990219729936, -32.94715174935227964, 6.911401339314957148 ) ) ;
#6054=VERTEX_POINT ( 'NONE', #22194 ) ;
#6058=ADVANCED_FACE ( 'NONE', ( #40697 ), #2857, .F. ) ;
#6060=EDGE_LOOP ( 'NONE', ( #26625, #260, #3503, #36638, #29501 ) ) ;
#6064=CARTESIAN_POINT ( 'NONE',  ( 1.158056475448751454, -26.21346265829786049, 6.894806418505346812 ) ) ;
#6069=CARTESIAN_POINT ( 'NONE',  ( -1.489921458977837565, -30.74547780039133116, 7.635761828346577573 ) ) ;
#6070=ADVANCED_FACE ( 'NONE', ( #25274 ), #8993, .F. ) ;
#6071=ORIENTED_EDGE ( 'NONE', *, *, #7592, .T. ) ;
#6077=CARTESIAN_POINT ( 'NONE',  ( -1.181303964486304814, -27.76553572604635534, 7.754798119455333705 ) ) ;
#6078=ORIENTED_EDGE ( 'NONE', *, *, #32287, .F. ) ;
#6081=ORIENTED_EDGE ( 'NONE', *, *, #10335, .F. ) ;
#6083=CARTESIAN_POINT ( 'NONE',  ( -1.799437424176533185, -29.60468789766325415, 7.677493265592890914 ) ) ;
#6085=CARTESIAN_POINT ( 'NONE',  ( -1.322875202110333603, -31.33341290337725837, 7.638132480492518361 ) ) ;
#6090=CARTESIAN_POINT ( 'NONE',  ( 3.721384798075928035, -32.30408232086368514, 6.939395833800444890 ) ) ;
#6092=CARTESIAN_POINT ( 'NONE',  ( -0.06129048428309483154, -26.54561512989744188, 7.635761828346575797 ) ) ;
#6104=CARTESIAN_POINT ( 'NONE',  ( 1.700390093233090871, -29.56993018339339940, 7.800000000000000711 ) ) ;
#6105=ADVANCED_FACE ( 'NONE', ( #12289 ), #9611, .F. ) ;
#6109=CARTESIAN_POINT ( 'NONE',  ( 2.290977028701361107, -26.12011756940199447, 7.750000000000000888 ) ) ;
#6114=CARTESIAN_POINT ( 'NONE',  ( 0.9075698686646886948, -32.88344056124241632, 7.386948897581447682 ) ) ;
#6120=CARTESIAN_POINT ( 'NONE',  ( -1.698424725305372363, -29.48016477088195231, 7.778050822775633755 ) ) ;
#6126=( BOUNDED_CURVE ( )  B_SPLINE_CURVE ( 3, ( #18104, #5976, #27380, #18516 ),
 .UNSPECIFIED., .F., .F. ) 
 B_SPLINE_CURVE_WITH_KNOTS ( ( 4, 4 ),
 ( 1.347909859412852907, 1.534781240595297636 ),
 .UNSPECIFIED. ) 
 CURVE ( )  GEOMETRIC_REPRESENTATION_ITEM ( )  RATIONAL_B_SPLINE_CURVE ( ( 1.000000000000000000, 0.9970920404276226723, 0.9970920404276226723, 1.000000000000000000 ) ) 
 REPRESENTATION_ITEM ( '' )  );
#6127=CARTESIAN_POINT ( 'NONE',  ( 4.966824528213045653, -30.82710434516975795, 6.870737987065015595 ) ) ;
#6129=CARTESIAN_POINT ( 'NONE',  ( 3.419158195859356653, -26.52102280379090971, 7.695279973900954751 ) ) ;
#6130=CARTESIAN_POINT ( 'NONE',  ( -0.01129010125266571157, -26.63221833370405633, 7.635761828346577573 ) ) ;
#6138=CARTESIAN_POINT ( 'NONE',  ( 0.6636879034114320230, -26.22699007480350986, 7.013842709614101167 ) ) ;
#6143=CARTESIAN_POINT ( 'NONE',  ( 3.985343101274590794, -26.91869073241397103, 6.880608371227950215 ) ) ;
#6144=EDGE_CURVE ( 'NONE', #29030, #24859, #17791, .T. ) ;
#6148=CARTESIAN_POINT ( 'NONE',  ( 1.907370182495600641, -26.17623391135161626, 6.979335674598003969 ) ) ;
#6149=ORIENTED_EDGE ( 'NONE', *, *, #12827, .T. ) ;
#6162=CARTESIAN_POINT ( 'NONE',  ( -0.4545477510665002496, -26.81228124332190532, 7.754798119455333705 ) ) ;
#6164=AXIS2_PLACEMENT_3D ( 'NONE', #17557, #14677, #26652 ) ;
#6167=CARTESIAN_POINT ( 'NONE',  ( 5.153279172109080264, -30.14225614731511982, 7.701614758090453705 ) ) ;
#6168=ORIENTED_EDGE ( 'NONE', *, *, #11372, .T. ) ;
#6173=CIRCLE ( 'NONE', #37675, 2.500000000000000000 ) ;
#6174=CARTESIAN_POINT ( 'NONE',  ( 4.749297472835600331, -31.28869828601962766, 7.695279973900954751 ) ) ;
#6177=CARTESIAN_POINT ( 'NONE',  ( 1.043334534275603742, -26.12523165986777585, 7.255881584735162093 ) ) ;
#6181=ORIENTED_EDGE ( 'NONE', *, *, #21170, .T. ) ;
#6182=CARTESIAN_POINT ( 'NONE',  ( 0.5037982502477853508, -26.38745190989316214, 7.695279973900954751 ) ) ;
#6184=CARTESIAN_POINT ( 'NONE',  ( 3.527976676500487851, -26.59338346714900680, 7.776484688137387025 ) ) ;
#6185=ORIENTED_EDGE ( 'NONE', *, *, #38506, .T. ) ;
#6197=CARTESIAN_POINT ( 'NONE',  ( 5.098690994628564788, -29.67766195414260366, 7.768425012602595103 ) ) ;
#6199=EDGE_CURVE ( 'NONE', #28383, #14367, #14170, .T. ) ;
#6201=CIRCLE ( 'NONE', #29844, 3.499999999999999556 ) ;
#6204=VERTEX_POINT ( 'NONE', #35161 ) ;
#6207=FACE_OUTER_BOUND ( 'NONE', #32119, .T. ) ;
#6212=CARTESIAN_POINT ( 'NONE',  ( 2.388817387744127441, -25.35382237095210201, 7.695279973900954751 ) ) ;
#6214=CARTESIAN_POINT ( 'NONE',  ( -0.9449608208177665558, -27.27818007888150120, 6.875671892026063325 ) ) ;
#6222=CARTESIAN_POINT ( 'NONE',  ( 2.947205120345838480, -26.40679055824786303, 7.778050822775630202 ) ) ;
#6223=ORIENTED_EDGE ( 'NONE', *, *, #15906, .T. ) ;
#6233=CARTESIAN_POINT ( 'NONE',  ( 0.5241206729324208169, -32.86635431953688169, 7.743886751744252450 ) ) ;
#6235=CARTESIAN_POINT ( 'NONE',  ( 4.269670580072574495, -31.94665014585129725, 7.013842709614101167 ) ) ;
#6236=CARTESIAN_POINT ( 'NONE',  ( -1.694095407703923861, -29.37624715910394002, 7.006423389747790331 ) ) ;
#6238=CARTESIAN_POINT ( 'NONE',  ( -1.411741797515851271, -31.17137799540083876, 7.013842709614101167 ) ) ;
#6240=CARTESIAN_POINT ( 'NONE',  ( 1.518277080292407044, -33.06519117755393466, 6.912143950357348743 ) ) ;
#6243=CARTESIAN_POINT ( 'NONE',  ( -0.6421092404456101299, -32.03421449887897410, 6.949473656533215582 ) ) ;
#6245=DIRECTION ( 'NONE',  ( -1.000000000000000000, 0.000000000000000000, 0.000000000000000000 ) ) ;
#6248=CARTESIAN_POINT ( 'NONE',  ( -0.9297026075730506767, -31.72462434039837476, 7.784838882742139532 ) ) ;
#6252=CARTESIAN_POINT ( 'NONE',  ( 2.104653383086854124, -32.94581586666951978, 6.895222827070023541 ) ) ;
#6259=CARTESIAN_POINT ( 'NONE',  ( -2.640659097302433533, -29.59008065498625939, 7.013842709614101167 ) ) ;
#6263=LINE ( 'NONE', #9330, #3572 ) ;
#6265=CARTESIAN_POINT ( 'NONE',  ( 1.314916516662855361, -26.19185006800425342, 6.979335674598003081 ) ) ;
#6267=ORIENTED_EDGE ( 'NONE', *, *, #16721, .T. ) ;
#6270=CARTESIAN_POINT ( 'NONE',  ( -1.749422520758312505, -28.97934324792513294, 7.750000000000000000 ) ) ;
#6274=CARTESIAN_POINT ( 'NONE',  ( -1.674636587911282781, -29.98134230076460227, 6.887945620086122211 ) ) ;
#6276=ADVANCED_FACE ( 'NONE', ( #22794 ), #35561, .F. ) ;
#6278=AXIS2_PLACEMENT_3D ( 'NONE', #5187, #11949, #8867 ) ;
#6279=CYLINDRICAL_SURFACE ( 'NONE', #37894, 0.09010775117052560734 ) ;
#6281=CARTESIAN_POINT ( 'NONE',  ( 2.852772058385760534, -32.76869315680232830, 7.775108481317161591 ) ) ;
#6285=VERTEX_POINT ( 'NONE', #38214 ) ;
#6290=CARTESIAN_POINT ( 'NONE',  ( -1.519086612902572631, -28.17966245796219127, 7.387053503561888945 ) ) ;
#6292=CARTESIAN_POINT ( 'NONE',  ( 5.401390093233090717, -29.44812577374269580, 7.754798119455333705 ) ) ;
#6295=CARTESIAN_POINT ( 'NONE',  ( 3.423404917024849059, -32.61643964784510530, 6.894806418505347700 ) ) ;
#6298=LINE ( 'NONE', #34322, #12825 ) ;
#6299=FACE_OUTER_BOUND ( 'NONE', #20512, .T. ) ;
#6304=ADVANCED_FACE ( 'NONE', ( #38819 ), #20090, .F. ) ;
#6314=ORIENTED_EDGE ( 'NONE', *, *, #37553, .F. ) ;
#6320=CARTESIAN_POINT ( 'NONE',  ( 5.150390093233091271, -29.56993018339339940, 7.800000000000000711 ) ) ;
#6323=ORIENTED_EDGE ( 'NONE', *, *, #34334, .F. ) ;
#6325=CARTESIAN_POINT ( 'NONE',  ( -1.739421677191636872, -28.95442883120933786, 7.773839561854632763 ) ) ;
#6327=FACE_OUTER_BOUND ( 'NONE', #1221, .T. ) ;
#6328=ORIENTED_EDGE ( 'NONE', *, *, #20916, .T. ) ;
#6329=VERTEX_POINT ( 'NONE', #974 ) ;
#6330=CARTESIAN_POINT ( 'NONE',  ( 0.002375005847796004751, -26.52616241155169874, 7.785344483711591934 ) ) ;
#6334=ADVANCED_FACE ( 'NONE', ( #16989 ), #26081, .F. ) ;
#6335=FACE_OUTER_BOUND ( 'NONE', #1880, .T. ) ;
#6337=ORIENTED_EDGE ( 'NONE', *, *, #7818, .T. ) ;
#6338=CARTESIAN_POINT ( 'NONE',  ( 4.826555071938813946, -30.90675198375193844, 7.013842709614101167 ) ) ;
#6339=EDGE_CURVE ( 'NONE', #33687, #24034, #113, .T. ) ;
#6340=ORIENTED_EDGE ( 'NONE', *, *, #33635, .F. ) ;
#6343=B_SPLINE_CURVE_WITH_KNOTS ( 'NONE', 3,
 ( #29220, #10267, #22847, #7586, #1030, #23633, #7978, #33118, #23048, #10862 ),
 .UNSPECIFIED., .F., .F.,
 ( 4, 3, 3, 4 ),
 ( 0.0001585009270395720371, 0.0001815657551981848989, 0.0002118214035944141318, 0.0002170292169044764612 ),
 .UNSPECIFIED. ) ;
#6348=CARTESIAN_POINT ( 'NONE',  ( -0.01851169824090236754, -32.61876219438834568, 7.700536657684222241 ) ) ;
#6350=DIRECTION ( 'NONE',  ( -0.000000000000000000, -0.000000000000000000, -1.000000000000000000 ) ) ;
#6354=VERTEX_POINT ( 'NONE', #22996 ) ;
#6359=ORIENTED_EDGE ( 'NONE', *, *, #12832, .F. ) ;
#6366=VERTEX_POINT ( 'NONE', #769 ) ;
#6374=( BOUNDED_CURVE ( )  B_SPLINE_CURVE ( 3, ( #2357, #31160, #11774, #40398 ),
 .UNSPECIFIED., .F., .T. ) 
 B_SPLINE_CURVE_WITH_KNOTS ( ( 4, 4 ),
 ( 4.748221474220558846, 4.941946782021393147 ),
 .UNSPECIFIED. ) 
 CURVE ( )  GEOMETRIC_REPRESENTATION_ITEM ( )  RATIONAL_B_SPLINE_CURVE ( ( 1.000000000000000000, 0.9968749865767494445, 0.9968749865767494445, 1.000000000000000000 ) ) 
 REPRESENTATION_ITEM ( '' )  );
#6380=ORIENTED_EDGE ( 'NONE', *, *, #3078, .F. ) ;
#6387=LINE ( 'NONE', #9451, #15895 ) ;
#6393=CARTESIAN_POINT ( 'NONE',  ( 3.509071552096934443, -26.58788102988029323, 7.782861076432732617 ) ) ;
#6394=CARTESIAN_POINT ( 'NONE',  ( 1.057972185589858727, -26.12939249603516245, 7.710604733652629328 ) ) ;
#6403=CARTESIAN_POINT ( 'NONE',  ( -1.341696911977036555, -27.83911289459152627, 7.743886751744255115 ) ) ;
#6404=CARTESIAN_POINT ( 'NONE',  ( 4.404419331614843003, -31.79214211702542769, 7.700536657684215136 ) ) ;
#6407=CARTESIAN_POINT ( 'NONE',  ( -1.249667454803414124, -31.26026423822809974, 7.775108481317162479 ) ) ;
#6411=FACE_OUTER_BOUND ( 'NONE', #5357, .T. ) ;
#6418=CARTESIAN_POINT ( 'NONE',  ( -1.652426028059061025, -33.50972191341452344, 7.695279973900954751 ) ) ;
#6423=B_SPLINE_CURVE_WITH_KNOTS ( 'NONE', 3,
 ( #25994, #35675, #13833, #1295, #29082, #10334, #22907, #29282, #13631, #20004 ),
 .UNSPECIFIED., .F., .F.,
 ( 4, 3, 3, 4 ),
 ( 0.0002170292169044812859, 0.0002420761345915979352, 0.0002723302478207015580, 0.0002816811360866826016 ),
 .UNSPECIFIED. ) ;
#6428=ORIENTED_EDGE ( 'NONE', *, *, #15119, .F. ) ;
#6430=CARTESIAN_POINT ( 'NONE',  ( 3.939802142412995423, -32.25249995964913552, 7.773839561854632763 ) ) ;
#6438=EDGE_LOOP ( 'NONE', ( #22855, #38440, #10052, #14557, #25400 ) ) ;
#6443=EDGE_CURVE ( 'NONE', #614, #3701, #24158, .T. ) ;
#6444=CARTESIAN_POINT ( 'NONE',  ( 0.5364714774190757485, -32.87073217714502249, 7.710604733652624887 ) ) ;
#6446=CARTESIAN_POINT ( 'NONE',  ( -0.3385372945680173995, -26.84912605459717838, 7.013842709614101167 ) ) ;
#6447=CARTESIAN_POINT ( 'NONE',  ( -1.698039391944944576, -29.46606476191993096, 6.864651958020303368 ) ) ;
#6451=CARTESIAN_POINT ( 'NONE',  ( 1.529222282396958787, -33.06574276064830542, 7.011627023500184741 ) ) ;
#6452=CARTESIAN_POINT ( 'NONE',  ( 1.700390093233090871, -29.56993018339339940, 7.750000000000000888 ) ) ;
#6459=CARTESIAN_POINT ( 'NONE',  ( 4.364743062397921314, -27.30029760200210731, 7.737115613922533441 ) ) ;
#6460=CARTESIAN_POINT ( 'NONE',  ( 0.3896649785617538608, -32.81498557016907114, 7.754798119455333705 ) ) ;
#6462=CARTESIAN_POINT ( 'NONE',  ( 2.147015419475138298, -32.94046809565001865, 6.868387053540521592 ) ) ;
#6464=VECTOR ( 'NONE', #33645, 1000.000000000000227 ) ;
#6465=CARTESIAN_POINT ( 'NONE',  ( -1.484082617398029491, -28.37865626222930260, 7.782167645815904145 ) ) ;
#6466=CARTESIAN_POINT ( 'NONE',  ( -1.511717022306371616, -30.68454846542563175, 6.892063359921933419 ) ) ;
#6467=ORIENTED_EDGE ( 'NONE', *, *, #35682, .T. ) ;
#6473=CARTESIAN_POINT ( 'NONE',  ( -0.9135791104145147834, -27.25323683387426144, 7.776484688137384360 ) ) ;
#6478=ORIENTED_EDGE ( 'NONE', *, *, #3719, .F. ) ;
#6480=DIRECTION ( 'NONE',  ( 0.6427876096865379196, 0.7660444431189792347, -0.000000000000000000 ) ) ;
#6482=FACE_OUTER_BOUND ( 'NONE', #38538, .T. ) ;
#6487=CARTESIAN_POINT ( 'NONE',  ( -1.003736583562490070, -27.34783681995376270, 7.695279973900954751 ) ) ;
#6492=ADVANCED_FACE ( 'NONE', ( #39216 ), #17383, .F. ) ;
#6493=CARTESIAN_POINT ( 'NONE',  ( -1.612909802052744812, -30.67534724370283783, 7.776484688137385248 ) ) ;
#6494=CARTESIAN_POINT ( 'NONE',  ( 1.887380280259158383, -26.17507603778478753, 7.013842709614101167 ) ) ;
#6496=CARTESIAN_POINT ( 'NONE',  ( 1.574364539997139767, -33.06766052747819629, 7.750000000000000888 ) ) ;
#6499=ORIENTED_EDGE ( 'NONE', *, *, #12745, .T. ) ;
#6501=CARTESIAN_POINT ( 'NONE',  ( -0.1082913656307287614, -32.55197933690651979, 7.782861076432731728 ) ) ;
#6502=ORIENTED_EDGE ( 'NONE', *, *, #7442, .T. ) ;
#6503=CARTESIAN_POINT ( 'NONE',  ( 1.705817689846350405, -32.96993596345505750, 7.763628509615286610 ) ) ;
#6506=CARTESIAN_POINT ( 'NONE',  ( -1.558322435399049244, -30.53987484972025612, 6.988553391373226731 ) ) ;
#6507=FACE_OUTER_BOUND ( 'NONE', #3570, .T. ) ;
#6509=CARTESIAN_POINT ( 'NONE',  ( -0.06636395565068713143, -26.54857616064916570, 7.643192810543817828 ) ) ;
#6511=DIRECTION ( 'NONE',  ( 1.000000000000000000, 0.000000000000000000, 0.000000000000000000 ) ) ;
#6512=DIRECTION ( 'NONE',  ( -0.000000000000000000, -0.000000000000000000, -1.000000000000000000 ) ) ;
#6514=CARTESIAN_POINT ( 'NONE',  ( 1.277170166547874075, -33.05113105426861608, 7.139344958878411695 ) ) ;
#6521=CARTESIAN_POINT ( 'NONE',  ( 2.199298596665589134, -33.03157230968192692, 7.766640943994644886 ) ) ;
#6526=CARTESIAN_POINT ( 'NONE',  ( 5.200390093233089317, -29.56542930052595608, 7.625529684960262067 ) ) ;
#6527=DIRECTION ( 'NONE',  ( 0.000000000000000000, -0.7541618601367562347, -0.6566885781822823231 ) ) ;
#6528=ORIENTED_EDGE ( 'NONE', *, *, #11372, .F. ) ;
#6530=EDGE_CURVE ( 'NONE', #3202, #18044, #15746, .T. ) ;
#6531=UNCERTAINTY_MEASURE_WITH_UNIT (LENGTH_MEASURE( 1.000000000000000082E-05 ), #39307, 'distance_accuracy_value', 'NONE');
#6532=VERTEX_POINT ( 'NONE', #12450 ) ;
#6536=CARTESIAN_POINT ( 'NONE',  ( -1.338646324113869968, -31.09448676743746631, 6.997764925645180156 ) ) ;
#6538=ORIENTED_EDGE ( 'NONE', *, *, #32161, .F. ) ;
#6540=EDGE_CURVE ( 'NONE', #19833, #32450, #29546, .T. ) ;
#6541=CARTESIAN_POINT ( 'NONE',  ( -0.5222764122352709926, -32.27358584779708650, 7.710604733652632881 ) ) ;
#6542=DIRECTION ( 'NONE',  ( 0.6662082868431823401, 0.000000000000000000, -0.7457657263118706581 ) ) ;
#6545=ORIENTED_EDGE ( 'NONE', *, *, #32505, .F. ) ;
#6547=VERTEX_POINT ( 'NONE', #6494 ) ;
#6548=CARTESIAN_POINT ( 'NONE',  ( -1.027740059687268559, -31.59904846300154446, 6.997764925645181933 ) ) ;
#6549=CARTESIAN_POINT ( 'NONE',  ( -1.652310497857324201, -29.00476380710052382, 7.652160403243381204 ) ) ;
#6555=CARTESIAN_POINT ( 'NONE',  ( -0.02444159985243907554, -32.61541136549380582, 7.730015791551954507 ) ) ;
#6560=CARTESIAN_POINT ( 'NONE',  ( 1.760763344459050472, -26.17046624469124083, 7.785172627573962778 ) ) ;
#6562=CARTESIAN_POINT ( 'NONE',  ( 4.627388605110565933, -27.83999205693219636, 7.712764235869106422 ) ) ;
#6567=AXIS2_PLACEMENT_3D ( 'NONE', #27592, #37054, #25123 ) ;
#6568=ORIENTED_EDGE ( 'NONE', *, *, #6574, .F. ) ;
#6572=CARTESIAN_POINT ( 'NONE',  ( 5.199086758562380339, -29.56349144210750168, 7.762460296495606649 ) ) ;
#6574=EDGE_CURVE ( 'NONE', #3561, #3356, #40673, .T. ) ;
#6575=CARTESIAN_POINT ( 'NONE',  ( -1.654012860102806570, -29.01496998062980381, 7.695279973900954751 ) ) ;
#6576=CARTESIAN_POINT ( 'NONE',  ( -0.4624984080477824722, -26.82151441493339306, 7.766640943994646662 ) ) ;
#6584=VERTEX_POINT ( 'NONE', #9562 ) ;
#6587=DIRECTION ( 'NONE',  ( -0.8660254037844415942, 0.4999999999999950040, -0.000000000000000000 ) ) ;
#6592=DIRECTION ( 'NONE',  ( -0.9848077530122067991, -0.1736481776669374644, -0.000000000000000000 ) ) ;
#6593=CARTESIAN_POINT ( 'NONE',  ( 5.200390093233090205, -29.36153111629380774, 7.162856560672870465 ) ) ;
#6597=VERTEX_POINT ( 'NONE', #21318 ) ;
#6601=CARTESIAN_POINT ( 'NONE',  ( 1.057393818175778932, -26.12950058953997612, 7.700536657684216912 ) ) ;
#6605=CARTESIAN_POINT ( 'NONE',  ( 0.4903620891694951966, -32.74734004133340903, 7.785868773668302545 ) ) ;
#6608=CARTESIAN_POINT ( 'NONE',  ( 5.100305588748021535, -29.54523758825880364, 7.740055089680398126 ) ) ;
#6609=CARTESIAN_POINT ( 'NONE',  ( 1.653914865439267912, -33.89923146551851829, 6.954324564059724878 ) ) ;
#6616=( BOUNDED_CURVE ( )  B_SPLINE_CURVE ( 3, ( #1918, #8055, #20614, #33200 ),
 .UNSPECIFIED., .F., .T. ) 
 B_SPLINE_CURVE_WITH_KNOTS ( ( 4, 4 ),
 ( 4.748221474220559735, 4.941946782021394036 ),
 .UNSPECIFIED. ) 
 CURVE ( )  GEOMETRIC_REPRESENTATION_ITEM ( )  RATIONAL_B_SPLINE_CURVE ( ( 1.000000000000000000, 0.9968749865767494445, 0.9968749865767494445, 1.000000000000000000 ) ) 
 REPRESENTATION_ITEM ( '' )  );
#6620=EDGE_CURVE ( 'NONE', #34388, #8430, #36470, .T. ) ;
#6621=ORIENTED_EDGE ( 'NONE', *, *, #12745, .F. ) ;
#6625=CARTESIAN_POINT ( 'NONE',  ( 4.956406565555597332, -28.59095027454233673, 7.006423389747790331 ) ) ;
#6626=DIRECTION ( 'NONE',  ( -0.1303762246624179666, -0.7394003126383923430, -0.6605219282605402364 ) ) ;
#6628=ORIENTED_EDGE ( 'NONE', *, *, #1590, .T. ) ;
#6631=CARTESIAN_POINT ( 'NONE',  ( 3.800390874224334858, -32.36993114662322313, 6.971170733404102648 ) ) ;
#6639=DIRECTION ( 'NONE',  ( -0.6427876096865430267, 0.7660444431189749048, -0.000000000000000000 ) ) ;
#6644=CARTESIAN_POINT ( 'NONE',  ( -2.652992490026568007, -32.06776532245774547, 7.635761828346577573 ) ) ;
#6647=CARTESIAN_POINT ( 'NONE',  ( 3.977572546501454642, -32.22783162523180067, 7.695279973900954751 ) ) ;
#6648=CARTESIAN_POINT ( 'NONE',  ( 2.945629123076408007, -32.84819949571223674, 7.255881584735162093 ) ) ;
#6650=CARTESIAN_POINT ( 'NONE',  ( -1.362284770087026642, -31.26406815671434813, 6.870737987065013819 ) ) ;
#6654=CARTESIAN_POINT ( 'NONE',  ( -0.6146738250898187150, -32.06000629750705855, 6.882085323592685100 ) ) ;
#6659=CARTESIAN_POINT ( 'NONE',  ( -0.9807834779648342272, -31.66069757387703731, 7.754798119455333705 ) ) ;
#6665=DIRECTION ( 'NONE',  ( 0.1736481776669273336, 0.9848077530122085754, -0.000000000000000000 ) ) ;
#6669=CARTESIAN_POINT ( 'NONE',  ( 2.326171464738295835, -32.91184545387483951, 7.695279973900954751 ) ) ;
#6673=VERTEX_POINT ( 'NONE', #22951 ) ;
#6674=CARTESIAN_POINT ( 'NONE',  ( -0.9708236080994220307, -27.31698449112596805, 7.773839561854632763 ) ) ;
#6678=CARTESIAN_POINT ( 'NONE',  ( 3.595293925934929025, -26.62725462111816199, 6.895394898881670009 ) ) ;
#6680=ORIENTED_EDGE ( 'NONE', *, *, #39750, .F. ) ;
#6681=DIRECTION ( 'NONE',  ( 0.7055275666422156089, 0.2567910337120342668, 0.6605219282605377940 ) ) ;
#6683=VERTEX_POINT ( 'NONE', #22753 ) ;
#6688=B_SPLINE_CURVE_WITH_KNOTS ( 'NONE', 3,
 ( #24113, #26614, #8460, #29692, #20417, #35891, #39556, #33420, #5190, #1505, #36480, #30513, #10944, #36677, #21044, #17722, #26418, #38946, #23524, #30306, #36280, #39352, #2118, #14636, #32998 ),
 .UNSPECIFIED., .F., .F.,
 ( 4, 3, 3, 3, 3, 3, 3, 3, 4 ),
 ( 6.468151674593654050E-05, 9.076621574722243315E-05, 0.0001210204262067992133, 0.0001512763324577413697, 0.0001815301820994213761, 0.0002117781465860721964, 0.0002420274594459754516, 0.0002722905548971139996, 0.0002816827545175585711 ),
 .UNSPECIFIED. ) ;
#6702=CARTESIAN_POINT ( 'NONE',  ( -1.544283425328523141, -28.25784841267573810, 7.753200566781599079 ) ) ;
#6703=ORIENTED_EDGE ( 'NONE', *, *, #30710, .F. ) ;
#6704=CARTESIAN_POINT ( 'NONE',  ( 1.713233352393388031, -32.96991108853358554, 7.756377446753163873 ) ) ;
#6707=CARTESIAN_POINT ( 'NONE',  ( 3.788778725684116999, -32.25297732395376471, 6.863904403958576594 ) ) ;
#6711=CARTESIAN_POINT ( 'NONE',  ( 4.927610109650206738, -30.92457071343696384, 7.013842709614101167 ) ) ;
#6717=ORIENTED_EDGE ( 'NONE', *, *, #11321, .F. ) ;
#6723=CARTESIAN_POINT ( 'NONE',  ( -0.4645989045071012846, -32.20074343675116069, 7.257242401810563237 ) ) ;
#6730=ORIENTED_EDGE ( 'NONE', *, *, #6846, .F. ) ;
#6732=CARTESIAN_POINT ( 'NONE',  ( -1.743143437565867870, -28.96217217187591686, 7.767720160662274331 ) ) ;
#6734=B_SPLINE_CURVE_WITH_KNOTS ( 'NONE', 3,
 ( #39826, #24176, #36730, #28896, #6674, #28075, #294, #19426, #31382, #703, #31997, #22330, #3803, #34898, #6473, #22122, #12432, #28486, #505 ),
 .UNSPECIFIED., .F., .F.,
 ( 4, 3, 3, 3, 3, 3, 4 ),
 ( 0.000000000000000000, 2.546128104244838633E-05, 5.711050680484096683E-05, 8.113074941676158883E-05, 0.0001053129305727108458, 0.0001360598016347157812, 0.0001612931755702065552 ),
 .UNSPECIFIED. ) ;
#6735=LINE ( 'NONE', #13506, #11803 ) ;
#6736=ORIENTED_EDGE ( 'NONE', *, *, #5456, .F. ) ;
#6738=CARTESIAN_POINT ( 'NONE',  ( 1.034849034344471397, -33.00608048689603891, 6.873189335546979528 ) ) ;
#6743=CIRCLE ( 'NONE', #29736, 3.499999999999999556 ) ;
#6745=CARTESIAN_POINT ( 'NONE',  ( -1.016762692402616741, -31.61373686903379365, 6.887945620086122211 ) ) ;
#6746=DIRECTION ( 'NONE',  ( 1.000000000000000000, 9.912705577010326536E-16, 0.000000000000000000 ) ) ;
#6750=FACE_OUTER_BOUND ( 'NONE', #36729, .T. ) ;
#6755=CARTESIAN_POINT ( 'NONE',  ( -0.8812738228061313128, -31.78239750451386669, 7.680992449362123331 ) ) ;
#6760=CARTESIAN_POINT ( 'NONE',  ( 4.642167673473801770, -27.86522685681402578, 7.763628509615289275 ) ) ;
#6768=CARTESIAN_POINT ( 'NONE',  ( -1.336977274318315922, -31.28272478379368238, 7.783750581861601070 ) ) ;
#6769=CARTESIAN_POINT ( 'NONE',  ( 2.925322604187870379, -32.84858052415668794, 7.660770905198782010 ) ) ;
#6773=CARTESIAN_POINT ( 'NONE',  ( -1.629351933014555165, -28.88225008802736582, 7.774064877406531515 ) ) ;
#6774=VERTEX_POINT ( 'NONE', #2140 ) ;
#6778=CARTESIAN_POINT ( 'NONE',  ( -1.501411291908892665, -28.42602797326624398, 7.643333865083954848 ) ) ;
#6792=ORIENTED_EDGE ( 'NONE', *, *, #9558, .T. ) ;
#6793=ORIENTED_EDGE ( 'NONE', *, *, #39351, .T. ) ;
#6799=ORIENTED_EDGE ( 'NONE', *, *, #22707, .T. ) ;
#6801=CARTESIAN_POINT ( 'NONE',  ( 2.726104662367788034, -32.91626305826840593, 6.998987538705434552 ) ) ;
#6805=DIRECTION ( 'NONE',  ( -3.491481338843133750E-15, 1.000000000000000000, -0.000000000000000000 ) ) ;
#6808=CARTESIAN_POINT ( 'NONE',  ( 4.999814617694763541, -28.40211264311544070, 6.894806418505347700 ) ) ;
#6810=DIRECTION ( 'NONE',  ( -1.000000000000000000, 0.000000000000000000, 0.000000000000000000 ) ) ;
#6811=CARTESIAN_POINT ( 'NONE',  ( -1.234667376850867138, -31.28615792099245141, 7.748216051605120391 ) ) ;
#6823=CARTESIAN_POINT ( 'NONE',  ( 4.961036936964867472, -28.60650807421071917, 6.959317978105165281 ) ) ;
#6831=ORIENTED_EDGE ( 'NONE', *, *, #336, .F. ) ;
#6833=CARTESIAN_POINT ( 'NONE',  ( 2.496059417767232169, -26.16157129296014716, 6.945385021654666424 ) ) ;
#6838=EDGE_LOOP ( 'NONE', ( #1041, #39712, #17076, #6323 ) ) ;
#6843=CARTESIAN_POINT ( 'NONE',  ( -0.1398724371309366943, -32.54709977595698689, 6.863784140767622333 ) ) ;
#6846=EDGE_CURVE ( 'NONE', #3701, #18601, #7692, .T. ) ;
#6848=CYLINDRICAL_SURFACE ( 'NONE', #18800, 0.09010775117052789718 ) ;
#6852=CARTESIAN_POINT ( 'NONE',  ( 0.1277747208011560942, -26.43548358150071920, 7.387053503561885393 ) ) ;
#6854=CARTESIAN_POINT ( 'NONE',  ( 1.679286629257385588, -26.06999342767483796, 7.744938106820261403 ) ) ;
#6858=CARTESIAN_POINT ( 'NONE',  ( 4.761529427573594653, -31.28080595366133920, 7.255881584735163869 ) ) ;
#6859=CARTESIAN_POINT ( 'NONE',  ( 1.713892699967802136, -33.06990413752668445, 7.635761828346576685 ) ) ;
#6860=( BOUNDED_CURVE ( )  B_SPLINE_CURVE ( 3, ( #33856, #5844, #21283, #30768 ),
 .UNSPECIFIED., .F., .T. ) 
 B_SPLINE_CURVE_WITH_KNOTS ( ( 4, 4 ),
 ( 4.886921905584122428, 4.895802057644188743 ),
 .UNSPECIFIED. ) 
 CURVE ( )  GEOMETRIC_REPRESENTATION_ITEM ( )  RATIONAL_B_SPLINE_CURVE ( ( 1.000000000000000000, 0.9999934285857451366, 0.9999934285857451366, 1.000000000000000000 ) ) 
 REPRESENTATION_ITEM ( '' )  );
#6861=CARTESIAN_POINT ( 'NONE',  ( 1.736346942945643512, -32.96974004645320377, 7.695279973900954751 ) ) ;
#6866=ORIENTED_EDGE ( 'NONE', *, *, #36209, .F. ) ;
#6871=CARTESIAN_POINT ( 'NONE',  ( -2.285626871745154887, -32.86765721485689795, 7.695279973900954751 ) ) ;
#6872=CARTESIAN_POINT ( 'NONE',  ( -1.598337266838639970, -28.40014481679224545, 7.730015791551951843 ) ) ;
#6874=CARTESIAN_POINT ( 'NONE',  ( 1.169535421114899387, -26.21162803541887598, 7.785172627573962778 ) ) ;
#6875=CARTESIAN_POINT ( 'NONE',  ( 1.155917636822889838, -26.11252790201630347, 6.870737987065012931 ) ) ;
#6878=CARTESIAN_POINT ( 'NONE',  ( 1.700390093233090871, -29.56993018339339940, 7.800000000000000711 ) ) ;
#6880=EDGE_CURVE ( 'NONE', #5651, #25105, #35480, .T. ) ;
#6883=ORIENTED_EDGE ( 'NONE', *, *, #28721, .F. ) ;
#6886=CARTESIAN_POINT ( 'NONE',  ( -1.677690022156054450, -29.95540375996364446, 6.979335674598007522 ) ) ;
#6890=ADVANCED_FACE ( 'NONE', ( #11766 ), #24764, .F. ) ;
#6896=ORIENTED_EDGE ( 'NONE', *, *, #33451, .T. ) ;
#6900=VECTOR ( 'NONE', #5934, 1000.000000000000114 ) ;
#6901=CARTESIAN_POINT ( 'NONE',  ( -0.9786402413886234886, -31.81717058986465574, 7.767720160662274331 ) ) ;
#6904=DIRECTION ( 'NONE',  ( -1.000000000000000000, 0.000000000000000000, 0.000000000000000000 ) ) ;
#6906=CARTESIAN_POINT ( 'NONE',  ( 5.197380002583291692, -29.71505624550104940, 6.875780273367528395 ) ) ;
#6907=CARTESIAN_POINT ( 'NONE',  ( -0.5767923600352571345, -26.91202874155497682, 7.686927408461907696 ) ) ;
#6913=ORIENTED_EDGE ( 'NONE', *, *, #13069, .F. ) ;
#6915=CARTESIAN_POINT ( 'NONE',  ( 2.280574181144366275, -26.11834879376533536, 7.733670252284491120 ) ) ;
#6920=CARTESIAN_POINT ( 'NONE',  ( 1.212983646527633130, -26.10426722441512837, 7.754798119455333705 ) ) ;
#6922=CARTESIAN_POINT ( 'NONE',  ( 3.940724359950557698, -26.88089151923329112, 7.756742906098588186 ) ) ;
#6923=AXIS2_PLACEMENT_3D ( 'NONE', #10483, #19761, #16650 ) ;
#6924=B_SPLINE_CURVE_WITH_KNOTS ( 'NONE', 3,
 ( #11153, #39363, #23723, #32615, #4997, #35900, #4795, #4205, #4410, #36290 ),
 .UNSPECIFIED., .F., .F.,
 ( 4, 3, 3, 4 ),
 ( 0.0002170292169044816383, 0.0002420761345915974473, 0.0002723302478207005281, 0.0002816811360866845531 ),
 .UNSPECIFIED. ) ;
#6925=VERTEX_POINT ( 'NONE', #34262 ) ;
#6928=CARTESIAN_POINT ( 'NONE',  ( -1.720424982935133906, -28.89024644203550807, 7.782861076432730840 ) ) ;
#6937=VERTEX_POINT ( 'NONE', #39996 ) ;
#6939=ADVANCED_FACE ( 'NONE', ( #40196 ), #6033, .F. ) ;
#6940=EDGE_CURVE ( 'NONE', #2116, #9668, #28611, .T. ) ;
#6945=CARTESIAN_POINT ( 'NONE',  ( -0.03056955003493260978, -26.64353671815714719, 7.691066658568943559 ) ) ;
#6955=VECTOR ( 'NONE', #7268, 1000.000000000000227 ) ;
#6957=CARTESIAN_POINT ( 'NONE',  ( 4.628654959960774917, -27.84213827743704428, 7.721096864323906850 ) ) ;
#6961=AXIS2_PLACEMENT_3D ( 'NONE', #36372, #33300, #20926 ) ;
#6966=CARTESIAN_POINT ( 'NONE',  ( 1.749140210850987920, -26.17027969752984973, 6.894806418505346812 ) ) ;
#6967=( BOUNDED_CURVE ( )  B_SPLINE_CURVE ( 3, ( #29552, #1370, #13903, #10795 ),
 .UNSPECIFIED., .F., .F. ) 
 B_SPLINE_CURVE_WITH_KNOTS ( ( 4, 4 ),
 ( 4.748221474220559735, 4.941946782021394036 ),
 .UNSPECIFIED. ) 
 CURVE ( )  GEOMETRIC_REPRESENTATION_ITEM ( )  RATIONAL_B_SPLINE_CURVE ( ( 1.000000000000000000, 0.9968749865767494445, 0.9968749865767494445, 1.000000000000000000 ) ) 
 REPRESENTATION_ITEM ( '' )  );
#6969=CARTESIAN_POINT ( 'NONE',  ( -1.260458514972081501, -27.70352715432887436, 6.870724624169666228 ) ) ;
#6976=CARTESIAN_POINT ( 'NONE',  ( -1.504497326213975361, -28.43472243647219599, 7.661510568013095934 ) ) ;
#6979=AXIS2_PLACEMENT_3D ( 'NONE', #3035, #21539, #27694 ) ;
#6981=CARTESIAN_POINT ( 'NONE',  ( -0.07675644365221842569, -32.46850745275099825, 7.778050822775631978 ) ) ;
#6983=LINE ( 'NONE', #32513, #5885 ) ;
#6988=ORIENTED_EDGE ( 'NONE', *, *, #591, .F. ) ;
#6995=CARTESIAN_POINT ( 'NONE',  ( 0.3480583263237562175, -32.68941832084690446, 6.920489980334475710 ) ) ;
#7001=CARTESIAN_POINT ( 'NONE',  ( 5.078732654515307310, -29.18677349682085520, 6.939395833800441338 ) ) ;
#7003=CARTESIAN_POINT ( 'NONE',  ( 6.149982165465896600, -31.13182306662183052, 7.695279973900954751 ) ) ;
#7006=CARTESIAN_POINT ( 'NONE',  ( 1.448106776224391101, -26.17217962422370192, 7.505001789837627335 ) ) ;
#7007=CARTESIAN_POINT ( 'NONE',  ( -1.287952588635929096, -31.19159846504654610, 7.778050822775631978 ) ) ;
#7012=CARTESIAN_POINT ( 'NONE',  ( 1.682289128304578885, -33.06116167229027525, 7.778495531946297170 ) ) ;
#7014=EDGE_CURVE ( 'NONE', #11999, #22200, #6010, .T. ) ;
#7019=CARTESIAN_POINT ( 'NONE',  ( -0.8688903936063803179, -27.19321022093548734, 7.013842709614101167 ) ) ;
#7025=CARTESIAN_POINT ( 'NONE',  ( 2.845604633296745067, -26.36860488639111111, 7.748216051605122168 ) ) ;
#7033=FACE_OUTER_BOUND ( 'NONE', #26275, .T. ) ;
#7034=AXIS2_PLACEMENT_3D ( 'NONE', #38826, #38224, #583 ) ;
#7035=PLANE ( 'NONE',  #33988 ) ;
#7037=EDGE_CURVE ( 'NONE', #6285, #34388, #34024, .T. ) ;
#7039=CARTESIAN_POINT ( 'NONE',  ( -0.2130646727215941838, -32.50057703731113889, 6.941203072598479906 ) ) ;
#7041=CARTESIAN_POINT ( 'NONE',  ( 2.261927316241842956, -26.21662072906820384, 7.730758795053807475 ) ) ;
#7045=CARTESIAN_POINT ( 'NONE',  ( 4.714834770645700779, -31.33122182330293981, 7.778495531946298058 ) ) ;
#7047=CARTESIAN_POINT ( 'NONE',  ( 2.713312946249484714, -24.92052936065920932, 6.894806418505347700 ) ) ;
#7049=CARTESIAN_POINT ( 'NONE',  ( -1.699609906766908818, -29.56993018339339940, 7.800000000000000711 ) ) ;
#7051=CARTESIAN_POINT ( 'NONE',  ( 3.347837293313452367, -32.54413893917154610, 7.785172627573962778 ) ) ;
#7052=CARTESIAN_POINT ( 'NONE',  ( 2.188233707926874327, -32.93476592962348803, 6.864651958020304257 ) ) ;
#7053=B_SPLINE_CURVE_WITH_KNOTS ( 'NONE', 3,
 ( #28466, #9519, #34468, #274, #12813, #25386, #83, #6243, #18789, #31366, #3189, #15705, #37926, #9731, #34879, #6654, #487, #19204, #13021, #686, #1094, #1294, #10333, #10527, #886, #10722, #25993, #32979, #32786, #39132, #35674 ),
 .UNSPECIFIED., .F., .F.,
 ( 4, 3, 3, 3, 3, 3, 3, 3, 3, 3, 4 ),
 ( 0.000000000000000000, 2.999644130997804130E-05, 6.002588995695083457E-05, 8.960886084588256043E-05, 0.0001190604700446506651, 0.0001489538463052726962, 0.0001796139255493990204, 0.0002109707048517074038, 0.0002426195318110327544, 0.0002740640997889978898, 0.0002849778069099865880 ),
 .UNSPECIFIED. ) ;
#7058=LINE ( 'NONE', #32397, #28422 ) ;
#7060=CARTESIAN_POINT ( 'NONE',  ( 5.101232590239002995, -29.77532064849933846, 7.386948897581448570 ) ) ;
#7065=CARTESIAN_POINT ( 'NONE',  ( 2.304086713256504382, -32.91590543598751850, 7.635761828346577573 ) ) ;
#7066=EDGE_CURVE ( 'NONE', #40076, #29262, #18611, .T. ) ;
#7071=CARTESIAN_POINT ( 'NONE',  ( 1.196425252463139355, -26.10638800769887169, 6.863784140767622333 ) ) ;
#7072=ORIENTED_EDGE ( 'NONE', *, *, #14605, .T. ) ;
#7080=CARTESIAN_POINT ( 'NONE',  ( -1.740641890886630128, -28.93016385758256348, 6.893199460713416826 ) ) ;
#7087=( BOUNDED_CURVE ( )  B_SPLINE_CURVE ( 3, ( #26078, #363, #12900, #16781 ),
 .UNSPECIFIED., .F., .T. ) 
 B_SPLINE_CURVE_WITH_KNOTS ( ( 4, 4 ),
 ( 4.748221474220560623, 4.886921905584129533 ),
 .UNSPECIFIED. ) 
 CURVE ( )  GEOMETRIC_REPRESENTATION_ITEM ( )  RATIONAL_B_SPLINE_CURVE ( ( 1.000000000000000000, 0.9983974916150919476, 0.9983974916150919476, 1.000000000000000000 ) ) 
 REPRESENTATION_ITEM ( '' )  );
#7092=ORIENTED_EDGE ( 'NONE', *, *, #25900, .T. ) ;
#7097=VECTOR ( 'NONE', #25278, 1000.000000000000000 ) ;
#7098=CARTESIAN_POINT ( 'NONE',  ( -1.048025675227300058, -31.73281868467400102, 7.766640943994351787 ) ) ;
#7101=CARTESIAN_POINT ( 'NONE',  ( 3.836079016935684205, -32.21547265350353229, 6.880147297696981745 ) ) ;
#7103=CARTESIAN_POINT ( 'NONE',  ( 5.196202670487992670, -29.74109799422956968, 7.011627023500181188 ) ) ;
#7107=EDGE_CURVE ( 'NONE', #33743, #33448, #8631, .T. ) ;
#7114=EDGE_CURVE ( 'NONE', #40564, #3554, #30586, .T. ) ;
#7117=CARTESIAN_POINT ( 'NONE',  ( -1.142130670890778799, -27.69163557441362755, 7.386948897581450346 ) ) ;
#7124=ORIENTED_EDGE ( 'NONE', *, *, #14327, .F. ) ;
#7125=CARTESIAN_POINT ( 'NONE',  ( 3.936759689487521641, -26.87759828911498516, 7.750000000000000888 ) ) ;
#7130=CARTESIAN_POINT ( 'NONE',  ( -1.284931719067040623, -31.19715287159715444, 6.870716933885665512 ) ) ;
#7131=EDGE_LOOP ( 'NONE', ( #10989, #37339, #19930, #34547 ) ) ;
#7141=CARTESIAN_POINT ( 'NONE',  ( -0.9952687000786839544, -31.64198801802082528, 6.868387053540522480 ) ) ;
#7142=CARTESIAN_POINT ( 'NONE',  ( -2.271193562574106650, -32.88485816291451869, 7.635761828346577573 ) ) ;
#7145=CARTESIAN_POINT ( 'NONE',  ( 4.722721840544713778, -27.80484921947353527, 7.750000000000000888 ) ) ;
#7150=CARTESIAN_POINT ( 'NONE',  ( 2.921884697477863835, -32.84986306847065407, 7.737115613922532553 ) ) ;
#7151=CYLINDRICAL_SURFACE ( 'NONE', #18633, 0.09010775117053204664 ) ;
#7155=CARTESIAN_POINT ( 'NONE',  ( -0.3564456010502966565, -26.86262611937285172, 6.876076431790004939 ) ) ;
#7163=ADVANCED_FACE ( 'NONE', ( #21535 ), #15338, .F. ) ;
#7166=DIRECTION ( 'NONE',  ( 0.9396926207859082059, 0.3420201433256695456, -0.000000000000000000 ) ) ;
#7167=CARTESIAN_POINT ( 'NONE',  ( -1.235538214096436826, -27.66458519074676303, 6.912143950357346966 ) ) ;
#7172=ADVANCED_FACE ( 'NONE', ( #12658 ), #22152, .F. ) ;
#7174=AXIS2_PLACEMENT_3D ( 'NONE', #10856, #13958, #36193 ) ;
#7175=ORIENTED_EDGE ( 'NONE', *, *, #13158, .F. ) ;
#7180=CARTESIAN_POINT ( 'NONE',  ( 5.026745426458600896, -30.27374936809274786, 6.864236717600932458 ) ) ;
#7181=CARTESIAN_POINT ( 'NONE',  ( 4.618939889237452689, -31.31408416873490097, 6.892063359921934307 ) ) ;
#7188=ORIENTED_EDGE ( 'NONE', *, *, #11233, .T. ) ;
#7189=VECTOR ( 'NONE', #31982, 1000.000000000000114 ) ;
#7192=ORIENTED_EDGE ( 'NONE', *, *, #21960, .F. ) ;
#7196=CARTESIAN_POINT ( 'NONE',  ( -1.790841395663789193, -29.55182921846484945, 7.778495531946296282 ) ) ;
#7197=ORIENTED_EDGE ( 'NONE', *, *, #40270, .T. ) ;
#7199=CARTESIAN_POINT ( 'NONE',  ( 5.069616211753222856, -29.11340517107872472, 6.865312560952602894 ) ) ;
#7200=AXIS2_PLACEMENT_3D ( 'NONE', #19695, #26080, #1182 ) ;
#7202=CARTESIAN_POINT ( 'NONE',  ( 0.5713750229309367823, -32.77700439067807281, 7.695279973900954751 ) ) ;
#7204=( BOUNDED_CURVE ( )  B_SPLINE_CURVE ( 3, ( #13384, #36227, #26366, #38493 ),
 .UNSPECIFIED., .F., .F. ) 
 B_SPLINE_CURVE_WITH_KNOTS ( ( 4, 4 ),
 ( 1.347909859412853351, 1.534781240595297636 ),
 .UNSPECIFIED. ) 
 CURVE ( )  GEOMETRIC_REPRESENTATION_ITEM ( )  RATIONAL_B_SPLINE_CURVE ( ( 1.000000000000000000, 0.9970920404276226723, 0.9970920404276226723, 1.000000000000000000 ) ) 
 REPRESENTATION_ITEM ( '' )  );
#7205=EDGE_LOOP ( 'NONE', ( #1169, #39297, #2018, #37281 ) ) ;
#7210=ORIENTED_EDGE ( 'NONE', *, *, #38857, .F. ) ;
#7212=CARTESIAN_POINT ( 'NONE',  ( 1.640982164150366795, -33.05455003082661136, 7.785593909369613819 ) ) ;
#7216=AXIS2_PLACEMENT_3D ( 'NONE', #13784, #6805, #2986 ) ;
#7217=EDGE_CURVE ( 'NONE', #24455, #4723, #26637, .T. ) ;
#7218=VERTEX_POINT ( 'NONE', #27689 ) ;
#7224=CARTESIAN_POINT ( 'NONE',  ( 2.586165941411596947, -24.87425163552211416, 7.013842709614101167 ) ) ;
#7229=ORIENTED_EDGE ( 'NONE', *, *, #18206, .F. ) ;
#7231=CARTESIAN_POINT ( 'NONE',  ( -1.600658481268678823, -28.40671124064021669, 7.686927408461905920 ) ) ;
#7235=B_SPLINE_CURVE_WITH_KNOTS ( 'NONE', 3,
 ( #502, #18806, #31379, #3205, #22328, #28278, #25599, #97, #26414, #29096, #26809, #32994, #17312, #4192, #20414, #10138, #22728, #1309, #4589, #10941, #1113, #22922, #4779, #10542, #20217, #19628, #29889, #32800, #1707, #32399, #23520 ),
 .UNSPECIFIED., .F., .F.,
 ( 4, 3, 3, 3, 3, 3, 3, 3, 3, 3, 4 ),
 ( 1.226634733346699349E-18, 3.077658087705631944E-05, 6.152638666998957247E-05, 9.267501192706370972E-05, 0.0001241882240135194695, 0.0001556618703051673421, 0.0001866161554452211652, 0.0002167966385860971171, 0.0002463805737537774895, 0.0002758761370306536285, 0.0002847094172290096569 ),
 .UNSPECIFIED. ) ;
#7236=CARTESIAN_POINT ( 'NONE',  ( 4.376998081151240783, -27.47332109273945733, 6.864276522220859711 ) ) ;
#7239=CARTESIAN_POINT ( 'NONE',  ( 1.685055500909720561, -26.06996366628073858, 7.637894019485640840 ) ) ;
#7241=CARTESIAN_POINT ( 'NONE',  ( -0.1737877179784135528, -32.52584925061469789, 6.875780273367531947 ) ) ;
#7243=CARTESIAN_POINT ( 'NONE',  ( 2.311026925537185139, -26.22520041558805914, 7.779495906702013741 ) ) ;
#7244=CARTESIAN_POINT ( 'NONE',  ( 3.569994541659591736, -26.73010724343094324, 6.997764925645180156 ) ) ;
#7246=DIRECTION ( 'NONE',  ( 0.000000000000000000, -0.6834397476448832442, -0.7300069255418734082 ) ) ;
#7249=CARTESIAN_POINT ( 'NONE',  ( 1.080192182740615126, -32.91288614359101672, 7.782167645815904145 ) ) ;
#7251=CARTESIAN_POINT ( 'NONE',  ( 3.306242093667368653, -32.56681097908001732, 7.768425012602591551 ) ) ;
#7253=LINE ( 'NONE', #10341, #30052 ) ;
#7256=ORIENTED_EDGE ( 'NONE', *, *, #28030, .F. ) ;
#7258=PLANE ( 'NONE',  #4763 ) ;
#7260=CARTESIAN_POINT ( 'NONE',  ( 1.713892699967726196, -25.86893018339335271, 7.635761828346577573 ) ) ;
#7266=CARTESIAN_POINT ( 'NONE',  ( 2.326171464738295835, -32.91184545387483951, 7.693875151218753317 ) ) ;
#7267=CARTESIAN_POINT ( 'NONE',  ( -1.457564949911021479, -28.30999727367718322, 6.864651958020304257 ) ) ;
#7268=DIRECTION ( 'NONE',  ( -0.4999999999999918954, -0.8660254037844432595, -0.000000000000000000 ) ) ;
#7269=LINE ( 'NONE', #29104, #28453 ) ;
#7270=VERTEX_POINT ( 'NONE', #536 ) ;
#7272=AXIS2_PLACEMENT_3D ( 'NONE', #38288, #10088, #34425 ) ;
#7273=CARTESIAN_POINT ( 'NONE',  ( -1.740147594125142749, -30.21234809103664176, 7.710604733652633769 ) ) ;
#7282=CARTESIAN_POINT ( 'NONE',  ( 5.118969260771242702, -33.45454016556441701, 7.754798119455333705 ) ) ;
#7288=CARTESIAN_POINT ( 'NONE',  ( -1.599034431228576247, -30.73774772367137942, 6.894806418505347700 ) ) ;
#7293=ORIENTED_EDGE ( 'NONE', *, *, #20123, .T. ) ;
#7295=ORIENTED_EDGE ( 'NONE', *, *, #9204, .T. ) ;
#7298=CARTESIAN_POINT ( 'NONE',  ( 3.281677335269463036, -32.69235404666142841, 6.941203072598471024 ) ) ;
#7299=CARTESIAN_POINT ( 'NONE',  ( -1.086691373026069884, -31.68704541418143705, 6.895394898881671786 ) ) ;
#7301=CARTESIAN_POINT ( 'NONE',  ( -0.8998472737371643326, -27.22723292372361570, 7.753200566781576875 ) ) ;
#7302=ADVANCED_FACE ( 'NONE', ( #29532 ), #29330, .T. ) ;
#7308=B_SPLINE_CURVE_WITH_KNOTS ( 'NONE', 3,
 ( #15158, #17617, #14953, #11852, #36178, #30626, #7959, #27716, #11438, #24428, #20508, #27520, #33304, #14332, #23801, #14734, #24003, #30195, #33091, #2015, #17824, #4875, #5287, #27306, #14532, #36578, #30405, #39868, #17410, #29994, #1808 ),
 .UNSPECIFIED., .F., .F.,
 ( 4, 3, 3, 3, 3, 3, 3, 3, 3, 3, 4 ),
 ( 0.000000000000000000, 2.999644130997589661E-05, 6.002588995694634868E-05, 8.960886084587892835E-05, 0.0001190604700446500010, 0.0001489538463052705820, 0.0001796139255493957678, 0.0002109707048517079188, 0.0002426195318110312908, 0.0002740640997890033651, 0.0002849778069099850159 ),
 .UNSPECIFIED. ) ;
#7309=CARTESIAN_POINT ( 'NONE',  ( 2.235028438126618333, -33.02886990452594063, 6.867280401193707640 ) ) ;
#7317=CARTESIAN_POINT ( 'NONE',  ( 2.251363620182238456, -32.92500435510202550, 7.784838882742139532 ) ) ;
#7318=CARTESIAN_POINT ( 'NONE',  ( 1.093737980128993037, -26.12620165286623930, 7.767720160662275219 ) ) ;
#7321=ORIENTED_EDGE ( 'NONE', *, *, #24917, .F. ) ;
#7323=B_SPLINE_CURVE_WITH_KNOTS ( 'NONE', 3,
 ( #21337, #14722, #8753, #4672, #33080, #17207, #4865, #17400, #14322, #33292 ),
 .UNSPECIFIED., .F., .F.,
 ( 4, 3, 3, 4 ),
 ( 0.000000000000000000, 3.025505781527821749E-05, 6.051003801291572674E-05, 6.468145402690739221E-05 ),
 .UNSPECIFIED. ) ;
#7326=DIRECTION ( 'NONE',  ( 0.3420201433256790380, -0.9396926207859046531, -0.000000000000000000 ) ) ;
#7330=CARTESIAN_POINT ( 'NONE',  ( 0.9751061736955158876, -32.99397343253602344, 6.865706122441728176 ) ) ;
#7331=CARTESIAN_POINT ( 'NONE',  ( -1.785187679209235379, -29.50141875348822751, 7.784513003884693916 ) ) ;
#7333=CARTESIAN_POINT ( 'NONE',  ( 4.946955026107762166, -30.87529236204174765, 7.761113333117553914 ) ) ;
#7346=CARTESIAN_POINT ( 'NONE',  ( 3.923056598701467834, -26.86627451898972652, 7.710604733652633769 ) ) ;
#7347=EDGE_CURVE ( 'NONE', #24455, #19192, #13879, .T. ) ;
#7352=CARTESIAN_POINT ( 'NONE',  ( 4.886820230737117576, -28.38388714888618480, 7.740055089680400791 ) ) ;
#7361=CARTESIAN_POINT ( 'NONE',  ( 4.826124500149282959, -30.90777074620061171, 6.895222827070020877 ) ) ;
#7362=CARTESIAN_POINT ( 'NONE',  ( 4.372846383550529126, -27.30984669459420289, 7.635761828346578461 ) ) ;
#7365=CARTESIAN_POINT ( 'NONE',  ( 4.907037958954144408, -30.70015833522101545, 7.712764235869105534 ) ) ;
#7374=ORIENTED_EDGE ( 'NONE', *, *, #30465, .F. ) ;
#7375=DIRECTION ( 'NONE',  ( 0.000000000000000000, 0.7541618601367601205, -0.6566885781822779933 ) ) ;
#7383=ORIENTED_EDGE ( 'NONE', *, *, #1940, .T. ) ;
#7384=CARTESIAN_POINT ( 'NONE',  ( 5.123272199033605645, -30.27793340842993786, 7.771081512783704071 ) ) ;
#7385=EDGE_CURVE ( 'NONE', #40564, #27839, #20610, .T. ) ;
#7390=ORIENTED_EDGE ( 'NONE', *, *, #32756, .F. ) ;
#7391=CARTESIAN_POINT ( 'NONE',  ( 0.3765978019783249309, -32.70163482617414275, 6.882085323592684212 ) ) ;
#7394=CYLINDRICAL_SURFACE ( 'NONE', #36478, 3.399999999999999911 ) ;
#7395=ORIENTED_EDGE ( 'NONE', *, *, #7107, .F. ) ;
#7396=EDGE_CURVE ( 'NONE', #19528, #5651, #29686, .T. ) ;
#7402=CARTESIAN_POINT ( 'NONE',  ( 0.5616195162123727158, -32.77355560770597975, 7.652160403243383868 ) ) ;
#7404=DIRECTION ( 'NONE',  ( 1.000000000000000000, 0.000000000000000000, 0.000000000000000000 ) ) ;
#7406=CARTESIAN_POINT ( 'NONE',  ( -1.641762495386305254, -30.19444782469885880, 7.712764235869103757 ) ) ;
#7407=CARTESIAN_POINT ( 'NONE',  ( 4.998738087972761868, -28.44140482322499963, 7.784725160561909441 ) ) ;
#7408=ORIENTED_EDGE ( 'NONE', *, *, #14620, .F. ) ;
#7411=CARTESIAN_POINT ( 'NONE',  ( -1.613161587038500766, -30.69708474973657530, 6.867280401193708528 ) ) ;
#7415=LINE ( 'NONE', #1265, #25983 ) ;
#7418=CARTESIAN_POINT ( 'NONE',  ( 3.805094080858060668, -32.36639755374996241, 6.989977667959446528 ) ) ;
#7424=VERTEX_POINT ( 'NONE', #32832 ) ;
#7426=CARTESIAN_POINT ( 'NONE',  ( -1.593833517588955972, -28.38751944612305422, 7.638132480492516585 ) ) ;
#7430=AXIS2_PLACEMENT_3D ( 'NONE', #2036, #29609, #20738 ) ;
#7432=CARTESIAN_POINT ( 'NONE',  ( 1.810168977974152105, -26.07424362682720442, 7.766640943994646662 ) ) ;
#7433=DIRECTION ( 'NONE',  ( -1.000000000000000000, 0.000000000000000000, 0.000000000000000000 ) ) ;
#7436=( BOUNDED_CURVE ( )  B_SPLINE_CURVE ( 3, ( #38688, #32934, #19958, #13790 ),
 .UNSPECIFIED., .F., .T. ) 
 B_SPLINE_CURVE_WITH_KNOTS ( ( 4, 4 ),
 ( 1.347909859412854017, 1.534781240595299634 ),
 .UNSPECIFIED. ) 
 CURVE ( )  GEOMETRIC_REPRESENTATION_ITEM ( )  RATIONAL_B_SPLINE_CURVE ( ( 1.000000000000000000, 0.9970920404276225613, 0.9970920404276225613, 1.000000000000000000 ) ) 
 REPRESENTATION_ITEM ( '' )  );
#7437=CARTESIAN_POINT ( 'NONE',  ( -0.2037329942765146173, -32.50665443916160058, 6.998987538705438105 ) ) ;
#7439=B_SPLINE_CURVE_WITH_KNOTS ( 'NONE', 3,
 ( #4032, #6702, #13267, #19251 ),
 .UNSPECIFIED., .F., .F.,
 ( 4, 4 ),
 ( 0.000000000000000000, 6.391136169898433355E-06 ),
 .UNSPECIFIED. ) ;
#7440=CARTESIAN_POINT ( 'NONE',  ( -0.8688903936063803179, -27.19321022093548734, 7.013842709614101167 ) ) ;
#7442=EDGE_CURVE ( 'NONE', #27839, #35245, #3027, .T. ) ;
#7451=DIRECTION ( 'NONE',  ( -0.000000000000000000, -0.000000000000000000, -1.000000000000000000 ) ) ;
#7455=AXIS2_PLACEMENT_3D ( 'NONE', #36732, #26859, #30364 ) ;
#7458=ORIENTED_EDGE ( 'NONE', *, *, #2864, .T. ) ;
#7460=PLANE ( 'NONE',  #39575 ) ;
#7462=LINE ( 'NONE', #7260, #11443 ) ;
#7463=ORIENTED_EDGE ( 'NONE', *, *, #9860, .T. ) ;
#7464=CARTESIAN_POINT ( 'NONE',  ( -1.577879219085749574, -30.81516921323670744, 7.255881584735163869 ) ) ;
#7467=CARTESIAN_POINT ( 'NONE',  ( 0.4728567017103387782, -26.29225390702066179, 7.670465701733746755 ) ) ;
#7469=CARTESIAN_POINT ( 'NONE',  ( 4.397682185089559326, -31.80032238106598186, 7.651421919295144924 ) ) ;
#7470=ORIENTED_EDGE ( 'NONE', *, *, #28244, .T. ) ;
#7475=AXIS2_PLACEMENT_3D ( 'NONE', #30738, #27423, #31137 ) ;
#7479=B_SPLINE_CURVE_WITH_KNOTS ( 'NONE', 3,
 ( #23894, #27400, #5180, #30292 ),
 .UNSPECIFIED., .F., .F.,
 ( 4, 4 ),
 ( 2.100641709190665082E-19, 6.391136169898844166E-06 ),
 .UNSPECIFIED. ) ;
#7481=CARTESIAN_POINT ( 'NONE',  ( -1.717161396028226150, -28.81472039912961591, 6.878836779550822733 ) ) ;
#7494=CARTESIAN_POINT ( 'NONE',  ( -1.057258846844102873, -31.72486802769777725, 7.754798119455333705 ) ) ;
#7495=EDGE_CURVE ( 'NONE', #19268, #39722, #29723, .T. ) ;
#7499=CARTESIAN_POINT ( 'NONE',  ( 5.108737389288024566, -30.36564925015480654, 6.941203072598473689 ) ) ;
#7502=CARTESIAN_POINT ( 'NONE',  ( 5.094274781369510841, -29.77377858573793645, 6.920489980334481928 ) ) ;
#7503=AXIS2_PLACEMENT_3D ( 'NONE', #4004, #35294, #32401 ) ;
#7504=CARTESIAN_POINT ( 'NONE',  ( 0.3457495631895174948, -32.79715019981050972, 7.013842709614101167 ) ) ;
#7505=CARTESIAN_POINT ( 'NONE',  ( 4.301450302647315205, -31.91148321001355370, 7.754798119455333705 ) ) ;
#7510=CARTESIAN_POINT ( 'NONE',  ( 2.273382508532649116, -26.11715138113199686, 7.707984471951054850 ) ) ;
#7517=FACE_OUTER_BOUND ( 'NONE', #14999, .T. ) ;
#7519=EDGE_LOOP ( 'NONE', ( #6621, #23845, #13661, #8467 ) ) ;
#7520=CARTESIAN_POINT ( 'NONE',  ( 5.200390093233090205, -29.78421258894830004, 7.376841543590331618 ) ) ;
#7525=CARTESIAN_POINT ( 'NONE',  ( -1.294668884637889983, -31.17919483241161771, 6.864651958020304257 ) ) ;
#7526=EDGE_CURVE ( 'NONE', #22132, #31681, #25093, .T. ) ;
#7529=CARTESIAN_POINT ( 'NONE',  ( 2.913833110970087681, -32.85284901314008010, 7.750000000000001776 ) ) ;
#7530=CARTESIAN_POINT ( 'NONE',  ( 4.037545593495729612, -27.10057719777305962, 6.988553391373222290 ) ) ;
#7534=VERTEX_POINT ( 'NONE', #24152 ) ;
#7535=DIRECTION ( 'NONE',  ( -0.9848077530122015810, -0.1736481776669674404, 0.000000000000000000 ) ) ;
#7537=CARTESIAN_POINT ( 'NONE',  ( -1.763152082461436843, -30.07389502416336668, 6.863784140767622333 ) ) ;
#7538=CARTESIAN_POINT ( 'NONE',  ( -0.5525555990343373747, -32.24114388472590775, 7.773839561854632763 ) ) ;
#7540=EDGE_CURVE ( 'NONE', #12025, #12828, #8358, .T. ) ;
#7542=FACE_OUTER_BOUND ( 'NONE', #6060, .T. ) ;
#7545=CYLINDRICAL_SURFACE ( 'NONE', #39766, 0.09010775117052929883 ) ;
#7548=CARTESIAN_POINT ( 'NONE',  ( 4.487153213455422396, -27.45239593059636363, 7.013842709614101167 ) ) ;
#7550=CARTESIAN_POINT ( 'NONE',  ( 5.149536281657578485, -30.16439681061213918, 7.635761828346576685 ) ) ;
#7552=B_SPLINE_CURVE_WITH_KNOTS ( 'NONE', 3,
 ( #26493, #26887, #10623, #1391, #17392, #20099, #35770, #23784, #29973, #13922, #11017, #4477, #36363, #29575, #39018, #8130, #10822, #20701, #35963, #5065, #4665, #33284, #17598, #27090, #5266 ),
 .UNSPECIFIED., .F., .F.,
 ( 4, 3, 3, 3, 3, 3, 3, 3, 4 ),
 ( 6.468151674593380289E-05, 9.076621574722002080E-05, 0.0001210204262067981427, 0.0001512763324577423183, 0.0001815301820994218098, 0.0002117781465860724133, 0.0002420274594459777555, 0.0002722905548971147043, 0.0002816827545175574869 ),
 .UNSPECIFIED. ) ;
#7555=EDGE_CURVE ( 'NONE', #25058, #9646, #40203, .T. ) ;
#7562=CARTESIAN_POINT ( 'NONE',  ( -1.292970362984873223, -27.75612332118079095, 6.867280401193707640 ) ) ;
#7563=ORIENTED_EDGE ( 'NONE', *, *, #37581, .F. ) ;
#7568=CYLINDRICAL_SURFACE ( 'NONE', #22138, 0.09010775117052938210 ) ;
#7579=CARTESIAN_POINT ( 'NONE',  ( 0.02833428261566706824, -32.53037429976859585, 7.721096864323904185 ) ) ;
#7581=LINE ( 'NONE', #10659, #1449 ) ;
#7585=VERTEX_POINT ( 'NONE', #18791 ) ;
#7586=CARTESIAN_POINT ( 'NONE',  ( 2.336689928817082151, -33.01160456067486848, 7.730015791551948290 ) ) ;
#7592=EDGE_CURVE ( 'NONE', #26219, #21380, #27051, .T. ) ;
#7593=ORIENTED_EDGE ( 'NONE', *, *, #36258, .T. ) ;
#7597=CARTESIAN_POINT ( 'NONE',  ( -0.4954141421830357550, -26.97407892422453202, 7.635761828346577573 ) ) ;
#7598=ORIENTED_EDGE ( 'NONE', *, *, #23247, .F. ) ;
#7600=DIRECTION ( 'NONE',  ( -1.000000000000000000, 0.000000000000000000, 0.000000000000000000 ) ) ;
#7603=CARTESIAN_POINT ( 'NONE',  ( 2.428848143534461101, -33.77897949353074836, 7.635761828346577573 ) ) ;
#7608=CARTESIAN_POINT ( 'NONE',  ( -1.133852526008121142, -27.69188090276239933, 6.969307238440509700 ) ) ;
#7609=ORIENTED_EDGE ( 'NONE', *, *, #34523, .F. ) ;
#7610=VERTEX_POINT ( 'NONE', #2770 ) ;
#7613=CARTESIAN_POINT ( 'NONE',  ( -0.5217032702065451666, -32.27405686018898479, 7.686927408461905920 ) ) ;
#7618=ORIENTED_EDGE ( 'NONE', *, *, #10630, .F. ) ;
#7621=CARTESIAN_POINT ( 'NONE',  ( 4.919815665899403889, -28.47658946930290469, 6.874555630061442990 ) ) ;
#7624=CARTESIAN_POINT ( 'NONE',  ( 4.355968852827314386, -27.44672806176293278, 7.782034975670476307 ) ) ;
#7628=EDGE_CURVE ( 'NONE', #35289, #28513, #6041, .T. ) ;
#7630=CARTESIAN_POINT ( 'NONE',  ( -1.317602929293604674, -31.34242190827973218, 7.737115613922529889 ) ) ;
#7632=CARTESIAN_POINT ( 'NONE',  ( -1.600658481268679267, -28.40671124064021669, 7.695279973900954751 ) ) ;
#7639=B_SPLINE_CURVE_WITH_KNOTS ( 'NONE', 3,
 ( #15345, #30816, #15139, #14718, #15555, #31216, #12038, #36970, #24828, #33697, #27901, #24413, #3037, #8550, #2823, #8749, #37372, #5682, #18019, #24616, #14938, #27698, #37171, #7796, #11626 ),
 .UNSPECIFIED., .F., .F.,
 ( 4, 3, 3, 3, 3, 3, 3, 3, 4 ),
 ( 6.468151674593702839E-05, 9.076621574722029185E-05, 0.0001210204262067993760, 0.0001512763324577439446, 0.0001815301820994234903, 0.0002117781465860706243, 0.0002420274594459773489, 0.0002722905548971168185, 0.0002816827545175608479 ),
 .UNSPECIFIED. ) ;
#7640=CARTESIAN_POINT ( 'NONE',  ( 1.700390093233090871, -29.56993018339339940, 7.750000000000000888 ) ) ;
#7642=CARTESIAN_POINT ( 'NONE',  ( 4.358291535071521672, -27.29274773012506827, 7.695279973900954751 ) ) ;
#7647=CARTESIAN_POINT ( 'NONE',  ( 2.403859601798915779, -26.24350106938568317, 7.761597726988851420 ) ) ;
#7648=CARTESIAN_POINT ( 'NONE',  ( -1.017153196554518857, -27.35348519339999029, 7.255881584735165646 ) ) ;
#7649=CARTESIAN_POINT ( 'NONE',  ( 4.668540769505296950, -31.42424039273510061, 7.754798119455333705 ) ) ;
#7651=CARTESIAN_POINT ( 'NONE',  ( 0.7091610176047873360, -26.31761870563095584, 6.887945620086119547 ) ) ;
#7652=CARTESIAN_POINT ( 'NONE',  ( 0.08572186079895513511, -26.46462327674753112, 6.880828092187099010 ) ) ;
#7654=CARTESIAN_POINT ( 'NONE',  ( 1.145429890469515932, -32.92433313672930240, 7.695279973900954751 ) ) ;
#7656=CARTESIAN_POINT ( 'NONE',  ( -1.553762755224460390, -28.32229481116360148, 7.785593909369613819 ) ) ;
#7660=CARTESIAN_POINT ( 'NONE',  ( 4.327092635631263562, -31.72873540009916837, 7.712764235869101093 ) ) ;
#7663=FACE_OUTER_BOUND ( 'NONE', #35038, .T. ) ;
#7665=CARTESIAN_POINT ( 'NONE',  ( 5.100363281305461349, -29.55642757665872722, 7.635761828346577573 ) ) ;
#7670=CARTESIAN_POINT ( 'NONE',  ( 0.9405239856375441354, -32.88393131473412012, 6.882085323592684212 ) ) ;
#7671=DIRECTION ( 'NONE',  ( -0.7055275666422152758, 0.2567910337120286601, -0.6605219282605402364 ) ) ;
#7672=DIRECTION ( 'NONE',  ( -0.000000000000000000, -0.000000000000000000, -1.000000000000000000 ) ) ;
#7679=EDGE_CURVE ( 'NONE', #347, #29836, #23617, .T. ) ;
#7685=CARTESIAN_POINT ( 'NONE',  ( -1.656077431862442717, -30.11226380117775037, 6.894806418505347700 ) ) ;
#7692=LINE ( 'NONE', #8078, #38661 ) ;
#7698=DIRECTION ( 'NONE',  ( -0.7660444431189813441, 0.6427876096865353661, -0.000000000000000000 ) ) ;
#7699=ORIENTED_EDGE ( 'NONE', *, *, #25169, .F. ) ;
#7702=CYLINDRICAL_SURFACE ( 'NONE', #24889, 0.09010775117052782779 ) ;
#7703=CARTESIAN_POINT ( 'NONE',  ( 5.110065143779969787, -30.35994034135222464, 6.921725064902949143 ) ) ;
#7705=CARTESIAN_POINT ( 'NONE',  ( -89.20959394718985891, -30.27593629695115496, 6.954324564059724878 ) ) ;
#7708=CARTESIAN_POINT ( 'NONE',  ( 2.140324932704912975, -33.04217115098462898, 6.895394898881669121 ) ) ;
#7714=VECTOR ( 'NONE', #8151, 1000.000000000000227 ) ;
#7723=CARTESIAN_POINT ( 'NONE',  ( 5.054776957217135269, -30.12498762792620255, 7.691066658568944447 ) ) ;
#7724=ORIENTED_EDGE ( 'NONE', *, *, #29155, .F. ) ;
#7725=EDGE_CURVE ( 'NONE', #5658, #40275, #17045, .T. ) ;
#7730=CARTESIAN_POINT ( 'NONE',  ( 6.053772676492744864, -27.07209504432901070, 7.635761828346577573 ) ) ;
#7731=AXIS2_PLACEMENT_3D ( 'NONE', #12305, #40101, #24879 ) ;
#7732=DIRECTION ( 'NONE',  ( -1.000000000000000000, 0.000000000000000000, 0.000000000000000000 ) ) ;
#7733=CARTESIAN_POINT ( 'NONE',  ( 3.934882339056233302, -27.00729354443371477, 6.880147297696980857 ) ) ;
#7738=CARTESIAN_POINT ( 'NONE',  ( -1.312560436656866392, -31.35097737660188244, 7.695279973900954751 ) ) ;
#7741=CARTESIAN_POINT ( 'NONE',  ( -0.03016364352379581268, -26.64329662474590066, 7.680992449362114449 ) ) ;
#7744=LINE ( 'NONE', #38829, #36722 ) ;
#7747=DIRECTION ( 'NONE',  ( 0.1736481776669127897, 0.9848077530122111289, 0.000000000000000000 ) ) ;
#7749=EDGE_CURVE ( 'NONE', #40076, #30228, #10124, .T. ) ;
#7750=CARTESIAN_POINT ( 'NONE',  ( 4.466905112401445166, -27.42599002650289819, 6.870724624169669781 ) ) ;
#7761=CARTESIAN_POINT ( 'NONE',  ( -0.4043138943918587747, -26.77346281303682218, 6.989977667959440311 ) ) ;
#7762=CARTESIAN_POINT ( 'NONE',  ( -1.233457003589831347, -27.66138591813160019, 6.921725064902950919 ) ) ;
#7768=EDGE_LOOP ( 'NONE', ( #1, #39472, #12966, #30977 ) ) ;
#7776=CARTESIAN_POINT ( 'NONE',  ( -0.7662878407683642035, -27.22994832146974176, 6.979335674598006634 ) ) ;
#7778=CARTESIAN_POINT ( 'NONE',  ( -0.04300629806284254203, -32.48894888815854642, 7.785868773668302545 ) ) ;
#7781=FACE_OUTER_BOUND ( 'NONE', #24645, .T. ) ;
#7785=VERTEX_POINT ( 'NONE', #10528 ) ;
#7795=ORIENTED_EDGE ( 'NONE', *, *, #2280, .F. ) ;
#7796=CARTESIAN_POINT ( 'NONE',  ( 5.067448495235368888, -29.09778390448199659, 7.757178535559534183 ) ) ;
#7797=CARTESIAN_POINT ( 'NONE',  ( 4.381563664431031846, -27.47916279290977570, 7.754798119455333705 ) ) ;
#7804=ORIENTED_EDGE ( 'NONE', *, *, #28965, .F. ) ;
#7805=CARTESIAN_POINT ( 'NONE',  ( -1.675359094926574866, -29.97529103330290212, 7.013842709614101167 ) ) ;
#7807=LINE ( 'NONE', #16654, #15199 ) ;
#7808=CARTESIAN_POINT ( 'NONE',  ( -1.133226946762783793, -27.69093715879794360, 6.949473656533220023 ) ) ;
#7810=ORIENTED_EDGE ( 'NONE', *, *, #12864, .T. ) ;
#7813=CARTESIAN_POINT ( 'NONE',  ( -0.5217032702065468319, -32.27405686018897768, 7.695279973900954751 ) ) ;
#7816=ORIENTED_EDGE ( 'NONE', *, *, #38021, .F. ) ;
#7818=EDGE_CURVE ( 'NONE', #18445, #30749, #6423, .T. ) ;
#7819=SHAPE_REPRESENTATION_RELATIONSHIP ( 'NONE' , 'NONE' ,  #23772, #21063 ) ;
#7822=CARTESIAN_POINT ( 'NONE',  ( 4.817771186832979780, -27.97871391774301486, 6.998987538705432776 ) ) ;
#7823=DIRECTION ( 'NONE',  ( -0.000000000000000000, -0.000000000000000000, -1.000000000000000000 ) ) ;
#7827=FACE_OUTER_BOUND ( 'NONE', #38939, .T. ) ;
#7830=B_SPLINE_CURVE_WITH_KNOTS ( 'NONE', 3,
 ( #19963, #26948, #10688, #23844, #36220, #7608, #23655, #7808, #20161, #26555, #8000, #32747, #20762, #39494, #33356, #4537, #5130, #13982, #29835, #20556, #39091, #10887, #14185, #36030, #20359, #4727, #17662, #24262, #14783, #5536, #24465 ),
 .UNSPECIFIED., .F., .F.,
 ( 4, 3, 3, 3, 3, 3, 3, 3, 3, 3, 4 ),
 ( 1.852685484479510593E-18, 2.999644130997501231E-05, 6.002588995694337391E-05, 8.960886084587722073E-05, 0.0001190604700446470872, 0.0001489538463052668957, 0.0001796139255493938976, 0.0002109707048517038531, 0.0002426195318110337031, 0.0002740640997890010340, 0.0002849778069099823054 ),
 .UNSPECIFIED. ) ;
#7832=CARTESIAN_POINT ( 'NONE',  ( 1.096693473209699121, -26.22395493079927320, 7.635761828346577573 ) ) ;
#7836=LINE ( 'NONE', #14813, #21779 ) ;
#7840=CARTESIAN_POINT ( 'NONE',  ( 5.053206214525213902, -25.63013845337225405, 7.695279973900954751 ) ) ;
#7850=CARTESIAN_POINT ( 'NONE',  ( -0.001601940877974058304, -26.51162622272786606, 6.875671892026061549 ) ) ;
#7853=CARTESIAN_POINT ( 'NONE',  ( -1.699583094839331787, -29.58343279012807159, 7.635761828346577573 ) ) ;
#7855=CARTESIAN_POINT ( 'NONE',  ( -1.550429272321787622, -28.30655406119563722, 7.782861076432732617 ) ) ;
#7859=EDGE_CURVE ( 'NONE', #18940, #26569, #19692, .T. ) ;
#7865=CARTESIAN_POINT ( 'NONE',  ( 4.716523069940627089, -27.79427549280784149, 7.660770905198780234 ) ) ;
#7871=CARTESIAN_POINT ( 'NONE',  ( 0.9202033279314624226, -32.87921311799081536, 7.006423389747790331 ) ) ;
#7873=CARTESIAN_POINT ( 'NONE',  ( 0.3560817122006099678, -32.80147640128887332, 6.883550009118462931 ) ) ;
#7876=CARTESIAN_POINT ( 'NONE',  ( -1.740039500620327972, -30.21292645845072400, 7.700536657684220465 ) ) ;
#7882=CARTESIAN_POINT ( 'NONE',  ( -1.729658636700265983, -28.87367900006760735, 6.864746396199586265 ) ) ;
#7886=AXIS2_PLACEMENT_3D ( 'NONE', #40186, #34045, #37100 ) ;
#7903=CARTESIAN_POINT ( 'NONE',  ( 3.283585891740897544, -32.69138896436592034, 6.931070083220553180 ) ) ;
#7904=CARTESIAN_POINT ( 'NONE',  ( 5.113812245512664667, -30.34358980514384285, 7.013842709614101167 ) ) ;
#7905=CARTESIAN_POINT ( 'NONE',  ( 6.173121028034443292, -31.06824956420287975, 7.754798119455333705 ) ) ;
#7907=ADVANCED_FACE ( 'NONE', ( #5174 ), #8040, .F. ) ;
#7908=CARTESIAN_POINT ( 'NONE',  ( 1.888561142012757044, -26.07499217873563779, 6.980586498568967180 ) ) ;
#7913=VECTOR ( 'NONE', #37773, 1000.000000000000000 ) ;
#7917=( BOUNDED_CURVE ( )  B_SPLINE_CURVE ( 3, ( #14237, #35888, #7060, #7665 ),
 .UNSPECIFIED., .F., .T. ) 
 B_SPLINE_CURVE_WITH_KNOTS ( ( 4, 4 ),
 ( 1.381924640371167579, 1.574767692156076260 ),
 .UNSPECIFIED. ) 
 CURVE ( )  GEOMETRIC_REPRESENTATION_ITEM ( )  RATIONAL_B_SPLINE_CURVE ( ( 1.000000000000000000, 0.9969033633783032089, 0.9969033633783032089, 1.000000000000000000 ) ) 
 REPRESENTATION_ITEM ( '' )  );
#7922=CARTESIAN_POINT ( 'NONE',  ( -1.752498985642892304, -28.99760421947164701, 7.695279973900954751 ) ) ;
#7924=EDGE_LOOP ( 'NONE', ( #37577, #27002, #28454, #16920 ) ) ;
#7926=CARTESIAN_POINT ( 'NONE',  ( 5.166053052204034657, -29.08252373668924307, 7.754798119455333705 ) ) ;
#7928=CARTESIAN_POINT ( 'NONE',  ( 0.5073350864888854783, -26.38612432390972273, 7.721096864323905073 ) ) ;
#7930=CARTESIAN_POINT ( 'NONE',  ( 4.038094055326753029, -27.10109490474136607, 6.920489980334480151 ) ) ;
#7933=ORIENTED_EDGE ( 'NONE', *, *, #12366, .F. ) ;
#7938=CARTESIAN_POINT ( 'NONE',  ( -0.3565594025764889374, -32.28597026120641544, 7.139196562012274150 ) ) ;
#7942=CARTESIAN_POINT ( 'NONE',  ( 3.369155479471896530, -26.60763004909045293, 7.695279973900954751 ) ) ;
#7944=CARTESIAN_POINT ( 'NONE',  ( 0.6797214339997408317, -26.22205989199040133, 6.921725064902949143 ) ) ;
#7945=EDGE_CURVE ( 'NONE', #16154, #32844, #15232, .T. ) ;
#7947=CARTESIAN_POINT ( 'NONE',  ( 3.977533665642330352, -32.22786493825372389, 7.698786668945015954 ) ) ;
#7950=CARTESIAN_POINT ( 'NONE',  ( 4.202471298688592150, -31.87203467081731745, 6.871394612369937427 ) ) ;
#7954=CARTESIAN_POINT ( 'NONE',  ( 2.278721782424116160, -33.01050799907499567, 7.781480525794717273 ) ) ;
#7958=B_SPLINE_CURVE_WITH_KNOTS ( 'NONE', 3,
 ( #33972, #2885, #15406, #2263, #24055, #14788, #19117, #6768, #12727, #19526, #25500, #22014, #13330, #25702, #11034, #29592, #4291, #20506, #29992 ),
 .UNSPECIFIED., .F., .F.,
 ( 4, 3, 3, 3, 3, 3, 4 ),
 ( 8.940560153363745023E-19, 2.546128104244470004E-05, 5.711050680484456503E-05, 8.113074941676400118E-05, 0.0001053129305727060346, 0.0001360598016347115799, 0.0001612931755713786319 ),
 .UNSPECIFIED. ) ;
#7959=CARTESIAN_POINT ( 'NONE',  ( -1.605123960799514249, -28.77395478264728723, 6.959317978105167057 ) ) ;
#7963=VERTEX_POINT ( 'NONE', #8650 ) ;
#7964=CARTESIAN_POINT ( 'NONE',  ( -0.5359795030213230227, -32.26226207767182785, 7.750000000000001776 ) ) ;
#7969=CARTESIAN_POINT ( 'NONE',  ( 4.737757460784507657, -27.85713558299313064, 7.783750581861600182 ) ) ;
#7972=CARTESIAN_POINT ( 'NONE',  ( 3.344239474442606941, -32.54613940854532217, 6.880147297696980857 ) ) ;
#7975=DIRECTION ( 'NONE',  ( 0.7126435865141255155, 0.000000000000000000, -0.7015262779114437297 ) ) ;
#7978=CARTESIAN_POINT ( 'NONE',  ( 2.343386368290429012, -33.01035977724681914, 7.700536657684215136 ) ) ;
#7987=CARTESIAN_POINT ( 'NONE',  ( 3.598499603178781037, -24.87029584672219329, 6.954324564059724878 ) ) ;
#7996=ORIENTED_EDGE ( 'NONE', *, *, #33635, .T. ) ;
#7998=CARTESIAN_POINT ( 'NONE',  ( -1.641525177248355227, -30.19571155489859393, 7.695279973900954751 ) ) ;
#7999=AXIS2_PLACEMENT_3D ( 'NONE', #19936, #35415, #13766 ) ;
#8000=CARTESIAN_POINT ( 'NONE',  ( -1.136876063035818785, -27.69644994437396690, 6.920489980334479263 ) ) ;
#8014=EDGE_CURVE ( 'NONE', #21404, #21657, #21285, .T. ) ;
#8015=B_SPLINE_CURVE_WITH_KNOTS ( 'NONE', 3,
 ( #3810, #19832, #38952, #35498, #20027, #7469, #35697, #16327, #13854, #4010 ),
 .UNSPECIFIED., .F., .F.,
 ( 4, 3, 3, 4 ),
 ( 0.0002170292169044733984, 0.0002420761345915937069, 0.0002723302478206994981, 0.0002816811360866810837 ),
 .UNSPECIFIED. ) ;
#8016=CARTESIAN_POINT ( 'NONE',  ( 5.200390093233090205, -29.56993018339339940, 7.202408869016171167 ) ) ;
#8020=CARTESIAN_POINT ( 'NONE',  ( -1.229291416742352983, -31.29531890774162761, 7.661510568013100375 ) ) ;
#8021=EDGE_LOOP ( 'NONE', ( #35000, #22591, #6071, #33571, #12427 ) ) ;
#8023=CARTESIAN_POINT ( 'NONE',  ( -1.797707963539134868, -29.45456127420909453, 6.865482280155369210 ) ) ;
#8028=DIRECTION ( 'NONE',  ( -3.491481338843133750E-15, 1.000000000000000000, -0.000000000000000000 ) ) ;
#8029=CARTESIAN_POINT ( 'NONE',  ( 2.255350295996689347, -26.21552723005750352, 7.695279973900954751 ) ) ;
#8036=CARTESIAN_POINT ( 'NONE',  ( 2.455443087130759761, -25.36557027936252950, 7.635761828346577573 ) ) ;
#8037=AXIS2_PLACEMENT_3D ( 'NONE', #19020, #15919, #4190 ) ;
#8038=CARTESIAN_POINT ( 'NONE',  ( -1.666363480296579214, -25.64183336440431660, 7.695279973900954751 ) ) ;
#8039=CARTESIAN_POINT ( 'NONE',  ( 0.6070493791425947139, -26.35050461072708217, 6.874555630061442102 ) ) ;
#8040=CYLINDRICAL_SURFACE ( 'NONE', #32195, 0.09010775117053089478 ) ;
#8044=CARTESIAN_POINT ( 'NONE',  ( 5.913132016808740232, -27.35729686493488444, 6.894806418505347700 ) ) ;
#8045=FACE_OUTER_BOUND ( 'NONE', #21369, .T. ) ;
#8052=CARTESIAN_POINT ( 'NONE',  ( -0.6423071664414388149, -32.17016755036935649, 7.753200566781599967 ) ) ;
#8053=ORIENTED_EDGE ( 'NONE', *, *, #38697, .T. ) ;
#8054=CARTESIAN_POINT ( 'NONE',  ( -0.5081950327262328981, -32.15491601341089734, 7.782167645815903256 ) ) ;
#8055=CARTESIAN_POINT ( 'NONE',  ( 2.041952719453895781, -26.17999055166718847, 7.505001789837626447 ) ) ;
#8058=CARTESIAN_POINT ( 'NONE',  ( 3.325856478880445000, -25.14347697372913615, 7.635761828346577573 ) ) ;
#8060=CARTESIAN_POINT ( 'NONE',  ( 3.375652116166204753, -26.60313850063288754, 7.257242401810563237 ) ) ;
#8061=ORIENTED_EDGE ( 'NONE', *, *, #10630, .T. ) ;
#8066=ORIENTED_EDGE ( 'NONE', *, *, #20621, .F. ) ;
#8077=CARTESIAN_POINT ( 'NONE',  ( 3.372445903850545879, -26.60948606701822072, 7.721096864323912179 ) ) ;
#8078=CARTESIAN_POINT ( 'NONE',  ( 0.9453370993353911178, -33.77429008742427641, 7.635761828346577573 ) ) ;
#8081=DIRECTION ( 'NONE',  ( 0.000000000000000000, 0.000000000000000000, 1.000000000000000000 ) ) ;
#8083=CARTESIAN_POINT ( 'NONE',  ( -1.798246035484871941, -29.45711074671229213, 7.076385936538748922 ) ) ;
#8085=CARTESIAN_POINT ( 'NONE',  ( 5.173998118306290195, -29.14088312892098998, 6.998987538705437217 ) ) ;
#8088=CARTESIAN_POINT ( 'NONE',  ( 3.353162068531330586, -32.65217298741799112, 7.766640943994647550 ) ) ;
#8089=CARTESIAN_POINT ( 'NONE',  ( 3.291606358883502725, -32.68731127699327033, 6.998987538705430111 ) ) ;
#8090=CARTESIAN_POINT ( 'NONE',  ( 5.123175978192011648, -30.30112382633142332, 6.867199677474202346 ) ) ;
#8091=CARTESIAN_POINT ( 'NONE',  ( 4.994613704055145043, -30.75234092066372682, 7.638132480492516585 ) ) ;
#8092=CARTESIAN_POINT ( 'NONE',  ( 2.784495919998266622, -32.79246250384788652, 6.870716933885665512 ) ) ;
#8093=CARTESIAN_POINT ( 'NONE',  ( 5.095188070987068940, -29.75802495820000360, 6.895222827070025318 ) ) ;
#8095=CARTESIAN_POINT ( 'NONE',  ( 1.854699838584355609, -26.07332139947373406, 6.880828092187096345 ) ) ;
#8096=ORIENTED_EDGE ( 'NONE', *, *, #11088, .T. ) ;
#8101=CARTESIAN_POINT ( 'NONE',  ( -1.261910041069868260, -27.90116479715461750, 7.695279973900954751 ) ) ;
#8108=CARTESIAN_POINT ( 'NONE',  ( 5.054338971983688644, -30.12764086567874244, 7.670860738520327793 ) ) ;
#8109=ADVANCED_FACE ( 'NONE', ( #11050 ), #17835, .F. ) ;
#8114=CARTESIAN_POINT ( 'NONE',  ( 0.6222788575979638637, -26.34538739974215815, 7.778050822775631978 ) ) ;
#8116=DIRECTION ( 'NONE',  ( 0.9396926207859126468, -0.3420201433256568890, -0.000000000000000000 ) ) ;
#8117=CARTESIAN_POINT ( 'NONE',  ( 0.9267304714826871681, -32.98335233567298275, 7.013842709614101167 ) ) ;
#8120=VERTEX_POINT ( 'NONE', #26722 ) ;
#8122=B_SPLINE_CURVE_WITH_KNOTS ( 'NONE', 3,
 ( #5351, #13997, #14801, #17889, #11706, #29854, #30470, #1665, #32761, #23671, #4942, #36237, #17470, #2277, #36438, #30062, #24283, #7624, #31089, #5960, #8624, #24695, #8826, #37639, #28393 ),
 .UNSPECIFIED., .F., .F.,
 ( 4, 3, 3, 3, 3, 3, 3, 3, 4 ),
 ( 6.468151674593574090E-05, 9.076621574722103724E-05, 0.0001210204262067975870, 0.0001512763324577450831, 0.0001815301820994219724, 0.0002117781465860735517, 0.0002420274594459779723, 0.0002722905548971180111, 0.0002816827545175614985 ),
 .UNSPECIFIED. ) ;
#8128=CARTESIAN_POINT ( 'NONE',  ( 2.489749636244892095, -26.26283001680391394, 6.988553391373222290 ) ) ;
#8130=CARTESIAN_POINT ( 'NONE',  ( -1.514709952630465484, -30.67588302826887414, 7.785172627573962778 ) ) ;
#8135=CARTESIAN_POINT ( 'NONE',  ( 4.487471559492266060, -27.45281495260537952, 6.895394898881672674 ) ) ;
#8137=CARTESIAN_POINT ( 'NONE',  ( 4.167068027234559047, -31.90991204531703929, 6.979335674598008410 ) ) ;
#8139=( BOUNDED_CURVE ( )  B_SPLINE_CURVE ( 3, ( #30184, #11024, #39646, #4484 ),
 .UNSPECIFIED., .F., .T. ) 
 B_SPLINE_CURVE_WITH_KNOTS ( ( 4, 4 ),
 ( 1.347909859412853351, 1.534781240595298302 ),
 .UNSPECIFIED. ) 
 CURVE ( )  GEOMETRIC_REPRESENTATION_ITEM ( )  RATIONAL_B_SPLINE_CURVE ( ( 1.000000000000000000, 0.9970920404276226723, 0.9970920404276226723, 1.000000000000000000 ) ) 
 REPRESENTATION_ITEM ( '' )  );
#8143=CARTESIAN_POINT ( 'NONE',  ( 2.254972451256867849, -33.01089166153567334, 7.785344483711591934 ) ) ;
#8149=CARTESIAN_POINT ( 'NONE',  ( -0.6791847275073886747, -32.13656744003537824, 7.009310105710484073 ) ) ;
#8150=ORIENTED_EDGE ( 'NONE', *, *, #11186, .F. ) ;
#8151=DIRECTION ( 'NONE',  ( -0.4999999999999918954, -0.8660254037844432595, -0.000000000000000000 ) ) ;
#8153=AXIS2_PLACEMENT_3D ( 'NONE', #1573, #14105, #26683 ) ;
#8159=CARTESIAN_POINT ( 'NONE',  ( -0.7689628923872616761, -27.23277468313077065, 6.988553391373223178 ) ) ;
#8164=CARTESIAN_POINT ( 'NONE',  ( 3.300358881314253257, -32.56994682954156417, 6.864276522220859711 ) ) ;
#8165=EDGE_CURVE ( 'NONE', #16587, #15980, #34441, .T. ) ;
#8169=CYLINDRICAL_SURFACE ( 'NONE', #10075, 0.09010775117052900740 ) ;
#8172=CARTESIAN_POINT ( 'NONE',  ( 0.9267304714826859469, -32.88073836111571779, 7.013842709614101167 ) ) ;
#8178=CARTESIAN_POINT ( 'NONE',  ( 5.123097946374971734, -30.30141562551846235, 7.750000000000000888 ) ) ;
#8180=CARTESIAN_POINT ( 'NONE',  ( -0.3426461445235795544, -32.42013594030808576, 7.501983001166816045 ) ) ;
#8191=CARTESIAN_POINT ( 'NONE',  ( 4.987265455424083171, -28.39286803235026113, 7.778495531946294506 ) ) ;
#8193=ORIENTED_EDGE ( 'NONE', *, *, #19675, .F. ) ;
#8196=CARTESIAN_POINT ( 'NONE',  ( -1.647280818465151064, -30.59125681868832913, 6.989977667959442975 ) ) ;
#8199=ORIENTED_EDGE ( 'NONE', *, *, #32196, .F. ) ;
#8200=CARTESIAN_POINT ( 'NONE',  ( 5.197301300333582397, -29.56993018336890700, 7.767301406056524193 ) ) ;
#8203=CARTESIAN_POINT ( 'NONE',  ( -2.496911308493820147, -30.36501393308138574, 7.695279973900954751 ) ) ;
#8207=ORIENTED_EDGE ( 'NONE', *, *, #30090, .F. ) ;
#8208=CARTESIAN_POINT ( 'NONE',  ( 4.767873141576740359, -27.88450741673118216, 6.867280401193708528 ) ) ;
#8214=AXIS2_PLACEMENT_3D ( 'NONE', #5593, #24526, #18135 ) ;
#8215=DIRECTION ( 'NONE',  ( -1.000000000000000000, 0.000000000000000000, 0.000000000000000000 ) ) ;
#8216=EDGE_CURVE ( 'NONE', #18044, #6925, #1543, .T. ) ;
#8220=CARTESIAN_POINT ( 'NONE',  ( -1.799471907747695942, -29.53885005966835919, 6.894806418505347700 ) ) ;
#8227=CARTESIAN_POINT ( 'NONE',  ( 4.878343045835490166, -30.77848925561357873, 6.894806418505348589 ) ) ;
#8228=CARTESIAN_POINT ( 'NONE',  ( -1.654007494988858573, -29.01493754880614517, 7.692469944509195301 ) ) ;
#8233=ORIENTED_EDGE ( 'NONE', *, *, #3313, .T. ) ;
#8238=CARTESIAN_POINT ( 'NONE',  ( 4.632207264391903223, -31.48159488532770212, 6.931070083220553180 ) ) ;
#8245=ORIENTED_EDGE ( 'NONE', *, *, #21712, .F. ) ;
#8247=CARTESIAN_POINT ( 'NONE',  ( -2.619165735930222727, -32.12635497920775407, 7.695279973900954751 ) ) ;
#8249=FACE_OUTER_BOUND ( 'NONE', #16143, .T. ) ;
#8256=B_SPLINE_CURVE_WITH_KNOTS ( 'NONE', 3,
 ( #39085, #26155, #3944, #13181 ),
 .UNSPECIFIED., .F., .F.,
 ( 4, 4 ),
 ( 0.000000000000000000, 6.391136169898598526E-06 ),
 .UNSPECIFIED. ) ;
#8257=CARTESIAN_POINT ( 'NONE',  ( 0.3642935312485215960, -32.80488561534932757, 6.877402575842993748 ) ) ;
#8263=CARTESIAN_POINT ( 'NONE',  ( -0.04602064563813425963, -32.48713041901819309, 6.889465824494256374 ) ) ;
#8264=EDGE_CURVE ( 'NONE', #36985, #14798, #31273, .T. ) ;
#8286=CARTESIAN_POINT ( 'NONE',  ( -1.795519090086910019, -29.40075872605237706, 7.013842709614101167 ) ) ;
#8288=CARTESIAN_POINT ( 'NONE',  ( -1.059169042549344519, -31.72279695996654780, 7.751599049952176301 ) ) ;
#8293=CARTESIAN_POINT ( 'NONE',  ( -0.07800893100938692537, -26.55541330231165986, 7.720710062488889136 ) ) ;
#8295=CARTESIAN_POINT ( 'NONE',  ( 1.736346942945644400, -33.06974547922812491, 7.695279973900954751 ) ) ;
#8297=CARTESIAN_POINT ( 'NONE',  ( 1.574364539997139767, -33.06766052747819629, 7.750000000000000888 ) ) ;
#8304=ADVANCED_FACE ( 'NONE', ( #6327 ), #15794, .F. ) ;
#8309=CARTESIAN_POINT ( 'NONE',  ( -0.8851743599023897957, -27.21093538503495068, 6.875780273367530171 ) ) ;
#8313=CARTESIAN_POINT ( 'NONE',  ( 2.202186418506070886, -32.93269696804298974, 7.778050822775631978 ) ) ;
#8314=ORIENTED_EDGE ( 'NONE', *, *, #2333, .F. ) ;
#8318=ORIENTED_EDGE ( 'NONE', *, *, #23697, .F. ) ;
#8324=B_SPLINE_CURVE_WITH_KNOTS ( 'NONE', 3,
 ( #26892, #1592, #2005, #36169, #8137, #10829, #8553, #14724, #39860, #26700, #2204, #1398, #13928, #36368, #23993, #20301, #39236, #7950, #39435, #36770, #14323, #26501, #39031, #36564, #23406, #14123, #33504, #32886, #35974, #4673, #8345 ),
 .UNSPECIFIED., .F., .F.,
 ( 4, 3, 3, 3, 3, 3, 3, 3, 3, 3, 4 ),
 ( 8.673617379884035472E-19, 2.999644130997317255E-05, 6.002588995694823926E-05, 8.960886084587800678E-05, 0.0001190604700446473311, 0.0001489538463052700670, 0.0001796139255493905637, 0.0002109707048517013323, 0.0002426195318110273063, 0.0002740640997889962093, 0.0002849778069099833354 ),
 .UNSPECIFIED. ) ;
#8329=EDGE_LOOP ( 'NONE', ( #24062, #13818, #35249, #14259, #28637 ) ) ;
#8334=CARTESIAN_POINT ( 'NONE',  ( 1.519484703345444609, -32.96512359005904358, 6.887945620086119547 ) ) ;
#8336=CARTESIAN_POINT ( 'NONE',  ( 4.907464300517769829, -30.69894525369553762, 7.695279973900954751 ) ) ;
#8337=CARTESIAN_POINT ( 'NONE',  ( 3.976216693700143523, -27.04394172819598907, 7.757178535559533294 ) ) ;
#8339=CARTESIAN_POINT ( 'NONE',  ( 0.5468258811901485217, -26.26548310648608009, 6.880608371227950215 ) ) ;
#8342=CARTESIAN_POINT ( 'NONE',  ( 4.500789674022213305, -27.47046303393648614, 6.941203072598479906 ) ) ;
#8343=EDGE_CURVE ( 'NONE', #20380, #25477, #27489, .T. ) ;
#8345=CARTESIAN_POINT ( 'NONE',  ( 4.273337484900067373, -31.79252814967387053, 6.894806418505345036 ) ) ;
#8351=DIRECTION ( 'NONE',  ( -1.000000000000000000, -0.000000000000000000, -0.000000000000000000 ) ) ;
#8357=CARTESIAN_POINT ( 'NONE',  ( -0.6928964808853791402, -32.12378599331628948, 6.941203072598472801 ) ) ;
#8358=B_SPLINE_CURVE_WITH_KNOTS ( 'NONE', 3,
 ( #36712, #30548, #2361, #2980, #15500, #37518, #24984, #18172, #21488, #9314 ),
 .UNSPECIFIED., .F., .F.,
 ( 4, 3, 3, 4 ),
 ( 0.0002170292169044720973, 0.0002420761345915967968, 0.0002723302478206991728, 0.0002816811360866699164 ),
 .UNSPECIFIED. ) ;
#8365=CARTESIAN_POINT ( 'NONE',  ( -1.538176338396153753, -28.24264443121935386, 6.872971584836694348 ) ) ;
#8366=AXIS2_PLACEMENT_3D ( 'NONE', #36660, #37464, #11525 ) ;
#8369=CARTESIAN_POINT ( 'NONE',  ( 4.752662398340829597, -27.88579754063074034, 7.784725160561909441 ) ) ;
#8377=CARTESIAN_POINT ( 'NONE',  ( 4.792526203416204389, -27.93020634197934982, 7.750000000000000888 ) ) ;
#8383=CARTESIAN_POINT ( 'NONE',  ( 2.896951166878261930, -32.75242002648047901, 7.692469944509197077 ) ) ;
#8387=( BOUNDED_CURVE ( )  B_SPLINE_CURVE ( 3, ( #29983, #34529, #6514, #34123 ),
 .UNSPECIFIED., .F., .T. ) 
 B_SPLINE_CURVE_WITH_KNOTS ( ( 4, 4 ),
 ( 4.708531083176465515, 4.895802057644187855 ),
 .UNSPECIFIED. ) 
 CURVE ( )  GEOMETRIC_REPRESENTATION_ITEM ( )  RATIONAL_B_SPLINE_CURVE ( ( 1.000000000000000000, 0.9970795998553221295, 0.9970795998553221295, 1.000000000000000000 ) ) 
 REPRESENTATION_ITEM ( '' )  );
#8392=EDGE_LOOP ( 'NONE', ( #11141, #149, #11893, #11167 ) ) ;
#8394=FACE_OUTER_BOUND ( 'NONE', #35744, .T. ) ;
#8395=EDGE_CURVE ( 'NONE', #34207, #19528, #7087, .T. ) ;
#8400=CARTESIAN_POINT ( 'NONE',  ( -0.3937826876777428264, -26.89141458432633769, 7.759451378593096749 ) ) ;
#8403=EDGE_CURVE ( 'NONE', #5452, #40540, #6735, .T. ) ;
#8404=EDGE_CURVE ( 'NONE', #18601, #39861, #11266, .T. ) ;
#8411=CARTESIAN_POINT ( 'NONE',  ( 3.817924346030161509, -32.35669330361569962, 7.013842709614101167 ) ) ;
#8412=ORIENTED_EDGE ( 'NONE', *, *, #28318, .T. ) ;
#8414=ORIENTED_EDGE ( 'NONE', *, *, #17357, .T. ) ;
#8416=DIRECTION ( 'NONE',  ( 1.000000000000000000, 1.288651725011342548E-14, 0.000000000000000000 ) ) ;
#8419=CARTESIAN_POINT ( 'NONE',  ( 4.758694053898627985, -27.86793814928234525, 6.875671892026064214 ) ) ;
#8423=CARTESIAN_POINT ( 'NONE',  ( 4.741166332522630533, -28.04885166386452156, 6.988553391373221402 ) ) ;
#8424=ORIENTED_EDGE ( 'NONE', *, *, #34584, .F. ) ;
#8430=VERTEX_POINT ( 'NONE', #32664 ) ;
#8439=CARTESIAN_POINT ( 'NONE',  ( 2.861759009453783253, -32.87163717142679786, 6.887161170156907097 ) ) ;
#8441=CARTESIAN_POINT ( 'NONE',  ( 0.6556028735496977067, -26.33441960479748545, 6.863904403958576594 ) ) ;
#8442=CARTESIAN_POINT ( 'NONE',  ( 0.1194166765537494485, -26.44734742936537231, 6.951256099901593544 ) ) ;
#8457=CARTESIAN_POINT ( 'NONE',  ( -0.5468503132381580256, -26.89089984877168149, 7.767720160662276108 ) ) ;
#8459=CARTESIAN_POINT ( 'NONE',  ( -1.666363480296579214, -25.64183336440431660, 7.695279973900954751 ) ) ;
#8460=CARTESIAN_POINT ( 'NONE',  ( 3.912314530024866954, -32.15206040780897467, 7.712764235869105534 ) ) ;
#8467=ORIENTED_EDGE ( 'NONE', *, *, #18169, .F. ) ;
#8472=CARTESIAN_POINT ( 'NONE',  ( -0.1599037489455041594, -32.41586408544110043, 6.895222827070020877 ) ) ;
#8482=ORIENTED_EDGE ( 'NONE', *, *, #25768, .T. ) ;
#8484=CARTESIAN_POINT ( 'NONE',  ( 3.492838994194323643, -26.68078115845596443, 7.768425012602587998 ) ) ;
#8488=CARTESIAN_POINT ( 'NONE',  ( -1.773393625443949073, -29.99752957843126566, 6.912143950357348743 ) ) ;
#8489=CARTESIAN_POINT ( 'NONE',  ( -1.675359094926574866, -29.97529103330290212, 7.013842709614101167 ) ) ;
#8498=CARTESIAN_POINT ( 'NONE',  ( 3.461020435952258278, -32.59486115124590100, 7.756742906098587298 ) ) ;
#8499=CARTESIAN_POINT ( 'NONE',  ( 1.144867377203080405, -32.92424005792490505, 7.680992449362117114 ) ) ;
#8500=CARTESIAN_POINT ( 'NONE',  ( 5.042305363714541855, -28.94414881188822619, 7.693875151218753317 ) ) ;
#8502=DIRECTION ( 'NONE',  ( 1.000000000000000000, -0.000000000000000000, -0.000000000000000000 ) ) ;
#8503=CARTESIAN_POINT ( 'NONE',  ( 4.626783558469344193, -27.83897054012538064, 7.691066658568949777 ) ) ;
#8508=CARTESIAN_POINT ( 'NONE',  ( 2.214914452921659560, -33.03191941985759428, 6.863805608295729499 ) ) ;
#8510=( BOUNDED_CURVE ( )  B_SPLINE_CURVE ( 3, ( #20927, #33513, #6723, #38394 ),
 .UNSPECIFIED., .F., .F. ) 
 B_SPLINE_CURVE_WITH_KNOTS ( ( 4, 4 ),
 ( 4.748221474220558846, 4.941946782021393147 ),
 .UNSPECIFIED. ) 
 CURVE ( )  GEOMETRIC_REPRESENTATION_ITEM ( )  RATIONAL_B_SPLINE_CURVE ( ( 1.000000000000000000, 0.9968749865767494445, 0.9968749865767494445, 1.000000000000000000 ) ) 
 REPRESENTATION_ITEM ( '' )  );
#8513=CARTESIAN_POINT ( 'NONE',  ( 4.141053437885626742, -27.19263799006747462, 7.505001789837625559 ) ) ;
#8517=CARTESIAN_POINT ( 'NONE',  ( 2.916291037025561916, -26.39477902244301433, 6.887041543973313473 ) ) ;
#8519=CARTESIAN_POINT ( 'NONE',  ( 1.253764766991059432, -26.19939227113678015, 6.868387053540519815 ) ) ;
#8521=ORIENTED_EDGE ( 'NONE', *, *, #29248, .F. ) ;
#8536=EDGE_CURVE ( 'NONE', #25105, #21404, #38101, .T. ) ;
#8544=CARTESIAN_POINT ( 'NONE',  ( 2.490483471607719324, -26.26300413327467353, 6.920489980334478375 ) ) ;
#8546=CARTESIAN_POINT ( 'NONE',  ( 4.905277512680163987, -30.70513793031458505, 7.661510568013099487 ) ) ;
#8550=CARTESIAN_POINT ( 'NONE',  ( 5.055464264941726071, -29.01895665644428135, 7.784838882742139532 ) ) ;
#8553=CARTESIAN_POINT ( 'NONE',  ( 4.165061536218790827, -31.91202212824329720, 6.959317978105167057 ) ) ;
#8557=CARTESIAN_POINT ( 'NONE',  ( 2.298492929235983695, -33.01280978164516000, 7.773839561854631874 ) ) ;
#8566=EDGE_CURVE ( 'NONE', #22017, #32517, #2943, .T. ) ;
#8573=CARTESIAN_POINT ( 'NONE',  ( -1.575827083862257005, -28.33849528819893848, 6.888594555015732368 ) ) ;
#8576=DIRECTION ( 'NONE',  ( -0.9848077530122011369, -0.1736481776669699106, 0.000000000000000000 ) ) ;
#8577=ORIENTED_EDGE ( 'NONE', *, *, #10590, .T. ) ;
#8580=CARTESIAN_POINT ( 'NONE',  ( 3.241318133241683608, -32.60070661927110081, 6.887945620086120435 ) ) ;
#8584=ADVANCED_FACE ( 'NONE', ( #4651 ), #23380, .F. ) ;
#8585=EDGE_CURVE ( 'NONE', #614, #39861, #14098, .T. ) ;
#8589=CARTESIAN_POINT ( 'NONE',  ( 5.199026221951053017, -29.68274962007452444, 7.076385936538754251 ) ) ;
#8593=CARTESIAN_POINT ( 'NONE',  ( 4.976842733950424424, -28.33913446795707358, 7.686927408461905920 ) ) ;
#8598=DIRECTION ( 'NONE',  ( -0.000000000000000000, -0.000000000000000000, -1.000000000000000000 ) ) ;
#8599=CARTESIAN_POINT ( 'NONE',  ( 4.081262659518896108, -27.00449731093159045, 7.006908160621414083 ) ) ;
#8602=CARTESIAN_POINT ( 'NONE',  ( -2.515717719208200531, -28.88150288888238393, 7.695279973900954751 ) ) ;
#8603=CARTESIAN_POINT ( 'NONE',  ( 1.899603570617604653, -26.17576915092285361, 6.997764925645181933 ) ) ;
#8604=ORIENTED_EDGE ( 'NONE', *, *, #32103, .T. ) ;
#8605=CARTESIAN_POINT ( 'NONE',  ( 2.851715340239886487, -32.85991820161709143, 7.785096263473212375 ) ) ;
#8609=ORIENTED_EDGE ( 'NONE', *, *, #34789, .T. ) ;
#8615=CARTESIAN_POINT ( 'NONE',  ( 3.431434570054124222, -32.49627346798381211, 7.695279973900954751 ) ) ;
#8616=ORIENTED_EDGE ( 'NONE', *, *, #8216, .T. ) ;
#8617=ORIENTED_EDGE ( 'NONE', *, *, #1421, .T. ) ;
#8618=DIRECTION ( 'NONE',  ( 0.6427876096865379196, 0.7660444431189792347, -0.000000000000000000 ) ) ;
#8620=B_SPLINE_CURVE_WITH_KNOTS ( 'NONE', 3,
 ( #10462, #19338, #16439, #28814, #13160, #19548, #29015, #29214, #19934, #35413, #38065, #13350, #12955, #3518, #1023, #16041, #32317, #35210, #22644, #3720, #819, #16244, #28608, #19741, #26131, #25925, #416, #13556, #38662, #7181, #22841 ),
 .UNSPECIFIED., .F., .F.,
 ( 4, 3, 3, 3, 3, 3, 3, 3, 3, 3, 4 ),
 ( 1.939479807224432123E-18, 2.999644130997966760E-05, 6.002588995695383646E-05, 8.960886084588199122E-05, 0.0001190604700446493640, 0.0001489538463052688202, 0.0001796139255493963912, 0.0002109707048517053167, 0.0002426195318110302337, 0.0002740640997889996788, 0.0002849778069099796491 ),
 .UNSPECIFIED. ) ;
#8624=CARTESIAN_POINT ( 'NONE',  ( 4.372888262200486764, -27.46807179431958446, 7.768425012602593327 ) ) ;
#8625=ORIENTED_EDGE ( 'NONE', *, *, #37467, .T. ) ;
#8626=ADVANCED_FACE ( 'NONE', ( #35948 ), #26677, .F. ) ;
#8631=( BOUNDED_CURVE ( )  B_SPLINE_CURVE ( 3, ( #39895, #27335, #18057, #2460 ),
 .UNSPECIFIED., .F., .T. ) 
 B_SPLINE_CURVE_WITH_KNOTS ( ( 4, 4 ),
 ( 4.708531083176467291, 4.895802057644189631 ),
 .UNSPECIFIED. ) 
 CURVE ( )  GEOMETRIC_REPRESENTATION_ITEM ( )  RATIONAL_B_SPLINE_CURVE ( ( 1.000000000000000000, 0.9970795998553221295, 0.9970795998553221295, 1.000000000000000000 ) ) 
 REPRESENTATION_ITEM ( '' )  );
#8633=CARTESIAN_POINT ( 'NONE',  ( 1.074608721727911442, -26.22801491291194864, 7.695279973900954751 ) ) ;
#8634=DIRECTION ( 'NONE',  ( -0.000000000000000000, -0.000000000000000000, -1.000000000000000000 ) ) ;
#8638=ORIENTED_EDGE ( 'NONE', *, *, #6339, .T. ) ;
#8639=EDGE_CURVE ( 'NONE', #9863, #37348, #9970, .T. ) ;
#8650=CARTESIAN_POINT ( 'NONE',  ( 3.481437286441587897, -32.58288071328335178, 7.695279973900954751 ) ) ;
#8653=CARTESIAN_POINT ( 'NONE',  ( 4.634237190056025746, -31.47847444865518085, 6.921725064902947366 ) ) ;
#8655=CARTESIAN_POINT ( 'NONE',  ( 4.304703044124503108, -31.90695999378015557, 7.761113333117553026 ) ) ;
#8656=CARTESIAN_POINT ( 'NONE',  ( 1.735671467128618861, -33.06975260603037725, 7.707984471951054850 ) ) ;
#8662=CYLINDRICAL_SURFACE ( 'NONE', #8214, 0.09010775117052882699 ) ;
#8664=CARTESIAN_POINT ( 'NONE',  ( 1.700390093233090871, -29.56993018339339940, 7.800000000000000711 ) ) ;
#8669=CARTESIAN_POINT ( 'NONE',  ( -1.146144745493847150, -27.71056485836612637, 7.013842709614101167 ) ) ;
#8670=CARTESIAN_POINT ( 'NONE',  ( -1.699609906766908818, -29.56898895464481569, 7.768009089657827104 ) ) ;
#8671=ORIENTED_EDGE ( 'NONE', *, *, #39224, .T. ) ;
#8676=ORIENTED_EDGE ( 'NONE', *, *, #39358, .T. ) ;
#8683=EDGE_LOOP ( 'NONE', ( #14398, #27571, #13564, #4938, #27874 ) ) ;
#8687=ADVANCED_FACE ( 'NONE', ( #19759 ), #25741, .F. ) ;
#8691=CARTESIAN_POINT ( 'NONE',  ( -1.694803313432552416, -29.38902479350574382, 6.887945620086119547 ) ) ;
#8693=CARTESIAN_POINT ( 'NONE',  ( -1.761599143231102671, -30.08445454308195721, 6.863805608295729499 ) ) ;
#8698=DIRECTION ( 'NONE',  ( 0.7394003126383942304, -0.1303762246624207699, 0.6605219282605376829 ) ) ;
#8699=CARTESIAN_POINT ( 'NONE',  ( -1.694464052375517671, -29.38293999636734810, 7.013842709614101167 ) ) ;
#8702=CARTESIAN_POINT ( 'NONE',  ( 3.371024467839934147, -32.63382312644299077, 7.780491323090173772 ) ) ;
#8704=CARTESIAN_POINT ( 'NONE',  ( -1.699609906766908818, -29.56993018339339940, 6.949309202340325342 ) ) ;
#8706=DIRECTION ( 'NONE',  ( 0.5000000000000072164, -0.8660254037844344888, 0.000000000000000000 ) ) ;
#8707=CYLINDRICAL_SURFACE ( 'NONE', #360, 0.09010775117052928496 ) ;
#8709=CARTESIAN_POINT ( 'NONE',  ( 4.934307971444643393, -28.52027331175976244, 7.757178535559533294 ) ) ;
#8712=CARTESIAN_POINT ( 'NONE',  ( -1.522142227221405131, -30.65403601015855273, 6.870716933885662847 ) ) ;
#8719=CARTESIAN_POINT ( 'NONE',  ( 1.822194502883806022, -33.27093018339341768, 7.754798119455333705 ) ) ;
#8722=CARTESIAN_POINT ( 'NONE',  ( -0.8685330176923784506, -27.19282394888199050, 6.895394898881665569 ) ) ;
#8723=CARTESIAN_POINT ( 'NONE',  ( 4.881456320988373676, -30.77031019809703238, 7.784838882742139532 ) ) ;
#8724=CARTESIAN_POINT ( 'NONE',  ( 2.174739121882255599, -32.93667912707378775, 7.759451378593095860 ) ) ;
#8725=ORIENTED_EDGE ( 'NONE', *, *, #25205, .T. ) ;
#8728=ORIENTED_EDGE ( 'NONE', *, *, #27334, .F. ) ;
#8732=B_SPLINE_CURVE_WITH_KNOTS ( 'NONE', 3,
 ( #26405, #29285, #26598, #1099, #23700, #23512, #26206, #29680, #39339, #17304 ),
 .UNSPECIFIED., .F., .F.,
 ( 4, 3, 3, 4 ),
 ( 0.0001585009270395812257, 0.0001815657551981893171, 0.0002118214035944172217, 0.0002170292169044841320 ),
 .UNSPECIFIED. ) ;
#8735=ADVANCED_FACE ( 'NONE', ( #21895 ), #640, .F. ) ;
#8736=CARTESIAN_POINT ( 'NONE',  ( 4.825889015811430482, -30.92609072608717824, 7.386948897581450346 ) ) ;
#8740=CARTESIAN_POINT ( 'NONE',  ( 2.357445652190597762, -33.01462870691901941, 7.255881584735164758 ) ) ;
#8745=CARTESIAN_POINT ( 'NONE',  ( 4.907453385184882499, -30.69897626116466682, 7.692469944509198854 ) ) ;
#8747=CARTESIAN_POINT ( 'NONE',  ( 3.477237270422150139, -26.55450084266673727, 6.894806418505347700 ) ) ;
#8749=CARTESIAN_POINT ( 'NONE',  ( 5.058692241207612739, -29.03907551127521103, 7.785172627573962778 ) ) ;
#8751=AXIS2_PLACEMENT_3D ( 'NONE', #3295, #22215, #16016 ) ;
#8753=CARTESIAN_POINT ( 'NONE',  ( 1.126346108378571076, -33.02253567017740465, 7.674970859709602244 ) ) ;
#8758=EDGE_CURVE ( 'NONE', #2006, #16194, #10269, .T. ) ;
#8759=CARTESIAN_POINT ( 'NONE',  ( 0.2633542768278205881, -25.48582225135028878, 6.954324564059724878 ) ) ;
#8766=CARTESIAN_POINT ( 'NONE',  ( 3.438683469850188690, -26.53211252316276259, 7.635761828346582014 ) ) ;
#8769=ADVANCED_FACE ( 'NONE', ( #39902 ), #39285, .F. ) ;
#8775=ORIENTED_EDGE ( 'NONE', *, *, #3716, .F. ) ;
#8778=CARTESIAN_POINT ( 'NONE',  ( 3.235878913814441038, -32.60345520914638939, 7.013842709614101167 ) ) ;
#8780=CARTESIAN_POINT ( 'NONE',  ( 4.651604549657131216, -31.25822317698004227, 7.635761828346577573 ) ) ;
#8783=DIRECTION ( 'NONE',  ( -0.000000000000000000, -0.000000000000000000, -1.000000000000000000 ) ) ;
#8786=LINE ( 'NONE', #12079, #16286 ) ;
#8787=AXIS2_PLACEMENT_3D ( 'NONE', #16922, #704, #32402 ) ;
#8788=CARTESIAN_POINT ( 'NONE',  ( -0.9576111974470827848, -31.84699608905852131, 7.700536657684214248 ) ) ;
#8790=CARTESIAN_POINT ( 'NONE',  ( 4.982636580400577664, -28.35466971852313733, 7.643192810543823157 ) ) ;
#8796=CARTESIAN_POINT ( 'NONE',  ( 4.662690227536056220, -31.23869556963216709, 7.703977250142846955 ) ) ;
#8797=EDGE_LOOP ( 'NONE', ( #30429, #12531, #2645, #1218, #22221 ) ) ;
#8802=DIRECTION ( 'NONE',  ( 0.000000000000000000, -0.7126435865141261816, -0.7015262779114429526 ) ) ;
#8803=CARTESIAN_POINT ( 'NONE',  ( 1.903485573815023146, -26.17600145318010973, 6.988553391373221402 ) ) ;
#8808=ORIENTED_EDGE ( 'NONE', *, *, #29421, .F. ) ;
#8816=ADVANCED_FACE ( 'NONE', ( #8394 ), #33344, .T. ) ;
#8817=CARTESIAN_POINT ( 'NONE',  ( 0.9689046511080217083, -32.99263803653528271, 7.750000000000000888 ) ) ;
#8821=FACE_OUTER_BOUND ( 'NONE', #5646, .T. ) ;
#8823=LINE ( 'NONE', #5757, #22777 ) ;
#8826=CARTESIAN_POINT ( 'NONE',  ( 4.378905692300169683, -27.47575740248258569, 7.759451378593096749 ) ) ;
#8830=ADVANCED_FACE ( 'NONE', ( #20968 ), #30033, .F. ) ;
#8831=VERTEX_POINT ( 'NONE', #39689 ) ;
#8833=CARTESIAN_POINT ( 'NONE',  ( 4.882903053830506934, -28.37343059892649677, 7.691066658568946224 ) ) ;
#8843=CARTESIAN_POINT ( 'NONE',  ( 3.357996495870312792, -32.53848892694827555, 6.894806418505347700 ) ) ;
#8844=VERTEX_POINT ( 'NONE', #1442 ) ;
#8847=B_SPLINE_CURVE_WITH_KNOTS ( 'NONE', 3,
 ( #38831, #10026, #22410, #3686, #32285, #10625, #22609, #32087, #13736, #3892, #16407, #23200, #20101, #17001, #13924, #28982, #785, #13315, #25888 ),
 .UNSPECIFIED., .F., .F.,
 ( 4, 3, 3, 3, 3, 3, 4 ),
 ( 1.084202172485504434E-18, 2.546128104244520487E-05, 5.711050680483435320E-05, 8.113074941675352508E-05, 0.0001053129305727020908, 0.0001360598016347060505, 0.0001612931755702085880 ),
 .UNSPECIFIED. ) ;
#8850=CARTESIAN_POINT ( 'NONE',  ( 2.477556199703359940, -25.36946941773652853, 7.695279973900954751 ) ) ;
#8854=CARTESIAN_POINT ( 'NONE',  ( 5.100341873444426355, -29.59048384115356711, 7.779495906702013741 ) ) ;
#8855=CARTESIAN_POINT ( 'NONE',  ( 4.677559685796697231, -31.41019271375740374, 6.863784140767622333 ) ) ;
#8857=EDGE_CURVE ( 'NONE', #6774, #29061, #24980, .T. ) ;
#8859=CARTESIAN_POINT ( 'NONE',  ( 1.717829174068238984, -33.06988673718940674, 7.750000000000000888 ) ) ;
#8866=EDGE_CURVE ( 'NONE', #774, #16334, #18384, .T. ) ;
#8867=DIRECTION ( 'NONE',  ( 0.000000000000000000, -0.6662082868431821181, -0.7457657263118708801 ) ) ;
#8871=CARTESIAN_POINT ( 'NONE',  ( 4.666500650180242182, -31.42793668606411117, 7.750000000000000888 ) ) ;
#8876=DIRECTION ( 'NONE',  ( -1.000000000000000000, 0.000000000000000000, 0.000000000000000000 ) ) ;
#8877=CARTESIAN_POINT ( 'NONE',  ( 5.029851253234809860, -28.49072197104846182, 7.751599049952172749 ) ) ;
#8882=CARTESIAN_POINT ( 'NONE',  ( -0.1645870765518833712, -32.41279934783806738, 7.006423389747792108 ) ) ;
#8885=CARTESIAN_POINT ( 'NONE',  ( 3.867374209161352994, -32.31247832666930719, 7.771081512783697853 ) ) ;
#8887=CARTESIAN_POINT ( 'NONE',  ( 0.5037982502477853508, -26.38745190989316214, 7.695279973900954751 ) ) ;
#8890=ORIENTED_EDGE ( 'NONE', *, *, #35540, .F. ) ;
#8894=CARTESIAN_POINT ( 'NONE',  ( 5.694018316346522113, -26.44898221431133578, 6.954324564059724878 ) ) ;
#8897=CARTESIAN_POINT ( 'NONE',  ( -1.419070666119118362, -31.15705752543471618, 6.989977667959445640 ) ) ;
#8898=CARTESIAN_POINT ( 'NONE',  ( -1.265720463714046895, -27.71192368072266277, 7.750000000000000888 ) ) ;
#8908=CARTESIAN_POINT ( 'NONE',  ( 3.448281132886812372, -32.59848922884697231, 7.767720160662273443 ) ) ;
#8910=CARTESIAN_POINT ( 'NONE',  ( -0.08052498442271191492, -26.55690155986885514, 7.700536657684214248 ) ) ;
#8911=CARTESIAN_POINT ( 'NONE',  ( 0.4087657880184312753, -32.81786754902258707, 7.771081512783700518 ) ) ;
#8912=DIRECTION ( 'NONE',  ( -0.4999999999999918954, -0.8660254037844432595, -0.000000000000000000 ) ) ;
#8913=CARTESIAN_POINT ( 'NONE',  ( 4.626733377823518012, -27.83888570657239470, 7.695279973900954751 ) ) ;
#8914=VECTOR ( 'NONE', #23608, 1000.000000000000000 ) ;
#8915=PLANE ( 'NONE',  #9657 ) ;
#8922=ORIENTED_EDGE ( 'NONE', *, *, #2297, .T. ) ;
#8923=DIRECTION ( 'NONE',  ( -0.000000000000000000, -0.000000000000000000, -1.000000000000000000 ) ) ;
#8925=CARTESIAN_POINT ( 'NONE',  ( -1.420557875848984741, -25.57630196027997727, 6.954324564059724878 ) ) ;
#8927=CARTESIAN_POINT ( 'NONE',  ( -1.418010585399023471, -28.21509543055201519, 6.929923840112064859 ) ) ;
#8928=CARTESIAN_POINT ( 'NONE',  ( 4.905245326634070757, -30.70523247011419699, 7.730758795053810140 ) ) ;
#8942=CARTESIAN_POINT ( 'NONE',  ( 4.435220079103089574, -27.54985462435614352, 6.949473656533212917 ) ) ;
#8943=CARTESIAN_POINT ( 'NONE',  ( 2.896981936218417264, -32.75240845689362601, 7.695279973900954751 ) ) ;
#8945=ORIENTED_EDGE ( 'NONE', *, *, #5799, .F. ) ;
#8947=CARTESIAN_POINT ( 'NONE',  ( 4.301450302647315205, -31.91148321001355370, 7.754798119455333705 ) ) ;
#8949=CARTESIAN_POINT ( 'NONE',  ( 1.650073881887274441, -32.96957273148993295, 7.785868773668302545 ) ) ;
#8953=CARTESIAN_POINT ( 'NONE',  ( 3.721376283916915106, -32.30408730072721823, 6.969307238440509700 ) ) ;
#8960=ORIENTED_EDGE ( 'NONE', *, *, #16666, .F. ) ;
#8964=CARTESIAN_POINT ( 'NONE',  ( 4.951209458787976914, -30.83330630559114383, 7.782861076432731728 ) ) ;
#8973=CARTESIAN_POINT ( 'NONE',  ( -1.554008717359405489, -30.55426820241236996, 6.895222827070025318 ) ) ;
#8976=CARTESIAN_POINT ( 'NONE',  ( 0.6964302473834028673, -32.82569116364354045, 7.139196562012269709 ) ) ;
#8981=ORIENTED_EDGE ( 'NONE', *, *, #21406, .T. ) ;
#8983=CARTESIAN_POINT ( 'NONE',  ( 2.896246704383601323, -32.76027228102909561, 7.257242401810563237 ) ) ;
#8990=( BOUNDED_CURVE ( )  B_SPLINE_CURVE ( 3, ( #11215, #7938, #21124, #17804 ),
 .UNSPECIFIED., .F., .F. ) 
 B_SPLINE_CURVE_WITH_KNOTS ( ( 4, 4 ),
 ( 1.381924640371169577, 1.574767692156077148 ),
 .UNSPECIFIED. ) 
 CURVE ( )  GEOMETRIC_REPRESENTATION_ITEM ( )  RATIONAL_B_SPLINE_CURVE ( ( 1.000000000000000000, 0.9969033633783033199, 0.9969033633783033199, 1.000000000000000000 ) ) 
 REPRESENTATION_ITEM ( '' )  );
#8993=CYLINDRICAL_SURFACE ( 'NONE', #27485, 0.09010775117052950700 ) ;
#9000=CARTESIAN_POINT ( 'NONE',  ( 2.044608497525232327, -26.08006147301429323, 7.501983001166817822 ) ) ;
#9003=DIRECTION ( 'NONE',  ( 1.000000000000000000, -0.000000000000000000, -0.000000000000000000 ) ) ;
#9006=CARTESIAN_POINT ( 'NONE',  ( 3.435265683109236967, -26.53015935524666347, 7.750000000000001776 ) ) ;
#9008=CARTESIAN_POINT ( 'NONE',  ( 2.882800830503455369, -26.27570657257135878, 7.638132480492517473 ) ) ;
#9009=DIRECTION ( 'NONE',  ( -0.1736481776669206722, -0.9848077530122096857, -0.000000000000000000 ) ) ;
#9010=EDGE_CURVE ( 'NONE', #27482, #39459, #30926, .T. ) ;
#9015=CARTESIAN_POINT ( 'NONE',  ( -0.4543040637718891994, -26.93983748258725797, 7.784838882742138644 ) ) ;
#9018=CARTESIAN_POINT ( 'NONE',  ( 4.279060409011795407, -31.78590715249458754, 7.784838882742138644 ) ) ;
#9026=CARTESIAN_POINT ( 'NONE',  ( 3.472176508934365913, -32.58834150085273507, 7.651421919295145813 ) ) ;
#9040=CARTESIAN_POINT ( 'NONE',  ( -1.635225080001443621, -33.52415522258557701, 7.635761828346577573 ) ) ;
#9041=ORIENTED_EDGE ( 'NONE', *, *, #31351, .F. ) ;
#9042=CARTESIAN_POINT ( 'NONE',  ( 4.888398419654542693, -28.38813185588637111, 7.643333865083955736 ) ) ;
#9045=CARTESIAN_POINT ( 'NONE',  ( 0.4869470754961160996, -26.28701135364670805, 7.750000000000001776 ) ) ;
#9050=VECTOR ( 'NONE', #3783, 1000.000000000000227 ) ;
#9058=CARTESIAN_POINT ( 'NONE',  ( 3.936759689487521641, -26.87759828911498516, 7.750000000000000888 ) ) ;
#9059=EDGE_CURVE ( 'NONE', #6937, #27683, #38781, .T. ) ;
#9061=CARTESIAN_POINT ( 'NONE',  ( -0.9270654228314927359, -27.41204290387628006, 7.691066658568940007 ) ) ;
#9066=CARTESIAN_POINT ( 'NONE',  ( 5.100205970968322511, -29.53454346407160358, 7.680992449362115337 ) ) ;
#9070=CARTESIAN_POINT ( 'NONE',  ( 1.732227763654782704, -33.06978601425814190, 7.724038915126860694 ) ) ;
#9094=CARTESIAN_POINT ( 'NONE',  ( -0.1647035100567555144, -32.41271505934994934, 6.903372536218456368 ) ) ;
#9095=ORIENTED_EDGE ( 'NONE', *, *, #12832, .T. ) ;
#9098=CARTESIAN_POINT ( 'NONE',  ( 0.6393374818712781460, -26.33972546746960575, 7.768425012602592439 ) ) ;
#9102=CARTESIAN_POINT ( 'NONE',  ( 1.682951012397970292, -26.06997362959739206, 7.750000000000000888 ) ) ;
#9110=EDGE_CURVE ( 'NONE', #11306, #1015, #13130, .T. ) ;
#9111=CARTESIAN_POINT ( 'NONE',  ( -1.381908803976582778, -31.22810341674602697, 6.863784140767622333 ) ) ;
#9113=CARTESIAN_POINT ( 'NONE',  ( 1.514465823680740453, -33.06498843269217502, 6.921725064902952695 ) ) ;
#9117=FACE_OUTER_BOUND ( 'NONE', #4706, .T. ) ;
#9124=LINE ( 'NONE', #15094, #39642 ) ;
#9126=CARTESIAN_POINT ( 'NONE',  ( 4.638101942922436827, -27.85824998890764448, 7.635761828346577573 ) ) ;
#9129=CARTESIAN_POINT ( 'NONE',  ( 2.829498134096899431, -26.36288870688320074, 7.691066658568949777 ) ) ;
#9135=CARTESIAN_POINT ( 'NONE',  ( 5.056857618328627346, -29.02759656560906976, 6.894806418505346812 ) ) ;
#9137=CARTESIAN_POINT ( 'NONE',  ( 5.007779359891471493, -28.42486414215694168, 6.875671892026061549 ) ) ;
#9138=CARTESIAN_POINT ( 'NONE',  ( 4.863529718378640787, -30.81674521050610949, 7.778050822775630202 ) ) ;
#9139=CARTESIAN_POINT ( 'NONE',  ( 5.030132119480741792, -30.25761027875940812, 7.774064877406528851 ) ) ;
#9142=FACE_OUTER_BOUND ( 'NONE', #20732, .T. ) ;
#9143=ORIENTED_EDGE ( 'NONE', *, *, #8403, .F. ) ;
#9145=CARTESIAN_POINT ( 'NONE',  ( -1.678079929080388721, -29.95195194214872814, 6.949473656533220023 ) ) ;
#9149=DIRECTION ( 'NONE',  ( -0.7660444431189813441, 0.6427876096865353661, -0.000000000000000000 ) ) ;
#9152=CARTESIAN_POINT ( 'NONE',  ( 2.754382185031206465, -32.80243705429514733, 7.761597726988848756 ) ) ;
#9154=VERTEX_POINT ( 'NONE', #17812 ) ;
#9156=CARTESIAN_POINT ( 'NONE',  ( -1.799583860900191734, -29.58343279012807159, 7.635761828346577573 ) ) ;
#9160=CARTESIAN_POINT ( 'NONE',  ( 1.619884156912658746, -32.96898955208958171, 7.782034975670476307 ) ) ;
#9164=CARTESIAN_POINT ( 'NONE',  ( 3.726385264851022061, -32.30037768601651749, 6.988553391373224954 ) ) ;
#9165=CARTESIAN_POINT ( 'NONE',  ( 3.967303130966486790, -27.03592930924035187, 7.768425012602596880 ) ) ;
#9167=B_SPLINE_CURVE_WITH_KNOTS ( 'NONE', 3,
 ( #31015, #28108, #15138, #18223, #3244, #18847, #15961, #31620, #37570, #9365 ),
 .UNSPECIFIED., .F., .F.,
 ( 4, 3, 3, 4 ),
 ( 2.742838647325547832E-18, 3.025570593003418284E-05, 6.051145698344212605E-05, 6.468151674594278821E-05 ),
 .UNSPECIFIED. ) ;
#9170=B_SPLINE_CURVE_WITH_KNOTS ( 'NONE', 3,
 ( #39215, #30382, #11208, #7530, #11409, #2186, #36152, #23186, #17382, #14102, #7930, #29963, #14304, #39418, #26874, #23975, #23773, #36350, #20089, #33272, #27081, #32666, #4466, #5054, #23588, #39626, #7733, #14506, #11003, #26479, #23384 ),
 .UNSPECIFIED., .F., .F.,
 ( 4, 3, 3, 3, 3, 3, 3, 3, 3, 3, 4 ),
 ( 1.226634733346699349E-18, 2.999644130997555441E-05, 6.002588995694558974E-05, 8.960886084587723428E-05, 0.0001190604700446452712, 0.0001489538463052706904, 0.0001796139255493956052, 0.0002109707048517044494, 0.0002426195318110353836, 0.0002740640997890060756, 0.0002849778069099853954 ),
 .UNSPECIFIED. ) ;
#9178=CARTESIAN_POINT ( 'NONE',  ( 4.981062705491726916, -30.77339773246524857, 7.773839561854630986 ) ) ;
#9184=ORIENTED_EDGE ( 'NONE', *, *, #20166, .T. ) ;
#9192=CARTESIAN_POINT ( 'NONE',  ( -1.698180065124302196, -29.47090112884363222, 7.774064877406529739 ) ) ;
#9194=CARTESIAN_POINT ( 'NONE',  ( -1.326714576903637033, -31.11803783986836791, 6.882085323592684212 ) ) ;
#9196=CARTESIAN_POINT ( 'NONE',  ( -0.02954975575422185557, -26.53738454105226197, 7.778495531946296282 ) ) ;
#9197=DIRECTION ( 'NONE',  ( 0.1736481776669404897, -0.9848077530122062440, -0.000000000000000000 ) ) ;
#9199=CARTESIAN_POINT ( 'NONE',  ( 2.562099542307729738, -33.75548367670988625, 7.754798119455333705 ) ) ;
#9202=ORIENTED_EDGE ( 'NONE', *, *, #6443, .F. ) ;
#9203=EDGE_CURVE ( 'NONE', #19738, #20650, #33415, .T. ) ;
#9204=EDGE_CURVE ( 'NONE', #10597, #10909, #15669, .T. ) ;
#9205=EDGE_CURVE ( 'NONE', #35449, #29219, #23049, .T. ) ;
#9210=CARTESIAN_POINT ( 'NONE',  ( 1.686887486498408029, -26.16995699532097319, 7.635761828346577573 ) ) ;
#9211=ORIENTED_EDGE ( 'NONE', *, *, #22710, .F. ) ;
#9212=FACE_OUTER_BOUND ( 'NONE', #14784, .T. ) ;
#9213=CARTESIAN_POINT ( 'NONE',  ( 3.446800832104334855, -26.65272994776861637, 6.889465824494256374 ) ) ;
#9220=CARTESIAN_POINT ( 'NONE',  ( -0.3956209610833227308, -26.89285385646818582, 7.761597726988853196 ) ) ;
#9231=CARTESIAN_POINT ( 'NONE',  ( -1.648904451518951042, -28.98487051485360411, 7.763628509615286610 ) ) ;
#9232=CARTESIAN_POINT ( 'NONE',  ( -0.4832139993529582234, -26.85040468425802018, 7.782861076432729952 ) ) ;
#9233=VERTEX_POINT ( 'NONE', #37572 ) ;
#9236=( BOUNDED_CURVE ( )  B_SPLINE_CURVE ( 3, ( #32634, #39588, #11373, #23939 ),
 .UNSPECIFIED., .F., .T. ) 
 B_SPLINE_CURVE_WITH_KNOTS ( ( 4, 4 ),
 ( 4.748221474220557958, 4.941946782021392259 ),
 .UNSPECIFIED. ) 
 CURVE ( )  GEOMETRIC_REPRESENTATION_ITEM ( )  RATIONAL_B_SPLINE_CURVE ( ( 1.000000000000000000, 0.9968749865767494445, 0.9968749865767494445, 1.000000000000000000 ) ) 
 REPRESENTATION_ITEM ( '' )  );
#9243=AXIS2_PLACEMENT_3D ( 'NONE', #33233, #8698, #23742 ) ;
#9261=CARTESIAN_POINT ( 'NONE',  ( 3.557203646265561847, -26.60307234877650018, 7.751599049952199394 ) ) ;
#9265=CARTESIAN_POINT ( 'NONE',  ( 5.098960251590484383, -29.66895923794316658, 7.774064877406529739 ) ) ;
#9269=CARTESIAN_POINT ( 'NONE',  ( -1.259118276085812171, -31.24364169136941882, 7.782167645815905033 ) ) ;
#9270=VECTOR ( 'NONE', #7166, 999.9999999999998863 ) ;
#9284=ORIENTED_EDGE ( 'NONE', *, *, #12792, .F. ) ;
#9290=CARTESIAN_POINT ( 'NONE',  ( -1.751823616877372869, -28.99354058093586772, 7.724038915126862470 ) ) ;
#9291=VERTEX_POINT ( 'NONE', #27293 ) ;
#9293=CARTESIAN_POINT ( 'NONE',  ( 2.365931152121737213, -26.13377987989076345, 6.873189335546979528 ) ) ;
#9298=ORIENTED_EDGE ( 'NONE', *, *, #38120, .F. ) ;
#9300=AXIS2_PLACEMENT_3D ( 'NONE', #10478, #23059, #16459 ) ;
#9304=CARTESIAN_POINT ( 'NONE',  ( 4.274037619018428380, -31.94193077376366574, 6.887547729233693516 ) ) ;
#9305=DIRECTION ( 'NONE',  ( -0.8660254037844345998, -0.5000000000000071054, -0.000000000000000000 ) ) ;
#9307=CARTESIAN_POINT ( 'NONE',  ( -1.416991000366785602, -31.16114644904380526, 6.998987538705435441 ) ) ;
#9312=CARTESIAN_POINT ( 'NONE',  ( 1.666437316484441933, -26.07009487170356721, 7.714178352335856026 ) ) ;
#9313=B_SPLINE_CURVE_WITH_KNOTS ( 'NONE', 3,
 ( #32958, #19981, #7630, #35455, #29261, #1467, #26777, #14001, #13399, #26572 ),
 .UNSPECIFIED., .F., .F.,
 ( 4, 3, 3, 4 ),
 ( 0.0001585009270395759944, 0.0001815657551981854682, 0.0002118214035944135625, 0.0002170292169044765425 ),
 .UNSPECIFIED. ) ;
#9314=CARTESIAN_POINT ( 'NONE',  ( 0.5160167997142889318, -32.86344804452599533, 7.635761828346576685 ) ) ;
#9319=CARTESIAN_POINT ( 'NONE',  ( -0.9173357114122402400, -31.73963204593200516, 7.779495906702015517 ) ) ;
#9320=FACE_OUTER_BOUND ( 'NONE', #40575, .T. ) ;
#9322=CARTESIAN_POINT ( 'NONE',  ( 1.664531801855456017, -26.17011927939601890, 7.691066658568947112 ) ) ;
#9325=CARTESIAN_POINT ( 'NONE',  ( -1.453346889880533954, -28.29951960356443408, 7.761597726988851420 ) ) ;
#9327=ORIENTED_EDGE ( 'NONE', *, *, #7628, .F. ) ;
#9330=CARTESIAN_POINT ( 'NONE',  ( -89.20959394718985891, -30.27593629695115496, 6.864216812889196717 ) ) ;
#9331=CARTESIAN_POINT ( 'NONE',  ( 0.04278369059588756074, -26.60137143983851615, 6.894806418505345924 ) ) ;
#9332=CARTESIAN_POINT ( 'NONE',  ( 5.010720015369884095, -28.43335788139641807, 6.870737987065012042 ) ) ;
#9335=CARTESIAN_POINT ( 'NONE',  ( 4.853254720949315093, -30.84250634616293851, 7.759451378593095860 ) ) ;
#9336=AXIS2_PLACEMENT_3D ( 'NONE', #9475, #22063, #32156 ) ;
#9337=CARTESIAN_POINT ( 'NONE',  ( 5.053699547558291094, -30.13146740640211974, 7.730758795053805699 ) ) ;
#9339=EDGE_CURVE ( 'NONE', #28028, #34419, #944, .T. ) ;
#9342=ORIENTED_EDGE ( 'NONE', *, *, #30841, .T. ) ;
#9345=CARTESIAN_POINT ( 'NONE',  ( -1.003265571170591786, -27.34726367792503510, 7.710604733652634657 ) ) ;
#9348=ORIENTED_EDGE ( 'NONE', *, *, #22760, .T. ) ;
#9349=CARTESIAN_POINT ( 'NONE',  ( 4.434542230703401700, -27.54893547855059310, 6.939395833800437785 ) ) ;
#9359=CARTESIAN_POINT ( 'NONE',  ( 1.736346942945643512, -32.96974004645320377, 7.703977250142847844 ) ) ;
#9360=CARTESIAN_POINT ( 'NONE',  ( 1.651639975615219580, -32.96958066925694908, 6.894806418505345036 ) ) ;
#9362=CARTESIAN_POINT ( 'NONE',  ( 3.813621333521583168, -32.23345227369436827, 6.866852738645443210 ) ) ;
#9363=CARTESIAN_POINT ( 'NONE',  ( 3.357996495870312792, -32.53848892694827555, 6.894806418505347700 ) ) ;
#9365=CARTESIAN_POINT ( 'NONE',  ( 4.327908163969746980, -31.72774129374395713, 7.695279973900954751 ) ) ;
#9367=CIRCLE ( 'NONE', #4788, 3.499999999999999556 ) ;
#9376=CARTESIAN_POINT ( 'NONE',  ( -1.664990407196974553, -30.05394385900508070, 7.768425012602593327 ) ) ;
#9385=ADVANCED_FACE ( 'NONE', ( #16366 ), #22567, .F. ) ;
#9387=CARTESIAN_POINT ( 'NONE',  ( 3.958376580442097392, -26.90712677766138938, 7.778495531946297170 ) ) ;
#9389=VERTEX_POINT ( 'NONE', #15765 ) ;
#9393=AXIS2_PLACEMENT_3D ( 'NONE', #27816, #15678, #18346 ) ;
#9394=CARTESIAN_POINT ( 'NONE',  ( 0.2020707124235944507, -34.04266111819475782, 7.754798119455333705 ) ) ;
#9400=CARTESIAN_POINT ( 'NONE',  ( 3.477237270422150139, -26.55450084266673727, 6.894806418505347700 ) ) ;
#9417=CARTESIAN_POINT ( 'NONE',  ( -1.611334115997590688, -28.41660772738555707, 7.255881584735162981 ) ) ;
#9423=ORIENTED_EDGE ( 'NONE', *, *, #32930, .F. ) ;
#9426=PLANE ( 'NONE',  #28739 ) ;
#9437=ORIENTED_EDGE ( 'NONE', *, *, #37007, .T. ) ;
#9440=B_SPLINE_CURVE_WITH_KNOTS ( 'NONE', 3,
 ( #24308, #18122, #30717, #20603 ),
 .UNSPECIFIED., .F., .F.,
 ( 4, 4 ),
 ( 0.000000000000000000, 6.391136169993328150E-06 ),
 .UNSPECIFIED. ) ;
#9442=ORIENTED_EDGE ( 'NONE', *, *, #24500, .F. ) ;
#9448=CARTESIAN_POINT ( 'NONE',  ( 4.744409466245708806, -31.29734294690251417, 7.737115613922532553 ) ) ;
#9451=CARTESIAN_POINT ( 'NONE',  ( -1.597336938230447867, -25.58391321841518007, 7.695279973900954751 ) ) ;
#9456=CYLINDRICAL_SURFACE ( 'NONE', #29559, 3.399999999999999911 ) ;
#9464=AXIS2_PLACEMENT_3D ( 'NONE', #5390, #2321, #9749 ) ;
#9466=CARTESIAN_POINT ( 'NONE',  ( 5.100263068043492609, -29.54054047169235986, 7.661510568013095934 ) ) ;
#9468=CARTESIAN_POINT ( 'NONE',  ( 4.392721987511531978, -31.80629977964779442, 7.749999999999998224 ) ) ;
#9474=( BOUNDED_CURVE ( )  B_SPLINE_CURVE ( 3, ( #38367, #13064, #10164, #25625 ),
 .UNSPECIFIED., .F., .T. ) 
 B_SPLINE_CURVE_WITH_KNOTS ( ( 4, 4 ),
 ( 1.381924640371167801, 1.574767692156076482 ),
 .UNSPECIFIED. ) 
 CURVE ( )  GEOMETRIC_REPRESENTATION_ITEM ( )  RATIONAL_B_SPLINE_CURVE ( ( 1.000000000000000000, 0.9969033633783032089, 0.9969033633783032089, 1.000000000000000000 ) ) 
 REPRESENTATION_ITEM ( '' )  );
#9475=CARTESIAN_POINT ( 'NONE',  ( 6.400024429904298984, -31.46803969333911866, 6.954324564059724878 ) ) ;
#9479=ADVANCED_FACE ( 'NONE', ( #3848 ), #9582, .T. ) ;
#9484=LINE ( 'NONE', #16479, #19397 ) ;
#9485=DIRECTION ( 'NONE',  ( 0.000000000000000000, 0.000000000000000000, 1.000000000000000000 ) ) ;
#9486=B_SPLINE_CURVE_WITH_KNOTS ( 'NONE', 3,
 ( #8220, #37049, #27780, #23869, #33783, #15023, #27586, #17479, #5560, #8023, #39522, #21419, #18101, #1883, #27377, #33583, #20791, #36851, #14809, #39940, #36648, #24289, #30897, #20579, #26977, #4952, #30692, #40138, #2499, #36445, #24494 ),
 .UNSPECIFIED., .F., .F.,
 ( 4, 3, 3, 3, 3, 3, 3, 3, 3, 3, 4 ),
 ( 8.673617379884035472E-19, 3.077658087705547241E-05, 6.152638666999100904E-05, 9.267501192706544444E-05, 0.0001241882240135173282, 0.0001556618703051625174, 0.0001866161554452157713, 0.0002167966385860940542, 0.0002463805737537739116, 0.0002758761370306490207, 0.0002847094172289989233 ),
 .UNSPECIFIED. ) ;
#9489=CARTESIAN_POINT ( 'NONE',  ( 3.900618212833813825, -32.29189216196311918, 6.870737987065012042 ) ) ;
#9490=ORIENTED_EDGE ( 'NONE', *, *, #11698, .T. ) ;
#9494=AXIS2_PLACEMENT_3D ( 'NONE', #38343, #22730, #36091 ) ;
#9499=B_SPLINE_CURVE_WITH_KNOTS ( 'NONE', 3,
 ( #27389, #40151, #9261, #34009 ),
 .UNSPECIFIED., .F., .F.,
 ( 4, 4 ),
 ( 0.000000000000000000, 6.391136169992404037E-06 ),
 .UNSPECIFIED. ) ;
#9501=CARTESIAN_POINT ( 'NONE',  ( 2.343537225896455745, -33.01033157941493101, 7.695279973900954751 ) ) ;
#9502=FACE_OUTER_BOUND ( 'NONE', #14136, .T. ) ;
#9506=ORIENTED_EDGE ( 'NONE', *, *, #11092, .T. ) ;
#9507=VECTOR ( 'NONE', #29504, 999.9999999999998863 ) ;
#9509=CARTESIAN_POINT ( 'NONE',  ( 0.5342690456537854127, -32.86995697391282079, 7.720710062488888248 ) ) ;
#9511=CARTESIAN_POINT ( 'NONE',  ( 4.256713912089230334, -31.96058041568350916, 6.980586498568968068 ) ) ;
#9518=CARTESIAN_POINT ( 'NONE',  ( 4.697119935056596418, -31.35014961918641063, 7.785096263473213263 ) ) ;
#9519=CARTESIAN_POINT ( 'NONE',  ( -0.6299129325132426516, -32.04575989041425998, 7.006423389747790331 ) ) ;
#9522=CARTESIAN_POINT ( 'NONE',  ( 3.442434176459446160, -26.65012155745640499, 6.894806418505343260 ) ) ;
#9523=CARTESIAN_POINT ( 'NONE',  ( 1.715724685556488494, -33.06989670050605667, 7.637894019485640840 ) ) ;
#9526=CARTESIAN_POINT ( 'NONE',  ( 0.9074459145065832955, -26.15392167357531505, 7.139344958878411695 ) ) ;
#9530=CARTESIAN_POINT ( 'NONE',  ( -1.506684114051581647, -28.44091511309124343, 7.695279973900954751 ) ) ;
#9538=VECTOR ( 'NONE', #27572, 1000.000000000000000 ) ;
#9542=EDGE_CURVE ( 'NONE', #18906, #33368, #28715, .T. ) ;
#9544=CARTESIAN_POINT ( 'NONE',  ( 5.043486035277081392, -28.53373062621871981, 6.895394898881670009 ) ) ;
#9545=CARTESIAN_POINT ( 'NONE',  ( 1.081163097807408935, -26.22679299245623952, 7.730758795053809251 ) ) ;
#9546=CARTESIAN_POINT ( 'NONE',  ( 5.045119861038438458, -30.18056701569746281, 7.779495906702012853 ) ) ;
#9550=DIRECTION ( 'NONE',  ( 1.000000000000000000, 0.000000000000000000, 0.000000000000000000 ) ) ;
#9554=CARTESIAN_POINT ( 'NONE',  ( -1.677244393547275392, -29.95926971864756538, 6.988553391373224066 ) ) ;
#9558=EDGE_CURVE ( 'NONE', #2658, #20612, #39169, .T. ) ;
#9561=CARTESIAN_POINT ( 'NONE',  ( -1.586324960283478580, -30.75679626155069712, 7.773839561854631874 ) ) ;
#9562=CARTESIAN_POINT ( 'NONE',  ( 4.361462012329716309, -31.84340686930758935, 6.894806418505347700 ) ) ;
#9565=CARTESIAN_POINT ( 'NONE',  ( 1.139664070701874143, -33.03161420323011299, 7.255881584735162093 ) ) ;
#9566=ORIENTED_EDGE ( 'NONE', *, *, #8264, .T. ) ;
#9572=CARTESIAN_POINT ( 'NONE',  ( 3.435265683109236967, -26.53015935524666347, 7.750000000000001776 ) ) ;
#9574=CARTESIAN_POINT ( 'NONE',  ( -1.553683706606911130, -30.55532538593644176, 7.013842709614101167 ) ) ;
#9579=ADVANCED_FACE ( 'NONE', ( #32436 ), #1544, .F. ) ;
#9582=CYLINDRICAL_SURFACE ( 'NONE', #5271, 3.399999999999999911 ) ;
#9589=CARTESIAN_POINT ( 'NONE',  ( 3.325856478880445000, -25.14347697372913615, 7.635761828346577573 ) ) ;
#9596=VECTOR ( 'NONE', #14219, 1000.000000000000114 ) ;
#9597=CARTESIAN_POINT ( 'NONE',  ( 5.200364047366366371, -29.55642757665872722, 7.635761828346577573 ) ) ;
#9598=CARTESIAN_POINT ( 'NONE',  ( 0.03153883250375685843, -32.53218194000729113, 7.691066658568948000 ) ) ;
#9601=B_SPLINE_CURVE_WITH_KNOTS ( 'NONE', 3,
 ( #39852, #5471, #36361, #8128, #30602, #11824, #27089, #11421, #20699, #4663, #8544, #2411, #33282, #20910, #23596, #14713, #27500, #27287, #17199, #5063, #24199, #21125, #29766, #30176, #26691, #2195, #17596, #1997, #14315, #39635, #24408 ),
 .UNSPECIFIED., .F., .F.,
 ( 4, 3, 3, 3, 3, 3, 3, 3, 3, 3, 4 ),
 ( 1.226634733346699349E-18, 2.999644130997734673E-05, 6.002588995694668750E-05, 8.960886084587991768E-05, 0.0001190604700446490252, 0.0001489538463052708802, 0.0001796139255493970418, 0.0002109707048517072412, 0.0002426195318110355734, 0.0002740640997890037987, 0.0002849778069099845822 ),
 .UNSPECIFIED. ) ;
#9605=CARTESIAN_POINT ( 'NONE',  ( -0.8622465457266019762, -27.33543793757026918, 6.880147297696980857 ) ) ;
#9606=EDGE_LOOP ( 'NONE', ( #25485, #22065, #30408, #23677, #31376 ) ) ;
#9607=EDGE_LOOP ( 'NONE', ( #22493, #32848, #12088, #20513, #15602 ) ) ;
#9609=CARTESIAN_POINT ( 'NONE',  ( 0.04256582245634059347, -26.49275466612191110, 7.771081512783703182 ) ) ;
#9610=CARTESIAN_POINT ( 'NONE',  ( -0.5240808859923175023, -32.27210411901214826, 7.720710062488896241 ) ) ;
#9611=PLANE ( 'NONE',  #13673 ) ;
#9612=CARTESIAN_POINT ( 'NONE',  ( 1.700390093233090871, -29.56993018339339940, 7.800000000000000711 ) ) ;
#9614=ORIENTED_EDGE ( 'NONE', *, *, #15999, .F. ) ;
#9616=CARTESIAN_POINT ( 'NONE',  ( -0.9352292415849461360, -31.71783863626873767, 6.894806418505345924 ) ) ;
#9620=CARTESIAN_POINT ( 'NONE',  ( 5.005904147265696658, -30.36590558413950802, 6.959317978105167057 ) ) ;
#9624=EDGE_LOOP ( 'NONE', ( #21860, #37898, #2487, #37598 ) ) ;
#9631=CARTESIAN_POINT ( 'NONE',  ( 1.687546834072821023, -26.16994927825320971, 7.756377446753164762 ) ) ;
#9632=FACE_OUTER_BOUND ( 'NONE', #12685, .T. ) ;
#9636=VERTEX_POINT ( 'NONE', #8297 ) ;
#9639=VERTEX_POINT ( 'NONE', #16758 ) ;
#9642=CARTESIAN_POINT ( 'NONE',  ( 2.921117467371362242, -32.85015253290869452, 7.651421919295145813 ) ) ;
#9643=ORIENTED_EDGE ( 'NONE', *, *, #26729, .F. ) ;
#9644=CARTESIAN_POINT ( 'NONE',  ( -1.642565866964522225, -28.94973227290090989, 7.782167645815903256 ) ) ;
#9645=CARTESIAN_POINT ( 'NONE',  ( -0.4769030174555436985, -26.84268727337696703, 7.780491323090171996 ) ) ;
#9646=VERTEX_POINT ( 'NONE', #7504 ) ;
#9652=AXIS2_PLACEMENT_3D ( 'NONE', #1685, #23099, #20589 ) ;
#9656=ORIENTED_EDGE ( 'NONE', *, *, #5344, .T. ) ;
#9657=AXIS2_PLACEMENT_3D ( 'NONE', #5849, #16118, #38536 ) ;
#9662=DIRECTION ( 'NONE',  ( 0.000000000000000000, 0.7126435865141257375, 0.7015262779114433966 ) ) ;
#9668=VERTEX_POINT ( 'NONE', #39819 ) ;
#9671=CARTESIAN_POINT ( 'NONE',  ( 3.554700302571109916, -26.60177950712765593, 7.754798119455333705 ) ) ;
#9672=CARTESIAN_POINT ( 'NONE',  ( 1.686887486498407140, -26.06995622926011436, 7.635761828346576685 ) ) ;
#9675=ORIENTED_EDGE ( 'NONE', *, *, #37330, .T. ) ;
#9682=CARTESIAN_POINT ( 'NONE',  ( 5.140321331941717808, -29.00739657781303293, 7.785096263473213263 ) ) ;
#9684=B_SPLINE_CURVE_WITH_KNOTS ( 'NONE', 3,
 ( #14744, #8573, #36589, #15164, #12063, #24013, #24642, #33718, #20728, #5497, #33524, #40277, #8365, #2441, #33101, #21358, #40080, #18248, #23808, #14962, #20938, #11858, #30837, #2647, #4886, #27722, #37193, #17417, #5294, #1819, #30415 ),
 .UNSPECIFIED., .F., .F.,
 ( 4, 3, 3, 3, 3, 3, 3, 3, 3, 3, 4 ),
 ( 6.484403375994506654E-05, 8.983333709522423050E-05, 0.0001203539973219388106, 0.0001514144607149688852, 0.0001828916862241641297, 0.0002144221682127289306, 0.0002455195857862220790, 0.0002758614570916278607, 0.0003055381793602574415, 0.0003350143730643698843, 0.0003497271997307904268 ),
 .UNSPECIFIED. ) ;
#9687=CARTESIAN_POINT ( 'NONE',  ( 4.620198719170100610, -31.31197426661971761, 6.894806418505346812 ) ) ;
#9689=AXIS2_PLACEMENT_3D ( 'NONE', #38653, #31899, #25910 ) ;
#9690=B_SPLINE_CURVE_WITH_KNOTS ( 'NONE', 3,
 ( #21879, #6233, #34666, #35069, #9509, #6444, #31354, #3776, #9721, #22505 ),
 .UNSPECIFIED., .F., .F.,
 ( 4, 3, 3, 4 ),
 ( 0.0001585009270395679984, 0.0001815657551981835979, 0.0002118214035944133186, 0.0002170292169044720973 ),
 .UNSPECIFIED. ) ;
#9693=ORIENTED_EDGE ( 'NONE', *, *, #35111, .F. ) ;
#9695=CARTESIAN_POINT ( 'NONE',  ( 4.638101942922436827, -27.85824998890764448, 7.635761828346577573 ) ) ;
#9696=CARTESIAN_POINT ( 'NONE',  ( 1.756997582572583649, -26.17040145250279437, 6.887041543973315250 ) ) ;
#9703=CARTESIAN_POINT ( 'NONE',  ( 3.922483456672744673, -26.86580350659783178, 7.695279973900954751 ) ) ;
#9710=ORIENTED_EDGE ( 'NONE', *, *, #32336, .F. ) ;
#9712=CARTESIAN_POINT ( 'NONE',  ( 3.901153242843497626, -32.27259905789637173, 7.785344483711591934 ) ) ;
#9718=ORIENTED_EDGE ( 'NONE', *, *, #28547, .T. ) ;
#9721=CARTESIAN_POINT ( 'NONE',  ( 0.5371711504799124848, -32.87097875789517332, 7.697032948437506406 ) ) ;
#9726=CARTESIAN_POINT ( 'NONE',  ( -1.396386647739597420, -31.20089878032661801, 6.870724624169666228 ) ) ;
#9727=DIRECTION ( 'NONE',  ( -1.000000000000000000, 0.000000000000000000, 0.000000000000000000 ) ) ;
#9728=CARTESIAN_POINT ( 'NONE',  ( 1.515152310805649938, -33.06502611812176440, 6.989977667959446528 ) ) ;
#9729=EDGE_CURVE ( 'NONE', #21194, #28994, #37084, .T. ) ;
#9730=DIRECTION ( 'NONE',  ( -0.1736481776669340227, 0.9848077530122073542, -0.000000000000000000 ) ) ;
#9731=CARTESIAN_POINT ( 'NONE',  ( -0.6258329412763763422, -32.04959131907094161, 6.895222827070021765 ) ) ;
#9732=CARTESIAN_POINT ( 'NONE',  ( -1.242570340174825594, -27.67546881208082965, 7.013842709614101167 ) ) ;
#9737=CARTESIAN_POINT ( 'NONE',  ( 4.362817617720858188, -27.29804117271309138, 7.730015791551950954 ) ) ;
#9738=( BOUNDED_CURVE ( )  B_SPLINE_CURVE ( 3, ( #12652, #9565, #22145, #6496 ),
 .UNSPECIFIED., .F., .T. ) 
 B_SPLINE_CURVE_WITH_KNOTS ( ( 4, 4 ),
 ( 1.347909859412854683, 1.534781240595300078 ),
 .UNSPECIFIED. ) 
 CURVE ( )  GEOMETRIC_REPRESENTATION_ITEM ( )  RATIONAL_B_SPLINE_CURVE ( ( 1.000000000000000000, 0.9970920404276226723, 0.9970920404276226723, 1.000000000000000000 ) ) 
 REPRESENTATION_ITEM ( '' )  );
#9741=CARTESIAN_POINT ( 'NONE',  ( 3.428181999189476858, -32.49819505012106902, 7.721096864323904185 ) ) ;
#9745=CARTESIAN_POINT ( 'NONE',  ( -1.506257772487957336, -28.43970203156576559, 7.712764235869102869 ) ) ;
#9747=CARTESIAN_POINT ( 'NONE',  ( -0.2563090734626436440, -34.23573776596825979, 6.894806418505347700 ) ) ;
#9749=DIRECTION ( 'NONE',  ( 0.9396926207859105373, 0.3420201433256629397, 0.000000000000000000 ) ) ;
#9751=CARTESIAN_POINT ( 'NONE',  ( -0.5769924795711234289, -32.09451502393404354, 7.754798119455333705 ) ) ;
#9756=ORIENTED_EDGE ( 'NONE', *, *, #1780, .T. ) ;
#9758=CYLINDRICAL_SURFACE ( 'NONE', #14255, 3.499999999999999556 ) ;
#9761=CARTESIAN_POINT ( 'NONE',  ( -1.194263764872669054, -31.54948795403056394, 7.501983001166817822 ) ) ;
#9762=ORIENTED_EDGE ( 'NONE', *, *, #32774, .F. ) ;
#9765=CARTESIAN_POINT ( 'NONE',  ( -1.676168523076433159, -29.96849248796560872, 6.903372536218459032 ) ) ;
#9768=CARTESIAN_POINT ( 'NONE',  ( -1.582528736513596490, -30.78337320113038444, 7.750000000000000000 ) ) ;
#9771=CARTESIAN_POINT ( 'NONE',  ( 3.300479879060630228, -34.00561972003898603, 7.635761828346577573 ) ) ;
#9772=ORIENTED_EDGE ( 'NONE', *, *, #6620, .F. ) ;
#9774=CARTESIAN_POINT ( 'NONE',  ( 0.4551510633898000480, -26.29166087107455496, 7.255881584735164758 ) ) ;
#9778=CARTESIAN_POINT ( 'NONE',  ( 1.585236220975464683, -32.96797956292043352, 7.761597726988851420 ) ) ;
#9782=CARTESIAN_POINT ( 'NONE',  ( 3.764702813991775976, -32.27154237255469127, 6.871394612369937427 ) ) ;
#9783=CARTESIAN_POINT ( 'NONE',  ( -1.000637662739485290, -31.79578935716557453, 6.894806418505347700 ) ) ;
#9786=DIRECTION ( 'NONE',  ( 0.000000000000000000, 0.000000000000000000, 1.000000000000000000 ) ) ;
#9795=CARTESIAN_POINT ( 'NONE',  ( 3.279379792629018020, -34.01329952344053709, 7.695279973900954751 ) ) ;
#9802=CARTESIAN_POINT ( 'NONE',  ( 1.169096226813607586, -26.12294996860957852, 7.782861076432730840 ) ) ;
#9803=ORIENTED_EDGE ( 'NONE', *, *, #33017, .F. ) ;
#9806=VERTEX_POINT ( 'NONE', #11787 ) ;
#9815=CARTESIAN_POINT ( 'NONE',  ( -0.04750094642060438688, -26.54137113793980873, 7.767720160662274331 ) ) ;
#9817=CARTESIAN_POINT ( 'NONE',  ( -0.5293678058294215560, -32.26774198379361280, 7.737115613922535218 ) ) ;
#9821=ORIENTED_EDGE ( 'NONE', *, *, #19143, .F. ) ;
#9825=CARTESIAN_POINT ( 'NONE',  ( 4.288407054171600841, -27.36489447023938126, 7.652160403243383868 ) ) ;
#9828=CARTESIAN_POINT ( 'NONE',  ( 0.1003003074055170557, -25.13424064674780922, 7.635761828346577573 ) ) ;
#9832=CARTESIAN_POINT ( 'NONE',  ( -0.5692424881582137663, -26.90557721422857895, 7.737115613922536106 ) ) ;
#9834=CARTESIAN_POINT ( 'NONE',  ( -1.580908707445344064, -30.78775612134597139, 7.743886751744248897 ) ) ;
#9840=CARTESIAN_POINT ( 'NONE',  ( 4.626733377823518012, -27.83888570657239470, 7.695279973900954751 ) ) ;
#9852=CARTESIAN_POINT ( 'NONE',  ( -1.635022261790646469, -28.91028966882242557, 7.784476445165073422 ) ) ;
#9853=ORIENTED_EDGE ( 'NONE', *, *, #40675, .F. ) ;
#9855=ORIENTED_EDGE ( 'NONE', *, *, #30502, .T. ) ;
#9859=CARTESIAN_POINT ( 'NONE',  ( 5.152950880260274147, -30.14423324962431749, 7.714178352335856026 ) ) ;
#9860=EDGE_CURVE ( 'NONE', #38473, #6204, #19882, .T. ) ;
#9863=VERTEX_POINT ( 'NONE', #25398 ) ;
#9867=CARTESIAN_POINT ( 'NONE',  ( 4.744454306064458393, -28.05544235445824697, 6.949473656533215582 ) ) ;
#9873=ORIENTED_EDGE ( 'NONE', *, *, #9110, .T. ) ;
#9877=AXIS2_PLACEMENT_3D ( 'NONE', #21742, #18629, #5270 ) ;
#9878=DIRECTION ( 'NONE',  ( -0.000000000000000000, -0.000000000000000000, -1.000000000000000000 ) ) ;
#9883=CARTESIAN_POINT ( 'NONE',  ( 0.4449537687655561458, -32.72967155099453151, 7.774064877406529739 ) ) ;
#9886=CYLINDRICAL_SURFACE ( 'NONE', #37793, 0.09010775117052900740 ) ;
#9898=EDGE_CURVE ( 'NONE', #28243, #33383, #37935, .T. ) ;
#9906=CARTESIAN_POINT ( 'NONE',  ( 3.808759754361716876, -32.36363944866005227, 6.998987538705436329 ) ) ;
#9907=ORIENTED_EDGE ( 'NONE', *, *, #16907, .T. ) ;
#9912=CARTESIAN_POINT ( 'NONE',  ( 2.910418097296712414, -26.39252032545340398, 7.785868773668302545 ) ) ;
#9913=ORIENTED_EDGE ( 'NONE', *, *, #26041, .F. ) ;
#9920=VERTEX_POINT ( 'NONE', #14430 ) ;
#9922=FACE_OUTER_BOUND ( 'NONE', #38031, .T. ) ;
#9925=CARTESIAN_POINT ( 'NONE',  ( -0.09718281214228366438, -32.57305050230510091, 6.875671892026060661 ) ) ;
#9928=CARTESIAN_POINT ( 'NONE',  ( -1.699420810764287859, -29.60578847477102116, 7.691066658568944447 ) ) ;
#9929=CARTESIAN_POINT ( 'NONE',  ( 3.573870332252533810, -26.73266402712449619, 6.920489980334476599 ) ) ;
#9930=CARTESIAN_POINT ( 'NONE',  ( 4.682439246746215922, -31.37861164225721211, 7.782861076432729064 ) ) ;
#9935=CARTESIAN_POINT ( 'NONE',  ( 5.128444259610362543, -30.27593629695848421, 6.864216812847430127 ) ) ;
#9936=CARTESIAN_POINT ( 'NONE',  ( 1.734605777361225565, -33.06976452674143019, 7.674970859709602244 ) ) ;
#9937=CARTESIAN_POINT ( 'NONE',  ( 1.736314072191997848, -32.96974039457447248, 7.692469944509197077 ) ) ;
#9941=ORIENTED_EDGE ( 'NONE', *, *, #16965, .T. ) ;
#9942=B_SPLINE_CURVE_WITH_KNOTS ( 'NONE', 3,
 ( #10870, #38470, #14167, #32524, #22655, #23054, #32726, #36011, #4711, #32136 ),
 .UNSPECIFIED., .F., .F.,
 ( 4, 3, 3, 4 ),
 ( 0.0005050348086185310918, 0.0005143352185143295566, 0.0005445898203825194584, 0.0005634294782181710655 ),
 .UNSPECIFIED. ) ;
#9947=ORIENTED_EDGE ( 'NONE', *, *, #14815, .F. ) ;
#9959=AXIS2_PLACEMENT_3D ( 'NONE', #4163, #29065, #872 ) ;
#9961=CARTESIAN_POINT ( 'NONE',  ( 0.6790956408842164782, -32.92475242180294259, 7.139344958878409919 ) ) ;
#9962=ORIENTED_EDGE ( 'NONE', *, *, #20675, .F. ) ;
#9970=( BOUNDED_CURVE ( )  B_SPLINE_CURVE ( 3, ( #17377, #1772, #17582, #30164 ),
 .UNSPECIFIED., .F., .T. ) 
 B_SPLINE_CURVE_WITH_KNOTS ( ( 4, 4 ),
 ( 4.748221474220559735, 4.941946782021394036 ),
 .UNSPECIFIED. ) 
 CURVE ( )  GEOMETRIC_REPRESENTATION_ITEM ( )  RATIONAL_B_SPLINE_CURVE ( ( 1.000000000000000000, 0.9968749865767494445, 0.9968749865767494445, 1.000000000000000000 ) ) 
 REPRESENTATION_ITEM ( '' )  );
#9978=CARTESIAN_POINT ( 'NONE',  ( -0.1489007850597646454, -32.54049873642831159, 7.761113333117550361 ) ) ;
#9982=CARTESIAN_POINT ( 'NONE',  ( 3.846394003886068891, -32.20710163246565116, 6.892063359921928090 ) ) ;
#9984=CARTESIAN_POINT ( 'NONE',  ( 5.196109512279864617, -29.74298762467820367, 7.009310105710483185 ) ) ;
#9985=CARTESIAN_POINT ( 'NONE',  ( -0.8989622146313063222, -27.22613634409080419, 7.751599049952198506 ) ) ;
#9994=DIRECTION ( 'NONE',  ( -0.8660254037844232755, 0.5000000000000265343, 0.000000000000000000 ) ) ;
#9998=PLANE ( 'NONE',  #13980 ) ;
#9999=CARTESIAN_POINT ( 'NONE',  ( 1.201481589801058014, -26.10828805710466582, 7.766640943994345569 ) ) ;
#10000=ORIENTED_EDGE ( 'NONE', *, *, #35456, .T. ) ;
#10002=EDGE_CURVE ( 'NONE', #9233, #19674, #4771, .T. ) ;
#10005=CARTESIAN_POINT ( 'NONE',  ( -0.08065709997538077214, -26.55697965350343281, 7.695279973900954751 ) ) ;
#10016=AXIS2_PLACEMENT_3D ( 'NONE', #8247, #20607, #27203 ) ;
#10018=CARTESIAN_POINT ( 'NONE',  ( -1.033762044237207522, -31.59092488823622702, 6.939395833800444002 ) ) ;
#10019=CARTESIAN_POINT ( 'NONE',  ( -1.489921458977837565, -30.74547780039133116, 7.635761828346577573 ) ) ;
#10021=CARTESIAN_POINT ( 'NONE',  ( 1.700390093233090871, -29.56993018339339940, 7.750000000000000888 ) ) ;
#10025=CARTESIAN_POINT ( 'NONE',  ( -0.5767534791761352864, -26.91199542853306070, 7.698786668945016842 ) ) ;
#10026=CARTESIAN_POINT ( 'NONE',  ( -1.336825994161656928, -27.83057829189845478, 7.756742906098587298 ) ) ;
#10030=DIRECTION ( 'NONE',  ( 1.047444401652940007E-14, -1.000000000000000000, -0.000000000000000000 ) ) ;
#10031=CARTESIAN_POINT ( 'NONE',  ( -0.3385372945680173995, -26.84912605459717838, 7.013842709614101167 ) ) ;
#10032=CARTESIAN_POINT ( 'NONE',  ( 4.659898462552006571, -27.89621867541739775, 7.782167645815905921 ) ) ;
#10033=CARTESIAN_POINT ( 'NONE',  ( -0.9969019986233668140, -27.33953798572080274, 7.651421919295150254 ) ) ;
#10034=B_SPLINE_CURVE_WITH_KNOTS ( 'NONE', 3,
 ( #19891, #10422, #27229, #8077, #36701, #29168, #23189, #11564, #29366, #32464, #21066, #14658, #36305, #23931, #13721, #24140, #38821, #5620, #5415, #20640, #8484, #35563, #976, #24346, #26287 ),
 .UNSPECIFIED., .F., .F.,
 ( 4, 3, 3, 3, 3, 3, 3, 3, 4 ),
 ( 6.468151674592953384E-05, 9.076621574722270420E-05, 0.0001210204262067992404, 0.0001512763324577443512, 0.0001815301820994240324, 0.0002117781465860730096, 0.0002420274594459778639, 0.0002722905548971166559, 0.0002816827545175487591 ),
 .UNSPECIFIED. ) ;
#10045=CARTESIAN_POINT ( 'NONE',  ( -0.4079795678955136506, -26.77622091812672878, 6.998987538705430111 ) ) ;
#10046=CARTESIAN_POINT ( 'NONE',  ( 2.782197798051136317, -32.89830469346890141, 7.754798119455333705 ) ) ;
#10052=ORIENTED_EDGE ( 'NONE', *, *, #16552, .F. ) ;
#10055=CARTESIAN_POINT ( 'NONE',  ( -1.503235331079484149, -28.43115960637267747, 7.652160403243382980 ) ) ;
#10060=CARTESIAN_POINT ( 'NONE',  ( 3.977572546501454642, -32.22783162523180067, 7.695279973900954751 ) ) ;
#10066=ORIENTED_EDGE ( 'NONE', *, *, #2825, .F. ) ;
#10067=EDGE_CURVE ( 'NONE', #30519, #32349, #34647, .T. ) ;
#10074=ORIENTED_EDGE ( 'NONE', *, *, #3010, .F. ) ;
#10075=AXIS2_PLACEMENT_3D ( 'NONE', #1833, #10859, #36195 ) ;
#10076=CARTESIAN_POINT ( 'NONE',  ( 0.5650878065122802996, -32.77478541679437285, 7.730758795053806587 ) ) ;
#10079=CARTESIAN_POINT ( 'NONE',  ( 5.076938436256279275, -29.17122450598600381, 7.006423389747788555 ) ) ;
#10081=CARTESIAN_POINT ( 'NONE',  ( 0.5713440154618105726, -32.77699347534518637, 7.692469944509197965 ) ) ;
#10083=EDGE_CURVE ( 'NONE', #25477, #22296, #4187, .T. ) ;
#10086=CARTESIAN_POINT ( 'NONE',  ( 1.230319205269136518, -26.20258206353872765, 7.754798119455333705 ) ) ;
#10088=DIRECTION ( 'NONE',  ( 0.7508067542896625923, 7.864283315039216110E-15, -0.6605219282605402364 ) ) ;
#10090=AXIS2_PLACEMENT_3D ( 'NONE', #3219, #37954, #4015 ) ;
#10092=ORIENTED_EDGE ( 'NONE', *, *, #6199, .T. ) ;
#10093=EDGE_LOOP ( 'NONE', ( #7810, #26024, #8245, #38543, #25403 ) ) ;
#10097=ORIENTED_EDGE ( 'NONE', *, *, #30189, .F. ) ;
#10098=EDGE_CURVE ( 'NONE', #34388, #14142, #30100, .T. ) ;
#10103=CARTESIAN_POINT ( 'NONE',  ( 2.929197463401206125, -26.39973560994384982, 7.784476445165072533 ) ) ;
#10104=ORIENTED_EDGE ( 'NONE', *, *, #31441, .F. ) ;
#10105=ORIENTED_EDGE ( 'NONE', *, *, #31485, .T. ) ;
#10111=CARTESIAN_POINT ( 'NONE',  ( 4.383437233793472387, -27.48154155094239570, 6.863904403958575706 ) ) ;
#10116=CARTESIAN_POINT ( 'NONE',  ( -0.9682691519857027362, -31.83449588853605405, 7.643192810543820492 ) ) ;
#10118=CARTESIAN_POINT ( 'NONE',  ( 2.406143767593636795, -26.24398412221321308, 7.759451378593096749 ) ) ;
#10119=CARTESIAN_POINT ( 'NONE',  ( 3.547885809248545019, -26.71567729002453362, 6.882085323592685100 ) ) ;
#10120=EDGE_CURVE ( 'NONE', #32660, #19192, #31716, .T. ) ;
#10121=AXIS2_PLACEMENT_3D ( 'NONE', #100, #15520, #40630 ) ;
#10123=CARTESIAN_POINT ( 'NONE',  ( 0.7304454269062439220, -26.31121765476125773, 6.988553391373222290 ) ) ;
#10124=LINE ( 'NONE', #7047, #7189 ) ;
#10128=CARTESIAN_POINT ( 'NONE',  ( 5.727845070442864284, -26.50757187106134083, 6.894806418505347700 ) ) ;
#10129=CARTESIAN_POINT ( 'NONE',  ( 4.370302737341240196, -27.30684236520528785, 7.750000000000000000 ) ) ;
#10130=CARTESIAN_POINT ( 'NONE',  ( -2.673316637388258865, -27.10729750018004935, 7.695279973900954751 ) ) ;
#10132=EDGE_CURVE ( 'NONE', #25920, #17641, #34020, .T. ) ;
#10134=CARTESIAN_POINT ( 'NONE',  ( -1.469804480216468701, -28.34112281322530791, 7.784476445165073422 ) ) ;
#10138=CARTESIAN_POINT ( 'NONE',  ( 3.055515830036299008, -26.34291387766242920, 6.895394898881666457 ) ) ;
#10143=CARTESIAN_POINT ( 'NONE',  ( 5.049964969917366986, -28.55486946145695271, 6.941203072598474577 ) ) ;
#10144=CARTESIAN_POINT ( 'NONE',  ( 1.085683504084817175, -26.22595486797094466, 7.740055089680402567 ) ) ;
#10145=CARTESIAN_POINT ( 'NONE',  ( 1.130000382093760747, -26.11671394750277742, 6.887161170156906209 ) ) ;
#10146=ORIENTED_EDGE ( 'NONE', *, *, #12433, .T. ) ;
#10148=CARTESIAN_POINT ( 'NONE',  ( 3.852146645688039328, -32.33035474113215457, 7.750000000000000888 ) ) ;
#10156=CARTESIAN_POINT ( 'NONE',  ( -1.708840123953186962, -28.77800258176304737, 6.927178575251052628 ) ) ;
#10164=CARTESIAN_POINT ( 'NONE',  ( 4.043747737267941567, -27.09675613275700101, 7.386948897581450346 ) ) ;
#10165=ORIENTED_EDGE ( 'NONE', *, *, #12062, .T. ) ;
#10168=CARTESIAN_POINT ( 'NONE',  ( -0.05447690023199193432, -32.59178206026290781, 7.773839561854630098 ) ) ;
#10171=CARTESIAN_POINT ( 'NONE',  ( -0.9974109439700435953, -31.77706419566279905, 7.785096263473211486 ) ) ;
#10172=EDGE_CURVE ( 'NONE', #35733, #17688, #15011, .T. ) ;
#10175=FACE_OUTER_BOUND ( 'NONE', #38403, .T. ) ;
#10177=CARTESIAN_POINT ( 'NONE',  ( 3.805292929746987074, -32.24004161184372919, 6.864651958020303368 ) ) ;
#10179=CARTESIAN_POINT ( 'NONE',  ( 5.195942103142157542, -29.74646048981854207, 6.903112506833881667 ) ) ;
#10180=CARTESIAN_POINT ( 'NONE',  ( -0.5720344077344724498, -26.90795824500195721, 7.660770905198787339 ) ) ;
#10184=AXIS2_PLACEMENT_3D ( 'NONE', #8203, #31641, #3461 ) ;
#10191=VERTEX_POINT ( 'NONE', #37280 ) ;
#10193=FACE_OUTER_BOUND ( 'NONE', #33775, .T. ) ;
#10195=ORIENTED_EDGE ( 'NONE', *, *, #18727, .T. ) ;
#10196=CARTESIAN_POINT ( 'NONE',  ( 2.864308709047130197, -26.26912818964179053, 7.710604733652628440 ) ) ;
#10198=FACE_OUTER_BOUND ( 'NONE', #5672, .T. ) ;
#10204=ORIENTED_EDGE ( 'NONE', *, *, #16173, .T. ) ;
#10206=( BOUNDED_CURVE ( )  B_SPLINE_CURVE ( 3, ( #38960, #4019, #1520, #16729 ),
 .UNSPECIFIED., .F., .T. ) 
 B_SPLINE_CURVE_WITH_KNOTS ( ( 4, 4 ),
 ( 1.381924640371167134, 1.574767692156074705 ),
 .UNSPECIFIED. ) 
 CURVE ( )  GEOMETRIC_REPRESENTATION_ITEM ( )  RATIONAL_B_SPLINE_CURVE ( ( 1.000000000000000000, 0.9969033633783033199, 0.9969033633783033199, 1.000000000000000000 ) ) 
 REPRESENTATION_ITEM ( '' )  );
#10208=CARTESIAN_POINT ( 'NONE',  ( -1.304540412773448566, -31.16068525338094730, 6.863904403958575706 ) ) ;
#10211=B_SPLINE_CURVE_WITH_KNOTS ( 'NONE', 3,
 ( #37231, #2480, #27153, #30457, #11286, #9026, #18083, #27563, #21399, #21605 ),
 .UNSPECIFIED., .F., .F.,
 ( 4, 3, 3, 4 ),
 ( 0.0002170292169044785754, 0.0002420761345915984773, 0.0002723302478207019375, 0.0002816811360866781563 ),
 .UNSPECIFIED. ) ;
#10212=CARTESIAN_POINT ( 'NONE',  ( -0.5323850565855563488, -32.26524778338716004, 7.743886751744255115 ) ) ;
#10213=CARTESIAN_POINT ( 'NONE',  ( -1.795296463333102999, -29.46015129865232751, 7.766640943994648438 ) ) ;
#10218=CARTESIAN_POINT ( 'NONE',  ( 5.200356001372292702, -29.55434199642423465, 7.638132480492515697 ) ) ;
#10220=CARTESIAN_POINT ( 'NONE',  ( 3.896194328649233984, -32.16578144256224903, 7.635761828346577573 ) ) ;
#10223=CARTESIAN_POINT ( 'NONE',  ( 4.370302737341240196, -27.30684236520528785, 7.750000000000000000 ) ) ;
#10229=CARTESIAN_POINT ( 'NONE',  ( -1.644402349235647653, -30.18018250254910839, 7.643333865083955736 ) ) ;
#10235=EDGE_CURVE ( 'NONE', #6673, #39610, #12374, .T. ) ;
#10237=CARTESIAN_POINT ( 'NONE',  ( -0.9920141182173938255, -27.33364690670997277, 7.640616322432102869 ) ) ;
#10238=B_SPLINE_CURVE_WITH_KNOTS ( 'NONE', 3,
 ( #39447, #32896, #29398, #23418, #11237, #13751, #20720, #33306, #17618, #13941, #2016, #39041, #26314, #38849, #35982, #20312, #4683, #17217, #29789 ),
 .UNSPECIFIED., .F., .F.,
 ( 4, 3, 3, 3, 3, 3, 4 ),
 ( 0.000000000000000000, 2.546128104244741393E-05, 5.711050680483831731E-05, 8.113074941675599164E-05, 0.0001053129305727048962, 0.0001360598016347087881, 0.0001612931755702011341 ),
 .UNSPECIFIED. ) ;
#10244=ORIENTED_EDGE ( 'NONE', *, *, #10002, .T. ) ;
#10246=CARTESIAN_POINT ( 'NONE',  ( 4.817466283527966020, -30.92780942099031449, 6.959317978105159952 ) ) ;
#10247=CARTESIAN_POINT ( 'NONE',  ( -1.238581594385354201, -27.66927444853685714, 6.903112506833889661 ) ) ;
#10251=CARTESIAN_POINT ( 'NONE',  ( 4.879927719065142000, -33.52973165241049713, 7.013842709614101167 ) ) ;
#10256=ORIENTED_EDGE ( 'NONE', *, *, #25717, .F. ) ;
#10259=ADVANCED_FACE ( 'NONE', ( #25547 ), #12370, .F. ) ;
#10260=CARTESIAN_POINT ( 'NONE',  ( 5.026976287143079425, -30.27265651311746453, 6.864276522220859711 ) ) ;
#10263=CARTESIAN_POINT ( 'NONE',  ( -1.261279527196320194, -27.90004417849888085, 7.712764235869103757 ) ) ;
#10267=CARTESIAN_POINT ( 'NONE',  ( 2.329922961629665945, -33.01285193709216514, 7.743886751744252450 ) ) ;
#10268=AXIS2_PLACEMENT_3D ( 'NONE', #16403, #32873, #10430 ) ;
#10269=B_SPLINE_CURVE_WITH_KNOTS ( 'NONE', 3,
 ( #13178, #10079, #32534, #13577, #22665, #22858, #35230, #38683, #7001, #15504, #4333, #19567, #10479, #3941, #16461, #29034, #35430, #838, #13370, #7199, #4132, #30235, #10878, #23834, #2250, #14176, #24252, #14773, #5121, #27344, #17654 ),
 .UNSPECIFIED., .F., .F.,
 ( 4, 3, 3, 3, 3, 3, 3, 3, 3, 3, 4 ),
 ( 1.734723475976807094E-18, 2.999644130997709601E-05, 6.002588995694745322E-05, 8.960886084588071728E-05, 0.0001190604700446499739, 0.0001489538463052708260, 0.0001796139255493996438, 0.0002109707048517061299, 0.0002426195318110375249, 0.0002740640997890022267, 0.0002849778069099830643 ),
 .UNSPECIFIED. ) ;
#10274=CARTESIAN_POINT ( 'NONE',  ( 0.4685308032799795352, -32.73893911755277486, 6.874555630061442102 ) ) ;
#10279=CARTESIAN_POINT ( 'NONE',  ( 2.735183283186696013, -32.91346230508531789, 7.011627023500183853 ) ) ;
#10288=CARTESIAN_POINT ( 'NONE',  ( 3.858226607809892794, -26.94243297489357403, 7.692469944509195301 ) ) ;
#10294=CARTESIAN_POINT ( 'NONE',  ( 1.597520268100450780, -33.06375448864240241, 7.771081512783701406 ) ) ;
#10300=CARTESIAN_POINT ( 'NONE',  ( 3.013805019779557171, -26.32571329602632559, 7.751599049952173637 ) ) ;
#10301=CARTESIAN_POINT ( 'NONE',  ( 2.293051275415638912, -26.12047319804549517, 7.637894019485641728 ) ) ;
#10305=CARTESIAN_POINT ( 'NONE',  ( 5.015318072754217482, -33.54151383920058294, 7.635761828346577573 ) ) ;
#10308=CARTESIAN_POINT ( 'NONE',  ( -1.231209508105928441, -31.29206202033822137, 7.652160403243386533 ) ) ;
#10312=CARTESIAN_POINT ( 'NONE',  ( 4.454149367520055414, -27.41100356581296182, 7.761113333116790081 ) ) ;
#10316=CARTESIAN_POINT ( 'NONE',  ( 4.417542878868808032, -27.52612349775301581, 6.887945620086116882 ) ) ;
#10318=VECTOR ( 'NONE', #13090, 999.9999999999998863 ) ;
#10321=CARTESIAN_POINT ( 'NONE',  ( 1.664433243520564654, -26.07011488755866679, 7.695279973900954751 ) ) ;
#10323=( BOUNDED_CURVE ( )  B_SPLINE_CURVE ( 3, ( #17566, #8513, #1969, #14488 ),
 .UNSPECIFIED., .F., .F. ) 
 B_SPLINE_CURVE_WITH_KNOTS ( ( 4, 4 ),
 ( 4.748221474220559735, 4.941946782021394924 ),
 .UNSPECIFIED. ) 
 CURVE ( )  GEOMETRIC_REPRESENTATION_ITEM ( )  RATIONAL_B_SPLINE_CURVE ( ( 1.000000000000000000, 0.9968749865767494445, 0.9968749865767494445, 1.000000000000000000 ) ) 
 REPRESENTATION_ITEM ( '' )  );
#10324=CARTESIAN_POINT ( 'NONE',  ( -0.1220456601027410937, -32.55802789346970627, 6.865554069792297653 ) ) ;
#10331=CARTESIAN_POINT ( 'NONE',  ( 4.722241970102593278, -31.32479717685847476, 7.773839561854635427 ) ) ;
#10332=EDGE_LOOP ( 'NONE', ( #28949, #19110, #36047, #27360, #37184 ) ) ;
#10333=CARTESIAN_POINT ( 'NONE',  ( -0.5636438011847132445, -32.10651479984770873, 6.864651958020304257 ) ) ;
#10334=CARTESIAN_POINT ( 'NONE',  ( 3.930782290905703746, -26.87263809153695249, 7.651421919295148477 ) ) ;
#10335=EDGE_CURVE ( 'NONE', #1123, #31321, #15943, .T. ) ;
#10337=CARTESIAN_POINT ( 'NONE',  ( 1.107165259060771456, -32.91777789440434532, 7.769368695748486431 ) ) ;
#10339=CARTESIAN_POINT ( 'NONE',  ( 3.425693392627762179, -32.49966342626535010, 7.730758795053806587 ) ) ;
#10340=CARTESIAN_POINT ( 'NONE',  ( 2.218073121325518482, -32.93030207017181965, 6.874555630061442102 ) ) ;
#10341=CARTESIAN_POINT ( 'NONE',  ( 5.796245933686637208, -28.19952006637477027, 6.894806418505347700 ) ) ;
#10345=ORIENTED_EDGE ( 'NONE', *, *, #19659, .F. ) ;
#10350=CARTESIAN_POINT ( 'NONE',  ( 4.713340623123058570, -27.78888299018493058, 7.695279973900954751 ) ) ;
#10351=VERTEX_POINT ( 'NONE', #35237 ) ;
#10353=CARTESIAN_POINT ( 'NONE',  ( -1.600411900518525110, -28.40601156757937673, 7.710604733652632881 ) ) ;
#10355=CARTESIAN_POINT ( 'NONE',  ( 5.046722968108102947, -28.54421561425872866, 6.998987538705433664 ) ) ;
#10356=CARTESIAN_POINT ( 'NONE',  ( 3.477237270422150139, -26.55450084266673727, 6.894806418505347700 ) ) ;
#10362=CARTESIAN_POINT ( 'NONE',  ( 4.945445480008764605, -30.88065529806472043, 7.754798119455333705 ) ) ;
#10364=DIRECTION ( 'NONE',  ( -0.000000000000000000, -0.000000000000000000, -1.000000000000000000 ) ) ;
#10368=CARTESIAN_POINT ( 'NONE',  ( -1.740083682737729731, -28.92717035510830925, 6.890142680165448397 ) ) ;
#10378=ORIENTED_EDGE ( 'NONE', *, *, #22349, .T. ) ;
#10383=ORIENTED_EDGE ( 'NONE', *, *, #35521, .T. ) ;
#10385=DIRECTION ( 'NONE',  ( -0.9396926207859005453, -0.3420201433256903067, 0.000000000000000000 ) ) ;
#10386=CARTESIAN_POINT ( 'NONE',  ( 3.300060709366284595, -32.68297658758336155, 7.011627023500182965 ) ) ;
#10387=CARTESIAN_POINT ( 'NONE',  ( -1.071744829033150603, -31.70657895489327416, 6.875780273367532835 ) ) ;
#10389=CARTESIAN_POINT ( 'NONE',  ( -0.5758935922563414023, -26.91125798201889197, 7.678495282201408756 ) ) ;
#10391=AXIS2_PLACEMENT_3D ( 'NONE', #36215, #35630, #7404 ) ;
#10396=CARTESIAN_POINT ( 'NONE',  ( 2.253737889363386593, -33.02591140679692927, 6.875671892026062437 ) ) ;
#10398=ORIENTED_EDGE ( 'NONE', *, *, #28772, .F. ) ;
#10401=EDGE_LOOP ( 'NONE', ( #13058, #2978, #13710, #25320 ) ) ;
#10405=CARTESIAN_POINT ( 'NONE',  ( 2.309267857255833167, -32.91496648640696776, 7.748216051605118615 ) ) ;
#10407=VERTEX_POINT ( 'NONE', #35833 ) ;
#10415=EDGE_CURVE ( 'NONE', #19773, #17567, #35155, .T. ) ;
#10422=CARTESIAN_POINT ( 'NONE',  ( 3.369155479471896530, -26.60763004909045293, 7.703977250142851396 ) ) ;
#10426=CARTESIAN_POINT ( 'NONE',  ( -0.5986408314062141578, -32.19260107032493323, 7.782861076432727288 ) ) ;
#10430=DIRECTION ( 'NONE',  ( -0.8660254037844261621, -0.5000000000000215383, 0.000000000000000000 ) ) ;
#10434=DIRECTION ( 'NONE',  ( -0.6427876096865235978, 0.7660444431189911141, 0.000000000000000000 ) ) ;
#10436=CARTESIAN_POINT ( 'NONE',  ( -0.4128411470553862705, -26.90640809309241632, 6.866852738645443210 ) ) ;
#10437=CARTESIAN_POINT ( 'NONE',  ( 4.956151073483226810, -30.57389002924307775, 7.139196562012274150 ) ) ;
#10438=CARTESIAN_POINT ( 'NONE',  ( -1.001523146005661946, -27.34514595843441498, 7.670465701733755637 ) ) ;
#10443=CARTESIAN_POINT ( 'NONE',  ( 4.823856784610486059, -30.91304441079773468, 6.903372536218454592 ) ) ;
#10449=DIRECTION ( 'NONE',  ( -0.5000000000000039968, 0.8660254037844363761, -0.000000000000000000 ) ) ;
#10455=ORIENTED_EDGE ( 'NONE', *, *, #18923, .T. ) ;
#10462=CARTESIAN_POINT ( 'NONE',  ( 4.546924931960046656, -31.42929550842064756, 7.013842709614101167 ) ) ;
#10464=CARTESIAN_POINT ( 'NONE',  ( -1.242570340174825594, -27.67546881208082965, 7.013842709614101167 ) ) ;
#10473=CARTESIAN_POINT ( 'NONE',  ( 0.3425108556361675105, -32.68700637368826989, 6.959317978105162616 ) ) ;
#10478=CARTESIAN_POINT ( 'NONE',  ( 4.221612433196463066, -25.23005020686840183, 7.635761828346577573 ) ) ;
#10479=CARTESIAN_POINT ( 'NONE',  ( 5.076948709542616456, -29.17136787882120785, 6.903372536218456368 ) ) ;
#10483=CARTESIAN_POINT ( 'NONE',  ( 1.700390093233090871, -29.56993018339339940, 6.800000000000000711 ) ) ;
#10486=CARTESIAN_POINT ( 'NONE',  ( 1.667813721708216956, -26.16298220691985676, 7.257242401810563237 ) ) ;
#10489=EDGE_LOOP ( 'NONE', ( #25045, #22038, #32154, #8053, #35989 ) ) ;
#10496=ORIENTED_EDGE ( 'NONE', *, *, #7945, .T. ) ;
#10497=CARTESIAN_POINT ( 'NONE',  ( 5.140927780591328933, -28.92751227575017481, 7.710604733652626663 ) ) ;
#10503=ORIENTED_EDGE ( 'NONE', *, *, #17306, .T. ) ;
#10509=EDGE_LOOP ( 'NONE', ( #12970, #28515, #2346, #36434, #33038 ) ) ;
#10512=CARTESIAN_POINT ( 'NONE',  ( 4.427633003249534127, -27.39263707270477965, 7.780491323090173772 ) ) ;
#10517=CARTESIAN_POINT ( 'NONE',  ( 1.709223551401949148, -26.07549619481818581, 7.773839561854632763 ) ) ;
#10522=CARTESIAN_POINT ( 'NONE',  ( -0.08946644513347716543, -32.57766927571074689, 6.880608371227948439 ) ) ;
#10524=CARTESIAN_POINT ( 'NONE',  ( 2.266461764120263123, -26.21737921967696039, 7.740055089680400791 ) ) ;
#10525=CARTESIAN_POINT ( 'NONE',  ( 3.560683935411703693, -26.72399628134570904, 6.895222827070020877 ) ) ;
#10527=CARTESIAN_POINT ( 'NONE',  ( -0.5557083577496700899, -32.11357244989347492, 6.866852738645443210 ) ) ;
#10528=CARTESIAN_POINT ( 'NONE',  ( -1.600658481268679267, -28.40671124064021669, 7.695279973900954751 ) ) ;
#10530=CARTESIAN_POINT ( 'NONE',  ( 1.145429890469515932, -32.92433313672930240, 7.703977250142847844 ) ) ;
#10532=CARTESIAN_POINT ( 'NONE',  ( -2.340808619595282636, -26.33796619817592699, 7.754798119455333705 ) ) ;
#10533=CARTESIAN_POINT ( 'NONE',  ( -1.574103479719520360, -28.35884934600536056, 7.778495531946295394 ) ) ;
#10540=DIRECTION ( 'NONE',  ( 0.3754033771448285206, 0.6502177225477927536, 0.6605219282605379050 ) ) ;
#10542=CARTESIAN_POINT ( 'NONE',  ( 3.075261667515430286, -26.35127567747291977, 6.971170733404098208 ) ) ;
#10549=CARTESIAN_POINT ( 'NONE',  ( -1.461482890078116936, -28.31986800979595031, 6.866852738645442322 ) ) ;
#10550=CARTESIAN_POINT ( 'NONE',  ( 3.612054795167425336, -26.63811301223460859, 6.931070083220558509 ) ) ;
#10552=ORIENTED_EDGE ( 'NONE', *, *, #39830, .T. ) ;
#10555=CARTESIAN_POINT ( 'NONE',  ( -1.740011302788441627, -30.21307731605675073, 7.697032948437509070 ) ) ;
#10557=EDGE_CURVE ( 'NONE', #24741, #27839, #7807, .T. ) ;
#10560=ORIENTED_EDGE ( 'NONE', *, *, #11698, .F. ) ;
#10564=CARTESIAN_POINT ( 'NONE',  ( -1.707873693682673055, -28.77385357979384040, 6.956915634232264445 ) ) ;
#10576=CARTESIAN_POINT ( 'NONE',  ( 0.6636879034114320230, -26.22699007480350986, 7.013842709614101167 ) ) ;
#10578=CARTESIAN_POINT ( 'NONE',  ( -0.06814292006501697363, -32.57731014431580263, 7.781480525794714609 ) ) ;
#10580=CARTESIAN_POINT ( 'NONE',  ( -1.002278781269885899, -31.77069333300380194, 7.785344483711591934 ) ) ;
#10584=CARTESIAN_POINT ( 'NONE',  ( -1.021571885336638674, -31.77015830299410837, 6.870737987065011154 ) ) ;
#10585=CARTESIAN_POINT ( 'NONE',  ( 5.199955032719538295, -29.62511382514724545, 6.875671892026065990 ) ) ;
#10588=CARTESIAN_POINT ( 'NONE',  ( 4.318185990598753854, -31.87765716460728882, 7.780491323090173772 ) ) ;
#10589=ORIENTED_EDGE ( 'NONE', *, *, #16233, .T. ) ;
#10590=EDGE_CURVE ( 'NONE', #1177, #34207, #26243, .T. ) ;
#10592=ADVANCED_FACE ( 'NONE', ( #11844 ), #33914, .T. ) ;
#10597=VERTEX_POINT ( 'NONE', #25048 ) ;
#10599=CYLINDRICAL_SURFACE ( 'NONE', #16589, 0.09010775117052739758 ) ;
#10600=CARTESIAN_POINT ( 'NONE',  ( 1.080526075423322796, -26.12525383235529119, 7.756742906098588186 ) ) ;
#10605=EDGE_CURVE ( 'NONE', #31392, #486, #30617, .T. ) ;
#10611=DIRECTION ( 'NONE',  ( -0.3754033771448376799, 0.6502177225477876465, 0.6605219282605379050 ) ) ;
#10615=ADVANCED_FACE ( 'NONE', ( #31226 ), #40063, .F. ) ;
#10616=CARTESIAN_POINT ( 'NONE',  ( -1.774306543252402557, -29.99004581285702997, 6.931070083220559397 ) ) ;
#10621=CARTESIAN_POINT ( 'NONE',  ( 2.242723711017451382, -32.92639770848892766, 6.894806418505347700 ) ) ;
#10623=CARTESIAN_POINT ( 'NONE',  ( -1.482541337455568931, -30.76531870494248366, 7.712764235869104645 ) ) ;
#10624=CARTESIAN_POINT ( 'NONE',  ( 3.953870441647290956, -27.02398707340232420, 7.778050822775634643 ) ) ;
#10625=CARTESIAN_POINT ( 'NONE',  ( -1.314054584179517704, -27.80863854348385189, 7.778495531946295394 ) ) ;
#10626=CARTESIAN_POINT ( 'NONE',  ( -1.642039206111510108, -30.19297164693361424, 7.670860738520328681 ) ) ;
#10629=CARTESIAN_POINT ( 'NONE',  ( 4.500391056462942352, -27.46992940240218672, 6.971170733404105313 ) ) ;
#10630=EDGE_CURVE ( 'NONE', #40685, #34893, #24783, .T. ) ;
#10632=CARTESIAN_POINT ( 'NONE',  ( 4.883321523921757112, -28.37454166184433646, 7.712764235869103757 ) ) ;
#10633=CARTESIAN_POINT ( 'NONE',  ( -0.9907592352440830474, -27.33213670732227030, 7.638132480492513920 ) ) ;
#10641=CARTESIAN_POINT ( 'NONE',  ( -0.3985195385088214359, -26.76911271758127597, 6.961115707816233567 ) ) ;
#10642=CARTESIAN_POINT ( 'NONE',  ( -1.230621875064890069, -27.65703250815151648, 6.971170733404100872 ) ) ;
#10644=EDGE_LOOP ( 'NONE', ( #19346, #19786, #12951, #19849, #13544 ) ) ;
#10648=CARTESIAN_POINT ( 'NONE',  ( 3.594851464545667952, -26.62696974998548782, 7.013842709614101167 ) ) ;
#10659=CARTESIAN_POINT ( 'NONE',  ( 4.178779287455901326, -33.93453988814196975, 7.695279973900954751 ) ) ;
#10661=CARTESIAN_POINT ( 'NONE',  ( 4.390205000165592786, -31.80932647847912875, 7.635761828346570468 ) ) ;
#10663=ORIENTED_EDGE ( 'NONE', *, *, #18494, .F. ) ;
#10664=CARTESIAN_POINT ( 'NONE',  ( 5.140201863657823722, -30.18543153557743608, 7.773839561854630986 ) ) ;
#10665=EDGE_CURVE ( 'NONE', #39112, #12351, #39492, .T. ) ;
#10669=CARTESIAN_POINT ( 'NONE',  ( 0.3625495304258689044, -32.69566459030958328, 6.895222827070020877 ) ) ;
#10672=B_SPLINE_CURVE_WITH_KNOTS ( 'NONE', 3,
 ( #37693, #31549, #34448, #18357, #6430, #18988, #22084, #15888, #25368, #9712, #22291, #15274, #40184, #11966, #24541, #8885, #12182, #21467, #6022 ),
 .UNSPECIFIED., .F., .F.,
 ( 4, 3, 3, 3, 3, 3, 4 ),
 ( 0.000000000000000000, 2.546128104244794248E-05, 5.711050680484199682E-05, 8.113074941676081634E-05, 0.0001053129305727044219, 0.0001360598016347131791, 0.0001612931755713729670 ),
 .UNSPECIFIED. ) ;
#10673=CARTESIAN_POINT ( 'NONE',  ( -1.553683706606911130, -30.55532538593644176, 7.013842709614101167 ) ) ;
#10676=DIRECTION ( 'NONE',  ( -0.1303762246624283472, 0.7394003126383926761, 0.6605219282605379050 ) ) ;
#10680=PLANE ( 'NONE',  #34579 ) ;
#10684=EDGE_CURVE ( 'NONE', #21155, #9806, #10034, .T. ) ;
#10687=ADVANCED_FACE ( 'NONE', ( #21269 ), #26083, .F. ) ;
#10688=CARTESIAN_POINT ( 'NONE',  ( -1.139432846729372173, -27.70032573496690986, 6.997764925645182821 ) ) ;
#10696=CARTESIAN_POINT ( 'NONE',  ( 3.423404917024849059, -32.61643964784510530, 6.894806418505347700 ) ) ;
#10697=ORIENTED_EDGE ( 'NONE', *, *, #40626, .T. ) ;
#10699=AXIS2_PLACEMENT_3D ( 'NONE', #33682, #8116, #20899 ) ;
#10703=CARTESIAN_POINT ( 'NONE',  ( 3.854318901935272379, -32.32856308795815892, 7.753200566781599079 ) ) ;
#10704=ORIENTED_EDGE ( 'NONE', *, *, #2237, .T. ) ;
#10705=CARTESIAN_POINT ( 'NONE',  ( 2.496367219260529957, -26.16164236867905046, 6.965379264086542399 ) ) ;
#10706=CARTESIAN_POINT ( 'NONE',  ( 0.9267304714826871681, -32.98335233567298275, 7.013842709614101167 ) ) ;
#10712=CARTESIAN_POINT ( 'NONE',  ( 1.743740428028915268, -26.08457629419881485, 7.785096263473212375 ) ) ;
#10714=CARTESIAN_POINT ( 'NONE',  ( 3.848298546108438245, -32.20554951821143419, 6.894806418505343260 ) ) ;
#10717=CARTESIAN_POINT ( 'NONE',  ( -0.2100398175957213787, -32.50254975568888938, 6.980586498568972509 ) ) ;
#10722=CARTESIAN_POINT ( 'NONE',  ( -0.5410438812439372080, -32.12650380312074816, 6.874555630061441214 ) ) ;
#10724=CARTESIAN_POINT ( 'NONE',  ( 0.1185081075117514898, -26.44780621764473949, 6.971170733404104425 ) ) ;
#10726=DIRECTION ( 'NONE',  ( -0.1736481776669206722, -0.9848077530122096857, -0.000000000000000000 ) ) ;
#10728=CARTESIAN_POINT ( 'NONE',  ( -1.799566460562916470, -29.58736926422850999, 7.749999999999998224 ) ) ;
#10736=CARTESIAN_POINT ( 'NONE',  ( 1.212983646527633130, -26.10426722441512837, 7.754798119455333705 ) ) ;
#10738=CARTESIAN_POINT ( 'NONE',  ( -1.348517286369408597, -27.85116208076715694, 7.686927408461905920 ) ) ;
#10744=CARTESIAN_POINT ( 'NONE',  ( 0.07492370758569941169, -33.99638339305766266, 7.635761828346577573 ) ) ;
#10745=CARTESIAN_POINT ( 'NONE',  ( 1.700390093233090871, -29.56993018339339940, 7.750000000000000888 ) ) ;
#10753=ORIENTED_EDGE ( 'NONE', *, *, #3588, .F. ) ;
#10765=ORIENTED_EDGE ( 'NONE', *, *, #22386, .F. ) ;
#10771=CARTESIAN_POINT ( 'NONE',  ( 6.073619586072577903, -32.40619529368077423, 6.894806418505347700 ) ) ;
#10775=DIRECTION ( 'NONE',  ( -0.4999999999999999445, -0.8660254037844387076, 0.000000000000000000 ) ) ;
#10776=DIRECTION ( 'NONE',  ( 0.6427876096865481337, -0.7660444431189706860, -0.000000000000000000 ) ) ;
#10777=CARTESIAN_POINT ( 'NONE',  ( 5.125310579500037100, -30.29098473247341161, 6.865482280155368322 ) ) ;
#10779=CARTESIAN_POINT ( 'NONE',  ( 2.685785295776140114, -32.82400398323339630, 7.013842709614101167 ) ) ;
#10782=VECTOR ( 'NONE', #32766, 1000.000000000000227 ) ;
#10784=EDGE_CURVE ( 'NONE', #6584, #22181, #5589, .T. ) ;
#10785=ORIENTED_EDGE ( 'NONE', *, *, #36921, .T. ) ;
#10790=( BOUNDED_CURVE ( )  B_SPLINE_CURVE ( 3, ( #319, #12858, #16545, #23343 ),
 .UNSPECIFIED., .F., .T. ) 
 B_SPLINE_CURVE_WITH_KNOTS ( ( 4, 4 ),
 ( 1.381924640371168467, 1.574767692156076260 ),
 .UNSPECIFIED. ) 
 CURVE ( )  GEOMETRIC_REPRESENTATION_ITEM ( )  RATIONAL_B_SPLINE_CURVE ( ( 1.000000000000000000, 0.9969033633783033199, 0.9969033633783033199, 1.000000000000000000 ) ) 
 REPRESENTATION_ITEM ( '' )  );
#10793=CARTESIAN_POINT ( 'NONE',  ( -1.699260392630454364, -29.52118006577551412, 6.894806418505346812 ) ) ;
#10795=CARTESIAN_POINT ( 'NONE',  ( 5.095244238841699413, -29.75692037041947913, 7.013842709614101167 ) ) ;
#10802=CARTESIAN_POINT ( 'NONE',  ( 0.5050015716840180469, -26.38699875270473427, 7.712764235869104645 ) ) ;
#10806=CARTESIAN_POINT ( 'NONE',  ( 1.700390093233090871, -29.56993018339339940, 7.800000000000000711 ) ) ;
#10807=B_SPLINE_CURVE_WITH_KNOTS ( 'NONE', 3,
 ( #36762, #23787, #32877, #21128 ),
 .UNSPECIFIED., .F., .F.,
 ( 4, 4 ),
 ( 8.940560153363745023E-19, 6.391136169898180939E-06 ),
 .UNSPECIFIED. ) ;
#10813=ORIENTED_EDGE ( 'NONE', *, *, #14119, .T. ) ;
#10814=CARTESIAN_POINT ( 'NONE',  ( 5.200270010222271644, -29.54093765580782005, 7.730015791551948290 ) ) ;
#10819=CARTESIAN_POINT ( 'NONE',  ( 4.713340623123058570, -27.78888299018493058, 7.695279973900954751 ) ) ;
#10822=CARTESIAN_POINT ( 'NONE',  ( -1.517981995599434475, -30.66637091792136260, 7.784476445165072533 ) ) ;
#10826=CARTESIAN_POINT ( 'NONE',  ( 4.454246376475485825, -27.40977380682100417, 6.865482280155369210 ) ) ;
#10827=CARTESIAN_POINT ( 'NONE',  ( -0.3249999971511661756, -26.83903245017845407, 6.920489980334477487 ) ) ;
#10828=CARTESIAN_POINT ( 'NONE',  ( 4.924932876884335009, -28.49181894775827928, 7.778050822775631090 ) ) ;
#10829=CARTESIAN_POINT ( 'NONE',  ( 4.165454363429216933, -31.91160874139497494, 6.969307238440509700 ) ) ;
#10831=LINE ( 'NONE', #23407, #5719 ) ;
#10834=ORIENTED_EDGE ( 'NONE', *, *, #23032, .F. ) ;
#10836=CARTESIAN_POINT ( 'NONE',  ( 4.234390967386161719, -31.83684322112676668, 7.768425012602597768 ) ) ;
#10840=CARTESIAN_POINT ( 'NONE',  ( -0.4112773674722806638, -26.77871049686494942, 6.903112506833885220 ) ) ;
#10842=CARTESIAN_POINT ( 'NONE',  ( 5.190258803612193717, -29.91414858768555618, 7.501983001166816045 ) ) ;
#10847=VERTEX_POINT ( 'NONE', #6446 ) ;
#10848=CARTESIAN_POINT ( 'NONE',  ( -1.722970638209900596, -28.84261588273779964, 7.754798119455333705 ) ) ;
#10854=CARTESIAN_POINT ( 'NONE',  ( 5.029153757140225167, -30.26234874276111242, 6.864651958020304257 ) ) ;
#10856=CARTESIAN_POINT ( 'NONE',  ( 5.401390093233090717, -29.58343279012807159, 7.635761828346577573 ) ) ;
#10857=CARTESIAN_POINT ( 'NONE',  ( -1.260054023142102464, -27.89787437277597348, 7.721096864323902409 ) ) ;
#10859=DIRECTION ( 'NONE',  ( 0.9396926207859080948, 0.3420201433256694901, -0.000000000000000000 ) ) ;
#10862=CARTESIAN_POINT ( 'NONE',  ( 2.343537225896455745, -33.01033157941493101, 7.695279973900954751 ) ) ;
#10865=AXIS2_PLACEMENT_3D ( 'NONE', #7987, #30234, #37013 ) ;
#10870=CARTESIAN_POINT ( 'NONE',  ( 1.109803157764845061, -33.01974279738480789, 7.750000000000000888 ) ) ;
#10873=CARTESIAN_POINT ( 'NONE',  ( -0.5124352759832019322, -26.98857319813297551, 7.691066658568944447 ) ) ;
#10875=ADVANCED_FACE ( 'NONE', ( #28459 ), #40195, .T. ) ;
#10876=AXIS2_PLACEMENT_3D ( 'NONE', #5533, #29683, #26603 ) ;
#10878=CARTESIAN_POINT ( 'NONE',  ( 5.065225839463185942, -29.08208656869964415, 6.864651958020304257 ) ) ;
#10887=CARTESIAN_POINT ( 'NONE',  ( -1.185231845581470767, -27.77182395009346294, 6.864276522220859711 ) ) ;
#10891=CARTESIAN_POINT ( 'NONE',  ( -1.601316894800309143, -30.73129909961408046, 6.887161170156907986 ) ) ;
#10897=CARTESIAN_POINT ( 'NONE',  ( 4.966384368437926078, -28.59977744957924628, 7.386948897581448570 ) ) ;
#10900=CARTESIAN_POINT ( 'NONE',  ( 4.754320870746903793, -27.86007999067432195, 6.880608371227952880 ) ) ;
#10902=ORIENTED_EDGE ( 'NONE', *, *, #38857, .T. ) ;
#10907=EDGE_CURVE ( 'NONE', #30228, #109, #31637, .T. ) ;
#10908=CARTESIAN_POINT ( 'NONE',  ( 3.853256869806246154, -32.32948931917582769, 7.751599049952172749 ) ) ;
#10909=VERTEX_POINT ( 'NONE', #6647 ) ;
#10917=CARTESIAN_POINT ( 'NONE',  ( -0.5596933955661176352, -26.89747389307597203, 7.635761828346574909 ) ) ;
#10918=EDGE_CURVE ( 'NONE', #2179, #17881, #34777, .T. ) ;
#10920=CARTESIAN_POINT ( 'NONE',  ( -1.261630184736219684, -27.90066804241507015, 7.680992449362118002 ) ) ;
#10925=DIRECTION ( 'NONE',  ( 1.000000000000000000, 0.000000000000000000, -0.000000000000000000 ) ) ;
#10930=CARTESIAN_POINT ( 'NONE',  ( 0.1171942947253034051, -26.44847140242086780, 6.931070083220560285 ) ) ;
#10933=CARTESIAN_POINT ( 'NONE',  ( -1.699600969445970833, -29.57893194192095976, 7.630645772256162473 ) ) ;
#10935=AXIS2_PLACEMENT_3D ( 'NONE', #15076, #30752, #37307 ) ;
#10936=CARTESIAN_POINT ( 'NONE',  ( -0.4747269484695719743, -32.18314005917732601, 7.635761828346577573 ) ) ;
#10941=CARTESIAN_POINT ( 'NONE',  ( 3.073907603833451851, -26.35069681102080708, 6.931070083220554068 ) ) ;
#10944=CARTESIAN_POINT ( 'NONE',  ( 3.862587397715897541, -32.19384001730296063, 7.782167645815905033 ) ) ;
#10945=LINE ( 'NONE', #23525, #9507 ) ;
#10946=CARTESIAN_POINT ( 'NONE',  ( 2.315998556607181236, -32.91373647356815013, 7.652160403243383868 ) ) ;
#10948=CARTESIAN_POINT ( 'NONE',  ( 1.275896657681770074, -26.09576640599786046, 6.989977667959447416 ) ) ;
#10957=CARTESIAN_POINT ( 'NONE',  ( 4.984671627384348547, -28.36018029005467866, 7.635761828346577573 ) ) ;
#10963=EDGE_CURVE ( 'NONE', #3554, #16444, #25720, .T. ) ;
#10964=CARTESIAN_POINT ( 'NONE',  ( -0.8909124383283257842, -27.36873829022893645, 7.779495906702011077 ) ) ;
#10969=CARTESIAN_POINT ( 'NONE',  ( -1.526028259963971401, -30.94401141093381113, 7.139344958878410807 ) ) ;
#10974=CARTESIAN_POINT ( 'NONE',  ( 2.322191688357494677, -25.34207446254166385, 7.754798119455333705 ) ) ;
#10979=CARTESIAN_POINT ( 'NONE',  ( 5.113370443964368128, -30.34553905407643626, 7.011627023500182965 ) ) ;
#10981=DIRECTION ( 'NONE',  ( 0.000000000000000000, 0.000000000000000000, -1.000000000000000000 ) ) ;
#10982=DIRECTION ( 'NONE',  ( 0.000000000000000000, -0.7541618601367581221, 0.6566885781822803247 ) ) ;
#10984=CARTESIAN_POINT ( 'NONE',  ( 2.194212249870564069, -33.03491787133889801, 6.865482280155368322 ) ) ;
#10988=AXIS2_PLACEMENT_3D ( 'NONE', #9612, #8783, #15993 ) ;
#10989=ORIENTED_EDGE ( 'NONE', *, *, #18544, .F. ) ;
#10991=PLANE ( 'NONE',  #35746 ) ;
#10992=CARTESIAN_POINT ( 'NONE',  ( -0.9258490509262529145, -27.25630360209614977, 6.865554069792297653 ) ) ;
#11001=CARTESIAN_POINT ( 'NONE',  ( 0.3869751666866692030, -32.81414707076048387, 7.751599049952199394 ) ) ;
#11003=CARTESIAN_POINT ( 'NONE',  ( 3.926835433623051763, -27.00030981652402318, 6.889465824494256374 ) ) ;
#11011=ORIENTED_EDGE ( 'NONE', *, *, #24795, .T. ) ;
#11014=CARTESIAN_POINT ( 'NONE',  ( -0.2169689478323021947, -26.75353354193401501, 7.505001789837628223 ) ) ;
#11017=CARTESIAN_POINT ( 'NONE',  ( -1.498372880175843580, -30.72231214854605952, 7.775108481317163367 ) ) ;
#11020=CARTESIAN_POINT ( 'NONE',  ( -0.07963814550968341399, -26.55637667292353754, 7.678495282201402539 ) ) ;
#11024=CARTESIAN_POINT ( 'NONE',  ( 5.145088616758716427, -28.91287462443592560, 7.255881584735162981 ) ) ;
#11034=CARTESIAN_POINT ( 'NONE',  ( -1.370619673614267287, -31.23390196357851778, 7.776484688137385248 ) ) ;
#11039=CARTESIAN_POINT ( 'NONE',  ( 1.314511067807684341, -26.19189860009866422, 6.929923840112063083 ) ) ;
#11045=APPLICATION_CONTEXT ( 'automotive_design' ) ;
#11050=FACE_OUTER_BOUND ( 'NONE', #24583, .T. ) ;
#11051=ORIENTED_EDGE ( 'NONE', *, *, #1420, .F. ) ;
#11052=CARTESIAN_POINT ( 'NONE',  ( 0.01666963137263145420, -32.52375573787565344, 7.748216051605119503 ) ) ;
#11053=AXIS2_PLACEMENT_3D ( 'NONE', #25182, #26202, #4382 ) ;
#11055=CARTESIAN_POINT ( 'NONE',  ( 1.700390093233090871, -29.56993018339339940, -8.199999999999999289 ) ) ;
#11057=CARTESIAN_POINT ( 'NONE',  ( -1.213445411319114209, -27.81791344477159100, 7.785172627573962778 ) ) ;
#11062=CARTESIAN_POINT ( 'NONE',  ( 5.124306173303248002, -30.29170089314414582, 7.761113333117553026 ) ) ;
#11066=CARTESIAN_POINT ( 'NONE',  ( 0.9730757925788008356, -32.99329091482906762, 7.754798119455333705 ) ) ;
#11073=DIRECTION ( 'NONE',  ( 0.2567910337120358211, -0.7055275666422125003, -0.6605219282605404585 ) ) ;
#11079=ORIENTED_EDGE ( 'NONE', *, *, #39358, .F. ) ;
#11080=CARTESIAN_POINT ( 'NONE',  ( 2.836375080312453445, -32.86472044869006481, 7.785593909369612931 ) ) ;
#11081=CARTESIAN_POINT ( 'NONE',  ( 3.417826084928983654, -32.50428837397927850, 7.643333865083954848 ) ) ;
#11087=CARTESIAN_POINT ( 'NONE',  ( -1.604056983674224224, -30.72349439543635441, 6.880608371227951992 ) ) ;
#11088=EDGE_CURVE ( 'NONE', #34426, #22624, #7744, .T. ) ;
#11092=EDGE_CURVE ( 'NONE', #21747, #23979, #16796, .T. ) ;
#11096=ORIENTED_EDGE ( 'NONE', *, *, #1832, .T. ) ;
#11098=CARTESIAN_POINT ( 'NONE',  ( 4.821180714308241910, -27.98542208956447652, 6.980586498568966292 ) ) ;
#11112=ORIENTED_EDGE ( 'NONE', *, *, #13158, .T. ) ;
#11115=B_SPLINE_CURVE_WITH_KNOTS ( 'NONE', 3,
 ( #26088, #38220, #6548, #37812, #25879, #19093, #22600, #982, #10018, #22802, #35373, #38419, #31662, #16590, #6745, #16399, #15804, #16000, #7141, #28568, #28773, #35169, #25280, #28973, #29172, #775, #18891, #38023, #19702, #13518, #9616 ),
 .UNSPECIFIED., .F., .F.,
 ( 4, 3, 3, 3, 3, 3, 3, 3, 3, 3, 4 ),
 ( 0.000000000000000000, 2.999644130997519527E-05, 6.002588995694434291E-05, 8.960886084587663797E-05, 0.0001190604700446430892, 0.0001489538463052673836, 0.0001796139255493884224, 0.0002109707048516977815, 0.0002426195318110361968, 0.0002740640997890006546, 0.0002849778069099816549 ),
 .UNSPECIFIED. ) ;
#11118=CARTESIAN_POINT ( 'NONE',  ( -1.258681128443422281, -27.89544593293122787, 7.661510568013095046 ) ) ;
#11119=FACE_OUTER_BOUND ( 'NONE', #35544, .T. ) ;
#11123=CARTESIAN_POINT ( 'NONE',  ( 4.657149580636700037, -31.24850351647889823, 7.740055089680397238 ) ) ;
#11130=CARTESIAN_POINT ( 'NONE',  ( -1.547547272396095464, -28.27830587817873820, 7.771081512783704959 ) ) ;
#11141=ORIENTED_EDGE ( 'NONE', *, *, #22165, .F. ) ;
#11142=CARTESIAN_POINT ( 'NONE',  ( -0.5600293521546132469, -32.10973131848952278, 7.774064877406533292 ) ) ;
#11144=CARTESIAN_POINT ( 'NONE',  ( 1.700390093233090871, -29.56993018339339940, 7.750000000000000888 ) ) ;
#11146=CARTESIAN_POINT ( 'NONE',  ( 1.027987119375220360, -32.90277795080599077, 6.870716933885664623 ) ) ;
#11147=CARTESIAN_POINT ( 'NONE',  ( 0.3457495631895174948, -32.79715019981050972, 7.013842709614101167 ) ) ;
#11153=CARTESIAN_POINT ( 'NONE',  ( -0.01837800939314739035, -32.61883756299590686, 7.695279973900954751 ) ) ;
#11161=AXIS2_PLACEMENT_3D ( 'NONE', #4044, #3246, #25441 ) ;
#11162=CARTESIAN_POINT ( 'NONE',  ( -0.8715445521076354840, -27.34613762201350795, 7.785868773668302545 ) ) ;
#11166=CARTESIAN_POINT ( 'NONE',  ( 4.465382618493274336, -31.56070191054703145, 7.505001789837627335 ) ) ;
#11167=ORIENTED_EDGE ( 'NONE', *, *, #39224, .F. ) ;
#11168=DIRECTION ( 'NONE',  ( -0.000000000000000000, -0.000000000000000000, -1.000000000000000000 ) ) ;
#11173=AXIS2_PLACEMENT_3D ( 'NONE', #34659, #31550, #3373 ) ;
#11174=CARTESIAN_POINT ( 'NONE',  ( 5.151060735156064219, -30.15551690657623851, 7.646866513072557936 ) ) ;
#11176=CARTESIAN_POINT ( 'NONE',  ( 3.454978868039249473, -32.59677836288253161, 7.762796336881260473 ) ) ;
#11177=CARTESIAN_POINT ( 'NONE',  ( 3.282272078954445060, -32.69205414914204511, 6.971170733404095543 ) ) ;
#11178=CARTESIAN_POINT ( 'NONE',  ( -1.086373026989221113, -31.68746443619045650, 7.013842709614101167 ) ) ;
#11182=CARTESIAN_POINT ( 'NONE',  ( 1.876920399658227989, -26.07437817348433384, 6.903112506833889661 ) ) ;
#11183=ORIENTED_EDGE ( 'NONE', *, *, #4584, .F. ) ;
#11186=EDGE_CURVE ( 'NONE', #6683, #38144, #7552, .T. ) ;
#11190=ADVANCED_FACE ( 'NONE', ( #28105 ), #31012, .T. ) ;
#11192=CARTESIAN_POINT ( 'NONE',  ( 3.024182384487883457, -26.43822554061266672, 6.882085323592686876 ) ) ;
#11193=CARTESIAN_POINT ( 'NONE',  ( -1.416686097061773397, -28.21205094579645589, 6.959317978105164393 ) ) ;
#11199=ORIENTED_EDGE ( 'NONE', *, *, #8395, .T. ) ;
#11201=ORIENTED_EDGE ( 'NONE', *, *, #5549, .F. ) ;
#11206=CARTESIAN_POINT ( 'NONE',  ( 0.6507332215994441338, -26.33601230518184977, 7.757178535559535959 ) ) ;
#11207=FACE_OUTER_BOUND ( 'NONE', #31266, .T. ) ;
#11208=CARTESIAN_POINT ( 'NONE',  ( 4.034721127530844775, -27.09790394036370031, 6.997764925645181933 ) ) ;
#11215=CARTESIAN_POINT ( 'NONE',  ( -0.5222078730473904695, -32.14287757506037480, 6.894806418505348589 ) ) ;
#11220=CARTESIAN_POINT ( 'NONE',  ( -0.7402732514194279023, -31.94722237671934906, 7.505001789837626447 ) ) ;
#11222=CARTESIAN_POINT ( 'NONE',  ( 0.5553240519966275990, -26.26254091673501989, 6.875671892026062437 ) ) ;
#11223=CARTESIAN_POINT ( 'NONE',  ( 4.434909129570597131, -27.38534655260518846, 6.865554069792296765 ) ) ;
#11227=CARTESIAN_POINT ( 'NONE',  ( 0.1069670619869697303, -26.56643171602332032, 7.754798119455333705 ) ) ;
#11233=EDGE_CURVE ( 'NONE', #3356, #33357, #13461, .T. ) ;
#11237=CARTESIAN_POINT ( 'NONE',  ( 2.315891445417157524, -26.13011841296867033, 7.773839561854632763 ) ) ;
#11238=CARTESIAN_POINT ( 'NONE',  ( -0.6902601390570299866, -32.12625400224952443, 6.980586498568965403 ) ) ;
#11239=EDGE_LOOP ( 'NONE', ( #9211, #29354, #36083, #39937 ) ) ;
#11240=CARTESIAN_POINT ( 'NONE',  ( -1.722830152274906990, -28.84121352662702975, 7.753200566781598191 ) ) ;
#11247=CARTESIAN_POINT ( 'NONE',  ( -0.7896860208805611681, -27.25486626507048271, 6.882085323592686876 ) ) ;
#11248=ORIENTED_EDGE ( 'NONE', *, *, #13033, .F. ) ;
#11250=CARTESIAN_POINT ( 'NONE',  ( 3.319000845420424284, -32.55994614210599991, 6.866852738645442322 ) ) ;
#11251=CARTESIAN_POINT ( 'NONE',  ( 0.4695943777967593880, -26.29347754267606874, 7.695279973900954751 ) ) ;
#11253=CARTESIAN_POINT ( 'NONE',  ( -1.238510913153971771, -27.86027243158510558, 7.775108481317160702 ) ) ;
#11254=CARTESIAN_POINT ( 'NONE',  ( 4.662410371202409642, -31.23919232437170734, 7.680992449362115337 ) ) ;
#11255=EDGE_CURVE ( 'NONE', #17262, #17544, #37526, .T. ) ;
#11258=CARTESIAN_POINT ( 'NONE',  ( 4.401417849205680355, -27.34407100962124559, 6.894806418505347700 ) ) ;
#11260=B_SPLINE_CURVE_WITH_KNOTS ( 'NONE', 3,
 ( #27983, #35208, #9448, #28606, #2903, #15422, #24911, #37446, #415, #6174 ),
 .UNSPECIFIED., .F., .F.,
 ( 4, 3, 3, 4 ),
 ( 0.0001585009270395677274, 0.0001815657551981809145, 0.0002118214035944089005, 0.0002170292169044720702 ),
 .UNSPECIFIED. ) ;
#11262=CARTESIAN_POINT ( 'NONE',  ( 2.890832430579337142, -32.75471385602386931, 7.661510568013097711 ) ) ;
#11266=( BOUNDED_CURVE ( )  B_SPLINE_CURVE ( 3, ( #19884, #25465, #25869, #32456 ),
 .UNSPECIFIED., .F., .T. ) 
 B_SPLINE_CURVE_WITH_KNOTS ( ( 4, 4 ),
 ( 4.708531083176465515, 4.895802057644186966 ),
 .UNSPECIFIED. ) 
 CURVE ( )  GEOMETRIC_REPRESENTATION_ITEM ( )  RATIONAL_B_SPLINE_CURVE ( ( 1.000000000000000000, 0.9970795998553221295, 0.9970795998553221295, 1.000000000000000000 ) ) 
 REPRESENTATION_ITEM ( '' )  );
#11269=CARTESIAN_POINT ( 'NONE',  ( -0.6763298692248193023, -32.13921067023287037, 7.013842709614101167 ) ) ;
#11271=DIRECTION ( 'NONE',  ( 0.000000000000000000, 0.6834397476448867970, -0.7300069255418700775 ) ) ;
#11277=CARTESIAN_POINT ( 'NONE',  ( 1.700390093233090871, -29.56993018339339940, 7.750000000000000888 ) ) ;
#11282=EDGE_LOOP ( 'NONE', ( #30468, #21596, #17429, #1068, #32900, #16045, #12939 ) ) ;
#11283=ORIENTED_EDGE ( 'NONE', *, *, #1940, .F. ) ;
#11285=CARTESIAN_POINT ( 'NONE',  ( -0.5344885137010326748, -32.26349986176969509, 7.643192810543824045 ) ) ;
#11286=CARTESIAN_POINT ( 'NONE',  ( 3.476044783818678763, -32.58606316010092030, 7.660770905198780234 ) ) ;
#11290=ORIENTED_EDGE ( 'NONE', *, *, #27383, .F. ) ;
#11300=FACE_OUTER_BOUND ( 'NONE', #14707, .T. ) ;
#11301=VERTEX_POINT ( 'NONE', #18424 ) ;
#11306=VERTEX_POINT ( 'NONE', #40248 ) ;
#11316=B_SPLINE_CURVE_WITH_KNOTS ( 'NONE', 3,
 ( #7654, #10530, #3988, #35477, #20007, #16509, #29085, #888, #38531, #10337, #1491, #22909, #7249, #23110, #20205, #4182, #16699, #29284, #32587, #1098, #4384, #29488, #4580, #17107, #27602 ),
 .UNSPECIFIED., .F., .F.,
 ( 4, 3, 3, 3, 3, 3, 3, 3, 4 ),
 ( 6.468151674593758404E-05, 9.076621574722010212E-05, 0.0001210204262067969094, 0.0001512763324577425894, 0.0001815301820994201292, 0.0002117781465860718712, 0.0002420274594459749366, 0.0002722905548971152464, 0.0002816827545175596011 ),
 .UNSPECIFIED. ) ;
#11319=EDGE_CURVE ( 'NONE', #17881, #31037, #1661, .T. ) ;
#11321=EDGE_CURVE ( 'NONE', #1511, #36985, #16568, .T. ) ;
#11322=DIRECTION ( 'NONE',  ( -0.000000000000000000, -0.000000000000000000, -1.000000000000000000 ) ) ;
#11323=CARTESIAN_POINT ( 'NONE',  ( 0.5834512725888432172, -26.35863018636138122, 6.894806418505347700 ) ) ;
#11327=PLANE ( 'NONE',  #19367 ) ;
#11329=CARTESIAN_POINT ( 'NONE',  ( 4.348731362533842848, -31.83831163058102476, 7.783750581861601070 ) ) ;
#11330=DIRECTION ( 'NONE',  ( 0.3420201433256790380, -0.9396926207859046531, -0.000000000000000000 ) ) ;
#11336=CARTESIAN_POINT ( 'NONE',  ( 4.299742401097503830, -31.91372402269596620, 7.751599049952198506 ) ) ;
#11343=CARTESIAN_POINT ( 'NONE',  ( 0.3285059592769975501, -32.78986077462409554, 6.925313231306332362 ) ) ;
#11344=VECTOR ( 'NONE', #24239, 999.9999999999998863 ) ;
#11349=ADVANCED_FACE ( 'NONE', ( #6507 ), #539, .F. ) ;
#11355=CARTESIAN_POINT ( 'NONE',  ( 2.255447537765926658, -26.21554331940935967, 7.691066658568947112 ) ) ;
#11360=ADVANCED_FACE ( 'NONE', ( #25237 ), #35332, .T. ) ;
#11370=CYLINDRICAL_SURFACE ( 'NONE', #36674, 0.09010775117052916006 ) ;
#11372=EDGE_CURVE ( 'NONE', #12118, #1128, #30807, .T. ) ;
#11373=CARTESIAN_POINT ( 'NONE',  ( 0.5657570339504449652, -32.78255583154504649, 7.257242401810563237 ) ) ;
#11375=CARTESIAN_POINT ( 'NONE',  ( 5.001387658970600114, -30.73329387158167947, 7.700536657684216024 ) ) ;
#11377=CARTESIAN_POINT ( 'NONE',  ( 5.149693937723391457, -30.16348207664124814, 7.636816916992231974 ) ) ;
#11380=CARTESIAN_POINT ( 'NONE',  ( 4.821338062315135176, -33.56355840650683575, 6.954324564059724878 ) ) ;
#11382=CARTESIAN_POINT ( 'NONE',  ( 2.735039440433452818, -32.80869545011542954, 6.865312560952602894 ) ) ;
#11383=CARTESIAN_POINT ( 'NONE',  ( 5.100040579096636328, -29.61868030101130245, 6.894806418505348589 ) ) ;
#11385=ORIENTED_EDGE ( 'NONE', *, *, #1083, .T. ) ;
#11392=CARTESIAN_POINT ( 'NONE',  ( -1.656077431862442717, -30.11226380117775037, 6.894806418505347700 ) ) ;
#11396=CARTESIAN_POINT ( 'NONE',  ( -0.5730865926811068434, -32.23100210249002373, 6.894806418505347700 ) ) ;
#11397=ORIENTED_EDGE ( 'NONE', *, *, #14574, .F. ) ;
#11405=VERTEX_POINT ( 'NONE', #13075 ) ;
#11406=EDGE_CURVE ( 'NONE', #22430, #6673, #37014, .T. ) ;
#11409=CARTESIAN_POINT ( 'NONE',  ( 4.040371955156762063, -27.10325224939195721, 6.979335674598004857 ) ) ;
#11421=CARTESIAN_POINT ( 'NONE',  ( 2.496911866804199409, -26.26454769719600080, 6.949473656533219135 ) ) ;
#11423=CARTESIAN_POINT ( 'NONE',  ( 3.866898022442308847, -26.94957171677655339, 7.740055089680397238 ) ) ;
#11425=CARTESIAN_POINT ( 'NONE',  ( -1.219418532703906877, -27.82788610016705988, 6.894806418505346812 ) ) ;
#11428=CARTESIAN_POINT ( 'NONE',  ( -0.4435737903242095159, -26.93109965651677129, 6.889465824494255486 ) ) ;
#11431=VERTEX_POINT ( 'NONE', #4226 ) ;
#11438=CARTESIAN_POINT ( 'NONE',  ( -1.605260786948502494, -28.77451848735744377, 6.939395833800443114 ) ) ;
#11443=VECTOR ( 'NONE', #29689, 1000.000000000000000 ) ;
#11444=ORIENTED_EDGE ( 'NONE', *, *, #3588, .T. ) ;
#11446=CARTESIAN_POINT ( 'NONE',  ( 3.293813124479239018, -32.57342865076346783, 7.754798119455333705 ) ) ;
#11451=ORIENTED_EDGE ( 'NONE', *, *, #23204, .F. ) ;
#11455=CARTESIAN_POINT ( 'NONE',  ( 5.001438667734867671, -30.73314912614656436, 7.695279973900954751 ) ) ;
#11460=ORIENTED_EDGE ( 'NONE', *, *, #34112, .F. ) ;
#11462=EDGE_CURVE ( 'NONE', #40258, #6329, #32122, .T. ) ;
#11467=CARTESIAN_POINT ( 'NONE',  ( 1.098862567954408842, -33.01645833599632596, 7.762796336881262249 ) ) ;
#11472=CARTESIAN_POINT ( 'NONE',  ( 1.700390093233090871, -29.56993018339339940, 7.800000000000000711 ) ) ;
#11473=B_SPLINE_CURVE_WITH_KNOTS ( 'NONE', 3,
 ( #25747, #16467, #26157, #13374, #19573, #21390, #17450, #14781, #8605, #21183, #11080, #2256, #33965, #33137, #2473, #27350, #36217, #20976, #14572 ),
 .UNSPECIFIED., .F., .F.,
 ( 4, 3, 3, 3, 3, 3, 4 ),
 ( 4.336808689942017736E-19, 2.546128104244632296E-05, 5.711050680483876455E-05, 8.113074941675923069E-05, 0.0001053129305727100597, 0.0001360598016347191693, 0.0001612931755713715575 ),
 .UNSPECIFIED. ) ;
#11476=VECTOR ( 'NONE', #34368, 1000.000000000000000 ) ;
#11477=DIRECTION ( 'NONE',  ( -0.000000000000000000, -0.000000000000000000, -1.000000000000000000 ) ) ;
#11483=CARTESIAN_POINT ( 'NONE',  ( 1.910837266068588836, -26.17644932986278050, 6.949473656533215582 ) ) ;
#11489=ORIENTED_EDGE ( 'NONE', *, *, #22423, .F. ) ;
#11494=ORIENTED_EDGE ( 'NONE', *, *, #15663, .F. ) ;
#11496=VERTEX_POINT ( 'NONE', #20656 ) ;
#11498=DIRECTION ( 'NONE',  ( -0.7660444431189813441, 0.6427876096865353661, -0.000000000000000000 ) ) ;
#11503=ORIENTED_EDGE ( 'NONE', *, *, #34232, .F. ) ;
#11506=ADVANCED_FACE ( 'NONE', ( #33030 ), #7702, .F. ) ;
#11509=CARTESIAN_POINT ( 'NONE',  ( 4.733915118986097958, -28.03444136281207832, 7.013842709614101167 ) ) ;
#11511=CARTESIAN_POINT ( 'NONE',  ( 2.562099542307729738, -33.75548367670988625, 7.754798119455333705 ) ) ;
#11523=CARTESIAN_POINT ( 'NONE',  ( 5.131593199136804451, -30.26047000558811106, 6.865554069792297653 ) ) ;
#11524=CARTESIAN_POINT ( 'NONE',  ( -1.799609906766908463, -29.73166366038556419, 7.383456277641972321 ) ) ;
#11525=DIRECTION ( 'NONE',  ( 0.000000000000000000, 0.6605219282605402364, 0.7508067542896625923 ) ) ;
#11526=DIRECTION ( 'NONE',  ( 0.8660254037844452579, -0.4999999999999886202, 0.000000000000000000 ) ) ;
#11527=CARTESIAN_POINT ( 'NONE',  ( 0.06039256278810246209, -26.47792186227242439, 6.867199677474203234 ) ) ;
#11530=CARTESIAN_POINT ( 'NONE',  ( 4.637114349001293157, -31.47405327090299565, 6.998987538705429223 ) ) ;
#11532=CARTESIAN_POINT ( 'NONE',  ( 4.326895721323773536, -31.86212065727518095, 7.784725160561909441 ) ) ;
#11536=CARTESIAN_POINT ( 'NONE',  ( 1.214349479236255247, -26.10391960397356925, 7.753200566781599967 ) ) ;
#11540=CARTESIAN_POINT ( 'NONE',  ( -0.5626977249550375593, -26.90001753928526540, 7.750000000000002665 ) ) ;
#11541=ORIENTED_EDGE ( 'NONE', *, *, #21102, .T. ) ;
#11542=CARTESIAN_POINT ( 'NONE',  ( -0.1539201161049026934, -32.53808085965915353, 7.754798119455333705 ) ) ;
#11543=LINE ( 'NONE', #6418, #20695 ) ;
#11545=EDGE_CURVE ( 'NONE', #14078, #30463, #36319, .T. ) ;
#11553=CARTESIAN_POINT ( 'NONE',  ( -0.07136309058874676370, -32.47180727514232501, 6.870716933885665512 ) ) ;
#11560=CARTESIAN_POINT ( 'NONE',  ( -0.9076542330089235611, -27.38860637533221976, 7.763628509615282169 ) ) ;
#11561=ORIENTED_EDGE ( 'NONE', *, *, #37226, .F. ) ;
#11562=EDGE_CURVE ( 'NONE', #25767, #38197, #37325, .T. ) ;
#11564=CARTESIAN_POINT ( 'NONE',  ( 3.389257957103017471, -26.61903871757985840, 7.756377446753170091 ) ) ;
#11565=DIRECTION ( 'NONE',  ( 0.1736481776669273336, 0.9848077530122085754, -0.000000000000000000 ) ) ;
#11570=ORIENTED_EDGE ( 'NONE', *, *, #6144, .T. ) ;
#11573=CARTESIAN_POINT ( 'NONE',  ( -0.5125101069461969194, -26.98863734761392053, 7.695279973900954751 ) ) ;
#11574=FACE_OUTER_BOUND ( 'NONE', #29891, .T. ) ;
#11575=CARTESIAN_POINT ( 'NONE',  ( 1.713892699967802136, -33.06990413752668445, 7.635761828346576685 ) ) ;
#11576=CARTESIAN_POINT ( 'NONE',  ( 5.172816400818245341, -29.13145608706553702, 7.011627023500183853 ) ) ;
#11579=CARTESIAN_POINT ( 'NONE',  ( 4.762748405565132792, -33.59738516060317437, 6.894806418505347700 ) ) ;
#11583=CARTESIAN_POINT ( 'NONE',  ( 2.666604916071043885, -32.82975288721481633, 6.979335674598003969 ) ) ;
#11589=ORIENTED_EDGE ( 'NONE', *, *, #30371, .T. ) ;
#11592=EDGE_LOOP ( 'NONE', ( #27062, #28214, #21472, #17984, #7374 ) ) ;
#11594=CARTESIAN_POINT ( 'NONE',  ( 0.1365689545988542086, -26.55089741178066021, 6.871394612369935651 ) ) ;
#11595=LINE ( 'NONE', #11796, #23505 ) ;
#11596=EDGE_CURVE ( 'NONE', #11926, #8831, #6860, .T. ) ;
#11602=CARTESIAN_POINT ( 'NONE',  ( 2.172536372144526773, -32.93698858539566743, 7.757178535559533294 ) ) ;
#11614=ORIENTED_EDGE ( 'NONE', *, *, #1421, .F. ) ;
#11617=AXIS2_PLACEMENT_3D ( 'NONE', #10021, #35376, #985 ) ;
#11621=CARTESIAN_POINT ( 'NONE',  ( -1.742489505018671725, -30.16803301939627602, 7.773839561854632763 ) ) ;
#11622=( BOUNDED_CURVE ( )  B_SPLINE_CURVE ( 3, ( #33517, #20722, #27108, #33307 ),
 .UNSPECIFIED., .F., .T. ) 
 B_SPLINE_CURVE_WITH_KNOTS ( ( 4, 4 ),
 ( 1.381924640371168689, 1.574767692156077370 ),
 .UNSPECIFIED. ) 
 CURVE ( )  GEOMETRIC_REPRESENTATION_ITEM ( )  RATIONAL_B_SPLINE_CURVE ( ( 1.000000000000000000, 0.9969033633783032089, 0.9969033633783032089, 1.000000000000000000 ) ) 
 REPRESENTATION_ITEM ( '' )  );
#11626=CARTESIAN_POINT ( 'NONE',  ( 5.067738213087761068, -29.09985929542945371, 7.754798119455333705 ) ) ;
#11629=B_SPLINE_CURVE_WITH_KNOTS ( 'NONE', 3,
 ( #368, #10212, #9817, #34963, #9610, #6541, #32069, #19497, #28762, #22193 ),
 .UNSPECIFIED., .F., .F.,
 ( 4, 3, 3, 4 ),
 ( 0.0001585009270395730399, 0.0001815657551981798032, 0.0002118214035944114755, 0.0002170292169044780875 ),
 .UNSPECIFIED. ) ;
#11631=CARTESIAN_POINT ( 'NONE',  ( 2.183653651549320340, -33.03640625185305879, 7.750000000000000888 ) ) ;
#11641=CARTESIAN_POINT ( 'NONE',  ( 1.888104015524238566, -33.07173515984538170, 7.139344958878410807 ) ) ;
#11655=CARTESIAN_POINT ( 'NONE',  ( -0.7665672367818757715, -27.23024611671144157, 6.929923840112066635 ) ) ;
#11659=CARTESIAN_POINT ( 'NONE',  ( 3.215381038209046416, -32.61374398135161812, 6.959317978105166169 ) ) ;
#11660=CARTESIAN_POINT ( 'NONE',  ( 4.973240196557726200, -30.81030636687787450, 6.880608371227952880 ) ) ;
#11662=DIRECTION ( 'NONE',  ( 0.6427876096865379196, 0.7660444431189793457, -0.000000000000000000 ) ) ;
#11664=CARTESIAN_POINT ( 'NONE',  ( -1.594400172063576981, -30.70591517047275332, 7.785593909369613819 ) ) ;
#11666=ORIENTED_EDGE ( 'NONE', *, *, #13112, .T. ) ;
#11669=CARTESIAN_POINT ( 'NONE',  ( 0.5502190760550982329, -32.76947806258566231, 7.635761828346577573 ) ) ;
#11675=CARTESIAN_POINT ( 'NONE',  ( 0.3856705772283747780, -32.81361829944838604, 7.750000000000000888 ) ) ;
#11679=CARTESIAN_POINT ( 'NONE',  ( -1.391746016950013320, -31.20965402480746320, 7.750000000000000888 ) ) ;
#11680=B_SPLINE_CURVE_WITH_KNOTS ( 'NONE', 3,
 ( #25342, #6403, #3537, #435, #2930, #34833, #24722, #12363, #15449, #37470 ),
 .UNSPECIFIED., .F., .F.,
 ( 4, 3, 3, 4 ),
 ( 0.0001585009270395724165, 0.0001815657551981832726, 0.0002118214035944120176, 0.0002170292169044778436 ),
 .UNSPECIFIED. ) ;
#11682=ORIENTED_EDGE ( 'NONE', *, *, #17454, .F. ) ;
#11686=ORIENTED_EDGE ( 'NONE', *, *, #35035, .T. ) ;
#11687=ORIENTED_EDGE ( 'NONE', *, *, #26554, .F. ) ;
#11693=ADVANCED_FACE ( 'NONE', ( #14883 ), #27651, .F. ) ;
#11694=ORIENTED_EDGE ( 'NONE', *, *, #17306, .F. ) ;
#11695=CARTESIAN_POINT ( 'NONE',  ( 0.5470676372252714081, -32.88165439262409251, 7.255881584735162981 ) ) ;
#11697=ORIENTED_EDGE ( 'NONE', *, *, #11319, .F. ) ;
#11698=EDGE_CURVE ( 'NONE', #6354, #8844, #4086, .T. ) ;
#11700=CARTESIAN_POINT ( 'NONE',  ( -2.184219888937934950, -32.98850935093154391, 7.754798119455333705 ) ) ;
#11704=VERTEX_POINT ( 'NONE', #21082 ) ;
#11706=CARTESIAN_POINT ( 'NONE',  ( 4.286018331208381937, -27.36209527917707263, 7.730758795053807475 ) ) ;
#11709=PLANE ( 'NONE',  #19327 ) ;
#11711=CARTESIAN_POINT ( 'NONE',  ( -0.01072294803718611307, -26.63188197674012159, 7.756377446753162097 ) ) ;
#11722=CARTESIAN_POINT ( 'NONE',  ( -1.654012860102806570, -29.01496998062980381, 7.695279973900954751 ) ) ;
#11726=CARTESIAN_POINT ( 'NONE',  ( 1.713892699967800581, -32.96990337146582561, 7.635761828346577573 ) ) ;
#11731=CARTESIAN_POINT ( 'NONE',  ( 5.185377850561007307, -29.62128986762933280, 7.785344483711591934 ) ) ;
#11732=CARTESIAN_POINT ( 'NONE',  ( 4.256814889047467076, -33.88948601255670212, 7.695279973900954751 ) ) ;
#11733=CARTESIAN_POINT ( 'NONE',  ( 4.363193498965130424, -31.82791667060237728, 7.778495531946297170 ) ) ;
#11739=CARTESIAN_POINT ( 'NONE',  ( 5.200390093233090205, -29.56993018339339940, 7.800000000000000711 ) ) ;
#11741=ORIENTED_EDGE ( 'NONE', *, *, #37238, .T. ) ;
#11742=CARTESIAN_POINT ( 'NONE',  ( -0.5720469289765105492, -32.09896754572934441, 7.761597726988858525 ) ) ;
#11744=ADVANCED_FACE ( 'NONE', ( #40009, #24780 ), #27049, .F. ) ;
#11746=CARTESIAN_POINT ( 'NONE',  ( 0.9976637635090632727, -32.89651637730339928, 6.864276522220859711 ) ) ;
#11750=CARTESIAN_POINT ( 'NONE',  ( 1.278812785396021612, -26.09541258039915590, 6.980586498568971621 ) ) ;
#11762=ORIENTED_EDGE ( 'NONE', *, *, #17560, .T. ) ;
#11763=CARTESIAN_POINT ( 'NONE',  ( -0.8270868501854790056, -27.29575654199287271, 7.759451378593098525 ) ) ;
#11765=CARTESIAN_POINT ( 'NONE',  ( 4.947714365125587932, -30.86868380840103043, 7.766640943994651103 ) ) ;
#11766=FACE_OUTER_BOUND ( 'NONE', #34892, .T. ) ;
#11771=CARTESIAN_POINT ( 'NONE',  ( 1.636219183984862990, -33.06935340522112909, 6.870737987065012931 ) ) ;
#11774=CARTESIAN_POINT ( 'NONE',  ( 1.140861248955154839, -32.93077579228409490, 7.257242401810563237 ) ) ;
#11775=LINE ( 'NONE', #33851, #33608 ) ;
#11776=B_SPLINE_CURVE_WITH_KNOTS ( 'NONE', 3,
 ( #20397, #8796, #14220, #26795, #39333, #11123, #23693, #30086, #1900, #37015, #27951, #30862, #40300, #12090, #24664, #37216, #21589, #34171, #12716, #19306, #28782, #589, #28156, #22000, #25086 ),
 .UNSPECIFIED., .F., .F.,
 ( 4, 3, 3, 3, 3, 3, 3, 3, 4 ),
 ( 6.468151674594163625E-05, 9.076621574722140316E-05, 0.0001210204262067974922, 0.0001512763324577456252, 0.0001815301820994263905, 0.0002117781465860695401, 0.0002420274594459763731, 0.0002722905548971228900, 0.0002816827545175647511 ),
 .UNSPECIFIED. ) ;
#11777=CARTESIAN_POINT ( 'NONE',  ( -1.058242811331675304, -31.72385899209557181, 7.753200566781599967 ) ) ;
#11780=CARTESIAN_POINT ( 'NONE',  ( 3.382900834235484933, -26.61540788991811013, 7.643333865083961065 ) ) ;
#11781=CARTESIAN_POINT ( 'NONE',  ( 5.044196383407847151, -28.95432172001934035, 7.652160403243382980 ) ) ;
#11784=FACE_OUTER_BOUND ( 'NONE', #19733, .T. ) ;
#11787=CARTESIAN_POINT ( 'NONE',  ( 3.504784550580148483, -26.68823612567400971, 7.754798119455333705 ) ) ;
#11789=EDGE_LOOP ( 'NONE', ( #27767, #15562, #31435, #21606, #16472, #27022 ) ) ;
#11790=CARTESIAN_POINT ( 'NONE',  ( 4.404516770028684469, -31.79202354683301834, 7.695279973900954751 ) ) ;
#11794=CARTESIAN_POINT ( 'NONE',  ( -2.271193562574106650, -32.88485816291451869, 7.635761828346577573 ) ) ;
#11796=CARTESIAN_POINT ( 'NONE',  ( 4.040170416529481834, -33.73639438183194983, 7.013842709614101167 ) ) ;
#11798=CARTESIAN_POINT ( 'NONE',  ( 1.311799688994542246, -26.19220832609979155, 6.920489980334476599 ) ) ;
#11800=CARTESIAN_POINT ( 'NONE',  ( 2.184403768844786597, -32.93531068382346660, 7.768425012602592439 ) ) ;
#11803=VECTOR ( 'NONE', #7326, 1000.000000000000000 ) ;
#11806=VERTEX_POINT ( 'NONE', #16759 ) ;
#11808=B_SPLINE_CURVE_WITH_KNOTS ( 'NONE', 3,
 ( #30759, #18167, #14664, #30339, #11771, #5014, #14873, #27235, #39801, #30543, #24351, #36915, #21275, #33847, #24769, #15701, #31564, #6240, #9113, #27843, #12408, #5833, #34674, #15290, #31363, #9728, #18784, #3387, #19004, #6451, #40396 ),
 .UNSPECIFIED., .F., .F.,
 ( 4, 3, 3, 3, 3, 3, 3, 3, 3, 3, 4 ),
 ( 1.084202172485504434E-18, 3.077658087705624490E-05, 6.152638666998984352E-05, 9.267501192706536313E-05, 0.0001241882240135194423, 0.0001556618703051674234, 0.0001866161554452220326, 0.0002167966385860974423, 0.0002463805737537784111, 0.0002758761370306540080, 0.0002847094172290046696 ),
 .UNSPECIFIED. ) ;
#11816=ORIENTED_EDGE ( 'NONE', *, *, #3950, .F. ) ;
#11823=CARTESIAN_POINT ( 'NONE',  ( -0.03129586030734986257, -26.63571487215777012, 7.257242401810563237 ) ) ;
#11824=CARTESIAN_POINT ( 'NONE',  ( 2.495811076861738975, -26.26428262444142447, 6.969307238440507923 ) ) ;
#11829=B_SPLINE_CURVE_WITH_KNOTS ( 'NONE', 3,
 ( #20108, #16018, #35386, #10438, #19312, #10033, #22615, #10237, #10633, #25896 ),
 .UNSPECIFIED., .F., .F.,
 ( 4, 3, 3, 4 ),
 ( 0.0002170292169044822075, 0.0002420761345915959837, 0.0002723302478206999860, 0.0002816811360866905162 ),
 .UNSPECIFIED. ) ;
#11840=CARTESIAN_POINT ( 'NONE',  ( 0.7149948906900660539, -26.31585638355339185, 7.013842709614101167 ) ) ;
#11844=FACE_OUTER_BOUND ( 'NONE', #14389, .T. ) ;
#11845=LINE ( 'NONE', #36979, #27308 ) ;
#11850=CARTESIAN_POINT ( 'NONE',  ( 2.321451664048270302, -33.01438696571141662, 7.635761828346576685 ) ) ;
#11851=EDGE_LOOP ( 'NONE', ( #16027, #16428, #16580, #8604, #1702 ) ) ;
#11852=CARTESIAN_POINT ( 'NONE',  ( -1.606710073356391266, -28.78057064038158686, 6.988553391373223178 ) ) ;
#11854=CARTESIAN_POINT ( 'NONE',  ( -0.6804824730526998211, -32.13536305585522257, 7.006908160621411419 ) ) ;
#11858=CARTESIAN_POINT ( 'NONE',  ( -1.518021638882832702, -28.19449355359958176, 6.945385021654667312 ) ) ;
#11860=CARTESIAN_POINT ( 'NONE',  ( -0.8725572984338751947, -27.34733221711291051, 6.894806418505345036 ) ) ;
#11861=ORIENTED_EDGE ( 'NONE', *, *, #4021, .T. ) ;
#11863=CARTESIAN_POINT ( 'NONE',  ( 3.264211231867342189, -32.58896295500613149, 6.871394612369936539 ) ) ;
#11864=( BOUNDED_CURVE ( )  B_SPLINE_CURVE ( 3, ( #15319, #15114, #12011, #300 ),
 .UNSPECIFIED., .F., .T. ) 
 B_SPLINE_CURVE_WITH_KNOTS ( ( 4, 4 ),
 ( 1.381924640371167579, 1.574767692156076260 ),
 .UNSPECIFIED. ) 
 CURVE ( )  GEOMETRIC_REPRESENTATION_ITEM ( )  RATIONAL_B_SPLINE_CURVE ( ( 1.000000000000000000, 0.9969033633783032089, 0.9969033633783032089, 1.000000000000000000 ) ) 
 REPRESENTATION_ITEM ( '' )  );
#11865=CARTESIAN_POINT ( 'NONE',  ( 4.921080693996054300, -30.94002217087347262, 6.921725064902942925 ) ) ;
#11871=ADVANCED_FACE ( 'NONE', ( #22774 ), #22164, .F. ) ;
#11875=CARTESIAN_POINT ( 'NONE',  ( -0.9665011745138262222, -31.83658251679149487, 7.743886751744248009 ) ) ;
#11876=CARTESIAN_POINT ( 'NONE',  ( 0.9786193834823287974, -32.99384626346355986, 7.761113333117547697 ) ) ;
#11885=CARTESIAN_POINT ( 'NONE',  ( 4.045015305582563059, -26.97130747677318041, 6.867199677474202346 ) ) ;
#11889=CARTESIAN_POINT ( 'NONE',  ( 1.888484868039683962, -26.17513220563941800, 6.895222827070021765 ) ) ;
#11892=CARTESIAN_POINT ( 'NONE',  ( 1.700390093233090871, -29.56993018339339940, 7.750000000000000888 ) ) ;
#11893=ORIENTED_EDGE ( 'NONE', *, *, #11562, .T. ) ;
#11902=ORIENTED_EDGE ( 'NONE', *, *, #19675, .T. ) ;
#11913=DIRECTION ( 'NONE',  ( -1.000000000000000000, -0.000000000000000000, -0.000000000000000000 ) ) ;
#11917=CARTESIAN_POINT ( 'NONE',  ( 4.890701645444022638, -28.39438256639548896, 7.635761828346577573 ) ) ;
#11926=VERTEX_POINT ( 'NONE', #4235 ) ;
#11927=CARTESIAN_POINT ( 'NONE',  ( -1.653558785517501795, -29.01221950110802794, 7.670860738520325128 ) ) ;
#11934=ORIENTED_EDGE ( 'NONE', *, *, #11406, .F. ) ;
#11935=CARTESIAN_POINT ( 'NONE',  ( 0.6356603237437735698, -26.34092700757140193, 6.864651958020303368 ) ) ;
#11938=ADVANCED_FACE ( 'NONE', ( #3851 ), #16369, .F. ) ;
#11940=DIRECTION ( 'NONE',  ( -0.9396926207859058744, -0.3420201433256757628, -0.000000000000000000 ) ) ;
#11941=CARTESIAN_POINT ( 'NONE',  ( 4.630844611799306954, -31.48367946546115803, 6.951256099901584662 ) ) ;
#11949=DIRECTION ( 'NONE',  ( 0.1303762246624232679, -0.7394003126383936753, 0.6605219282605379050 ) ) ;
#11952=FACE_OUTER_BOUND ( 'NONE', #19250, .T. ) ;
#11954=ORIENTED_EDGE ( 'NONE', *, *, #39255, .T. ) ;
#11957=ORIENTED_EDGE ( 'NONE', *, *, #14605, .F. ) ;
#11962=CARTESIAN_POINT ( 'NONE',  ( 2.829405163535267942, -26.36285597610873310, 7.695279973900954751 ) ) ;
#11966=CARTESIAN_POINT ( 'NONE',  ( 3.877683203921740596, -32.29717309340981757, 7.780491323090171996 ) ) ;
#11975=CARTESIAN_POINT ( 'NONE',  ( 1.700390093233090871, -29.56993018339339940, 7.800000000000000711 ) ) ;
#11976=CARTESIAN_POINT ( 'NONE',  ( -1.699138637657512829, -29.51332269405392239, 6.887041543973317026 ) ) ;
#11977=EDGE_LOOP ( 'NONE', ( #31554, #25764, #34651, #30185, #29918 ) ) ;
#11980=CARTESIAN_POINT ( 'NONE',  ( -1.649141860557009176, -30.19362195415678229, 7.257242401810564125 ) ) ;
#11984=FACE_OUTER_BOUND ( 'NONE', #15720, .T. ) ;
#11987=CARTESIAN_POINT ( 'NONE',  ( 5.152995580017100785, -30.14397416824791165, 7.674970859709603133 ) ) ;
#11989=CARTESIAN_POINT ( 'NONE',  ( 3.364361873418217463, -32.64093995024074957, 7.776484688137385248 ) ) ;
#11991=CARTESIAN_POINT ( 'NONE',  ( 5.042305363714541855, -28.94414881188822619, 7.695279973900954751 ) ) ;
#11992=CARTESIAN_POINT ( 'NONE',  ( 0.4601917647012155888, -32.82718141592015115, 7.785344483711591934 ) ) ;
#11993=LINE ( 'NONE', #37124, #19420 ) ;
#11998=CARTESIAN_POINT ( 'NONE',  ( -1.538375173488943259, -30.60457953059374248, 6.865312560952604670 ) ) ;
#11999=VERTEX_POINT ( 'NONE', #22971 ) ;
#12003=ORIENTED_EDGE ( 'NONE', *, *, #10907, .T. ) ;
#12004=CYLINDRICAL_SURFACE ( 'NONE', #12733, 3.399999999999999911 ) ;
#12005=FACE_OUTER_BOUND ( 'NONE', #33609, .T. ) ;
#12009=ADVANCED_FACE ( 'NONE', ( #35534 ), #31832, .F. ) ;
#12011=CARTESIAN_POINT ( 'NONE',  ( -1.425108829345238082, -28.21376964069959925, 7.386948897581449458 ) ) ;
#12012=VERTEX_POINT ( 'NONE', #38188 ) ;
#12023=CARTESIAN_POINT ( 'NONE',  ( -0.9304231601246585326, -27.40494118565320392, 7.257242401810566790 ) ) ;
#12025=VERTEX_POINT ( 'NONE', #39962 ) ;
#12027=VECTOR ( 'NONE', #26173, 1000.000000000000000 ) ;
#12028=DIRECTION ( 'NONE',  ( -0.1736481776669174526, -0.9848077530122102408, 0.000000000000000000 ) ) ;
#12030=CARTESIAN_POINT ( 'NONE',  ( 1.660390578422507035, -32.96970878852050646, 7.784838882742139532 ) ) ;
#12034=CARTESIAN_POINT ( 'NONE',  ( 3.733953510012606891, -32.29475398685401899, 7.006423389747790331 ) ) ;
#12036=CARTESIAN_POINT ( 'NONE',  ( 5.113812245512664667, -30.34358980514384285, 7.013842709614101167 ) ) ;
#12038=CARTESIAN_POINT ( 'NONE',  ( 5.045426396246663003, -28.96105241937069152, 7.748216051605119503 ) ) ;
#12046=CARTESIAN_POINT ( 'NONE',  ( 4.969183729906043290, -30.78936915658119489, 7.781480525794718162 ) ) ;
#12052=CARTESIAN_POINT ( 'NONE',  ( -1.559314410350653546, -30.53653586789760865, 6.929923840112069300 ) ) ;
#12055=EDGE_CURVE ( 'NONE', #5814, #19731, #3149, .T. ) ;
#12057=ORIENTED_EDGE ( 'NONE', *, *, #14327, .T. ) ;
#12059=ORIENTED_EDGE ( 'NONE', *, *, #14968, .F. ) ;
#12061=B_SPLINE_CURVE_WITH_KNOTS ( 'NONE', 3,
 ( #14521, #1791, #8339, #11222, #23990, #23601, #32879, #14936, #4669, #14320, #18018, #1586, #36165, #39639, #27291, #21129, #23788, #36365, #7944, #20496, #30181, #4862, #33287, #5068, #36763, #36560, #17601, #27093, #20914, #5269, #17810 ),
 .UNSPECIFIED., .F., .F.,
 ( 4, 3, 3, 3, 3, 3, 3, 3, 3, 3, 4 ),
 ( 0.000000000000000000, 3.077658087705648207E-05, 6.152638666998854248E-05, 9.267501192706494300E-05, 0.0001241882240135190358, 0.0001556618703051665289, 0.0001866161554452196744, 0.0002167966385860968731, 0.0002463805737537766763, 0.0002758761370306527069, 0.0002847094172290049949 ),
 .UNSPECIFIED. ) ;
#12062=EDGE_CURVE ( 'NONE', #40343, #9636, #9440, .T. ) ;
#12063=CARTESIAN_POINT ( 'NONE',  ( -1.567987374133025247, -28.31781895025901008, 6.873189335546978640 ) ) ;
#12067=B_SPLINE_CURVE_WITH_KNOTS ( 'NONE', 3,
 ( #19039, #31601, #24810, #9554, #6886, #37351, #28090, #9145, #37550, #21926, #34500, #3224, #9765, #12849, #6274, #18822, #15740, #15935, #22345, #521, #13054, #34915, #22546, #35108, #31804, #3618, #16146, #25616, #16939, #19646, #7685 ),
 .UNSPECIFIED., .F., .F.,
 ( 4, 3, 3, 3, 3, 3, 3, 3, 3, 3, 4 ),
 ( 0.000000000000000000, 2.999644130997671654E-05, 6.002588995694646388E-05, 8.960886084588062241E-05, 0.0001190604700446481443, 0.0001489538463052721812, 0.0001796139255494020562, 0.0002109707048517091657, 0.0002426195318110370642, 0.0002740640997890078645, 0.0002849778069099885396 ),
 .UNSPECIFIED. ) ;
#12072=CARTESIAN_POINT ( 'NONE',  ( 3.327612781436851463, -32.55525199569353134, 6.870716933885663735 ) ) ;
#12075=CARTESIAN_POINT ( 'NONE',  ( 1.646239191775039412, -25.86893018339335981, 7.695279973900954751 ) ) ;
#12076=CARTESIAN_POINT ( 'NONE',  ( 0.1778422052069661419, -26.52201895416361310, 7.386948897581448570 ) ) ;
#12079=CARTESIAN_POINT ( 'NONE',  ( -2.965417489341782176, -27.61323101669772484, 6.894806418505347700 ) ) ;
#12084=CARTESIAN_POINT ( 'NONE',  ( 5.006586777994688653, -30.36307495321339900, 6.979335674598005745 ) ) ;
#12088=ORIENTED_EDGE ( 'NONE', *, *, #10235, .F. ) ;
#12089=CARTESIAN_POINT ( 'NONE',  ( 1.700390093233090871, -29.56993018339339940, 7.800000000000000711 ) ) ;
#12090=CARTESIAN_POINT ( 'NONE',  ( 4.624684975110706198, -31.30446008192196317, 7.784838882742139532 ) ) ;
#12098=AXIS2_PLACEMENT_3D ( 'NONE', #723, #28096, #34921 ) ;
#12106=ORIENTED_EDGE ( 'NONE', *, *, #39787, .T. ) ;
#12108=VERTEX_POINT ( 'NONE', #15045 ) ;
#12112=( BOUNDED_CURVE ( )  B_SPLINE_CURVE ( 3, ( #9522, #28681, #19010, #491 ),
 .UNSPECIFIED., .F., .T. ) 
 B_SPLINE_CURVE_WITH_KNOTS ( ( 4, 4 ),
 ( 1.381924640371167357, 1.574767692156076482 ),
 .UNSPECIFIED. ) 
 CURVE ( )  GEOMETRIC_REPRESENTATION_ITEM ( )  RATIONAL_B_SPLINE_CURVE ( ( 1.000000000000000000, 0.9969033633783032089, 0.9969033633783032089, 1.000000000000000000 ) ) 
 REPRESENTATION_ITEM ( '' )  );
#12115=ORIENTED_EDGE ( 'NONE', *, *, #3388, .T. ) ;
#12118=VERTEX_POINT ( 'NONE', #2726 ) ;
#12132=CARTESIAN_POINT ( 'NONE',  ( 0.5099477558868652505, -26.38514651076292239, 7.661510568013098599 ) ) ;
#12135=AXIS2_PLACEMENT_3D ( 'NONE', #21790, #5520, #12508 ) ;
#12136=CARTESIAN_POINT ( 'NONE',  ( 1.700390093233090871, -29.56993018339339940, 7.800000000000000711 ) ) ;
#12139=AXIS2_PLACEMENT_3D ( 'NONE', #17558, #27053, #39598 ) ;
#12148=CARTESIAN_POINT ( 'NONE',  ( 5.098360399818202993, -29.68741740107808980, 7.759451378593097637 ) ) ;
#12149=CARTESIAN_POINT ( 'NONE',  ( 4.666673777302699833, -31.42768917297451026, 6.867199677474199682 ) ) ;
#12160=EDGE_CURVE ( 'NONE', #9154, #2808, #7479, .T. ) ;
#12161=CARTESIAN_POINT ( 'NONE',  ( -0.5207487492606875934, -26.87946823591146384, 7.781480525794719050 ) ) ;
#12171=CARTESIAN_POINT ( 'NONE',  ( 1.700390093233090871, -29.56993018339339940, 6.800000000000000711 ) ) ;
#12173=VERTEX_POINT ( 'NONE', #40356 ) ;
#12179=CARTESIAN_POINT ( 'NONE',  ( -0.04839779602465103803, -32.48570468057000227, 6.887041543973315250 ) ) ;
#12182=CARTESIAN_POINT ( 'NONE',  ( 3.863278594513700259, -32.31834595185378589, 7.766640943994342905 ) ) ;
#12184=CARTESIAN_POINT ( 'NONE',  ( 0.5402140142766861386, -26.37399660057016604, 7.769368695748487319 ) ) ;
#12186=CARTESIAN_POINT ( 'NONE',  ( -0.8065408690586024498, -32.02206539088906112, 7.501983001166816933 ) ) ;
#12189=CARTESIAN_POINT ( 'NONE',  ( 1.870512271622051026, -32.97271924194787829, 7.139196562012272373 ) ) ;
#12194=CARTESIAN_POINT ( 'NONE',  ( -1.693328789480683216, -29.36335781081668017, 6.929923840112063971 ) ) ;
#12196=CARTESIAN_POINT ( 'NONE',  ( -1.346119371218626792, -31.29294500718514271, 6.894806418505347700 ) ) ;
#12202=VECTOR ( 'NONE', #2414, 1000.000000000000000 ) ;
#12208=CARTESIAN_POINT ( 'NONE',  ( 1.145429890469515932, -32.92433313672930240, 7.693875151218753317 ) ) ;
#12210=CARTESIAN_POINT ( 'NONE',  ( 0.4370139710353302398, -32.82074954894827812, 7.782861076432731728 ) ) ;
#12212=CARTESIAN_POINT ( 'NONE',  ( 5.098819578411125875, -29.67379560486689982, 6.864651958020303368 ) ) ;
#12213=AXIS2_PLACEMENT_3D ( 'NONE', #40263, #2834, #27912 ) ;
#12215=CARTESIAN_POINT ( 'NONE',  ( 2.839160670253830343, -26.36630475908082971, 7.652160403243387421 ) ) ;
#12219=LINE ( 'NONE', #24792, #27762 ) ;
#12222=DIRECTION ( 'NONE',  ( -1.000000000000000000, 0.000000000000000000, 0.000000000000000000 ) ) ;
#12223=CARTESIAN_POINT ( 'NONE',  ( 0.06461229748503910519, -26.58927154175672669, 6.874555630061441214 ) ) ;
#12224=CARTESIAN_POINT ( 'NONE',  ( 1.163078168714447802, -26.21265396905771183, 6.889465824494257262 ) ) ;
#12225=CARTESIAN_POINT ( 'NONE',  ( 5.041572579232883378, -30.19968737494692235, 7.784838882742138644 ) ) ;
#12226=ADVANCED_FACE ( 'NONE', ( #16959 ), #26048, .F. ) ;
#12231=B_SPLINE_CURVE_WITH_KNOTS ( 'NONE', 3,
 ( #3961, #18974, #19378, #658, #29051, #19585, #19174, #10301, #25558, #22878 ),
 .UNSPECIFIED., .F., .F.,
 ( 4, 3, 3, 4 ),
 ( 0.000000000000000000, 3.025505781527808535E-05, 6.051003801291533372E-05, 6.468145402690609117E-05 ),
 .UNSPECIFIED. ) ;
#12233=EDGE_CURVE ( 'NONE', #357, #16534, #1744, .T. ) ;
#12236=FACE_OUTER_BOUND ( 'NONE', #33884, .T. ) ;
#12241=CARTESIAN_POINT ( 'NONE',  ( 2.778501328868240083, -32.79447296704462644, 7.778050822775631978 ) ) ;
#12243=ORIENTED_EDGE ( 'NONE', *, *, #13933, .T. ) ;
#12251=CARTESIAN_POINT ( 'NONE',  ( 3.720917640761610468, -32.30442619357121004, 6.959317978105168834 ) ) ;
#12253=CARTESIAN_POINT ( 'NONE',  ( 1.749140210850987920, -26.17027969752984973, 6.894806418505346812 ) ) ;
#12260=B_SPLINE_CURVE_WITH_KNOTS ( 'NONE', 3,
 ( #10362, #29309, #35500, #29701 ),
 .UNSPECIFIED., .F., .F.,
 ( 4, 4 ),
 ( 0.000000000000000000, 6.391136169993780466E-06 ),
 .UNSPECIFIED. ) ;
#12265=DIRECTION ( 'NONE',  ( 1.047444401652940007E-14, -1.000000000000000000, -0.000000000000000000 ) ) ;
#12266=AXIS2_PLACEMENT_3D ( 'NONE', #38423, #16794, #32674 ) ;
#12271=VERTEX_POINT ( 'NONE', #17348 ) ;
#12274=ORIENTED_EDGE ( 'NONE', *, *, #34161, .F. ) ;
#12280=CARTESIAN_POINT ( 'NONE',  ( -1.746138059369836570, -28.96840265811469806, 7.762796336881261361 ) ) ;
#12283=ORIENTED_EDGE ( 'NONE', *, *, #10172, .T. ) ;
#12287=CARTESIAN_POINT ( 'NONE',  ( 4.940354242878053803, -30.89383239149909599, 6.870724624169665340 ) ) ;
#12289=FACE_OUTER_BOUND ( 'NONE', #38351, .T. ) ;
#12299=FACE_OUTER_BOUND ( 'NONE', #8021, .T. ) ;
#12305=CARTESIAN_POINT ( 'NONE',  ( 5.628486912222185445, -26.20317660986373909, 7.695279973900954751 ) ) ;
#12311=CARTESIAN_POINT ( 'NONE',  ( 1.774094287987110441, -26.17071518185239754, 6.874555630061442990 ) ) ;
#12322=CARTESIAN_POINT ( 'NONE',  ( 4.273337484900067373, -31.79252814967387053, 6.894806418505345036 ) ) ;
#12328=ORIENTED_EDGE ( 'NONE', *, *, #32300, .F. ) ;
#12337=CARTESIAN_POINT ( 'NONE',  ( 4.681048734869769135, -27.93415238764535857, 6.874555630061442990 ) ) ;
#12339=CARTESIAN_POINT ( 'NONE',  ( 4.883069014757387194, -28.37387203058899487, 7.680992449362118002 ) ) ;
#12341=DIRECTION ( 'NONE',  ( -0.000000000000000000, -0.000000000000000000, -1.000000000000000000 ) ) ;
#12342=CARTESIAN_POINT ( 'NONE',  ( 0.5135240150758065836, -26.28321512987682596, 7.773839561854632763 ) ) ;
#12347=ADVANCED_FACE ( 'NONE', ( #10175 ), #22765, .F. ) ;
#12348=AXIS2_PLACEMENT_3D ( 'NONE', #35166, #373, #21990 ) ;
#12350=CARTESIAN_POINT ( 'NONE',  ( 3.435265683109236967, -26.53015935524666347, 7.750000000000001776 ) ) ;
#12351=VERTEX_POINT ( 'NONE', #22961 ) ;
#12356=AXIS2_PLACEMENT_3D ( 'NONE', #39536, #11322, #4576 ) ;
#12358=ORIENTED_EDGE ( 'NONE', *, *, #36340, .F. ) ;
#12360=CARTESIAN_POINT ( 'NONE',  ( -1.681553744649562532, -29.97427170972491695, 7.405500484323178867 ) ) ;
#12362=CARTESIAN_POINT ( 'NONE',  ( -1.715618416584987704, -30.36287436211992130, 7.139344958878412584 ) ) ;
#12363=CARTESIAN_POINT ( 'NONE',  ( -1.348492144037532814, -27.85111747872926813, 7.698786668945014178 ) ) ;
#12364=B_SPLINE_CURVE_WITH_KNOTS ( 'NONE', 3,
 ( #15244, #12974, #40351, #37270, #31319, #5992, #18530, #37875, #9682, #31114, #2929, #15448, #37469, #19569, #38887, #13180, #22462, #31932, #32342 ),
 .UNSPECIFIED., .F., .F.,
 ( 4, 3, 3, 3, 3, 3, 4 ),
 ( 8.673617379884035472E-19, 2.546128104245028707E-05, 5.711050680484775665E-05, 8.113074941676622380E-05, 0.0001053129305727147218, 0.0001360598016347234519, 0.0001612931755702011341 ),
 .UNSPECIFIED. ) ;
#12366=EDGE_CURVE ( 'NONE', #30637, #10351, #25217, .T. ) ;
#12370=PLANE ( 'NONE',  #7272 ) ;
#12372=ORIENTED_EDGE ( 'NONE', *, *, #33305, .T. ) ;
#12374=( BOUNDED_CURVE ( )  B_SPLINE_CURVE ( 3, ( #33607, #17921, #30505, #3540 ),
 .UNSPECIFIED., .F., .T. ) 
 B_SPLINE_CURVE_WITH_KNOTS ( ( 4, 4 ),
 ( 1.347909859412853351, 1.534781240595298302 ),
 .UNSPECIFIED. ) 
 CURVE ( )  GEOMETRIC_REPRESENTATION_ITEM ( )  RATIONAL_B_SPLINE_CURVE ( ( 1.000000000000000000, 0.9970920404276226723, 0.9970920404276226723, 1.000000000000000000 ) ) 
 REPRESENTATION_ITEM ( '' )  );
#12376=ORIENTED_EDGE ( 'NONE', *, *, #29299, .F. ) ;
#12378=ORIENTED_EDGE ( 'NONE', *, *, #25406, .F. ) ;
#12385=EDGE_LOOP ( 'NONE', ( #23391, #7072, #31799, #9327, #24593 ) ) ;
#12394=CARTESIAN_POINT ( 'NONE',  ( 2.344207582906673970, -26.12964968137214683, 6.888594555015730592 ) ) ;
#12399=VERTEX_POINT ( 'NONE', #18381 ) ;
#12400=CARTESIAN_POINT ( 'NONE',  ( 2.088670072939348366, -32.95477192119402332, 7.386948897581450346 ) ) ;
#12404=CARTESIAN_POINT ( 'NONE',  ( 4.258720360809321370, -31.95843491878680354, 6.989977667959444751 ) ) ;
#12407=CARTESIAN_POINT ( 'NONE',  ( -1.357913867432435362, -31.27192221750447487, 6.875671892026062437 ) ) ;
#12408=CARTESIAN_POINT ( 'NONE',  ( 1.508613083882804684, -33.06467219138443880, 6.941203072598477242 ) ) ;
#12418=CARTESIAN_POINT ( 'NONE',  ( -0.9609532066394848027, -31.68588194093026189, 7.778050822775630202 ) ) ;
#12421=CARTESIAN_POINT ( 'NONE',  ( 2.119804661062819839, -32.94396210681857440, 6.882085323592686876 ) ) ;
#12427=ORIENTED_EDGE ( 'NONE', *, *, #31745, .T. ) ;
#12431=ORIENTED_EDGE ( 'NONE', *, *, #35860, .T. ) ;
#12432=CARTESIAN_POINT ( 'NONE',  ( -0.9068966613934061893, -27.23885067285716843, 7.766640943994647550 ) ) ;
#12433=EDGE_CURVE ( 'NONE', #14367, #21155, #36000, .T. ) ;
#12434=CARTESIAN_POINT ( 'NONE',  ( 1.212983646527633130, -26.10426722441512837, 7.754798119455333705 ) ) ;
#12436=CARTESIAN_POINT ( 'NONE',  ( 5.054793046568992310, -30.12489038615697012, 7.695279973900954751 ) ) ;
#12440=ORIENTED_EDGE ( 'NONE', *, *, #22710, .T. ) ;
#12448=CARTESIAN_POINT ( 'NONE',  ( 4.336009428051142756, -27.42202173051807890, 6.894806418505345924 ) ) ;
#12450=CARTESIAN_POINT ( 'NONE',  ( -1.000637662739485290, -31.79578935716557453, 6.894806418505347700 ) ) ;
#12452=CARTESIAN_POINT ( 'NONE',  ( -1.599034431228576247, -30.73774772367137942, 6.894806418505347700 ) ) ;
#12453=ORIENTED_EDGE ( 'NONE', *, *, #38331, .F. ) ;
#12465=PLANE ( 'NONE',  #33289 ) ;
#12466=CARTESIAN_POINT ( 'NONE',  ( 3.480798653453814673, -32.58325819489262187, 7.710604733652628440 ) ) ;
#12467=EDGE_CURVE ( 'NONE', #24834, #5389, #27243, .T. ) ;
#12469=CARTESIAN_POINT ( 'NONE',  ( 3.896194328649233984, -32.16578144256224903, 7.635761828346577573 ) ) ;
#12477=DIRECTION ( 'NONE',  ( 0.9848077530122075762, 0.1736481776669329402, 0.000000000000000000 ) ) ;
#12479=DIRECTION ( 'NONE',  ( -0.6834397476448844655, 0.000000000000000000, -0.7300069255418721870 ) ) ;
#12486=B_SPLINE_CURVE_WITH_KNOTS ( 'NONE', 3,
 ( #16137, #10145, #28699, #22736, #6875, #19430, #35299, #32004, #7071, #19636, #32210, #906, #13444, #26019, #30113, #5194, #1510, #24327, #2123, #23530, #20421, #5396, #39153, #36284, #11750, #10948, #27212, #39561, #26618, #14244, #33621 ),
 .UNSPECIFIED., .F., .F.,
 ( 4, 3, 3, 3, 3, 3, 3, 3, 3, 3, 4 ),
 ( 0.000000000000000000, 3.077658087705726812E-05, 6.152638666999176798E-05, 9.267501192706665062E-05, 0.0001241882240135210144, 0.0001556618703051689684, 0.0001866161554452226018, 0.0002167966385860985265, 0.0002463805737537792784, 0.0002758761370306543332, 0.0002847094172290032059 ),
 .UNSPECIFIED. ) ;
#12488=LINE ( 'NONE', #3655, #27876 ) ;
#12493=CARTESIAN_POINT ( 'NONE',  ( 4.207321055524802844, -27.11779497589776255, 7.501983001166816045 ) ) ;
#12495=CARTESIAN_POINT ( 'NONE',  ( -0.8561835264942624368, -27.32849620891636633, 6.874555630061441214 ) ) ;
#12497=CARTESIAN_POINT ( 'NONE',  ( -0.06469087068677582819, -26.54759843608177761, 7.750000000000000888 ) ) ;
#12499=DIRECTION ( 'NONE',  ( -0.4826092789263580207, -0.5751513419797943394, -0.6605219282605403475 ) ) ;
#12500=CYLINDRICAL_SURFACE ( 'NONE', #10988, 3.499999999999999556 ) ;
#12508=DIRECTION ( 'NONE',  ( 0.8660254037844252739, 0.5000000000000230926, 0.000000000000000000 ) ) ;
#12509=VERTEX_POINT ( 'NONE', #9935 ) ;
#12510=DIRECTION ( 'NONE',  ( 0.000000000000000000, 0.6662082868431838945, 0.7457657263118692148 ) ) ;
#12512=CARTESIAN_POINT ( 'NONE',  ( 4.021697826674504483, -26.95045787073729215, 6.863805608295730387 ) ) ;
#12514=CARTESIAN_POINT ( 'NONE',  ( -1.799609906766908685, -29.77832925049299462, 7.162856560672855366 ) ) ;
#12519=B_SPLINE_CURVE_WITH_KNOTS ( 'NONE', 3,
 ( #23513, #17305, #13838, #1102, #3993, #10533, #26407, #29883, #35680, #32590, #7656, #16513, #7855, #14230, #4388, #11130, #38937, #23113, #1301 ),
 .UNSPECIFIED., .F., .F.,
 ( 4, 3, 3, 3, 3, 3, 4 ),
 ( 0.000000000000000000, 2.546128104244680068E-05, 5.711050680483461070E-05, 8.113074941675478546E-05, 0.0001053129305727011422, 0.0001360598016347041802, 0.0001612931755713763551 ),
 .UNSPECIFIED. ) ;
#12521=ORIENTED_EDGE ( 'NONE', *, *, #2333, .T. ) ;
#12524=CARTESIAN_POINT ( 'NONE',  ( 2.915650558103385137, -32.85217667056087265, 7.643192810543821381 ) ) ;
#12527=VECTOR ( 'NONE', #11330, 1000.000000000000000 ) ;
#12531=ORIENTED_EDGE ( 'NONE', *, *, #19547, .T. ) ;
#12542=CARTESIAN_POINT ( 'NONE',  ( 1.869561550574128761, -26.07402100007339740, 7.013842709614101167 ) ) ;
#12543=CARTESIAN_POINT ( 'NONE',  ( 4.883850366368126750, -28.37594736283919516, 7.670860738520327793 ) ) ;
#12550=ORIENTED_EDGE ( 'NONE', *, *, #16773, .T. ) ;
#12554=CARTESIAN_POINT ( 'NONE',  ( 1.070857224836541999, -26.12700842969462656, 7.743886751744251562 ) ) ;
#12563=CARTESIAN_POINT ( 'NONE',  ( 3.222937981259239582, -32.61784141262317860, 7.386948897581449458 ) ) ;
#12564=FACE_OUTER_BOUND ( 'NONE', #24546, .T. ) ;
#12566=CIRCLE ( 'NONE', #29006, 3.499999999999999556 ) ;
#12568=CARTESIAN_POINT ( 'NONE',  ( -1.227874773494582961, -31.29772208934977229, 7.721096864323905073 ) ) ;
#12569=CIRCLE ( 'NONE', #4078, 3.499999999999999556 ) ;
#12579=DIRECTION ( 'NONE',  ( 0.9848077530122083534, -0.1736481776669292765, 0.000000000000000000 ) ) ;
#12580=CARTESIAN_POINT ( 'NONE',  ( 4.960873579530714395, -28.60595147853699416, 6.939395833800442226 ) ) ;
#12588=CARTESIAN_POINT ( 'NONE',  ( 2.975028622394660260, -26.41789893177788784, 7.757178535559533294 ) ) ;
#12592=CARTESIAN_POINT ( 'NONE',  ( 1.822194502883780931, -26.07228119081829476, 7.754798119455333705 ) ) ;
#12594=EDGE_CURVE ( 'NONE', #30463, #15830, #40259, .T. ) ;
#12600=EDGE_CURVE ( 'NONE', #17652, #21194, #12112, .T. ) ;
#12603=CARTESIAN_POINT ( 'NONE',  ( -1.000637662739485290, -31.79578935716557453, 6.894806418505347700 ) ) ;
#12605=CARTESIAN_POINT ( 'NONE',  ( 4.265822965694919588, -31.95080274967918044, 7.006908160621414083 ) ) ;
#12606=CARTESIAN_POINT ( 'NONE',  ( -1.576479427848138437, -30.79961771809308502, 7.678495282201401650 ) ) ;
#12612=CARTESIAN_POINT ( 'NONE',  ( 1.672399062804430070, -26.07003816115788553, 7.733670252284492008 ) ) ;
#12614=DIRECTION ( 'NONE',  ( -0.000000000000000000, -0.000000000000000000, -1.000000000000000000 ) ) ;
#12618=CARTESIAN_POINT ( 'NONE',  ( -0.9425575444375865475, -31.70881488915268420, 7.785172627573962778 ) ) ;
#12619=( BOUNDED_CURVE ( )  B_SPLINE_CURVE ( 3, ( #18340, #37079, #39972, #8871 ),
 .UNSPECIFIED., .F., .T. ) 
 B_SPLINE_CURVE_WITH_KNOTS ( ( 4, 4 ),
 ( 1.347909859412855793, 1.534781240595300744 ),
 .UNSPECIFIED. ) 
 CURVE ( )  GEOMETRIC_REPRESENTATION_ITEM ( )  RATIONAL_B_SPLINE_CURVE ( ( 1.000000000000000000, 0.9970920404276226723, 0.9970920404276226723, 1.000000000000000000 ) ) 
 REPRESENTATION_ITEM ( '' )  );
#12620=LINE ( 'NONE', #30556, #25212 ) ;
#12621=CARTESIAN_POINT ( 'NONE',  ( 2.685785295776140114, -32.82400398323339630, 7.013842709614101167 ) ) ;
#12622=CARTESIAN_POINT ( 'NONE',  ( 0.7510407426356037197, -34.24246986869614773, 6.954324564059724878 ) ) ;
#12628=ORIENTED_EDGE ( 'NONE', *, *, #6199, .F. ) ;
#12629=CARTESIAN_POINT ( 'NONE',  ( 4.180804271322692500, -31.89534315857266122, 7.013842709614101167 ) ) ;
#12633=CARTESIAN_POINT ( 'NONE',  ( 5.045511443222842729, -28.54026521025475205, 6.903112506833890549 ) ) ;
#12634=CARTESIAN_POINT ( 'NONE',  ( 3.505675341739891593, -26.57142622932152420, 6.870737987065012931 ) ) ;
#12636=CARTESIAN_POINT ( 'NONE',  ( 5.035802448256832875, -30.22957069796434837, 7.784476445165073422 ) ) ;
#12645=CARTESIAN_POINT ( 'NONE',  ( -1.001783842385659096, -27.34545920416798737, 7.720710062488897130 ) ) ;
#12650=CARTESIAN_POINT ( 'NONE',  ( 2.750046964866756927, -32.80384806160494549, 7.757178535559533294 ) ) ;
#12652=CARTESIAN_POINT ( 'NONE',  ( 0.9267304714826871681, -32.98335233567298275, 7.013842709614101167 ) ) ;
#12653=ORIENTED_EDGE ( 'NONE', *, *, #36340, .T. ) ;
#12655=CARTESIAN_POINT ( 'NONE',  ( -1.799561124051049621, -29.58932634693233865, 7.642460958331693810 ) ) ;
#12656=EDGE_LOOP ( 'NONE', ( #33837, #21910, #37615, #24732 ) ) ;
#12658=FACE_OUTER_BOUND ( 'NONE', #36347, .T. ) ;
#12659=CARTESIAN_POINT ( 'NONE',  ( 1.643782603893625849, -32.96945891428400444, 6.887041543973315250 ) ) ;
#12661=DIRECTION ( 'NONE',  ( -0.000000000000000000, -0.000000000000000000, 1.000000000000000000 ) ) ;
#12662=CARTESIAN_POINT ( 'NONE',  ( -1.799601224800568167, -29.57893194075474597, 7.630645770930537530 ) ) ;
#12664=CARTESIAN_POINT ( 'NONE',  ( -0.06478834963175583717, -26.54765481601611654, 7.640616322432097540 ) ) ;
#12679=CARTESIAN_POINT ( 'NONE',  ( 2.119043635923744784, -33.04480253866695705, 6.971170733404100872 ) ) ;
#12680=ORIENTED_EDGE ( 'NONE', *, *, #14574, .T. ) ;
#12684=LINE ( 'NONE', #37790, #37133 ) ;
#12685=EDGE_LOOP ( 'NONE', ( #18921, #14335, #10105, #7395 ) ) ;
#12687=EDGE_CURVE ( 'NONE', #35977, #20092, #16313, .T. ) ;
#12690=CARTESIAN_POINT ( 'NONE',  ( 4.792526203416204389, -27.93020634197934982, 7.750000000000000888 ) ) ;
#12697=CARTESIAN_POINT ( 'NONE',  ( -2.297321782777200561, -26.28614060416741438, 7.695279973900954751 ) ) ;
#12700=DIRECTION ( 'NONE',  ( 0.1736481776669404897, -0.9848077530122062440, -0.000000000000000000 ) ) ;
#12701=LINE ( 'NONE', #25275, #3146 ) ;
#12707=CARTESIAN_POINT ( 'NONE',  ( -1.652934641495917178, -29.00849165296052234, 7.661510568013094158 ) ) ;
#12713=CARTESIAN_POINT ( 'NONE',  ( -0.5767923600352592439, -26.91202874155498037, 7.695279973900954751 ) ) ;
#12715=CARTESIAN_POINT ( 'NONE',  ( 2.873744954996579892, -26.27246564945127716, 7.651421919295144036 ) ) ;
#12716=CARTESIAN_POINT ( 'NONE',  ( 4.598967362590697050, -31.34707672027869307, 7.778050822775632867 ) ) ;
#12718=CARTESIAN_POINT ( 'NONE',  ( 4.052584231663811210, -26.97816100332664035, 6.870724624169668004 ) ) ;
#12727=CARTESIAN_POINT ( 'NONE',  ( -1.339690083386215758, -31.27506463679495496, 7.785096263473212375 ) ) ;
#12728=CARTESIAN_POINT ( 'NONE',  ( 2.931185808669443116, -32.84638282411072652, 7.686927408461905920 ) ) ;
#12730=CARTESIAN_POINT ( 'NONE',  ( -1.652160870483347921, -29.00385851250623404, 7.740055089680398126 ) ) ;
#12731=ORIENTED_EDGE ( 'NONE', *, *, #8343, .T. ) ;
#12733=AXIS2_PLACEMENT_3D ( 'NONE', #23955, #8923, #12222 ) ;
#12734=VECTOR ( 'NONE', #2956, 1000.000000000000114 ) ;
#12735=ORIENTED_EDGE ( 'NONE', *, *, #25028, .F. ) ;
#12740=ORIENTED_EDGE ( 'NONE', *, *, #19659, .T. ) ;
#12744=CARTESIAN_POINT ( 'NONE',  ( 4.705320599239643187, -27.97917511340586927, 6.863904403958575706 ) ) ;
#12745=EDGE_CURVE ( 'NONE', #18362, #13356, #38734, .T. ) ;
#12746=CARTESIAN_POINT ( 'NONE',  ( 4.882868366733327470, -28.37333834040810032, 7.693875151218753317 ) ) ;
#12748=CARTESIAN_POINT ( 'NONE',  ( 1.700390093233090871, -29.56993018339339940, 7.750000000000000888 ) ) ;
#12749=CARTESIAN_POINT ( 'NONE',  ( 0.4917814316705931832, -26.28522446336723561, 7.756742906098588186 ) ) ;
#12764=CARTESIAN_POINT ( 'NONE',  ( 3.412070287718869999, -32.50764203308273181, 7.635761828346577573 ) ) ;
#12766=CARTESIAN_POINT ( 'NONE',  ( 4.404516770028684469, -31.79202354683301834, 7.695279973900954751 ) ) ;
#12768=CARTESIAN_POINT ( 'NONE',  ( 1.700390093233090871, -29.56993018339339940, 7.800000000000000711 ) ) ;
#12769=CIRCLE ( 'NONE', #17363, 3.499999999999999556 ) ;
#12770=CARTESIAN_POINT ( 'NONE',  ( -1.283534637189521543, -31.19973968173253098, 7.782034975670475418 ) ) ;
#12772=EDGE_LOOP ( 'NONE', ( #38357, #10753, #33911, #39489 ) ) ;
#12776=CARTESIAN_POINT ( 'NONE',  ( 4.839780649812301938, -28.24624522621548195, 7.139196562012268821 ) ) ;
#12780=CARTESIAN_POINT ( 'NONE',  ( 1.295029243323604806, -26.19418099523372945, 7.013842709614101167 ) ) ;
#12781=CARTESIAN_POINT ( 'NONE',  ( 4.939155359955127444, -28.53528083619306699, 6.865312560952603782 ) ) ;
#12785=EDGE_LOOP ( 'NONE', ( #7229, #37012, #2916, #8808 ) ) ;
#12791=CARTESIAN_POINT ( 'NONE',  ( 2.873739498108726309, -26.37879873393239905, 7.775108481317164255 ) ) ;
#12792=EDGE_CURVE ( 'NONE', #14030, #4303, #35282, .T. ) ;
#12806=CARTESIAN_POINT ( 'NONE',  ( 4.305930965742039263, -31.90684198354446721, 6.865482280155368322 ) ) ;
#12813=CARTESIAN_POINT ( 'NONE',  ( -0.6395917686905666644, -32.03660811739485581, 6.979335674598003969 ) ) ;
#12817=CARTESIAN_POINT ( 'NONE',  ( -0.8920574397464721139, -31.76975194634333732, 7.748216051605121280 ) ) ;
#12822=AXIS2_PLACEMENT_3D ( 'NONE', #27956, #34582, #8802 ) ;
#12825=VECTOR ( 'NONE', #28524, 1000.000000000000114 ) ;
#12827=EDGE_CURVE ( 'NONE', #8844, #19268, #11316, .T. ) ;
#12828=VERTEX_POINT ( 'NONE', #18119 ) ;
#12832=EDGE_CURVE ( 'NONE', #33252, #10847, #27637, .T. ) ;
#12837=CARTESIAN_POINT ( 'NONE',  ( 5.026985514822023937, -28.48192149727754696, 6.865482280155368322 ) ) ;
#12838=CARTESIAN_POINT ( 'NONE',  ( 3.574567904444611255, -26.61401111617210802, 6.875780273367531947 ) ) ;
#12839=FACE_OUTER_BOUND ( 'NONE', #35044, .T. ) ;
#12844=CARTESIAN_POINT ( 'NONE',  ( 0.4761165981717114803, -26.29103488020206569, 7.730015791551946513 ) ) ;
#12849=CARTESIAN_POINT ( 'NONE',  ( -1.675495590043027727, -29.97419347324715133, 6.895222827070023541 ) ) ;
#12856=CARTESIAN_POINT ( 'NONE',  ( 4.732352950855482909, -31.12399458443864120, 7.139196562012272373 ) ) ;
#12858=CARTESIAN_POINT ( 'NONE',  ( 5.103179151787565537, -29.39980800500447344, 7.139196562012274150 ) ) ;
#12862=ORIENTED_EDGE ( 'NONE', *, *, #31206, .F. ) ;
#12863=VECTOR ( 'NONE', #19504, 1000.000000000000114 ) ;
#12864=EDGE_CURVE ( 'NONE', #4851, #24034, #36871, .T. ) ;
#12866=CARTESIAN_POINT ( 'NONE',  ( 1.610624680721678414, -32.96874500193186464, 7.778050822775632867 ) ) ;
#12869=CARTESIAN_POINT ( 'NONE',  ( -1.560095160591656205, -30.53389918434378458, 6.969307238440510588 ) ) ;
#12870=CARTESIAN_POINT ( 'NONE',  ( 3.394528066554050927, -32.63260504671350759, 6.870737987065015595 ) ) ;
#12872=CARTESIAN_POINT ( 'NONE',  ( 5.195169754196312439, -29.76104218084410036, 6.971170733404093767 ) ) ;
#12876=MANIFOLD_SOLID_BREP ( 'Boss-Extrude14', #22940 ) ;
#12884=ADVANCED_FACE ( 'NONE', ( #15041 ), #36267, .F. ) ;
#12887=AXIS2_PLACEMENT_3D ( 'NONE', #28026, #2949, #8876 ) ;
#12895=CARTESIAN_POINT ( 'NONE',  ( 3.999421017872402562, -26.94725929646187268, 7.782861076432729952 ) ) ;
#12896=VERTEX_POINT ( 'NONE', #39541 ) ;
#12898=CARTESIAN_POINT ( 'NONE',  ( -1.697910808162383267, -29.46219841264419514, 7.768425012602595103 ) ) ;
#12900=CARTESIAN_POINT ( 'NONE',  ( -1.699609906766908596, -29.72725013975003350, 7.398254066345574920 ) ) ;
#12903=CARTESIAN_POINT ( 'NONE',  ( -1.641525177248355227, -30.19571155489859393, 7.695279973900954751 ) ) ;
#12904=CARTESIAN_POINT ( 'NONE',  ( 3.428517765372728121, -26.52631247858627006, 7.651421919295140484 ) ) ;
#12905=CARTESIAN_POINT ( 'NONE',  ( 0.5834512725888432172, -26.35863018636138122, 6.894806418505347700 ) ) ;
#12909=EDGE_LOOP ( 'NONE', ( #5077, #5699, #5802, #33984, #7210 ) ) ;
#12911=CARTESIAN_POINT ( 'NONE',  ( -1.113355428119774393, -31.66294493508353014, 7.387053503561886281 ) ) ;
#12912=CARTESIAN_POINT ( 'NONE',  ( 4.291939159219374744, -27.36903995105183185, 7.643333865083957512 ) ) ;
#12914=CARTESIAN_POINT ( 'NONE',  ( 0.9232239867627912711, -33.77039094905028804, 7.695279973900954751 ) ) ;
#12919=EDGE_LOOP ( 'NONE', ( #33317, #19019, #6185, #10256 ) ) ;
#12923=B_SPLINE_CURVE_WITH_KNOTS ( 'NONE', 3,
 ( #2080, #30261, #10900, #8419, #39309, #8208, #4549, #36046, #27164, #23478, #4941, #32954, #17272, #23670, #1873, #33376, #36639, #23860, #1462, #14396, #17074, #17679, #13996, #20783, #11098, #26771, #7822, #26967, #17888, #39720, #2276 ),
 .UNSPECIFIED., .F., .F.,
 ( 4, 3, 3, 3, 3, 3, 3, 3, 3, 3, 4 ),
 ( 5.204170427930421283E-18, 3.077658087706037842E-05, 6.152638666999422099E-05, 9.267501192707186834E-05, 0.0001241882240135245381, 0.0001556618703051713265, 0.0001866161554452296491, 0.0002167966385861026736, 0.0002463805737537830189, 0.0002758761370306596458, 0.0002847094172290124217 ),
 .UNSPECIFIED. ) ;
#12924=EDGE_CURVE ( 'NONE', #5805, #18940, #4972, .T. ) ;
#12931=B_SPLINE_CURVE_WITH_KNOTS ( 'NONE', 3,
 ( #15052, #2733, #28848, #13191 ),
 .UNSPECIFIED., .F., .F.,
 ( 4, 4 ),
 ( 9.697399036122160616E-19, 6.391136169992784355E-06 ),
 .UNSPECIFIED. ) ;
#12935=VERTEX_POINT ( 'NONE', #2103 ) ;
#12938=CARTESIAN_POINT ( 'NONE',  ( -1.161450586000340790, -31.41865484090261518, 7.139196562012271485 ) ) ;
#12939=ORIENTED_EDGE ( 'NONE', *, *, #8395, .F. ) ;
#12940=CARTESIAN_POINT ( 'NONE',  ( -1.653803645021777902, -29.01370129510289431, 7.712764235869101093 ) ) ;
#12944=ORIENTED_EDGE ( 'NONE', *, *, #31401, .T. ) ;
#12948=CARTESIAN_POINT ( 'NONE',  ( 5.153279172109078488, -30.14225614731512337, 7.695279973900954751 ) ) ;
#12949=VECTOR ( 'NONE', #31409, 1000.000000000000114 ) ;
#12951=ORIENTED_EDGE ( 'NONE', *, *, #32559, .F. ) ;
#12955=CARTESIAN_POINT ( 'NONE',  ( 4.543174969189649026, -31.43502378668323161, 6.903372536218457256 ) ) ;
#12962=B_SPLINE_CURVE_WITH_KNOTS ( 'NONE', 3,
 ( #39761, #24734, #11336, #2316 ),
 .UNSPECIFIED., .F., .F.,
 ( 4, 4 ),
 ( 8.673617379884035472E-19, 6.391136169996031032E-06 ),
 .UNSPECIFIED. ) ;
#12966=ORIENTED_EDGE ( 'NONE', *, *, #19481, .T. ) ;
#12970=ORIENTED_EDGE ( 'NONE', *, *, #32659, .T. ) ;
#12974=CARTESIAN_POINT ( 'NONE',  ( 5.145066444271201966, -28.95006616558363888, 7.756742906098589074 ) ) ;
#12975=CARTESIAN_POINT ( 'NONE',  ( -0.4513664592218429861, -26.80950562565463358, 7.750000000000000888 ) ) ;
#12980=EDGE_CURVE ( 'NONE', #31466, #15576, #40353, .T. ) ;
#12981=EDGE_CURVE ( 'NONE', #18407, #19773, #30794, .T. ) ;
#12985=ORIENTED_EDGE ( 'NONE', *, *, #1279, .T. ) ;
#12992=CARTESIAN_POINT ( 'NONE',  ( 4.932661409899757210, -28.51521593988763570, 6.864276522220859711 ) ) ;
#12993=ORIENTED_EDGE ( 'NONE', *, *, #34334, .T. ) ;
#12995=CARTESIAN_POINT ( 'NONE',  ( 3.817924346030161509, -32.35669330361569962, 7.013842709614101167 ) ) ;
#13000=CARTESIAN_POINT ( 'NONE',  ( 2.970800673062078179, -26.41619320027978191, 7.761597726988848756 ) ) ;
#13004=CARTESIAN_POINT ( 'NONE',  ( -1.660455515657601300, -29.01040133911542540, 7.257242401810563237 ) ) ;
#13012=ORIENTED_EDGE ( 'NONE', *, *, #35537, .T. ) ;
#13016=CARTESIAN_POINT ( 'NONE',  ( -0.9575113486053222767, -31.84711263666175540, 7.695279973900954751 ) ) ;
#13018=CARTESIAN_POINT ( 'NONE',  ( 2.259077079022228318, -26.21614592499068408, 7.721096864323904185 ) ) ;
#13019=CARTESIAN_POINT ( 'NONE',  ( 3.576488244632886726, -26.73439304370792513, 6.979335674598003081 ) ) ;
#13020=CARTESIAN_POINT ( 'NONE',  ( 4.702397412420262768, -31.34397018411862845, 7.783750581861601958 ) ) ;
#13021=CARTESIAN_POINT ( 'NONE',  ( -0.5945065188923343014, -32.07860504069461172, 6.868387053540520704 ) ) ;
#13026=CARTESIAN_POINT ( 'NONE',  ( -0.8809027425463855643, -31.78283038357269419, 7.695279973900954751 ) ) ;
#13028=CARTESIAN_POINT ( 'NONE',  ( 1.729779804934170606, -32.96980315820380270, 7.661510568013096822 ) ) ;
#13029=CARTESIAN_POINT ( 'NONE',  ( 2.105750943142600029, -32.94567937155306225, 7.013842709614101167 ) ) ;
#13032=CARTESIAN_POINT ( 'NONE',  ( -1.480676134522186382, -28.36955016868974511, 7.784838882742138644 ) ) ;
#13033=EDGE_CURVE ( 'NONE', #9668, #13794, #30537, .T. ) ;
#13036=CARTESIAN_POINT ( 'NONE',  ( -1.439000463346111536, -30.89361514057134173, 7.139196562012272373 ) ) ;
#13043=CARTESIAN_POINT ( 'NONE',  ( 1.700390093233090871, -29.56993018339339940, 7.750000000000000888 ) ) ;
#13044=CARTESIAN_POINT ( 'NONE',  ( -1.629504578382812818, -30.64779913458552230, 7.750000000000000888 ) ) ;
#13049=CARTESIAN_POINT ( 'NONE',  ( -1.060034464505671403, -31.72168673584834053, 7.750000000000000888 ) ) ;
#13054=CARTESIAN_POINT ( 'NONE',  ( -1.667391206268897141, -30.03700422179043272, 6.863904403958576594 ) ) ;
#13058=ORIENTED_EDGE ( 'NONE', *, *, #19487, .F. ) ;
#13060=CARTESIAN_POINT ( 'NONE',  ( -1.585154604418644197, -30.77225614172792589, 7.762796336881262249 ) ) ;
#13064=CARTESIAN_POINT ( 'NONE',  ( 4.197725314243516692, -27.25233838877152692, 7.139196562012272373 ) ) ;
#13068=AXIS2_PLACEMENT_3D ( 'NONE', #32043, #19063, #31626 ) ;
#13069=EDGE_CURVE ( 'NONE', #37904, #21810, #12364, .T. ) ;
#13075=CARTESIAN_POINT ( 'NONE',  ( -1.526829923184012339, -28.21528965334980654, 7.013842709614101167 ) ) ;
#13077=DIRECTION ( 'NONE',  ( 0.7660444431189771253, 0.6427876096865405842, -0.000000000000000000 ) ) ;
#13080=CARTESIAN_POINT ( 'NONE',  ( 1.738310589916949978, -26.07012892756137035, 6.887161170156906209 ) ) ;
#13084=DIRECTION ( 'NONE',  ( 0.6605219282605377940, 0.000000000000000000, -0.7508067542896645907 ) ) ;
#13088=CARTESIAN_POINT ( 'NONE',  ( 2.272716057154847924, -26.11704110451741556, 7.701614758090453705 ) ) ;
#13090=DIRECTION ( 'NONE',  ( 0.6427876096865481337, -0.7660444431189707970, -0.000000000000000000 ) ) ;
#13091=ORIENTED_EDGE ( 'NONE', *, *, #31861, .F. ) ;
#13095=CARTESIAN_POINT ( 'NONE',  ( 1.195000870879840749, -26.11132176225047985, 7.771081512783698741 ) ) ;
#13099=CARTESIAN_POINT ( 'NONE',  ( 4.031469603769337162, -26.96264342876691700, 7.766640943994645774 ) ) ;
#13102=EDGE_LOOP ( 'NONE', ( #15968, #1081, #34348, #25716, #23085 ) ) ;
#13110=CARTESIAN_POINT ( 'NONE',  ( 1.025391769970868561, -33.00423873498635174, 6.869132338375688818 ) ) ;
#13112=EDGE_CURVE ( 'NONE', #17239, #29803, #33889, .T. ) ;
#13117=CARTESIAN_POINT ( 'NONE',  ( -1.361968219098981914, -25.54247520618363509, 6.894806418505347700 ) ) ;
#13120=CARTESIAN_POINT ( 'NONE',  ( -0.6411629333918610341, -32.17099039281331585, 7.754798119455333705 ) ) ;
#13122=DIRECTION ( 'NONE',  ( -1.000000000000000000, 0.000000000000000000, 0.000000000000000000 ) ) ;
#13127=CARTESIAN_POINT ( 'NONE',  ( 2.928305877310407368, -32.84746552919321516, 7.720710062488892689 ) ) ;
#13130=LINE ( 'NONE', #26105, #18429 ) ;
#13132=DIRECTION ( 'NONE',  ( -0.3420201433256725987, 0.9396926207859068736, -0.000000000000000000 ) ) ;
#13141=ORIENTED_EDGE ( 'NONE', *, *, #6339, .F. ) ;
#13146=CARTESIAN_POINT ( 'NONE',  ( -1.624655799086301533, -28.85995144147929992, 7.754798119455333705 ) ) ;
#13156=EDGE_CURVE ( 'NONE', #29262, #14158, #15273, .T. ) ;
#13158=EDGE_CURVE ( 'NONE', #15576, #38704, #1335, .T. ) ;
#13160=CARTESIAN_POINT ( 'NONE',  ( 4.535927232918584018, -31.44602833479315862, 6.979335674598002193 ) ) ;
#13165=ORIENTED_EDGE ( 'NONE', *, *, #21960, .T. ) ;
#13168=ADVANCED_FACE ( 'NONE', ( #35233 ), #9886, .F. ) ;
#13172=CARTESIAN_POINT ( 'NONE',  ( 1.700390093233090871, -29.56993018339339940, 6.800000000000000711 ) ) ;
#13175=VERTEX_POINT ( 'NONE', #16856 ) ;
#13176=CARTESIAN_POINT ( 'NONE',  ( 0.4715827230650022073, -32.74012475684295964, 7.784476445165072533 ) ) ;
#13178=CARTESIAN_POINT ( 'NONE',  ( 5.076139281392760161, -29.16456933348392511, 7.013842709614101167 ) ) ;
#13180=CARTESIAN_POINT ( 'NONE',  ( 5.158998514376012423, -29.06454096104016571, 7.771081512783696077 ) ) ;
#13181=CARTESIAN_POINT ( 'NONE',  ( -1.766085975226569404, -30.05319374170961666, 7.750000000000000888 ) ) ;
#13189=CARTESIAN_POINT ( 'NONE',  ( -1.477562859369297987, -28.36137111117319520, 6.894806418505348589 ) ) ;
#13191=CARTESIAN_POINT ( 'NONE',  ( -0.4513664592218429861, -26.80950562565463358, 7.750000000000000888 ) ) ;
#13192=ADVANCED_FACE ( 'NONE', ( #26355 ), #10680, .F. ) ;
#13198=CARTESIAN_POINT ( 'NONE',  ( 3.812057553938478893, -32.36114986992183873, 6.903112506833892326 ) ) ;
#13199=ORIENTED_EDGE ( 'NONE', *, *, #30745, .F. ) ;
#13206=CARTESIAN_POINT ( 'NONE',  ( 4.373635312142695852, -27.31077402155920097, 7.756742906098587298 ) ) ;
#13209=ORIENTED_EDGE ( 'NONE', *, *, #25349, .F. ) ;
#13213=CARTESIAN_POINT ( 'NONE',  ( 1.775729607206522065, -26.08305913168524626, 7.782861076432730840 ) ) ;
#13214=ADVANCED_FACE ( 'NONE', ( #5327 ), #2470, .F. ) ;
#13217=( BOUNDED_CURVE ( )  B_SPLINE_CURVE ( 3, ( #22043, #18945, #16052, #34621 ),
 .UNSPECIFIED., .F., .F. ) 
 B_SPLINE_CURVE_WITH_KNOTS ( ( 4, 4 ),
 ( 4.748221474220559735, 4.941946782021394924 ),
 .UNSPECIFIED. ) 
 CURVE ( )  GEOMETRIC_REPRESENTATION_ITEM ( )  RATIONAL_B_SPLINE_CURVE ( ( 1.000000000000000000, 0.9968749865767494445, 0.9968749865767494445, 1.000000000000000000 ) ) 
 REPRESENTATION_ITEM ( '' )  );
#13218=CARTESIAN_POINT ( 'NONE',  ( -0.1573688963480438519, -32.53621386746299038, 6.867199677474203234 ) ) ;
#13221=CARTESIAN_POINT ( 'NONE',  ( 2.272301947206582184, -26.21837579307170785, 7.748216051605119503 ) ) ;
#13223=CARTESIAN_POINT ( 'NONE',  ( 3.204051609024970659, -33.64229020702606476, 7.013842709614101167 ) ) ;
#13233=CARTESIAN_POINT ( 'NONE',  ( -1.498939527478906575, -28.41913694277257108, 7.756377446753163873 ) ) ;
#13238=ORIENTED_EDGE ( 'NONE', *, *, #4021, .F. ) ;
#13239=FACE_OUTER_BOUND ( 'NONE', #5462, .T. ) ;
#13242=CARTESIAN_POINT ( 'NONE',  ( 0.9485833586031139353, -32.88577924541437625, 6.876076431790004051 ) ) ;
#13243=CARTESIAN_POINT ( 'NONE',  ( 1.112807738419320458, -26.22108755103345246, 7.769368695748488207 ) ) ;
#13249=VECTOR ( 'NONE', #18336, 1000.000000000000000 ) ;
#13267=CARTESIAN_POINT ( 'NONE',  ( -1.543826794133986269, -28.25651525684694576, 7.751599049952173637 ) ) ;
#13270=CARTESIAN_POINT ( 'NONE',  ( 3.367954892094448205, -32.64715822689380786, 6.863805608295729499 ) ) ;
#13272=LINE ( 'NONE', #19666, #36389 ) ;
#13277=CIRCLE ( 'NONE', #38893, 3.499999999999999556 ) ;
#13287=CARTESIAN_POINT ( 'NONE',  ( 2.956026735610348233, -26.31784691181716340, 7.784725160561909441 ) ) ;
#13290=CARTESIAN_POINT ( 'NONE',  ( 3.948490735960236364, -26.89162167269672921, 7.767720160662274331 ) ) ;
#13291=ORIENTED_EDGE ( 'NONE', *, *, #11319, .T. ) ;
#13293=CARTESIAN_POINT ( 'NONE',  ( -1.720551146415195021, -28.88027794134619697, 7.780491323090172884 ) ) ;
#13295=CARTESIAN_POINT ( 'NONE',  ( -1.699609906766908374, -29.55367944812416070, 6.931117832418181912 ) ) ;
#13298=CARTESIAN_POINT ( 'NONE',  ( -1.797340250851707344, -29.44390463015740522, 7.750000000000000888 ) ) ;
#13299=ADVANCED_FACE ( 'NONE', ( #39905 ), #39693, .F. ) ;
#13300=CARTESIAN_POINT ( 'NONE',  ( 0.9127401033365564187, -32.98015121632014512, 6.916197352289366940 ) ) ;
#13305=CARTESIAN_POINT ( 'NONE',  ( 5.200304181073969190, -29.54472379604562704, 7.651421919295144036 ) ) ;
#13306=ORIENTED_EDGE ( 'NONE', *, *, #22760, .F. ) ;
#13307=CARTESIAN_POINT ( 'NONE',  ( -1.238405014327524922, -31.48339769696754331, 7.139344958878411695 ) ) ;
#13308=DIRECTION ( 'NONE',  ( 0.7660444431189770143, 0.6427876096865404731, -0.000000000000000000 ) ) ;
#13310=CARTESIAN_POINT ( 'NONE',  ( 5.144846875551112753, -28.94886861257825572, 7.635761828346576685 ) ) ;
#13314=CARTESIAN_POINT ( 'NONE',  ( -0.01902423455012235490, -32.61847323140942478, 7.710604733652635545 ) ) ;
#13315=CARTESIAN_POINT ( 'NONE',  ( -1.270178459801816206, -27.72063930510053709, 7.761113333117549473 ) ) ;
#13317=CARTESIAN_POINT ( 'NONE',  ( 1.664433243520564876, -26.17012032033359148, 7.703977250142848732 ) ) ;
#13318=CARTESIAN_POINT ( 'NONE',  ( -0.3285218188496327740, -26.84164346155765557, 6.911401339314955372 ) ) ;
#13319=CARTESIAN_POINT ( 'NONE',  ( 4.646307801825953376, -27.87241174337603766, 7.769368695748489095 ) ) ;
#13320=CARTESIAN_POINT ( 'NONE',  ( 4.812521983982041895, -27.96848237138598137, 7.013842709614101167 ) ) ;
#13325=B_SPLINE_CURVE_WITH_KNOTS ( 'NONE', 3,
 ( #35223, #39071, #16640, #20146, #29817, #32920, #10473, #1241, #1628, #35619, #6995, #13777, #19753, #10669, #19945, #7391, #19560, #16453, #29225, #26345, #23250, #29027, #830, #35816, #13361, #10274, #4522, #17042, #25936, #29621, #32331 ),
 .UNSPECIFIED., .F., .F.,
 ( 4, 3, 3, 3, 3, 3, 3, 3, 3, 3, 4 ),
 ( 0.000000000000000000, 2.999644130997832929E-05, 6.002588995695094977E-05, 8.960886084588270950E-05, 0.0001190604700446527250, 0.0001489538463052755965, 0.0001796139255493990746, 0.0002109707048517114154, 0.0002426195318110371997, 0.0002740640997890095992, 0.0002849778069099847449 ),
 .UNSPECIFIED. ) ;
#13329=LINE ( 'NONE', #23218, #9270 ) ;
#13330=CARTESIAN_POINT ( 'NONE',  ( -1.356998574253440948, -31.24811977623772918, 7.782861076432731728 ) ) ;
#13333=CIRCLE ( 'NONE', #29762, 3.499999999999999556 ) ;
#13338=LINE ( 'NONE', #10251, #34700 ) ;
#13340=EDGE_LOOP ( 'NONE', ( #67, #9718, #5935, #8061, #40267 ) ) ;
#13341=ORIENTED_EDGE ( 'NONE', *, *, #4988, .F. ) ;
#13345=VERTEX_POINT ( 'NONE', #36614 ) ;
#13346=VERTEX_POINT ( 'NONE', #11679 ) ;
#13348=CARTESIAN_POINT ( 'NONE',  ( 5.076139281392760161, -29.16456933348392511, 7.013842709614101167 ) ) ;
#13350=CARTESIAN_POINT ( 'NONE',  ( 4.540072660877648048, -31.43975234032491528, 6.911401339314955372 ) ) ;
#13356=VERTEX_POINT ( 'NONE', #14179 ) ;
#13357=CARTESIAN_POINT ( 'NONE',  ( 5.025435985552490159, -30.27990892530747047, 7.754798119455333705 ) ) ;
#13361=CARTESIAN_POINT ( 'NONE',  ( 0.4594594901768997985, -32.73538295328250314, 6.870716933885664623 ) ) ;
#13370=CARTESIAN_POINT ( 'NONE',  ( 5.070928005489710344, -29.12330485715137840, 6.868387053540519815 ) ) ;
#13372=DIRECTION ( 'NONE',  ( -0.3420201433256663259, -0.9396926207859092051, 0.000000000000000000 ) ) ;
#13374=CARTESIAN_POINT ( 'NONE',  ( 2.895822981304927879, -32.85599670560755925, 7.767720160662274331 ) ) ;
#13382=CARTESIAN_POINT ( 'NONE',  ( 1.699828613893618945, -33.06668477344420154, 7.767720160662275219 ) ) ;
#13384=CARTESIAN_POINT ( 'NONE',  ( 3.594851464545667952, -26.62696974998548782, 7.013842709614101167 ) ) ;
#13389=DIRECTION ( 'NONE',  ( -1.000000000000000000, -0.000000000000000000, -0.000000000000000000 ) ) ;
#13395=CARTESIAN_POINT ( 'NONE',  ( 3.814825531500412481, -32.35904579807917258, 7.009310105710486738 ) ) ;
#13399=CARTESIAN_POINT ( 'NONE',  ( -1.312560436656867724, -31.35097737660188244, 7.697032948437508182 ) ) ;
#13408=CYLINDRICAL_SURFACE ( 'NONE', #39203, 0.09010775117052842453 ) ;
#13414=CARTESIAN_POINT ( 'NONE',  ( 3.559755418260376114, -26.72339534466646427, 7.013842709614101167 ) ) ;
#13417=CARTESIAN_POINT ( 'NONE',  ( 1.700390093233090871, -29.56993018339339940, 7.800000000000000711 ) ) ;
#13418=CARTESIAN_POINT ( 'NONE',  ( 0.7149948906900660539, -26.31585638355339185, 7.013842709614101167 ) ) ;
#13424=CARTESIAN_POINT ( 'NONE',  ( 3.322058374886247556, -32.55827286526241693, 7.778050822775631090 ) ) ;
#13430=ORIENTED_EDGE ( 'NONE', *, *, #12687, .T. ) ;
#13432=LINE ( 'NONE', #9747, #33698 ) ;
#13443=DIRECTION ( 'NONE',  ( -0.000000000000000000, -0.000000000000000000, -1.000000000000000000 ) ) ;
#13444=CARTESIAN_POINT ( 'NONE',  ( 1.236065439282523437, -26.10086653224289321, 6.875780273367531947 ) ) ;
#13451=ORIENTED_EDGE ( 'NONE', *, *, #35088, .F. ) ;
#13453=( BOUNDED_CURVE ( )  B_SPLINE_CURVE ( 3, ( #23367, #39199, #7117, #32850 ),
 .UNSPECIFIED., .F., .F. ) 
 B_SPLINE_CURVE_WITH_KNOTS ( ( 4, 4 ),
 ( 1.381924640371168467, 1.574767692156078258 ),
 .UNSPECIFIED. ) 
 CURVE ( )  GEOMETRIC_REPRESENTATION_ITEM ( )  RATIONAL_B_SPLINE_CURVE ( ( 1.000000000000000000, 0.9969033633783032089, 0.9969033633783032089, 1.000000000000000000 ) ) 
 REPRESENTATION_ITEM ( '' )  );
#13455=CARTESIAN_POINT ( 'NONE',  ( -1.712075311290714108, -28.79206138794767611, 6.899963164400790383 ) ) ;
#13461=B_SPLINE_CURVE_WITH_KNOTS ( 'NONE', 3,
 ( #2196, #37167, #36760, #8546, #36557, #33498, #21738, #8745, #14714, #8336 ),
 .UNSPECIFIED., .F., .F.,
 ( 4, 3, 3, 4 ),
 ( 8.673617379884035472E-19, 3.025570593003197716E-05, 6.051145698344131290E-05, 6.468151674593491419E-05 ),
 .UNSPECIFIED. ) ;
#13468=AXIS2_PLACEMENT_3D ( 'NONE', #38579, #35331, #10385 ) ;
#13469=VECTOR ( 'NONE', #1198, 1000.000000000000227 ) ;
#13470=CARTESIAN_POINT ( 'NONE',  ( 1.700390093233090871, -29.56993018339339940, 7.800000000000000711 ) ) ;
#13471=ORIENTED_EDGE ( 'NONE', *, *, #5354, .T. ) ;
#13476=CARTESIAN_POINT ( 'NONE',  ( 5.110926626256952154, -30.35622219256811150, 6.912143950357345190 ) ) ;
#13477=FACE_OUTER_BOUND ( 'NONE', #33098, .T. ) ;
#13479=CARTESIAN_POINT ( 'NONE',  ( 5.094086365274872463, -29.77691027265591828, 6.979335674598010186 ) ) ;
#13487=ADVANCED_FACE ( 'NONE', ( #40500 ), #25295, .F. ) ;
#13494=CARTESIAN_POINT ( 'NONE',  ( -0.4881783139857213683, -26.85647531738399252, 7.784725160561908552 ) ) ;
#13496=CARTESIAN_POINT ( 'NONE',  ( 2.326171464738295835, -32.91184545387483951, 7.703977250142848732 ) ) ;
#13499=CARTESIAN_POINT ( 'NONE',  ( 5.054793046568992310, -30.12489038615697012, 7.693875151218752428 ) ) ;
#13502=ORIENTED_EDGE ( 'NONE', *, *, #5841, .T. ) ;
#13506=CARTESIAN_POINT ( 'NONE',  ( -0.6393902300633312885, -25.40346598495485253, 7.013842709614101167 ) ) ;
#13507=ORIENTED_EDGE ( 'NONE', *, *, #21772, .T. ) ;
#13510=CARTESIAN_POINT ( 'NONE',  ( 0.9376568889370265891, -32.98581865358281107, 6.883550009118462931 ) ) ;
#13511=DIRECTION ( 'NONE',  ( 0.000000000000000000, -0.7126435865141276249, 0.7015262779114413982 ) ) ;
#13515=ORIENTED_EDGE ( 'NONE', *, *, #18923, .F. ) ;
#13518=CARTESIAN_POINT ( 'NONE',  ( -0.9367813558391736573, -31.71593409404636787, 6.892063359921931642 ) ) ;
#13519=CARTESIAN_POINT ( 'NONE',  ( 4.282054009272330930, -27.35746286227295343, 7.680992449362119778 ) ) ;
#13525=B_SPLINE_CURVE_WITH_KNOTS ( 'NONE', 3,
 ( #26270, #13496, #38995, #26069, #22581, #20270, #10405, #32853, #1557, #4642, #35548, #17176, #32056, #7317, #3862, #25859, #38398, #40030, #8313, #30156, #11800, #39831, #8724, #11602, #21304 ),
 .UNSPECIFIED., .F., .F.,
 ( 4, 3, 3, 3, 3, 3, 3, 3, 4 ),
 ( 6.468151674593655405E-05, 9.076621574722012922E-05, 0.0001210204262067964080, 0.0001512763324577413155, 0.0001815301820994202919, 0.0002117781465860697028, 0.0002420274594459747739, 0.0002722905548971149212, 0.0002816827545175575411 ),
 .UNSPECIFIED. ) ;
#13527=CARTESIAN_POINT ( 'NONE',  ( -0.8851723638970985242, -31.77784023144311476, 7.661510568013098599 ) ) ;
#13528=CARTESIAN_POINT ( 'NONE',  ( 3.930147992295620174, -26.87211838299319311, 7.737115613922535218 ) ) ;
#13532=CARTESIAN_POINT ( 'NONE',  ( -0.3879985392179198245, -26.88688304283302344, 6.863904403958575706 ) ) ;
#13541=CARTESIAN_POINT ( 'NONE',  ( 4.818790771865216982, -30.92476493623475164, 6.929923840112062194 ) ) ;
#13542=CARTESIAN_POINT ( 'NONE',  ( -1.229875790497353405, -27.65589205167745490, 6.961115707816238007 ) ) ;
#13544=ORIENTED_EDGE ( 'NONE', *, *, #31523, .F. ) ;
#13548=ORIENTED_EDGE ( 'NONE', *, *, #30724, .F. ) ;
#13552=ORIENTED_EDGE ( 'NONE', *, *, #20624, .T. ) ;
#13555=CARTESIAN_POINT ( 'NONE',  ( 5.033237860645672690, -30.24233315725131277, 6.870716933885662847 ) ) ;
#13556=CARTESIAN_POINT ( 'NONE',  ( 4.616164590409697510, -31.31871807265113006, 6.887041543973317914 ) ) ;
#13564=ORIENTED_EDGE ( 'NONE', *, *, #5052, .F. ) ;
#13577=CARTESIAN_POINT ( 'NONE',  ( 5.078024580013459577, -29.18059064813925829, 6.988553391373222290 ) ) ;
#13584=CARTESIAN_POINT ( 'NONE',  ( 1.887380280259158383, -26.17507603778478753, 7.013842709614101167 ) ) ;
#13591=LINE ( 'NONE', #23272, #15926 ) ;
#13601=CARTESIAN_POINT ( 'NONE',  ( 3.813414093473169064, -32.36011468883553732, 7.006908160621414972 ) ) ;
#13607=ORIENTED_EDGE ( 'NONE', *, *, #26602, .F. ) ;
#13609=CARTESIAN_POINT ( 'NONE',  ( -1.599498859172472809, -28.40342561769650231, 7.670465701733752972 ) ) ;
#13620=B_SPLINE_CURVE_WITH_KNOTS ( 'NONE', 3,
 ( #23028, #35595, #7365, #32495, #8928, #24382, #15317, #18194, #30988, #33671, #31386, #37539, #21915, #8723, #25002, #14138, #26714, #5863, #9138, #15522, #5656, #27474, #9335, #15113, #24801 ),
 .UNSPECIFIED., .F., .F.,
 ( 4, 3, 3, 3, 3, 3, 3, 3, 4 ),
 ( 6.468151674593491419E-05, 9.076621574722202658E-05, 0.0001210204262067985493, 0.0001512763324577458149, 0.0001815301820994193703, 0.0002117781465860703533, 0.0002420274594459763189, 0.0002722905548971134033, 0.0002816827545175533670 ),
 .UNSPECIFIED. ) ;
#13622=EDGE_CURVE ( 'NONE', #38197, #19595, #31874, .T. ) ;
#13624=CARTESIAN_POINT ( 'NONE',  ( 2.369913428640782804, -26.23648987328603610, 7.782034975670476307 ) ) ;
#13626=CARTESIAN_POINT ( 'NONE',  ( 3.573240303917499361, -26.73224942468579357, 6.988553391373220514 ) ) ;
#13628=EDGE_CURVE ( 'NONE', #463, #8120, #11829, .T. ) ;
#13630=CARTESIAN_POINT ( 'NONE',  ( -2.689021718275399042, -31.29716697405881476, 7.754798119455333705 ) ) ;
#13631=CARTESIAN_POINT ( 'NONE',  ( 3.938183569304232634, -26.87878085491623636, 7.638132480492516585 ) ) ;
#13635=CARTESIAN_POINT ( 'NONE',  ( -1.699609906766908818, -29.56993018339339940, 7.222147233343546802 ) ) ;
#13636=CARTESIAN_POINT ( 'NONE',  ( 2.234964567898549692, -32.92764222152831621, 6.887041543973314361 ) ) ;
#13650=CARTESIAN_POINT ( 'NONE',  ( 5.049345966743696401, -28.55282231546490479, 6.931070083220556732 ) ) ;
#13652=CARTESIAN_POINT ( 'NONE',  ( 0.3491796791923181265, -32.79858786375961444, 6.890920332093119605 ) ) ;
#13655=CARTESIAN_POINT ( 'NONE',  ( -1.696743409393115520, -30.44007608545301125, 7.501983001166816933 ) ) ;
#13661=ORIENTED_EDGE ( 'NONE', *, *, #7555, .T. ) ;
#13664=CARTESIAN_POINT ( 'NONE',  ( -1.735425026873168575, -28.90271622936575113, 6.872994525451590953 ) ) ;
#13668=LINE ( 'NONE', #7282, #28019 ) ;
#13672=ORIENTED_EDGE ( 'NONE', *, *, #7014, .F. ) ;
#13673=AXIS2_PLACEMENT_3D ( 'NONE', #9199, #21576, #6542 ) ;
#13676=VERTEX_POINT ( 'NONE', #22416 ) ;
#13680=CARTESIAN_POINT ( 'NONE',  ( -2.735299443412492426, -31.17001996922091678, 7.635761828346577573 ) ) ;
#13681=CIRCLE ( 'NONE', #4489, 3.449999999999999734 ) ;
#13682=CARTESIAN_POINT ( 'NONE',  ( -0.9856834644577864291, -31.80018438340522025, 7.778495531946295394 ) ) ;
#13686=CARTESIAN_POINT ( 'NONE',  ( 3.301837905240542881, -32.68206207414233688, 7.013842709614101167 ) ) ;
#13687=CARTESIAN_POINT ( 'NONE',  ( 5.128444259610362543, -30.27593629695848421, 6.864216812847430127 ) ) ;
#13688=CARTESIAN_POINT ( 'NONE',  ( 5.199619722107929221, -29.64405277551909279, 6.867280401193710304 ) ) ;
#13690=CARTESIAN_POINT ( 'NONE',  ( 5.095244238841699413, -29.75692037041947913, 7.013842709614101167 ) ) ;
#13697=B_SPLINE_CURVE_WITH_KNOTS ( 'NONE', 3,
 ( #36651, #24499, #21010, #12132, #36855, #30696, #27590, #37052, #18310, #6182 ),
 .UNSPECIFIED., .F., .F.,
 ( 4, 3, 3, 4 ),
 ( 1.022834283856302764E-18, 3.025570593003066596E-05, 6.051145698344103507E-05, 6.468151674593461604E-05 ),
 .UNSPECIFIED. ) ;
#13702=CARTESIAN_POINT ( 'NONE',  ( 2.881058359821971226, -26.27508231979332010, 7.750000000000000000 ) ) ;
#13704=DIRECTION ( 'NONE',  ( 0.9848077530122103518, -0.1736481776669172583, -0.000000000000000000 ) ) ;
#13706=CARTESIAN_POINT ( 'NONE',  ( 1.122058404042096447, -26.12935236771179603, 7.781480525794718162 ) ) ;
#13710=ORIENTED_EDGE ( 'NONE', *, *, #38903, .T. ) ;
#13713=B_SPLINE_CURVE_WITH_KNOTS ( 'NONE', 3,
 ( #9783, #34930, #29334, #19859, #10584, #29537, #23749, #36320, #14277, #14072, #26255, #1350, #10387, #26846, #13884, #7299, #23156, #32431, #20657, #35528, #17156, #4434, #1539, #39387, #1153, #17556, #35926, #26050, #38978, #36123, #11178 ),
 .UNSPECIFIED., .F., .F.,
 ( 4, 3, 3, 3, 3, 3, 3, 3, 3, 3, 4 ),
 ( 1.084202172485504434E-18, 3.077658087705642108E-05, 6.152638666998993839E-05, 9.267501192706701653E-05, 0.0001241882240135197676, 0.0001556618703051697815, 0.0001866161554452206231, 0.0002167966385861002613, 0.0002463805737537787905, 0.0002758761370306537911, 0.0002847094172290030433 ),
 .UNSPECIFIED. ) ;
#13718=CARTESIAN_POINT ( 'NONE',  ( 0.9066789574456146639, -32.97874561297109608, 6.974994249511788702 ) ) ;
#13721=CARTESIAN_POINT ( 'NONE',  ( 3.443786484529058889, -26.65091147862827370, 7.785868773668302545 ) ) ;
#13726=ADVANCED_FACE ( 'NONE', ( #32293 ), #19910, .F. ) ;
#13728=CARTESIAN_POINT ( 'NONE',  ( -0.6306894173035869633, -32.17721693801968996, 7.766640943994337576 ) ) ;
#13735=CARTESIAN_POINT ( 'NONE',  ( 6.074096823854431726, -32.03256286660679564, 7.695279973900954751 ) ) ;
#13736=CARTESIAN_POINT ( 'NONE',  ( -1.296339748590412677, -27.78971074760038462, 7.785096263473211486 ) ) ;
#13738=CARTESIAN_POINT ( 'NONE',  ( 1.665718984681162418, -26.17010605203765650, 7.712764235869103757 ) ) ;
#13741=CARTESIAN_POINT ( 'NONE',  ( 3.855327937537480487, -32.32757912347058493, 7.754798119455333705 ) ) ;
#13749=CARTESIAN_POINT ( 'NONE',  ( -0.4068137048510813703, -26.77534493328523979, 6.912143950357340749 ) ) ;
#13750=CARTESIAN_POINT ( 'NONE',  ( -1.230256760684643291, -27.65647541743870974, 6.941203072598475465 ) ) ;
#13751=CARTESIAN_POINT ( 'NONE',  ( 2.324462049692062937, -26.13488154514125128, 7.778495531946297170 ) ) ;
#13756=VERTEX_POINT ( 'NONE', #13741 ) ;
#13762=VERTEX_POINT ( 'NONE', #791 ) ;
#13763=CARTESIAN_POINT ( 'NONE',  ( 0.03162470699431464694, -32.53223031769636009, 7.695279973900954751 ) ) ;
#13765=CARTESIAN_POINT ( 'NONE',  ( 3.963564119169153077, -32.23977037706391258, 7.640616322432101981 ) ) ;
#13766=DIRECTION ( 'NONE',  ( 0.000000000000000000, -0.6834397476448824671, 0.7300069255418740743 ) ) ;
#13771=VERTEX_POINT ( 'NONE', #13320 ) ;
#13773=EDGE_CURVE ( 'NONE', #21380, #36954, #3046, .T. ) ;
#13777=CARTESIAN_POINT ( 'NONE',  ( 0.3520804393569469948, -32.69116280221577853, 6.911401339314952708 ) ) ;
#13780=CARTESIAN_POINT ( 'NONE',  ( -1.303108374136985104, -31.16335321463953534, 7.754798119455333705 ) ) ;
#13781=EDGE_LOOP ( 'NONE', ( #14585, #21204, #9710, #17041, #17951 ) ) ;
#13784=CARTESIAN_POINT ( 'NONE',  ( 1.754540994691119460, -33.27093018339341768, 7.695279973900954751 ) ) ;
#13785=CIRCLE ( 'NONE', #23643, 3.499999999999999556 ) ;
#13790=CARTESIAN_POINT ( 'NONE',  ( 3.558396595903837056, -26.60381962644626697, 7.750000000000000888 ) ) ;
#13792=CARTESIAN_POINT ( 'NONE',  ( -1.645707253693945438, -30.17297881286834027, 7.756377446753163873 ) ) ;
#13794=VERTEX_POINT ( 'NONE', #20707 ) ;
#13798=EDGE_CURVE ( 'NONE', #31681, #12012, #8139, .T. ) ;
#13803=CARTESIAN_POINT ( 'NONE',  ( 5.142603739873976565, -28.93654719523409824, 7.737115613922530777 ) ) ;
#13807=CARTESIAN_POINT ( 'NONE',  ( 3.868607535801338315, -32.31746327423868337, 6.863784140767623221 ) ) ;
#13808=ORIENTED_EDGE ( 'NONE', *, *, #12467, .T. ) ;
#13814=CARTESIAN_POINT ( 'NONE',  ( -0.8980191362577285563, -27.22509128144364610, 7.750000000000000888 ) ) ;
#13818=ORIENTED_EDGE ( 'NONE', *, *, #26041, .T. ) ;
#13821=DIRECTION ( 'NONE',  ( -0.6502177225477864253, -0.3754033771448399559, 0.6605219282605377940 ) ) ;
#13833=CARTESIAN_POINT ( 'NONE',  ( 3.923398576026549289, -26.86655477908580281, 7.678495282201406980 ) ) ;
#13837=CARTESIAN_POINT ( 'NONE',  ( -1.799514919472523955, -29.59631703906507738, 7.736930692279464949 ) ) ;
#13838=CARTESIAN_POINT ( 'NONE',  ( -1.589323393843971477, -28.37905787987142148, 7.762796336881261361 ) ) ;
#13839=CARTESIAN_POINT ( 'NONE',  ( -0.4574210171174863948, -32.19744825413003753, 7.693875151218751540 ) ) ;
#13843=FACE_OUTER_BOUND ( 'NONE', #38550, .T. ) ;
#13845=CARTESIAN_POINT ( 'NONE',  ( -1.348517286369409263, -27.85116208076715694, 7.695279973900954751 ) ) ;
#13847=DIRECTION ( 'NONE',  ( 0.1736481776669404897, -0.9848077530122062440, -0.000000000000000000 ) ) ;
#13850=CARTESIAN_POINT ( 'NONE',  ( 0.4695943777967604427, -26.29347754267606874, 7.686927408461904143 ) ) ;
#13851=CARTESIAN_POINT ( 'NONE',  ( -1.445707822656724373, -28.28067938226085332, 6.865312560952602894 ) ) ;
#13853=PLANE ( 'NONE',  #25387 ) ;
#13854=CARTESIAN_POINT ( 'NONE',  ( 4.391539421710277225, -31.80772365946451430, 7.638132480492513032 ) ) ;
#13865=CARTESIAN_POINT ( 'NONE',  ( -1.727598588168507421, -28.86353026780088982, 6.863641214238739074 ) ) ;
#13869=AXIS2_PLACEMENT_3D ( 'NONE', #30404, #24218, #26709 ) ;
#13870=EDGE_CURVE ( 'NONE', #16321, #5140, #8324, .T. ) ;
#13879=LINE ( 'NONE', #26044, #3293 ) ;
#13882=B_SPLINE_CURVE_WITH_KNOTS ( 'NONE', 3,
 ( #32741, #39086, #32539, #4338, #23457, #20551, #4918, #17448, #30038, #36616, #18277, #5329, #21181, #9015, #2056, #36820, #40306, #2254, #17864, #34176, #27753, #9220, #8400, #2676, #14779 ),
 .UNSPECIFIED., .F., .F.,
 ( 4, 3, 3, 3, 3, 3, 3, 3, 4 ),
 ( 6.468151674593884443E-05, 9.076621574721885528E-05, 0.0001210204262067969636, 0.0001512763324577432399, 0.0001815301820994194787, 0.0002117781465860675073, 0.0002420274594459734729, 0.0002722905548971120480, 0.0002816827545175622032 ),
 .UNSPECIFIED. ) ;
#13883=CARTESIAN_POINT ( 'NONE',  ( 3.290306094747008636, -32.68797150366361137, 6.912143950357342526 ) ) ;
#13884=CARTESIAN_POINT ( 'NONE',  ( -1.082483681122714980, -31.69258464036479239, 6.887547729233692628 ) ) ;
#13886=CARTESIAN_POINT ( 'NONE',  ( 2.673814629606090065, -32.82760982625630675, 6.911401339314953596 ) ) ;
#13887=PLANE ( 'NONE',  #21077 ) ;
#13890=DIRECTION ( 'NONE',  ( 0.9848077530122080203, 0.1736481776669307198, -0.000000000000000000 ) ) ;
#13891=CARTESIAN_POINT ( 'NONE',  ( 2.164714747183682952, -33.03899383454390204, 6.875780273367530171 ) ) ;
#13893=ORIENTED_EDGE ( 'NONE', *, *, #31027, .F. ) ;
#13896=CARTESIAN_POINT ( 'NONE',  ( 2.272716057154847924, -26.11704110451741556, 7.695279973900954751 ) ) ;
#13900=CARTESIAN_POINT ( 'NONE',  ( 2.885910282437001761, -26.27682094667402879, 7.756742906098588186 ) ) ;
#13903=CARTESIAN_POINT ( 'NONE',  ( 5.107338069706632844, -29.53735381186853814, 7.257242401810562349 ) ) ;
#13904=ORIENTED_EDGE ( 'NONE', *, *, #18077, .F. ) ;
#13917=AXIS2_PLACEMENT_3D ( 'NONE', #16246, #18511, #9662 ) ;
#13919=CARTESIAN_POINT ( 'NONE',  ( 4.718383115759797519, -27.79743845850708794, 7.737115613922531665 ) ) ;
#13920=CARTESIAN_POINT ( 'NONE',  ( -1.699583094839331787, -29.58343279012807159, 7.635761828346577573 ) ) ;
#13922=CARTESIAN_POINT ( 'NONE',  ( -1.495543489590137165, -30.73010626234981402, 7.769368695748488207 ) ) ;
#13923=CARTESIAN_POINT ( 'NONE',  ( 3.901581986397568702, -26.97862765183199585, 7.779495906702011965 ) ) ;
#13924=CARTESIAN_POINT ( 'NONE',  ( -1.276156623011316382, -27.74234360012602352, 7.776484688137388801 ) ) ;
#13925=DIRECTION ( 'NONE',  ( 0.7660444431189771253, 0.6427876096865405842, -0.000000000000000000 ) ) ;
#13926=CARTESIAN_POINT ( 'NONE',  ( 4.401417849205680355, -27.34407100962124559, 6.894806418505347700 ) ) ;
#13928=CARTESIAN_POINT ( 'NONE',  ( 4.176116573831426315, -31.90033323721567271, 6.903372536218459921 ) ) ;
#13929=( BOUNDED_CURVE ( )  B_SPLINE_CURVE ( 3, ( #5215, #27842, #11980, #8489 ),
 .UNSPECIFIED., .F., .T. ) 
 B_SPLINE_CURVE_WITH_KNOTS ( ( 4, 4 ),
 ( 4.748221474220559735, 4.941946782021393147 ),
 .UNSPECIFIED. ) 
 CURVE ( )  GEOMETRIC_REPRESENTATION_ITEM ( )  RATIONAL_B_SPLINE_CURVE ( ( 1.000000000000000000, 0.9968749865767494445, 0.9968749865767494445, 1.000000000000000000 ) ) 
 REPRESENTATION_ITEM ( '' )  );
#13930=CARTESIAN_POINT ( 'NONE',  ( 3.858201203583684791, -26.94241211265677194, 7.695279973900954751 ) ) ;
#13933=EDGE_CURVE ( 'NONE', #27494, #1015, #8387, .T. ) ;
#13939=CARTESIAN_POINT ( 'NONE',  ( -0.4998380263676178714, -26.84796820482366897, 6.870737987065016483 ) ) ;
#13940=CARTESIAN_POINT ( 'NONE',  ( 3.791157483716739218, -32.25110375459131973, 7.754798119455333705 ) ) ;
#13941=CARTESIAN_POINT ( 'NONE',  ( 2.356131281712445791, -26.14680573639735428, 7.785344483711591934 ) ) ;
#13942=ORIENTED_EDGE ( 'NONE', *, *, #16233, .F. ) ;
#13958=DIRECTION ( 'NONE',  ( 0.000000000000000000, -0.7508067542896625923, -0.6605219282605402364 ) ) ;
#13959=CARTESIAN_POINT ( 'NONE',  ( -1.261910041069867372, -27.90116479715461750, 7.703977250142847844 ) ) ;
#13961=CARTESIAN_POINT ( 'NONE',  ( 4.250209030067871652, -31.97748039036408230, 7.387053503561884504 ) ) ;
#13964=CARTESIAN_POINT ( 'NONE',  ( 5.143923624032054498, -30.17768819491086063, 7.767720160662274331 ) ) ;
#13968=CARTESIAN_POINT ( 'NONE',  ( 4.045228995182856835, -26.97152095390259063, 7.750000000000000888 ) ) ;
#13971=CARTESIAN_POINT ( 'NONE',  ( -0.5125101069461960313, -26.98863734761392053, 7.693875151218752428 ) ) ;
#13972=ORIENTED_EDGE ( 'NONE', *, *, #35812, .T. ) ;
#13974=DIRECTION ( 'NONE',  ( 0.000000000000000000, -1.000000000000000000, 0.000000000000000000 ) ) ;
#13980=AXIS2_PLACEMENT_3D ( 'NONE', #35940, #29152, #16978 ) ;
#13982=CARTESIAN_POINT ( 'NONE',  ( -1.163435125605633225, -27.73728167763614039, 6.871394612369936539 ) ) ;
#13983=EDGE_LOOP ( 'NONE', ( #38701, #2668, #35614, #32697 ) ) ;
#13986=CARTESIAN_POINT ( 'NONE',  ( -1.649184783451180136, -30.58499090532986386, 6.941203072598473689 ) ) ;
#13993=DIRECTION ( 'NONE',  ( -0.1736481776669340227, 0.9848077530122073542, -0.000000000000000000 ) ) ;
#13996=CARTESIAN_POINT ( 'NONE',  ( 4.823128680976433103, -27.98926455409796432, 6.961115707816236231 ) ) ;
#13997=CARTESIAN_POINT ( 'NONE',  ( 4.281682929012584182, -27.35702998321412593, 7.703977250142848732 ) ) ;
#14001=CARTESIAN_POINT ( 'NONE',  ( -1.312586491988795956, -31.35093330168482595, 7.698786668945012401 ) ) ;
#14003=CARTESIAN_POINT ( 'NONE',  ( 0.01005603839840271338, -26.61987263535688797, 7.775108481317159814 ) ) ;
#14004=CARTESIAN_POINT ( 'NONE',  ( 4.403058967736086515, -27.36916703378302174, 7.785344483711591934 ) ) ;
#14011=DIRECTION ( 'NONE',  ( -0.6427876096865328126, -0.7660444431189835646, -0.000000000000000000 ) ) ;
#14017=CARTESIAN_POINT ( 'NONE',  ( 1.700390093233090871, -29.56993018339339940, 7.800000000000000711 ) ) ;
#14019=FACE_OUTER_BOUND ( 'NONE', #31935, .T. ) ;
#14021=AXIS2_PLACEMENT_3D ( 'NONE', #26300, #16800, #7747 ) ;
#14022=CARTESIAN_POINT ( 'NONE',  ( 0.09322448663572599492, -26.46073943648378091, 6.887547729233691740 ) ) ;
#14025=DIRECTION ( 'NONE',  ( 0.000000000000000000, 0.000000000000000000, 1.000000000000000000 ) ) ;
#14029=CARTESIAN_POINT ( 'NONE',  ( 4.316965410430217531, -31.74099757282072076, 7.748216051605115062 ) ) ;
#14030=VERTEX_POINT ( 'NONE', #23640 ) ;
#14032=DIRECTION ( 'NONE',  ( -1.000000000000000000, 0.000000000000000000, 0.000000000000000000 ) ) ;
#14034=CARTESIAN_POINT ( 'NONE',  ( -1.345438465516780369, -27.84570974966549173, 7.660770905198783787 ) ) ;
#14036=B_SPLINE_CURVE_WITH_KNOTS ( 'NONE', 3,
 ( #30705, #40149, #5370, #19300, #2511, #31871, #11523, #17908, #14822, #15035 ),
 .UNSPECIFIED., .F., .F.,
 ( 4, 3, 3, 4 ),
 ( 4.982613841084487634E-18, 3.077658087705387998E-05, 6.152638666998344673E-05, 7.730982992130896385E-05 ),
 .UNSPECIFIED. ) ;
#14038=CARTESIAN_POINT ( 'NONE',  ( 1.736346942945643512, -32.96974004645320377, 7.695279973900954751 ) ) ;
#14041=CARTESIAN_POINT ( 'NONE',  ( 4.984671627384348547, -28.36018029005467866, 7.635761828346577573 ) ) ;
#14042=CARTESIAN_POINT ( 'NONE',  ( 0.4741610271200560334, -32.84809465111302984, 6.894806418505347700 ) ) ;
#14043=CARTESIAN_POINT ( 'NONE',  ( -1.699178655868960552, -29.51577928193538369, 7.785387725071490905 ) ) ;
#14044=ORIENTED_EDGE ( 'NONE', *, *, #9204, .F. ) ;
#14053=CARTESIAN_POINT ( 'NONE',  ( 5.116398603051176330, -28.77698600466689882, 7.139344958878411695 ) ) ;
#14061=EDGE_CURVE ( 'NONE', #15530, #38080, #19236, .T. ) ;
#14067=ORIENTED_EDGE ( 'NONE', *, *, #31485, .F. ) ;
#14068=CARTESIAN_POINT ( 'NONE',  ( 5.162379329697287744, -29.05540582370486291, 6.863805608295729499 ) ) ;
#14071=CARTESIAN_POINT ( 'NONE',  ( 3.281363509912449850, -32.69251293742141939, 6.951256099901584662 ) ) ;
#14072=CARTESIAN_POINT ( 'NONE',  ( -1.053466190009290315, -31.73008655996581595, 6.865482280155370098 ) ) ;
#14075=DIRECTION ( 'NONE',  ( 0.9396926207859126468, -0.3420201433256568335, -0.000000000000000000 ) ) ;
#14076=ADVANCED_FACE ( 'NONE', ( #27137 ), #24040, .F. ) ;
#14078=VERTEX_POINT ( 'NONE', #24249 ) ;
#14085=CARTESIAN_POINT ( 'NONE',  ( -1.797258899342013549, -29.44812577374269580, 7.754798119455333705 ) ) ;
#14088=CARTESIAN_POINT ( 'NONE',  ( 2.140846989427893643, -33.04210496623404225, 7.013842709614101167 ) ) ;
#14095=B_SPLINE_CURVE_WITH_KNOTS ( 'NONE', 3,
 ( #28037, #12394, #24962, #37496, #9293, #21871, #35459, #4161, #29265, #19984, #22890, #35059, #23091, #35656, #1077, #16678, #38715, #26382, #32568, #31963, #23284, #6833, #4557, #10705, #35853, #22695, #38913, #28659, #465, #4364, #16884 ),
 .UNSPECIFIED., .F., .F.,
 ( 4, 3, 3, 3, 3, 3, 3, 3, 3, 3, 4 ),
 ( 6.484403375994724850E-05, 8.983333709522357997E-05, 0.0001203539973219380516, 0.0001514144607149691020, 0.0001828916862241622594, 0.0002144221682127272230, 0.0002455195857862213201, 0.0002758614570916287823, 0.0003055381793602585799, 0.0003350143730643718900, 0.0003497271997307932457 ),
 .UNSPECIFIED. ) ;
#14098=LINE ( 'NONE', #29557, #34877 ) ;
#14102=CARTESIAN_POINT ( 'NONE',  ( 4.040074159915059582, -27.10297285337844286, 6.929923840112066635 ) ) ;
#14105=DIRECTION ( 'NONE',  ( -0.000000000000000000, -0.000000000000000000, -1.000000000000000000 ) ) ;
#14111=CARTESIAN_POINT ( 'NONE',  ( -0.4747269484695719743, -32.18314005917732601, 7.635761828346577573 ) ) ;
#14116=CARTESIAN_POINT ( 'NONE',  ( -0.08065709997538077214, -26.55697965350343281, 7.695279973900954751 ) ) ;
#14118=ADVANCED_FACE ( 'NONE', ( #4716 ), #33128, .T. ) ;
#14119=EDGE_CURVE ( 'NONE', #109, #1708, #5276, .T. ) ;
#14121=CARTESIAN_POINT ( 'NONE',  ( 3.967042426631197216, -32.23682145114030817, 7.743886751744254227 ) ) ;
#14123=CARTESIAN_POINT ( 'NONE',  ( 4.256963712960452284, -31.81136415787042537, 6.874555630061438549 ) ) ;
#14124=CARTESIAN_POINT ( 'NONE',  ( 2.277526804980155362, -33.02201842327861669, 6.894806418505347700 ) ) ;
#14132=CARTESIAN_POINT ( 'NONE',  ( 1.669309969508061764, -33.06979218437418666, 6.894806418505347700 ) ) ;
#14134=CARTESIAN_POINT ( 'NONE',  ( -1.236334162535101644, -27.66580709588378539, 6.998987538705434552 ) ) ;
#14136=EDGE_LOOP ( 'NONE', ( #32276, #26455, #6793, #16626, #7293 ) ) ;
#14138=CARTESIAN_POINT ( 'NONE',  ( 4.874192403021982756, -30.78934762560861671, 7.785172627573962778 ) ) ;
#14140=ORIENTED_EDGE ( 'NONE', *, *, #5684, .F. ) ;
#14142=VERTEX_POINT ( 'NONE', #5522 ) ;
#14144=ORIENTED_EDGE ( 'NONE', *, *, #24687, .F. ) ;
#14149=CARTESIAN_POINT ( 'NONE',  ( 4.727238272722242840, -27.81534140858726900, 7.762796336881262249 ) ) ;
#14150=ORIENTED_EDGE ( 'NONE', *, *, #36080, .T. ) ;
#14152=DIRECTION ( 'NONE',  ( 0.4826092789263659033, -0.5751513419797880111, -0.6605219282605402364 ) ) ;
#14154=CARTESIAN_POINT ( 'NONE',  ( 1.062037487868057184, -33.01122440958558002, 6.894806418505347700 ) ) ;
#14158=VERTEX_POINT ( 'NONE', #26744 ) ;
#14159=CARTESIAN_POINT ( 'NONE',  ( 5.121105927283316817, -30.24177255004237352, 7.784725160561910329 ) ) ;
#14160=EDGE_CURVE ( 'NONE', #23979, #13676, #27879, .T. ) ;
#14167=CARTESIAN_POINT ( 'NONE',  ( 1.113415308591769737, -33.02035961353927718, 7.744938106820260515 ) ) ;
#14170=( BOUNDED_CURVE ( )  B_SPLINE_CURVE ( 3, ( #1381, #32271, #16585, #32462 ),
 .UNSPECIFIED., .F., .T. ) 
 B_SPLINE_CURVE_WITH_KNOTS ( ( 4, 4 ),
 ( 1.381924640371169133, 1.574767692156078036 ),
 .UNSPECIFIED. ) 
 CURVE ( )  GEOMETRIC_REPRESENTATION_ITEM ( )  RATIONAL_B_SPLINE_CURVE ( ( 1.000000000000000000, 0.9969033633783032089, 0.9969033633783032089, 1.000000000000000000 ) ) 
 REPRESENTATION_ITEM ( '' )  );
#14175=ADVANCED_FACE ( 'NONE', ( #17653 ), #2048, .F. ) ;
#14176=CARTESIAN_POINT ( 'NONE',  ( 5.060761980011518446, -29.05224715530099999, 6.874555630061443878 ) ) ;
#14179=CARTESIAN_POINT ( 'NONE',  ( 0.4741610271200560334, -32.84809465111302984, 6.894806418505347700 ) ) ;
#14185=CARTESIAN_POINT ( 'NONE',  ( -1.190803463164421094, -27.78076534723357582, 6.864651958020304257 ) ) ;
#14186=VERTEX_POINT ( 'NONE', #16012 ) ;
#14189=CARTESIAN_POINT ( 'NONE',  ( -0.5358931834503292135, -32.26233439484389010, 7.640616322432101093 ) ) ;
#14192=ORIENTED_EDGE ( 'NONE', *, *, #26657, .F. ) ;
#14196=CARTESIAN_POINT ( 'NONE',  ( 5.144146178010085890, -28.94499496390147186, 7.750000000000002665 ) ) ;
#14203=CARTESIAN_POINT ( 'NONE',  ( -1.237321756456247979, -31.28161037787917209, 7.635761828346577573 ) ) ;
#14205=CARTESIAN_POINT ( 'NONE',  ( 0.04414393643251195848, -26.60059526728241863, 7.785868773668302545 ) ) ;
#14207=DIRECTION ( 'NONE',  ( 0.000000000000000000, 0.000000000000000000, 1.000000000000000000 ) ) ;
#14209=VERTEX_POINT ( 'NONE', #25085 ) ;
#14215=CYLINDRICAL_SURFACE ( 'NONE', #9652, 3.499999999999999556 ) ;
#14219=DIRECTION ( 'NONE',  ( -0.5000000000000039968, 0.8660254037844363761, -0.000000000000000000 ) ) ;
#14220=CARTESIAN_POINT ( 'NONE',  ( 4.662059713662509708, -31.23981618828790374, 7.712764235869101981 ) ) ;
#14224=CARTESIAN_POINT ( 'NONE',  ( 4.163022776446456241, -25.19622345277205966, 7.695279973900954751 ) ) ;
#14228=( NAMED_UNIT ( * ) PLANE_ANGLE_UNIT ( ) SI_UNIT ( $, .RADIAN. ) );
#14229=FACE_OUTER_BOUND ( 'NONE', #1991, .T. ) ;
#14230=CARTESIAN_POINT ( 'NONE',  ( -1.548822507116328184, -28.29671509637249827, 7.780491323090174660 ) ) ;
#14232=CARTESIAN_POINT ( 'NONE',  ( 5.252969295392960092, -25.75565214092510047, 6.894806418505347700 ) ) ;
#14237=CARTESIAN_POINT ( 'NONE',  ( 5.039926880157825195, -30.20828278875847062, 6.894806418505346812 ) ) ;
#14239=CARTESIAN_POINT ( 'NONE',  ( -0.5309917997555131386, -32.13526346537501865, 7.785172627573962778 ) ) ;
#14242=CARTESIAN_POINT ( 'NONE',  ( 1.059624283225857999, -32.90900568614345190, 6.892063359921933419 ) ) ;
#14243=CARTESIAN_POINT ( 'NONE',  ( 0.3399341882483242760, -32.79470409825933785, 7.006248344249653925 ) ) ;
#14244=CARTESIAN_POINT ( 'NONE',  ( 1.261915996905217163, -26.09750387580824693, 7.011627023500182965 ) ) ;
#14247=CARTESIAN_POINT ( 'NONE',  ( -1.743365991543899485, -30.19486540288534826, 7.750000000000001776 ) ) ;
#14255=AXIS2_PLACEMENT_3D ( 'NONE', #6878, #28494, #15526 ) ;
#14259=ORIENTED_EDGE ( 'NONE', *, *, #26429, .F. ) ;
#14261=CARTESIAN_POINT ( 'NONE',  ( -0.9247287804614536810, -27.40920093173490102, 7.721096864323897080 ) ) ;
#14267=DIRECTION ( 'NONE',  ( 0.6427876096865379196, 0.7660444431189793457, -0.000000000000000000 ) ) ;
#14269=VERTEX_POINT ( 'NONE', #384 ) ;
#14271=CARTESIAN_POINT ( 'NONE',  ( 5.163932268927621472, -29.06596534262345699, 6.863784140767622333 ) ) ;
#14275=CARTESIAN_POINT ( 'NONE',  ( 3.398405180618411237, -32.61369795523508230, 7.785344483711591934 ) ) ;
#14276=CARTESIAN_POINT ( 'NONE',  ( 3.307555699830478702, -32.67912093030300014, 6.887547729233684635 ) ) ;
#14277=CARTESIAN_POINT ( 'NONE',  ( -1.047142997612213078, -31.73814762596163064, 6.863784140767623221 ) ) ;
#14280=CARTESIAN_POINT ( 'NONE',  ( 5.093905639142482400, -29.77981643751997964, 6.959317978105170610 ) ) ;
#14281=CARTESIAN_POINT ( 'NONE',  ( 4.437609036105186533, -27.54124898828658630, 7.386948897581451234 ) ) ;
#14283=( BOUNDED_CURVE ( )  B_SPLINE_CURVE ( 3, ( #39818, #10437, #20107, #17973 ),
 .UNSPECIFIED., .F., .F. ) 
 B_SPLINE_CURVE_WITH_KNOTS ( ( 4, 4 ),
 ( 1.381924640371168467, 1.574767692156076260 ),
 .UNSPECIFIED. ) 
 CURVE ( )  GEOMETRIC_REPRESENTATION_ITEM ( )  RATIONAL_B_SPLINE_CURVE ( ( 1.000000000000000000, 0.9969033633783033199, 0.9969033633783033199, 1.000000000000000000 ) ) 
 REPRESENTATION_ITEM ( '' )  );
#14285=B_SPLINE_CURVE_WITH_KNOTS ( 'NONE', 3,
 ( #10321, #4757, #38723, #16894, #17291, #36254, #29869, #7239, #39329, #4171 ),
 .UNSPECIFIED., .F., .F.,
 ( 4, 3, 3, 4 ),
 ( 0.000000000000000000, 3.025505781527817344E-05, 6.051003801291506945E-05, 6.468145402690557617E-05 ),
 .UNSPECIFIED. ) ;
#14288=EDGE_LOOP ( 'NONE', ( #33096, #12378, #37243, #28346 ) ) ;
#14291=CARTESIAN_POINT ( 'NONE',  ( -0.8982326133871421092, -27.22530497104394343, 6.867199677474200570 ) ) ;
#14292=ADVANCED_FACE ( 'NONE', ( #9212 ), #34576, .T. ) ;
#14296=CARTESIAN_POINT ( 'NONE',  ( -1.752498985642891860, -28.99760421947165057, 7.685194954629195330 ) ) ;
#14297=EDGE_LOOP ( 'NONE', ( #16430, #6831, #22586, #18652 ) ) ;
#14301=CARTESIAN_POINT ( 'NONE',  ( 0.6527267737179240914, -26.33536660093865578, 7.754798119455333705 ) ) ;
#14304=CARTESIAN_POINT ( 'NONE',  ( 4.030793147055388381, -27.09420370279508816, 6.903372536218459032 ) ) ;
#14314=CARTESIAN_POINT ( 'NONE',  ( -0.3903772972505400451, -26.88875661219547553, 7.754798119455333705 ) ) ;
#14315=CARTESIAN_POINT ( 'NONE',  ( 2.343738134713599486, -26.23135099740764531, 6.889465824494255486 ) ) ;
#14317=DIRECTION ( 'NONE',  ( 0.9848077530122103518, -0.1736481776669172583, -0.000000000000000000 ) ) ;
#14319=CARTESIAN_POINT ( 'NONE',  ( -0.08065709997537935660, -26.55697965350343281, 7.686927408461904143 ) ) ;
#14320=CARTESIAN_POINT ( 'NONE',  ( 0.6123814071172324347, -26.24333476180446567, 6.865482280155368322 ) ) ;
#14322=CARTESIAN_POINT ( 'NONE',  ( 1.106838199985236137, -33.01923402788369799, 7.636816916992232862 ) ) ;
#14323=CARTESIAN_POINT ( 'NONE',  ( 4.222957656326197906, -31.84957092882903495, 6.863904403958576594 ) ) ;
#14327=EDGE_CURVE ( 'NONE', #3514, #26672, #14743, .T. ) ;
#14328=CARTESIAN_POINT ( 'NONE',  ( 2.239018498799941082, -33.01413523298945307, 7.784725160561910329 ) ) ;
#14332=CARTESIAN_POINT ( 'NONE',  ( -1.610170960295353781, -28.79519250847841150, 6.895222827070023541 ) ) ;
#14335=ORIENTED_EDGE ( 'NONE', *, *, #12981, .F. ) ;
#14336=CARTESIAN_POINT ( 'NONE',  ( -0.6858270280168272670, -32.13039545693963106, 6.912143950357345190 ) ) ;
#14340=EDGE_CURVE ( 'NONE', #33808, #14142, #33892, .T. ) ;
#14345=CARTESIAN_POINT ( 'NONE',  ( -0.7841952061120170958, -27.24896036044557945, 6.887945620086121323 ) ) ;
#14347=EDGE_CURVE ( 'NONE', #28596, #19820, #30444, .T. ) ;
#14349=CARTESIAN_POINT ( 'NONE',  ( 3.229767211660741655, -32.60654106225653948, 6.903372536218458144 ) ) ;
#14353=CARTESIAN_POINT ( 'NONE',  ( -1.228758070621239762, -27.64172748556450543, 7.387053503561887169 ) ) ;
#14354=FACE_OUTER_BOUND ( 'NONE', #21118, .T. ) ;
#14355=CARTESIAN_POINT ( 'NONE',  ( 4.662674093641094863, -31.23872421060049831, 7.692469944509195301 ) ) ;
#14358=CARTESIAN_POINT ( 'NONE',  ( -1.749609906766908640, -29.56993018339339940, 6.850000000000000533 ) ) ;
#14361=CARTESIAN_POINT ( 'NONE',  ( 2.894372913787321089, -32.75339045652842884, 7.670860738520328681 ) ) ;
#14362=EDGE_CURVE ( 'NONE', #38041, #2116, #34416, .T. ) ;
#14367=VERTEX_POINT ( 'NONE', #25686 ) ;
#14370=DIRECTION ( 'NONE',  ( -1.000000000000000000, 0.000000000000000000, 0.000000000000000000 ) ) ;
#14383=CARTESIAN_POINT ( 'NONE',  ( -1.619657530256499056, -30.67780588394286667, 6.863805608295729499 ) ) ;
#14389=EDGE_LOOP ( 'NONE', ( #12431, #33713, #38592 ) ) ;
#14392=CARTESIAN_POINT ( 'NONE',  ( 5.021941733704682775, -28.81150442415370705, 7.139196562012270597 ) ) ;
#14396=CARTESIAN_POINT ( 'NONE',  ( 4.821848874205628022, -27.98673438488562581, 6.931070083220556732 ) ) ;
#14398=ORIENTED_EDGE ( 'NONE', *, *, #26657, .T. ) ;
#14400=EDGE_CURVE ( 'NONE', #16672, #3667, #8847, .T. ) ;
#14411=EDGE_LOOP ( 'NONE', ( #9437, #20966, #37634, #28849, #33931 ) ) ;
#14412=CARTESIAN_POINT ( 'NONE',  ( -2.239401636788067140, -26.21711406210128104, 7.695279973900954751 ) ) ;
#14423=CARTESIAN_POINT ( 'NONE',  ( 0.1054938181805689934, -26.45442818934983009, 6.903112506833893214 ) ) ;
#14426=DIRECTION ( 'NONE',  ( 0.000000000000000000, 0.6834397476448849096, -0.7300069255418718539 ) ) ;
#14430=CARTESIAN_POINT ( 'NONE',  ( 2.321451664048270302, -33.01438696571141662, 7.635761828346576685 ) ) ;
#14431=ORIENTED_EDGE ( 'NONE', *, *, #15308, .F. ) ;
#14439=EDGE_CURVE ( 'NONE', #31083, #8831, #4861, .T. ) ;
#14441=CYLINDRICAL_SURFACE ( 'NONE', #17996, 0.09010775117052929883 ) ;
#14443=CARTESIAN_POINT ( 'NONE',  ( 0.4206787789642892905, -32.82760425591565223, 6.864368109219935121 ) ) ;
#14444=CARTESIAN_POINT ( 'NONE',  ( 3.180781611337405668, -26.50125022492531102, 7.505001789837628223 ) ) ;
#14445=ORIENTED_EDGE ( 'NONE', *, *, #30465, .T. ) ;
#14461=CARTESIAN_POINT ( 'NONE',  ( 4.351629544212539003, -31.85488319143487601, 6.880608371227950215 ) ) ;
#14465=ORIENTED_EDGE ( 'NONE', *, *, #38947, .T. ) ;
#14466=CARTESIAN_POINT ( 'NONE',  ( 1.700390093233090871, -29.56993018339339940, 7.800000000000000711 ) ) ;
#14469=CARTESIAN_POINT ( 'NONE',  ( -2.297321782777200561, -26.28614060416741438, 7.695279973900954751 ) ) ;
#14472=CARTESIAN_POINT ( 'NONE',  ( 5.149995510507904939, -30.16172614916897743, 7.638991368224662182 ) ) ;
#14475=DIRECTION ( 'NONE',  ( -0.8660254037844212771, -0.5000000000000298650, 0.000000000000000000 ) ) ;
#14478=CARTESIAN_POINT ( 'NONE',  ( 2.775199688670615839, -32.79558988863323066, 6.866852738645443210 ) ) ;
#14481=CARTESIAN_POINT ( 'NONE',  ( 2.127989488270969787, -33.04371390207043646, 6.912143950357346966 ) ) ;
#14488=CARTESIAN_POINT ( 'NONE',  ( 4.421194222029321885, -27.53100279559231112, 7.013842709614101167 ) ) ;
#14489=ORIENTED_EDGE ( 'NONE', *, *, #28081, .F. ) ;
#14492=CARTESIAN_POINT ( 'NONE',  ( 2.998870170862291129, -26.42764606383958892, 6.868387053540520704 ) ) ;
#14495=ORIENTED_EDGE ( 'NONE', *, *, #37520, .F. ) ;
#14504=CARTESIAN_POINT ( 'NONE',  ( 0.6486176734534436772, -26.33669956561429260, 7.759451378593096749 ) ) ;
#14506=CARTESIAN_POINT ( 'NONE',  ( 3.928928892870411360, -27.00212668263422700, 6.887041543973314361 ) ) ;
#14514=CARTESIAN_POINT ( 'NONE',  ( -2.712160580843945734, -31.23359347163986399, 7.695279973900954751 ) ) ;
#14515=DIRECTION ( 'NONE',  ( 1.000000000000000000, -7.930164461608261228E-15, 0.000000000000000000 ) ) ;
#14518=( BOUNDED_CURVE ( )  B_SPLINE_CURVE ( 3, ( #15282, #12189, #12400, #15483 ),
 .UNSPECIFIED., .F., .F. ) 
 B_SPLINE_CURVE_WITH_KNOTS ( ( 4, 4 ),
 ( 1.381924640371167801, 1.574767692156076482 ),
 .UNSPECIFIED. ) 
 CURVE ( )  GEOMETRIC_REPRESENTATION_ITEM ( )  RATIONAL_B_SPLINE_CURVE ( ( 1.000000000000000000, 0.9969033633783032089, 0.9969033633783032089, 1.000000000000000000 ) ) 
 REPRESENTATION_ITEM ( '' )  );
#14519=CARTESIAN_POINT ( 'NONE',  ( 3.861119344891603244, -26.94481130969886706, 7.721096864323898856 ) ) ;
#14521=CARTESIAN_POINT ( 'NONE',  ( 0.5325725529551263993, -26.27050565893173228, 6.894806418505347700 ) ) ;
#14522=CARTESIAN_POINT ( 'NONE',  ( 4.405768222705582993, -27.34935008554416669, 6.887161170156904433 ) ) ;
#14523=AXIS2_PLACEMENT_3D ( 'NONE', #18701, #37629, #31686 ) ;
#14526=VERTEX_POINT ( 'NONE', #5474 ) ;
#14529=CARTESIAN_POINT ( 'NONE',  ( 2.213664895657379006, -33.02484726641009871, 7.776484688137383472 ) ) ;
#14531=CARTESIAN_POINT ( 'NONE',  ( 4.875541254183488604, -30.78583112718583692, 6.887041543973317026 ) ) ;
#14532=CARTESIAN_POINT ( 'NONE',  ( -1.632457674179491391, -28.89752720953548604, 6.870716933885662847 ) ) ;
#14534=CARTESIAN_POINT ( 'NONE',  ( -0.6056525554631260189, -32.20285051197402026, 6.867280401193708528 ) ) ;
#14539=DIRECTION ( 'NONE',  ( 0.7541618601367534591, 0.000000000000000000, 0.6566885781822856538 ) ) ;
#14550=CARTESIAN_POINT ( 'NONE',  ( -1.795519090086910019, -29.40075872605237706, 7.013842709614101167 ) ) ;
#14551=CARTESIAN_POINT ( 'NONE',  ( 5.165995621756787948, -25.65200095290807880, 7.013842709614101167 ) ) ;
#14557=ORIENTED_EDGE ( 'NONE', *, *, #25668, .F. ) ;
#14561=ORIENTED_EDGE ( 'NONE', *, *, #23146, .T. ) ;
#14569=EDGE_CURVE ( 'NONE', #29836, #24849, #21444, .T. ) ;
#14572=CARTESIAN_POINT ( 'NONE',  ( 2.782197798051136317, -32.89830469346890141, 7.754798119455333705 ) ) ;
#14574=EDGE_CURVE ( 'NONE', #16283, #17660, #20779, .T. ) ;
#14575=CARTESIAN_POINT ( 'NONE',  ( 4.985095813259256659, -28.36132152183090582, 7.756742906098588186 ) ) ;
#14584=CARTESIAN_POINT ( 'NONE',  ( -1.020414035563122601, -31.60885757119451256, 7.013842709614101167 ) ) ;
#14585=ORIENTED_EDGE ( 'NONE', *, *, #21170, .F. ) ;
#14587=CYLINDRICAL_SURFACE ( 'NONE', #10184, 0.09010775117053103356 ) ;
#14591=EDGE_LOOP ( 'NONE', ( #40298, #33978, #4143, #8890 ) ) ;
#14594=ORIENTED_EDGE ( 'NONE', *, *, #1204, .T. ) ;
#14598=CARTESIAN_POINT ( 'NONE',  ( 0.05294289315275076124, -26.59572142761524205, 7.785172627573962778 ) ) ;
#14605=EDGE_CURVE ( 'NONE', #6597, #13346, #10807, .T. ) ;
#14606=DIRECTION ( 'NONE',  ( -0.8660254037844345998, -0.5000000000000071054, -0.000000000000000000 ) ) ;
#14607=CARTESIAN_POINT ( 'NONE',  ( 1.294658908450306845, -26.08664770627206053, 7.387053503561885393 ) ) ;
#14613=CARTESIAN_POINT ( 'NONE',  ( -2.639489883291917138, -27.04870784343005141, 7.635761828346577573 ) ) ;
#14618=CARTESIAN_POINT ( 'NONE',  ( 4.630655976963546472, -31.48396831510932969, 6.961115707816232678 ) ) ;
#14619=EDGE_CURVE ( 'NONE', #15871, #37640, #1790, .T. ) ;
#14620=EDGE_CURVE ( 'NONE', #17512, #7534, #15721, .T. ) ;
#14622=B_SPLINE_CURVE_WITH_KNOTS ( 'NONE', 3,
 ( #2567, #33853, #11987, #30138, #33235, #11174, #14472, #27241, #11377, #40204 ),
 .UNSPECIFIED., .F., .F.,
 ( 4, 3, 3, 4 ),
 ( 8.673617379884035472E-19, 3.025505781527810907E-05, 6.051003801291621463E-05, 6.468145402690745997E-05 ),
 .UNSPECIFIED. ) ;
#14623=ADVANCED_FACE ( 'NONE', ( #24825 ), #15137, .T. ) ;
#14629=B_SPLINE_CURVE_WITH_KNOTS ( 'NONE', 3,
 ( #13687, #4227, #35723, #10777, #8090, #5024, #939, #26651, #38789, #23357, #22963, #13476, #7703, #16753, #7499, #32639, #38581, #16961, #29728, #20253, #32837, #4629, #39184, #10979, #7904 ),
 .UNSPECIFIED., .F., .F.,
 ( 4, 3, 3, 3, 3, 3, 3, 3, 4 ),
 ( 7.730982992130896385E-05, 9.267501192706072816E-05, 0.0001241882240135149700, 0.0001556618703051600237, 0.0001866161554452170994, 0.0002167966385860923466, 0.0002463805737537726106, 0.0002758761370306489122, 0.0002847094172290014712 ),
 .UNSPECIFIED. ) ;
#14635=CARTESIAN_POINT ( 'NONE',  ( -0.4584151234726890900, -32.19663272579155944, 7.712764235869099316 ) ) ;
#14636=CARTESIAN_POINT ( 'NONE',  ( 3.792809966073827255, -32.24981515609748328, 7.757178535559530630 ) ) ;
#14639=VERTEX_POINT ( 'NONE', #33906 ) ;
#14645=ORIENTED_EDGE ( 'NONE', *, *, #11255, .T. ) ;
#14646=CARTESIAN_POINT ( 'NONE',  ( -0.1065785265816254768, -32.45002973820478331, 6.863904403958575706 ) ) ;
#14655=CARTESIAN_POINT ( 'NONE',  ( -2.652992490026568007, -32.06776532245774547, 7.635761828346577573 ) ) ;
#14658=CARTESIAN_POINT ( 'NONE',  ( 3.418165973099760890, -26.63576239896834608, 7.779495906702016406 ) ) ;
#14664=CARTESIAN_POINT ( 'NONE',  ( 1.654198408036650969, -33.06963691447906939, 6.880608371227948439 ) ) ;
#14668=CARTESIAN_POINT ( 'NONE',  ( 1.686887486498407140, -26.06995622926011436, 7.635761828346576685 ) ) ;
#14669=DIRECTION ( 'NONE',  ( -0.000000000000000000, -0.000000000000000000, -1.000000000000000000 ) ) ;
#14670=CARTESIAN_POINT ( 'NONE',  ( 5.175423985860502007, -29.15262985496314130, 6.961115707816242448 ) ) ;
#14675=DIRECTION ( 'NONE',  ( 1.000000000000000000, 0.000000000000000000, -0.000000000000000000 ) ) ;
#14676=CARTESIAN_POINT ( 'NONE',  ( 5.043507888204011635, -28.95060522107654677, 7.661510568013096822 ) ) ;
#14677=DIRECTION ( 'NONE',  ( -0.000000000000000000, -0.000000000000000000, -1.000000000000000000 ) ) ;
#14680=CARTESIAN_POINT ( 'NONE',  ( 4.930594809156889191, -28.50887757203159012, 7.768425012602591551 ) ) ;
#14690=CARTESIAN_POINT ( 'NONE',  ( 1.057242960569752199, -26.12952878737186424, 7.695279973900954751 ) ) ;
#14691=CARTESIAN_POINT ( 'NONE',  ( 0.1853991482571498706, -26.52611638543517003, 6.959317978105165281 ) ) ;
#14693=CARTESIAN_POINT ( 'NONE',  ( -2.949010729501093220, -28.55700733037702221, 6.894806418505347700 ) ) ;
#14702=ORIENTED_EDGE ( 'NONE', *, *, #24547, .T. ) ;
#14703=DIRECTION ( 'NONE',  ( -0.7394003126383920099, 0.1303762246624204368, -0.6605219282605403475 ) ) ;
#14705=CARTESIAN_POINT ( 'NONE',  ( 2.493210317801513476, -26.25641980554438604, 7.386948897581451234 ) ) ;
#14707=EDGE_LOOP ( 'NONE', ( #10146, #1402, #38117, #5859, #10092 ) ) ;
#14713=CARTESIAN_POINT ( 'NONE',  ( 2.460256200828665918, -26.25592905205268224, 6.882085323592685988 ) ) ;
#14714=CARTESIAN_POINT ( 'NONE',  ( 4.907464300517769829, -30.69894525369553762, 7.693875151218754205 ) ) ;
#14718=CARTESIAN_POINT ( 'NONE',  ( 5.042998615515850602, -28.94786244852631896, 7.721096864323902409 ) ) ;
#14722=CARTESIAN_POINT ( 'NONE',  ( 1.128064129311358244, -33.02281926226938680, 7.685194954629195330 ) ) ;
#14723=EDGE_CURVE ( 'NONE', #28994, #3514, #18625, .T. ) ;
#14724=CARTESIAN_POINT ( 'NONE',  ( 4.164674408718673781, -31.91242951707208420, 6.949473656533220023 ) ) ;
#14725=VECTOR ( 'NONE', #24752, 1000.000000000000114 ) ;
#14732=FACE_OUTER_BOUND ( 'NONE', #33881, .T. ) ;
#14734=CARTESIAN_POINT ( 'NONE',  ( -1.613611038107622520, -28.81006407579781126, 6.882085323592686876 ) ) ;
#14735=CARTESIAN_POINT ( 'NONE',  ( 4.911690090265110165, -28.45299136274915952, 6.894806418505345924 ) ) ;
#14736=CARTESIAN_POINT ( 'NONE',  ( -0.6288947886013260824, -32.18231164535578159, 6.863784140767622333 ) ) ;
#14737=VERTEX_POINT ( 'NONE', #37370 ) ;
#14743=B_SPLINE_CURVE_WITH_KNOTS ( 'NONE', 3,
 ( #3290, #28366, #30861, #19102, #27746, #12715, #24663, #37215, #9008, #21588 ),
 .UNSPECIFIED., .F., .F.,
 ( 4, 3, 3, 4 ),
 ( 0.0002170292169044746994, 0.0002420761345915958753, 0.0002723302478206996065, 0.0002816811360866696996 ),
 .UNSPECIFIED. ) ;
#14744=CARTESIAN_POINT ( 'NONE',  ( -1.577774374486538678, -28.34370111728035013, 6.894806418505347700 ) ) ;
#14747=CARTESIAN_POINT ( 'NONE',  ( 4.764283036282700223, -27.89929580878658655, 7.780491323090172884 ) ) ;
#14751=CARTESIAN_POINT ( 'NONE',  ( 3.217988213875103920, -32.61244741234136768, 6.979335674598004857 ) ) ;
#14752=( BOUNDED_CURVE ( )  B_SPLINE_CURVE ( 3, ( #21503, #34081, #25196, #37727 ),
 .UNSPECIFIED., .F., .T. ) 
 B_SPLINE_CURVE_WITH_KNOTS ( ( 4, 4 ),
 ( 4.708531083176468179, 4.895802057644189631 ),
 .UNSPECIFIED. ) 
 CURVE ( )  GEOMETRIC_REPRESENTATION_ITEM ( )  RATIONAL_B_SPLINE_CURVE ( ( 1.000000000000000000, 0.9970795998553221295, 0.9970795998553221295, 1.000000000000000000 ) ) 
 REPRESENTATION_ITEM ( '' )  );
#14755=DIRECTION ( 'NONE',  ( 0.6502177225477915323, -0.3754033771448308521, 0.6605219282605377940 ) ) ;
#14756=LINE ( 'NONE', #14551, #15621 ) ;
#14757=CARTESIAN_POINT ( 'NONE',  ( -1.622027358445928158, -30.66236699258251264, 7.766640943994648438 ) ) ;
#14772=AXIS2_PLACEMENT_3D ( 'NONE', #27135, #20344, #32923 ) ;
#14773=CARTESIAN_POINT ( 'NONE',  ( 5.058102131368015009, -29.03535570872796967, 6.887041543973314361 ) ) ;
#14777=DIRECTION ( 'NONE',  ( -0.6662082868431838945, 0.000000000000000000, -0.7457657263118692148 ) ) ;
#14779=CARTESIAN_POINT ( 'NONE',  ( -0.3903772972505400451, -26.88875661219547553, 7.754798119455333705 ) ) ;
#14780=VERTEX_POINT ( 'NONE', #12253 ) ;
#14781=CARTESIAN_POINT ( 'NONE',  ( 2.859730186744443348, -32.85857677678156819, 7.783750581861600182 ) ) ;
#14782=AXIS2_PLACEMENT_3D ( 'NONE', #5548, #3260, #8416 ) ;
#14783=CARTESIAN_POINT ( 'NONE',  ( -1.216810142391697047, -27.82351944452216586, 6.889465824494253710 ) ) ;
#14784=EDGE_LOOP ( 'NONE', ( #32644, #5404, #32326, #27661, #32767 ) ) ;
#14785=VERTEX_POINT ( 'NONE', #34729 ) ;
#14788=CARTESIAN_POINT ( 'NONE',  ( -1.332155549108038795, -31.29987003238072418, 7.778495531946297170 ) ) ;
#14798=VERTEX_POINT ( 'NONE', #133 ) ;
#14801=CARTESIAN_POINT ( 'NONE',  ( 4.282520317648695674, -27.35800574660165196, 7.712764235869103757 ) ) ;
#14805=VECTOR ( 'NONE', #33813, 1000.000000000000114 ) ;
#14807=CARTESIAN_POINT ( 'NONE',  ( -0.02491320616155640738, -26.64019694052143805, 7.730758795053802146 ) ) ;
#14809=CARTESIAN_POINT ( 'NONE',  ( -1.794668156065684084, -29.38400591384104032, 6.921725064902950031 ) ) ;
#14811=ORIENTED_EDGE ( 'NONE', *, *, #14620, .T. ) ;
#14813=CARTESIAN_POINT ( 'NONE',  ( 4.200390093233091093, -29.56993018339339940, -8.199999999999999289 ) ) ;
#14815=EDGE_CURVE ( 'NONE', #26672, #38094, #3748, .T. ) ;
#14816=CARTESIAN_POINT ( 'NONE',  ( -0.02262473055865150268, -26.52342071894167574, 6.894806418505347700 ) ) ;
#14817=FACE_OUTER_BOUND ( 'NONE', #30889, .T. ) ;
#14822=CARTESIAN_POINT ( 'NONE',  ( 5.129509330119056187, -30.27076478451887809, 6.864216812888783714 ) ) ;
#14823=CARTESIAN_POINT ( 'NONE',  ( -1.766085975226569404, -30.05319374170961666, 7.750000000000000888 ) ) ;
#14826=CARTESIAN_POINT ( 'NONE',  ( -0.009460099485995122209, -26.51599940587959381, 6.880608371227948439 ) ) ;
#14835=VERTEX_POINT ( 'NONE', #12036 ) ;
#14842=ORIENTED_EDGE ( 'NONE', *, *, #20828, .T. ) ;
#14843=DIRECTION ( 'NONE',  ( 0.7660444431189790127, 0.6427876096865381417, 0.000000000000000000 ) ) ;
#14847=ORIENTED_EDGE ( 'NONE', *, *, #17643, .F. ) ;
#14848=DIRECTION ( 'NONE',  ( 1.000000000000000000, 0.000000000000000000, 0.000000000000000000 ) ) ;
#14849=CARTESIAN_POINT ( 'NONE',  ( 3.559755418260376114, -26.72339534466646427, 7.013842709614101167 ) ) ;
#14860=ADVANCED_FACE ( 'NONE', ( #13477 ), #16754, .F. ) ;
#14865=CARTESIAN_POINT ( 'NONE',  ( -0.9263124491650691628, -27.41112496668761622, 7.712764235869100204 ) ) ;
#14868=CARTESIAN_POINT ( 'NONE',  ( -1.695213279257311800, -29.39707840662554617, 6.882085323592685100 ) ) ;
#14871=CARTESIAN_POINT ( 'NONE',  ( -1.770976519370218494, -30.01676597940898361, 6.887547729233690852 ) ) ;
#14873=CARTESIAN_POINT ( 'NONE',  ( 1.616163289117390711, -33.06891658597750450, 6.865554069792297653 ) ) ;
#14876=CARTESIAN_POINT ( 'NONE',  ( 6.119163499495797964, -31.21649665547238683, 7.695279973900954751 ) ) ;
#14877=PLANE ( 'NONE',  #4671 ) ;
#14878=DIRECTION ( 'NONE',  ( -0.1736481776669206722, -0.9848077530122096857, -0.000000000000000000 ) ) ;
#14880=EDGE_CURVE ( 'NONE', #8831, #36530, #36274, .T. ) ;
#14883=FACE_OUTER_BOUND ( 'NONE', #24759, .T. ) ;
#14884=DIRECTION ( 'NONE',  ( 1.000000000000000000, -0.000000000000000000, -0.000000000000000000 ) ) ;
#14885=EDGE_CURVE ( 'NONE', #38704, #14835, #13272, .T. ) ;
#14886=CARTESIAN_POINT ( 'NONE',  ( 0.4527547210032973890, -32.82408303185094667, 7.785593909369613819 ) ) ;
#14889=CARTESIAN_POINT ( 'NONE',  ( 4.915490139096653444, -28.46397733851794243, 7.785172627573962778 ) ) ;
#14893=ORIENTED_EDGE ( 'NONE', *, *, #32505, .T. ) ;
#14902=CARTESIAN_POINT ( 'NONE',  ( 3.052029408395551702, -26.45014314551610823, 6.988553391373223178 ) ) ;
#14904=CARTESIAN_POINT ( 'NONE',  ( -0.9051507792758500814, -27.23301838324232449, 6.865482280155367434 ) ) ;
#14905=CARTESIAN_POINT ( 'NONE',  ( 1.160481914523016078, -26.21307075903531114, 6.892063359921932530 ) ) ;
#14906=VECTOR ( 'NONE', #13308, 1000.000000000000114 ) ;
#14911=ORIENTED_EDGE ( 'NONE', *, *, #23703, .F. ) ;
#14925=EDGE_LOOP ( 'NONE', ( #17775, #34575, #35100, #803, #17799 ) ) ;
#14927=CARTESIAN_POINT ( 'NONE',  ( -1.799419790741071168, -29.60642027013681599, 7.697588729724128775 ) ) ;
#14928=CARTESIAN_POINT ( 'NONE',  ( 3.198709474042557233, -25.09719924859204454, 7.754798119455333705 ) ) ;
#14931=CARTESIAN_POINT ( 'NONE',  ( 1.513399906207050449, -32.96478432900200062, 7.013842709614101167 ) ) ;
#14932=DIRECTION ( 'NONE',  ( -0.000000000000000000, -0.000000000000000000, -1.000000000000000000 ) ) ;
#14933=CARTESIAN_POINT ( 'NONE',  ( -1.739611863387223512, -30.14058980792885123, 7.783750581861600182 ) ) ;
#14936=CARTESIAN_POINT ( 'NONE',  ( 0.5925143926836328179, -26.24988255990380281, 6.863805608295729499 ) ) ;
#14938=CARTESIAN_POINT ( 'NONE',  ( 5.065770593663160071, -29.08591650778173587, 7.768425012602593327 ) ) ;
#14943=ORIENTED_EDGE ( 'NONE', *, *, #8758, .T. ) ;
#14946=CARTESIAN_POINT ( 'NONE',  ( 4.993499329952471477, -30.75545037259727366, 7.756742906098588186 ) ) ;
#14947=ADVANCED_FACE ( 'NONE', ( #3843 ), #16360, .F. ) ;
#14950=CARTESIAN_POINT ( 'NONE',  ( 4.865842863122197492, -30.81086078644958093, 6.870716933885666400 ) ) ;
#14951=CARTESIAN_POINT ( 'NONE',  ( -1.555661392733006965, -30.54877068150224417, 6.903372536218459921 ) ) ;
#14953=CARTESIAN_POINT ( 'NONE',  ( -1.607612949201309815, -28.78435332836398075, 6.997764925645182821 ) ) ;
#14955=CARTESIAN_POINT ( 'NONE',  ( -0.6365217069179813780, -32.17547105590234224, 6.865482280155367434 ) ) ;
#14958=EDGE_LOOP ( 'NONE', ( #35660, #25759, #22184, #18079 ) ) ;
#14962=CARTESIAN_POINT ( 'NONE',  ( -1.519540497997595052, -28.19804604943728421, 6.925313231306334139 ) ) ;
#14965=CARTESIAN_POINT ( 'NONE',  ( 4.744157865074793534, -27.87191509600810946, 7.785344483711591934 ) ) ;
#14968=EDGE_CURVE ( 'NONE', #23776, #17087, #18612, .T. ) ;
#14973=CARTESIAN_POINT ( 'NONE',  ( 4.978554560952730412, -30.79615924950642025, 6.894806418505347700 ) ) ;
#14981=CARTESIAN_POINT ( 'NONE',  ( 2.882188420740142920, -32.75793850981484212, 7.643333865083957512 ) ) ;
#14982=CARTESIAN_POINT ( 'NONE',  ( 1.020706351875211304, -32.99074525956162773, 7.782861076432729952 ) ) ;
#14985=CARTESIAN_POINT ( 'NONE',  ( -1.799471907747695942, -29.53885005966835919, 6.894806418505347700 ) ) ;
#14987=AXIS2_PLACEMENT_3D ( 'NONE', #29166, #25874, #31856 ) ;
#14995=CARTESIAN_POINT ( 'NONE',  ( 1.887380280259158383, -26.17507603778478753, 7.013842709614101167 ) ) ;
#14999=EDGE_LOOP ( 'NONE', ( #25, #1844, #358, #4061 ) ) ;
#15009=CARTESIAN_POINT ( 'NONE',  ( 0.01209709964644558461, -32.52114463981743597, 7.635761828346577573 ) ) ;
#15011=( BOUNDED_CURVE ( )  B_SPLINE_CURVE ( 3, ( #34226, #21445, #5792, #18329 ),
 .UNSPECIFIED., .F., .T. ) 
 B_SPLINE_CURVE_WITH_KNOTS ( ( 4, 4 ),
 ( 4.748221474220559735, 4.941946782021394036 ),
 .UNSPECIFIED. ) 
 CURVE ( )  GEOMETRIC_REPRESENTATION_ITEM ( )  RATIONAL_B_SPLINE_CURVE ( ( 1.000000000000000000, 0.9968749865767494445, 0.9968749865767494445, 1.000000000000000000 ) ) 
 REPRESENTATION_ITEM ( '' )  );
#15018=DIRECTION ( 'NONE',  ( -0.5751513419797927851, 0.4826092789263599636, -0.6605219282605403475 ) ) ;
#15020=EDGE_LOOP ( 'NONE', ( #31692, #13502, #31833, #8616, #39892 ) ) ;
#15021=CARTESIAN_POINT ( 'NONE',  ( 3.343728876470205336, -32.65988526930982516, 7.754798119455333705 ) ) ;
#15023=CARTESIAN_POINT ( 'NONE',  ( -1.798839535641747034, -29.49580759126772023, 6.867280401193707640 ) ) ;
#15026=ORIENTED_EDGE ( 'NONE', *, *, #22486, .T. ) ;
#15027=VECTOR ( 'NONE', #33075, 1000.000000000000227 ) ;
#15031=DIRECTION ( 'NONE',  ( -0.9396926207859104263, 0.3420201433256631063, -0.000000000000000000 ) ) ;
#15035=CARTESIAN_POINT ( 'NONE',  ( 5.128444259610362543, -30.27593629695848421, 6.864216812847430127 ) ) ;
#15036=CARTESIAN_POINT ( 'NONE',  ( 2.718906344516694329, -32.91845592554787459, 6.980586498568968068 ) ) ;
#15037=CARTESIAN_POINT ( 'NONE',  ( 0.6162842664679426541, -26.34739786293889807, 6.870716933885664623 ) ) ;
#15038=CARTESIAN_POINT ( 'NONE',  ( -1.699609906766908374, -29.77250410202202602, 7.176074147390429481 ) ) ;
#15041=FACE_OUTER_BOUND ( 'NONE', #35153, .T. ) ;
#15042=CARTESIAN_POINT ( 'NONE',  ( 5.197249530360846137, -29.57011687675261413, 7.767441775592068609 ) ) ;
#15043=DIRECTION ( 'NONE',  ( -0.8660254037844261621, -0.5000000000000215383, 0.000000000000000000 ) ) ;
#15044=EDGE_CURVE ( 'NONE', #32450, #5814, #19931, .T. ) ;
#15045=CARTESIAN_POINT ( 'NONE',  ( 2.410368835147195021, -26.24488429107400478, 7.754798119455333705 ) ) ;
#15047=ORIENTED_EDGE ( 'NONE', *, *, #33353, .F. ) ;
#15052=CARTESIAN_POINT ( 'NONE',  ( -0.4545477510665002496, -26.81228124332190532, 7.754798119455333705 ) ) ;
#15056=CARTESIAN_POINT ( 'NONE',  ( -0.4872815388214248311, -32.17263893204430047, 7.769368695748482878 ) ) ;
#15061=CARTESIAN_POINT ( 'NONE',  ( 4.626733377823518012, -27.83888570657239470, 7.695279973900954751 ) ) ;
#15066=B_SPLINE_CURVE_WITH_KNOTS ( 'NONE', 3,
 ( #28874, #3980, #19999, #13018, #7041, #10524, #13221, #680, #4376, #38728, #19609, #7243, #38321, #16899, #22708, #29671, #29480, #13624, #25787, #26397, #883, #7647, #10118, #16691, #35670 ),
 .UNSPECIFIED., .F., .F.,
 ( 4, 3, 3, 3, 3, 3, 3, 3, 4 ),
 ( 6.468151674593620168E-05, 9.076621574722086106E-05, 0.0001210204262067974786, 0.0001512763324577443783, 0.0001815301820994217827, 0.0002117781465860715459, 0.0002420274594459759666, 0.0002722905548971157885, 0.0002816827545175587338 ),
 .UNSPECIFIED. ) ;
#15067=CARTESIAN_POINT ( 'NONE',  ( 2.338742698598150316, -26.23039339646865287, 6.894806418505346812 ) ) ;
#15069=ORIENTED_EDGE ( 'NONE', *, *, #15999, .T. ) ;
#15075=ORIENTED_EDGE ( 'NONE', *, *, #10172, .F. ) ;
#15076=CARTESIAN_POINT ( 'NONE',  ( 1.700390093233090871, -29.56993018339339940, 7.800000000000000711 ) ) ;
#15079=CARTESIAN_POINT ( 'NONE',  ( -1.696497448580634781, -29.42448250114750863, 6.868387053540520704 ) ) ;
#15087=PLANE ( 'NONE',  #9243 ) ;
#15094=CARTESIAN_POINT ( 'NONE',  ( -0.02684669743237798334, -25.18051837188491149, 7.754798119455333705 ) ) ;
#15096=CARTESIAN_POINT ( 'NONE',  ( 4.627023651880590727, -27.83937644663651412, 7.680992449362121555 ) ) ;
#15102=CARTESIAN_POINT ( 'NONE',  ( -1.519035479433219038, -30.66327089748390122, 6.874555630061440326 ) ) ;
#15105=B_SPLINE_CURVE_WITH_KNOTS ( 'NONE', 3,
 ( #13845, #10738, #23318, #1501, #14034, #39146, #39348, #34027, #36475, #2317 ),
 .UNSPECIFIED., .F., .F.,
 ( 4, 3, 3, 4 ),
 ( 0.0002170292169044778436, 0.0002420761345915944658, 0.0002723302478206986307, 0.0002816811360866790779 ),
 .UNSPECIFIED. ) ;
#15111=CARTESIAN_POINT ( 'NONE',  ( 5.002097081266497547, -28.40856126717273611, 6.887161170156906209 ) ) ;
#15112=CARTESIAN_POINT ( 'NONE',  ( -1.416461651392222354, -28.21153572011717614, 6.949473656533217358 ) ) ;
#15113=CARTESIAN_POINT ( 'NONE',  ( 4.852421344848616869, -30.84456871255493482, 7.757178535559533294 ) ) ;
#15114=CARTESIAN_POINT ( 'NONE',  ( -1.331572764389289398, -28.01586578234813985, 7.139196562012272373 ) ) ;
#15119=EDGE_CURVE ( 'NONE', #6204, #14209, #36124, .T. ) ;
#15131=CARTESIAN_POINT ( 'NONE',  ( 5.916497905674401814, -30.25835747790444330, 7.695279973900954751 ) ) ;
#15132=CARTESIAN_POINT ( 'NONE',  ( 3.037211893591657219, -26.44376520468768632, 7.013842709614101167 ) ) ;
#15133=CARTESIAN_POINT ( 'NONE',  ( 1.580679853655120093, -32.96782274345532926, 7.757178535559534183 ) ) ;
#15136=CARTESIAN_POINT ( 'NONE',  ( 3.723260060725158471, -32.30269659105433533, 6.979335674598008410 ) ) ;
#15137=PLANE ( 'NONE',  #6979 ) ;
#15138=CARTESIAN_POINT ( 'NONE',  ( 4.321330788254073241, -31.73572891817300601, 7.652160403243379427 ) ) ;
#15139=CARTESIAN_POINT ( 'NONE',  ( 5.042542681852490993, -28.94541254208796133, 7.712764235869103757 ) ) ;
#15142=CARTESIAN_POINT ( 'NONE',  ( 3.913215462449400217, -32.15128716865380909, 7.691066658568949777 ) ) ;
#15149=CARTESIAN_POINT ( 'NONE',  ( 4.995237956833183723, -30.75059844998224179, 7.750000000000001776 ) ) ;
#15150=ADVANCED_FACE ( 'NONE', ( #39388 ), #30770, .T. ) ;
#15158=CARTESIAN_POINT ( 'NONE',  ( -1.610418084489225299, -28.79627056164295595, 7.013842709614101167 ) ) ;
#15159=CARTESIAN_POINT ( 'NONE',  ( -0.6931531239536370403, -32.12354543778459970, 6.951256099901587326 ) ) ;
#15164=CARTESIAN_POINT ( 'NONE',  ( -1.571041143654955619, -28.32584913204942012, 6.878641987404677138 ) ) ;
#15166=DIRECTION ( 'NONE',  ( 0.6834397476448829112, 0.000000000000000000, -0.7300069255418737413 ) ) ;
#15170=CARTESIAN_POINT ( 'NONE',  ( 3.281726478462255958, -32.57982635458228060, 6.865312560952604670 ) ) ;
#15172=CARTESIAN_POINT ( 'NONE',  ( 4.963238934339704755, -30.83638965544459154, 6.867280401193710304 ) ) ;
#15174=CARTESIAN_POINT ( 'NONE',  ( 3.436873281388448831, -26.53107670108079219, 7.638132480492518361 ) ) ;
#15175=DIRECTION ( 'NONE',  ( -1.000000000000000000, -0.000000000000000000, -0.000000000000000000 ) ) ;
#15177=ORIENTED_EDGE ( 'NONE', *, *, #19034, .F. ) ;
#15178=CARTESIAN_POINT ( 'NONE',  ( 4.107940300203791750, -27.02011124655863838, 7.387053503561884504 ) ) ;
#15188=CARTESIAN_POINT ( 'NONE',  ( 3.507358713047826093, -26.68983062858202970, 6.863904403958575706 ) ) ;
#15189=ADVANCED_FACE ( 'NONE', ( #9320 ), #33655, .F. ) ;
#15199=VECTOR ( 'NONE', #29242, 1000.000000000000114 ) ;
#15200=ADVANCED_FACE ( 'NONE', ( #31170 ), #34475, .F. ) ;
#15201=EDGE_CURVE ( 'NONE', #19164, #36530, #36927, .T. ) ;
#15204=ORIENTED_EDGE ( 'NONE', *, *, #27658, .F. ) ;
#15213=ORIENTED_EDGE ( 'NONE', *, *, #37455, .F. ) ;
#15224=CARTESIAN_POINT ( 'NONE',  ( -1.740011302788441183, -30.21307731605675073, 7.695279973900954751 ) ) ;
#15225=CARTESIAN_POINT ( 'NONE',  ( 0.5197218266442334977, -32.86477804699348582, 7.750000000000000888 ) ) ;
#15226=DIRECTION ( 'NONE',  ( 1.000000000000000000, -5.253733955815473636E-14, 0.000000000000000000 ) ) ;
#15227=CARTESIAN_POINT ( 'NONE',  ( 5.200390093233090205, -29.56993018339339940, 6.929570838012950595 ) ) ;
#15232=B_SPLINE_CURVE_WITH_KNOTS ( 'NONE', 3,
 ( #27392, #34421, #40154, #24719, #5990, #36868, #18739, #18527, #5577, #37268 ),
 .UNSPECIFIED., .F., .F.,
 ( 4, 3, 3, 4 ),
 ( 0.0002170292169044763799, 0.0002420761345915966613, 0.0002723302478207007449, 0.0002816811360866726269 ),
 .UNSPECIFIED. ) ;
#15235=ORIENTED_EDGE ( 'NONE', *, *, #22628, .F. ) ;
#15239=FACE_OUTER_BOUND ( 'NONE', #2047, .T. ) ;
#15244=CARTESIAN_POINT ( 'NONE',  ( 5.144146178010085890, -28.94499496390147186, 7.750000000000002665 ) ) ;
#15245=CARTESIAN_POINT ( 'NONE',  ( 5.185743982427674759, -29.61328051818922802, 7.785096263473210598 ) ) ;
#15247=EDGE_CURVE ( 'NONE', #8430, #40124, #9124, .T. ) ;
#15259=ORIENTED_EDGE ( 'NONE', *, *, #7679, .F. ) ;
#15261=CARTESIAN_POINT ( 'NONE',  ( -1.594457770366995319, -28.38926191680453925, 7.750000000000000888 ) ) ;
#15270=CARTESIAN_POINT ( 'NONE',  ( -0.1724601174513000490, -32.40761094210100879, 6.988553391373221402 ) ) ;
#15271=ORIENTED_EDGE ( 'NONE', *, *, #3950, .T. ) ;
#15273=B_SPLINE_CURVE_WITH_KNOTS ( 'NONE', 3,
 ( #25947, #32537, #7402, #16262, #28834, #22667, #38481, #10081, #35828, #7202 ),
 .UNSPECIFIED., .F., .F.,
 ( 4, 3, 3, 4 ),
 ( 1.022834283856302764E-18, 3.025570593003244134E-05, 6.051145698344170592E-05, 6.468151674593708260E-05 ),
 .UNSPECIFIED. ) ;
#15274=CARTESIAN_POINT ( 'NONE',  ( 3.888958500451919154, -32.28338504940279563, 7.784725160561908552 ) ) ;
#15275=DIRECTION ( 'NONE',  ( -0.000000000000000000, -0.000000000000000000, -1.000000000000000000 ) ) ;
#15281=EDGE_LOOP ( 'NONE', ( #28338, #455, #37677, #32175 ) ) ;
#15282=CARTESIAN_POINT ( 'NONE',  ( 1.651639975615219580, -32.96958066925694908, 6.894806418505345036 ) ) ;
#15286=CARTESIAN_POINT ( 'NONE',  ( -1.693125452676301768, -29.36004392926684758, 6.959317978105164393 ) ) ;
#15288=CARTESIAN_POINT ( 'NONE',  ( -1.417651227037130868, -31.15984618490730540, 6.912143950357346966 ) ) ;
#15290=CARTESIAN_POINT ( 'NONE',  ( 1.509278095782431217, -33.06470984435662075, 6.971170733404103537 ) ) ;
#15292=FACE_OUTER_BOUND ( 'NONE', #34953, .T. ) ;
#15296=CARTESIAN_POINT ( 'NONE',  ( 5.198039085808181525, -29.69173459304409946, 7.754798119455333705 ) ) ;
#15300=DIRECTION ( 'NONE',  ( -0.5000000000000039968, 0.8660254037844362651, -0.000000000000000000 ) ) ;
#15302=CARTESIAN_POINT ( 'NONE',  ( -0.8560347025813198618, -25.25037435423009669, 7.695279973900954751 ) ) ;
#15308=EDGE_CURVE ( 'NONE', #4723, #40343, #12620, .T. ) ;
#15310=ORIENTED_EDGE ( 'NONE', *, *, #25355, .T. ) ;
#15316=CARTESIAN_POINT ( 'NONE',  ( 0.1004213051519422251, -26.56991353724522398, 6.864276522220859711 ) ) ;
#15317=CARTESIAN_POINT ( 'NONE',  ( 4.901715390235392711, -30.71514472345701563, 7.748216051605120391 ) ) ;
#15318=B_SPLINE_CURVE_WITH_KNOTS ( 'NONE', 3,
 ( #10736, #11536, #39759, #36275 ),
 .UNSPECIFIED., .F., .F.,
 ( 4, 4 ),
 ( 0.000000000000000000, 6.391136169898659513E-06 ),
 .UNSPECIFIED. ) ;
#15319=CARTESIAN_POINT ( 'NONE',  ( -1.219418532703906877, -27.82788610016705988, 6.894806418505346812 ) ) ;
#15325=CARTESIAN_POINT ( 'NONE',  ( -1.003639145148646827, -27.34771824976135335, 7.700536657684222241 ) ) ;
#15338=PLANE ( 'NONE',  #15743 ) ;
#15339=CARTESIAN_POINT ( 'NONE',  ( 3.427802856742246274, -26.52591081038080389, 7.737115613922529000 ) ) ;
#15345=CARTESIAN_POINT ( 'NONE',  ( 5.042305363714541855, -28.94414881188822619, 7.695279973900954751 ) ) ;
#15351=EDGE_CURVE ( 'NONE', #637, #11496, #3429, .T. ) ;
#15355=DIRECTION ( 'NONE',  ( 0.1736481776669404897, -0.9848077530122062440, -0.000000000000000000 ) ) ;
#15368=( BOUNDED_CURVE ( )  B_SPLINE_CURVE ( 3, ( #17575, #7520, #17371, #4644 ),
 .UNSPECIFIED., .F., .F. ) 
 B_SPLINE_CURVE_WITH_KNOTS ( ( 4, 4 ),
 ( 4.712388980384689674, 4.895802057644191407 ),
 .UNSPECIFIED. ) 
 CURVE ( )  GEOMETRIC_REPRESENTATION_ITEM ( )  RATIONAL_B_SPLINE_CURVE ( ( 1.000000000000000000, 0.9971986010846198845, 0.9971986010846198845, 1.000000000000000000 ) ) 
 REPRESENTATION_ITEM ( '' )  );
#15369=CARTESIAN_POINT ( 'NONE',  ( -1.748552835046873311, -28.97426312752735811, 7.756742906098587298 ) ) ;
#15371=CARTESIAN_POINT ( 'NONE',  ( -1.336220785630046981, -31.09930730182104242, 6.903372536218455480 ) ) ;
#15372=ORIENTED_EDGE ( 'NONE', *, *, #35111, .T. ) ;
#15376=CARTESIAN_POINT ( 'NONE',  ( 4.927610109650206738, -30.92457071343696384, 7.013842709614101167 ) ) ;
#15383=ORIENTED_EDGE ( 'NONE', *, *, #19766, .F. ) ;
#15385=ADVANCED_FACE ( 'NONE', ( #9632 ), #18903, .F. ) ;
#15395=CARTESIAN_POINT ( 'NONE',  ( 5.028764603308605530, -28.48812247857538438, 7.754798119455333705 ) ) ;
#15396=CARTESIAN_POINT ( 'NONE',  ( 4.089396484546625743, -27.01207004994921590, 6.921725064902951807 ) ) ;
#15397=CARTESIAN_POINT ( 'NONE',  ( -0.9919418010453353585, -27.33356058713898307, 7.750000000000000888 ) ) ;
#15400=CARTESIAN_POINT ( 'NONE',  ( 1.864984047224969688, -26.17390644987066040, 6.876076431790004939 ) ) ;
#15403=ORIENTED_EDGE ( 'NONE', *, *, #37238, .F. ) ;
#15406=CARTESIAN_POINT ( 'NONE',  ( -1.326458086256048663, -31.32451895819955112, 7.762796336881259585 ) ) ;
#15408=CARTESIAN_POINT ( 'NONE',  ( -1.268168650321787716, -31.22753658603060956, 6.894806418505346812 ) ) ;
#15411=ORIENTED_EDGE ( 'NONE', *, *, #8639, .T. ) ;
#15412=VERTEX_POINT ( 'NONE', #15397 ) ;
#15414=CARTESIAN_POINT ( 'NONE',  ( -1.505759322122861787, -28.43828526875796214, 7.670860738520326905 ) ) ;
#15422=CARTESIAN_POINT ( 'NONE',  ( 4.748933141249126244, -31.28934451117660487, 7.710604733652628440 ) ) ;
#15426=CARTESIAN_POINT ( 'NONE',  ( 2.105750943142600029, -32.94567937155306225, 7.013842709614101167 ) ) ;
#15431=ADVANCED_FACE ( 'NONE', ( #3693 ), #34581, .F. ) ;
#15435=CARTESIAN_POINT ( 'NONE',  ( 3.536390127705351993, -26.59562449125457917, 7.771081512783702294 ) ) ;
#15437=CARTESIAN_POINT ( 'NONE',  ( 1.064090257649125792, -26.12825580611192677, 7.730015791551948290 ) ) ;
#15442=AXIS2_PLACEMENT_3D ( 'NONE', #18294, #33772, #24063 ) ;
#15448=CARTESIAN_POINT ( 'NONE',  ( 5.144595142829149204, -29.03130177782659160, 7.784725160561909441 ) ) ;
#15449=CARTESIAN_POINT ( 'NONE',  ( -1.348517286369408597, -27.85116208076715694, 7.697032948437507294 ) ) ;
#15450=ORIENTED_EDGE ( 'NONE', *, *, #36484, .F. ) ;
#15452=CARTESIAN_POINT ( 'NONE',  ( -1.225953191357326499, -31.30097466021442187, 7.703977250142848732 ) ) ;
#15466=CARTESIAN_POINT ( 'NONE',  ( 1.700390093233090871, -29.56993018339339940, 6.850000000000000533 ) ) ;
#15475=DIRECTION ( 'NONE',  ( 0.9396926207859001012, 0.3420201433256914170, 0.000000000000000000 ) ) ;
#15481=EDGE_CURVE ( 'NONE', #38247, #40564, #21265, .T. ) ;
#15483=CARTESIAN_POINT ( 'NONE',  ( 2.304086713256504382, -32.91590543598751850, 7.635761828346577573 ) ) ;
#15484=EDGE_CURVE ( 'NONE', #25871, #7218, #37613, .T. ) ;
#15487=B_SPLINE_CURVE_WITH_KNOTS ( 'NONE', 3,
 ( #1811, #17619, #36984, #5086, #2216, #14534, #39658, #5289, #14736, #14955, #5701, #21145, #23803, #39870, #39449, #17413, #27521, #14336, #18035, #20932, #8357, #15159, #26906, #2017, #11238, #5491, #40075, #11854, #8149, #33712, #24633 ),
 .UNSPECIFIED., .F., .F.,
 ( 4, 3, 3, 3, 3, 3, 3, 3, 3, 3, 4 ),
 ( 2.531095456908227149E-18, 3.077658087705945685E-05, 6.152638666999577953E-05, 9.267501192706705719E-05, 0.0001241882240135256765, 0.0001556618703051725191, 0.0001866161554452253123, 0.0002167966385861005865, 0.0002463805737537804711, 0.0002758761370306588869, 0.0002847094172290117711 ),
 .UNSPECIFIED. ) ;
#15489=DIRECTION ( 'NONE',  ( 0.8660254037844380415, 0.5000000000000009992, -0.000000000000000000 ) ) ;
#15491=CARTESIAN_POINT ( 'NONE',  ( -1.400655036095836525, -31.19274228153209805, 6.875780273367530171 ) ) ;
#15496=ORIENTED_EDGE ( 'NONE', *, *, #22523, .F. ) ;
#15498=CARTESIAN_POINT ( 'NONE',  ( -0.7622425899803056959, -33.94363691401473915, 7.695279973900954751 ) ) ;
#15500=CARTESIAN_POINT ( 'NONE',  ( 0.5312670209085799122, -32.86889349860920362, 7.660770905198776681 ) ) ;
#15504=CARTESIAN_POINT ( 'NONE',  ( 5.078421676527827167, -29.18405115796800331, 6.929923840112063971 ) ) ;
#15505=CARTESIAN_POINT ( 'NONE',  ( -0.9551886663611179884, -31.69313230502388024, 7.782034975670474530 ) ) ;
#15509=CARTESIAN_POINT ( 'NONE',  ( 2.098952397805311065, -32.94648879970292654, 6.903372536218458144 ) ) ;
#15512=CARTESIAN_POINT ( 'NONE',  ( 2.829405163535267942, -26.36285597610873310, 7.695279973900954751 ) ) ;
#15513=CARTESIAN_POINT ( 'NONE',  ( -1.516055275688932502, -30.67199249048969278, 6.880147297696980857 ) ) ;
#15516=LINE ( 'NONE', #6259, #16645 ) ;
#15519=CARTESIAN_POINT ( 'NONE',  ( -2.972149592069638580, -28.62058083279596588, 6.954324564059724878 ) ) ;
#15520=DIRECTION ( 'NONE',  ( -0.7660444431189813441, 0.6427876096865353661, -0.000000000000000000 ) ) ;
#15522=CARTESIAN_POINT ( 'NONE',  ( 4.860131460834224981, -30.82536650786092380, 7.774064877406526186 ) ) ;
#15524=EDGE_LOOP ( 'NONE', ( #40146, #37659, #9423, #18500, #14144 ) ) ;
#15526=DIRECTION ( 'NONE',  ( -1.000000000000000000, 0.000000000000000000, 0.000000000000000000 ) ) ;
#15529=ORIENTED_EDGE ( 'NONE', *, *, #12924, .F. ) ;
#15530=VERTEX_POINT ( 'NONE', #31472 ) ;
#15533=CYLINDRICAL_SURFACE ( 'NONE', #24321, 3.399999999999999911 ) ;
#15540=CARTESIAN_POINT ( 'NONE',  ( 4.668540769505296950, -31.42424039273510061, 7.754798119455333705 ) ) ;
#15542=CARTESIAN_POINT ( 'NONE',  ( -1.250824363190944588, -27.88163718980674233, 7.635761828346577573 ) ) ;
#15543=ORIENTED_EDGE ( 'NONE', *, *, #7725, .F. ) ;
#15545=CARTESIAN_POINT ( 'NONE',  ( -0.5767923600352592439, -26.91202874155498037, 7.695279973900954751 ) ) ;
#15546=ORIENTED_EDGE ( 'NONE', *, *, #17643, .T. ) ;
#15549=CARTESIAN_POINT ( 'NONE',  ( 1.646554145741061737, -32.96950506480602883, 6.889465824494256374 ) ) ;
#15551=DIRECTION ( 'NONE',  ( -0.000000000000000000, -0.000000000000000000, -1.000000000000000000 ) ) ;
#15555=CARTESIAN_POINT ( 'NONE',  ( 5.043527284170251868, -28.95070318796772213, 7.730758795053806587 ) ) ;
#15562=ORIENTED_EDGE ( 'NONE', *, *, #2067, .T. ) ;
#15567=CARTESIAN_POINT ( 'NONE',  ( 4.964848989002191182, -30.79572542994174000, 7.783750581861601070 ) ) ;
#15568=CARTESIAN_POINT ( 'NONE',  ( -1.060034464505671403, -31.72168673584834053, 7.750000000000000888 ) ) ;
#15570=VECTOR ( 'NONE', #18414, 1000.000000000000000 ) ;
#15576=VERTEX_POINT ( 'NONE', #1397 ) ;
#15581=CARTESIAN_POINT ( 'NONE',  ( -1.698895226757518362, -29.49949936766056169, 7.784476445165074310 ) ) ;
#15583=CARTESIAN_POINT ( 'NONE',  ( -0.8674134075260871990, -27.34139138375608979, 6.887041543973313473 ) ) ;
#15586=CARTESIAN_POINT ( 'NONE',  ( 0.02975571862627216652, -26.50603724034379383, 7.780491323090173772 ) ) ;
#15594=ORIENTED_EDGE ( 'NONE', *, *, #39787, .F. ) ;
#15598=CARTESIAN_POINT ( 'NONE',  ( 5.010951146761534858, -30.34466785830838376, 6.895222827070022653 ) ) ;
#15601=CYLINDRICAL_SURFACE ( 'NONE', #12135, 0.09010775117053032579 ) ;
#15602=ORIENTED_EDGE ( 'NONE', *, *, #11462, .F. ) ;
#15606=CARTESIAN_POINT ( 'NONE',  ( 4.093933310419832772, -27.01631492900221687, 6.951256099901589991 ) ) ;
#15607=CARTESIAN_POINT ( 'NONE',  ( -1.744066689084928345, -30.19099175420856440, 7.635761828346576685 ) ) ;
#15621=VECTOR ( 'NONE', #2035, 1000.000000000000114 ) ;
#15623=EDGE_CURVE ( 'NONE', #1123, #31660, #16806, .T. ) ;
#15626=CARTESIAN_POINT ( 'NONE',  ( 1.007971533865419156, -32.89869384730054236, 6.864651958020304257 ) ) ;
#15635=CARTESIAN_POINT ( 'NONE',  ( 4.907464300517769829, -30.69894525369553762, 7.695279973900954751 ) ) ;
#15637=CARTESIAN_POINT ( 'NONE',  ( 3.341357570912008246, -32.66140680771919591, 7.751599049952198506 ) ) ;
#15640=CARTESIAN_POINT ( 'NONE',  ( 0.6020978191758283860, -26.25162571309269310, 7.771081512783698741 ) ) ;
#15642=ORIENTED_EDGE ( 'NONE', *, *, #36258, .F. ) ;
#15647=CARTESIAN_POINT ( 'NONE',  ( 3.449253643630207922, -26.54193261727931485, 7.767720160662275219 ) ) ;
#15650=CARTESIAN_POINT ( 'NONE',  ( -1.610418084489225299, -28.79627056164295595, 7.013842709614101167 ) ) ;
#15653=ORIENTED_EDGE ( 'NONE', *, *, #30609, .F. ) ;
#15654=AXIS2_PLACEMENT_3D ( 'NONE', #35026, #31514, #25737 ) ;
#15655=EDGE_LOOP ( 'NONE', ( #28689, #28804, #39879, #7124 ) ) ;
#15658=CARTESIAN_POINT ( 'NONE',  ( 2.817328913877361618, -32.78123018042540338, 6.894806418505346812 ) ) ;
#15659=CARTESIAN_POINT ( 'NONE',  ( 0.9730757925788008356, -32.99329091482906762, 7.754798119455333705 ) ) ;
#15662=B_SPLINE_CURVE_WITH_KNOTS ( 'NONE', 3,
 ( #30191, #18235, #30825, #29988, #8557, #36172, #7954, #20502, #17405, #8143, #1803, #14328, #5080, #2010, #14529, #34742, #6521, #37179, #28329 ),
 .UNSPECIFIED., .F., .F.,
 ( 4, 3, 3, 3, 3, 3, 4 ),
 ( 4.336808689942017736E-19, 2.546128104244783067E-05, 5.711050680483586430E-05, 8.113074941675582901E-05, 0.0001053129305727050724, 0.0001360598016347148054, 0.0001612931755702014865 ),
 .UNSPECIFIED. ) ;
#15663=EDGE_CURVE ( 'NONE', #10847, #32112, #35356, .T. ) ;
#15665=ORIENTED_EDGE ( 'NONE', *, *, #10098, .T. ) ;
#15669=B_SPLINE_CURVE_WITH_KNOTS ( 'NONE', 3,
 ( #17206, #14121, #32684, #4481, #39234, #23603, #36167, #7947, #24205, #40665 ),
 .UNSPECIFIED., .F., .F.,
 ( 4, 3, 3, 4 ),
 ( 0.0001585009270395744765, 0.0001815657551981843297, 0.0002118214035944115297, 0.0002170292169044783044 ),
 .UNSPECIFIED. ) ;
#15673=DIRECTION ( 'NONE',  ( -0.9396926207859057634, -0.3420201433256757073, -0.000000000000000000 ) ) ;
#15678=DIRECTION ( 'NONE',  ( 0.5751513419797943394, -0.4826092789263614069, 0.6605219282605379050 ) ) ;
#15686=CARTESIAN_POINT ( 'NONE',  ( 2.332967242263025653, -33.01229566874723531, 7.651421919295144036 ) ) ;
#15687=CYLINDRICAL_SURFACE ( 'NONE', #21726, 3.399999999999999911 ) ;
#15696=CARTESIAN_POINT ( 'NONE',  ( 4.299012799853332290, -31.91455539574284472, 6.867199677474202346 ) ) ;
#15697=CARTESIAN_POINT ( 'NONE',  ( -1.694080628484398332, -29.37610418048680572, 6.903372536218456368 ) ) ;
#15701=CARTESIAN_POINT ( 'NONE',  ( 1.530693017522448462, -33.06581389177033259, 6.895394898881670009 ) ) ;
#15703=EDGE_LOOP ( 'NONE', ( #25505, #37407, #23473, #26712, #6428 ) ) ;
#15705=CARTESIAN_POINT ( 'NONE',  ( -0.6341309666911102427, -32.04178038199096079, 6.911401339314954484 ) ) ;
#15706=CARTESIAN_POINT ( 'NONE',  ( 1.680239621640250647, -25.22888099285786012, 7.013842709614101167 ) ) ;
#15710=CARTESIAN_POINT ( 'NONE',  ( 1.731267656427840862, -33.06979397732754933, 7.665454363767879364 ) ) ;
#15711=CARTESIAN_POINT ( 'NONE',  ( 0.4675928667938681893, -32.83026482617694342, 7.785096263473211486 ) ) ;
#15712=CARTESIAN_POINT ( 'NONE',  ( 1.749297880632027846, -33.07639249659003866, 7.255881584735164758 ) ) ;
#15713=CARTESIAN_POINT ( 'NONE',  ( 0.4906401998943609177, -26.28564864924214461, 7.635761828346577573 ) ) ;
#15720=EDGE_LOOP ( 'NONE', ( #34211, #22456, #31607, #2260, #32129 ) ) ;
#15721=B_SPLINE_CURVE_WITH_KNOTS ( 'NONE', 3,
 ( #14116, #14319, #11020, #26889, #39430, #37569, #6509, #12664, #31014, #6092 ),
 .UNSPECIFIED., .F., .F.,
 ( 4, 3, 3, 4 ),
 ( 0.0002170292169044741302, 0.0002420761345915971492, 0.0002723302478207005281, 0.0002816811360866754458 ),
 .UNSPECIFIED. ) ;
#15726=DIRECTION ( 'NONE',  ( 0.7660444431189770143, 0.6427876096865404731, -0.000000000000000000 ) ) ;
#15727=EDGE_CURVE ( 'NONE', #16031, #2342, #7323, .T. ) ;
#15730=CARTESIAN_POINT ( 'NONE',  ( 1.223729437044696500, -26.20350854924802064, 7.761597726988849644 ) ) ;
#15740=CARTESIAN_POINT ( 'NONE',  ( -1.672621849119248827, -29.99755011404314331, 6.876076431790006716 ) ) ;
#15743=AXIS2_PLACEMENT_3D ( 'NONE', #6292, #19051, #34515 ) ;
#15746=( BOUNDED_CURVE ( )  B_SPLINE_CURVE ( 3, ( #6077, #21727, #12023, #40648 ),
 .UNSPECIFIED., .F., .T. ) 
 B_SPLINE_CURVE_WITH_KNOTS ( ( 4, 4 ),
 ( 4.748221474220558846, 4.941946782021391371 ),
 .UNSPECIFIED. ) 
 CURVE ( )  GEOMETRIC_REPRESENTATION_ITEM ( )  RATIONAL_B_SPLINE_CURVE ( ( 1.000000000000000000, 0.9968749865767494445, 0.9968749865767494445, 1.000000000000000000 ) ) 
 REPRESENTATION_ITEM ( '' )  );
#15747=CARTESIAN_POINT ( 'NONE',  ( 2.875320765573441850, -32.76047449742785034, 7.756377446753164762 ) ) ;
#15755=VECTOR ( 'NONE', #16784, 1000.000000000000227 ) ;
#15758=CARTESIAN_POINT ( 'NONE',  ( -1.799609906766908463, -29.57443106626083562, 7.625529684960262067 ) ) ;
#15764=B_SPLINE_CURVE_WITH_KNOTS ( 'NONE', 3,
 ( #376, #12912, #9825, #3679, #19703, #13519, #16400, #4268, #23002, #1192 ),
 .UNSPECIFIED., .F., .F.,
 ( 4, 3, 3, 4 ),
 ( 0.000000000000000000, 3.025570593003164513E-05, 6.051145698344131968E-05, 6.468151674593574090E-05 ),
 .UNSPECIFIED. ) ;
#15765=CARTESIAN_POINT ( 'NONE',  ( 5.067738213087761068, -29.09985929542945371, 7.754798119455333705 ) ) ;
#15769=VERTEX_POINT ( 'NONE', #11631 ) ;
#15770=EDGE_LOOP ( 'NONE', ( #9284, #8482, #32025, #25832, #32754, #10503 ) ) ;
#15779=LINE ( 'NONE', #34745, #10318 ) ;
#15780=B_SPLINE_CURVE_WITH_KNOTS ( 'NONE', 3,
 ( #30229, #36808, #11467, #1840, #18058, #33736, #24035, #20961, #36606, #5516, #27336, #39278, #14982, #39896, #30649, #30856, #33951, #11876, #11066 ),
 .UNSPECIFIED., .F., .F.,
 ( 4, 3, 3, 3, 3, 3, 4 ),
 ( 1.563658610346375379E-18, 2.546128104244800347E-05, 5.711050680483675200E-05, 8.113074941675925780E-05, 0.0001053129305727098293, 0.0001360598016347188441, 0.0001612931755702000228 ),
 .UNSPECIFIED. ) ;
#15781=EDGE_LOOP ( 'NONE', ( #19121, #5980, #39562, #10704, #3745 ) ) ;
#15789=AXIS2_PLACEMENT_3D ( 'NONE', #37907, #6639, #21334 ) ;
#15794=PLANE ( 'NONE',  #30920 ) ;
#15796=ORIENTED_EDGE ( 'NONE', *, *, #29482, .F. ) ;
#15798=CARTESIAN_POINT ( 'NONE',  ( 1.700390093233090871, -29.56993018339339940, 7.750000000000000888 ) ) ;
#15804=CARTESIAN_POINT ( 'NONE',  ( -1.006913970787454371, -31.62676587767679237, 6.876076431790007604 ) ) ;
#15807=LINE ( 'NONE', #12914, #23493 ) ;
#15815=CARTESIAN_POINT ( 'NONE',  ( 3.979067762612290338, -26.91330170476399530, 6.887161170156906209 ) ) ;
#15820=ORIENTED_EDGE ( 'NONE', *, *, #1283, .F. ) ;
#15828=ORIENTED_EDGE ( 'NONE', *, *, #28086, .T. ) ;
#15830=VERTEX_POINT ( 'NONE', #29594 ) ;
#15835=CARTESIAN_POINT ( 'NONE',  ( 5.150202707224498688, -30.16051711886163744, 7.750000000000001776 ) ) ;
#15838=ORIENTED_EDGE ( 'NONE', *, *, #7540, .F. ) ;
#15845=EDGE_CURVE ( 'NONE', #4130, #25231, #10238, .T. ) ;
#15849=CARTESIAN_POINT ( 'NONE',  ( 3.474430093958352117, -26.56792286420624549, 7.783750581861600182 ) ) ;
#15850=CARTESIAN_POINT ( 'NONE',  ( 1.057242960569753309, -26.12952878737186424, 7.697032948437507294 ) ) ;
#15852=B_SPLINE_CURVE_WITH_KNOTS ( 'NONE', 3,
 ( #9468, #1050, #31724, #29038, #842, #35434, #6404, #28420, #226, #12766 ),
 .UNSPECIFIED., .F., .F.,
 ( 4, 3, 3, 4 ),
 ( 0.0001585009270395733923, 0.0001815657551981825950, 0.0002118214035944112044, 0.0002170292169044733984 ),
 .UNSPECIFIED. ) ;
#15857=CARTESIAN_POINT ( 'NONE',  ( 0.4278139304635389939, -32.72279481110962251, 7.759451378593096749 ) ) ;
#15862=( BOUNDED_CURVE ( )  B_SPLINE_CURVE ( 3, ( #9597, #5908, #6526, #18447 ),
 .UNSPECIFIED., .F., .T. ) 
 B_SPLINE_CURVE_WITH_KNOTS ( ( 4, 4 ),
 ( 4.708531083176466403, 4.712388980384689674 ),
 .UNSPECIFIED. ) 
 CURVE ( )  GEOMETRIC_REPRESENTATION_ITEM ( )  RATIONAL_B_SPLINE_CURVE ( ( 1.000000000000000000, 0.9999987597194787137, 0.9999987597194787137, 1.000000000000000000 ) ) 
 REPRESENTATION_ITEM ( '' )  );
#15864=CARTESIAN_POINT ( 'NONE',  ( -1.254331348952123282, -31.25210608373809507, 7.779495906702013741 ) ) ;
#15870=LINE ( 'NONE', #18963, #24471 ) ;
#15871=VERTEX_POINT ( 'NONE', #14735 ) ;
#15874=ORIENTED_EDGE ( 'NONE', *, *, #2166, .F. ) ;
#15876=CARTESIAN_POINT ( 'NONE',  ( 4.919866799368763033, -30.96019790882458622, 7.387053503561884504 ) ) ;
#15877=CARTESIAN_POINT ( 'NONE',  ( 4.954788903825591007, -28.58559216437443595, 6.895222827070022653 ) ) ;
#15878=CARTESIAN_POINT ( 'NONE',  ( 4.995237956833183723, -30.75059844998224179, 7.750000000000001776 ) ) ;
#15885=CARTESIAN_POINT ( 'NONE',  ( -1.750311609132544799, -28.98456041880788092, 7.742274884880765207 ) ) ;
#15888=CARTESIAN_POINT ( 'NONE',  ( 3.914596803305051331, -32.26372945462702546, 7.783750581861601070 ) ) ;
#15889=FACE_OUTER_BOUND ( 'NONE', #26898, .T. ) ;
#15893=ORIENTED_EDGE ( 'NONE', *, *, #34525, .F. ) ;
#15895=VECTOR ( 'NONE', #3324, 999.9999999999998863 ) ;
#15896=CARTESIAN_POINT ( 'NONE',  ( -0.7071601137375974622, -32.11974912022817108, 7.387053503561887169 ) ) ;
#15906=EDGE_CURVE ( 'NONE', #2075, #32186, #34339, .T. ) ;
#15908=CARTESIAN_POINT ( 'NONE',  ( 1.677658713487880870, -26.07000400068970336, 7.742274884880762542 ) ) ;
#15912=CARTESIAN_POINT ( 'NONE',  ( 4.643350526641022213, -31.46439155470594073, 7.013842709614101167 ) ) ;
#15913=CARTESIAN_POINT ( 'NONE',  ( 4.358391383913280848, -27.29286427772829526, 7.700536657684219577 ) ) ;
#15915=CARTESIAN_POINT ( 'NONE',  ( 3.365638799831626837, -32.53422458008159168, 7.784838882742139532 ) ) ;
#15917=CARTESIAN_POINT ( 'NONE',  ( -1.451641158382428243, -28.29529165423184622, 7.757178535559533294 ) ) ;
#15919=DIRECTION ( 'NONE',  ( -0.6427876096865430267, 0.7660444431189749048, -0.000000000000000000 ) ) ;
#15925=CARTESIAN_POINT ( 'NONE',  ( 1.189432498329193288, -26.20853045501920064, 7.782034975670475418 ) ) ;
#15926=VECTOR ( 'NONE', #26952, 999.9999999999998863 ) ;
#15930=LINE ( 'NONE', #3610, #24766 ) ;
#15931=CARTESIAN_POINT ( 'NONE',  ( -1.116006548226288642, -31.48728922445879519, 7.505001789837628223 ) ) ;
#15935=CARTESIAN_POINT ( 'NONE',  ( -1.671431054133620586, -30.00687134634513242, 6.871394612369935651 ) ) ;
#15940=EDGE_CURVE ( 'NONE', #18417, #18768, #7830, .T. ) ;
#15941=CARTESIAN_POINT ( 'NONE',  ( -1.617914377067610765, -30.66822245745067477, 7.771081512783700518 ) ) ;
#15943=B_SPLINE_CURVE_WITH_KNOTS ( 'NONE', 3,
 ( #28209, #15452, #39, #12568, #25137, #3348, #6811, #31936, #37668, #37473, #6407, #15864, #9269, #648, #28423, #18957, #31522, #12770, #7007, #25343, #37880, #22269, #28634, #25749, #34837 ),
 .UNSPECIFIED., .F., .F.,
 ( 4, 3, 3, 3, 3, 3, 3, 3, 4 ),
 ( 6.468151674593483288E-05, 9.076621574722077974E-05, 0.0001210204262067974109, 0.0001512763324577400957, 0.0001815301820994215929, 0.0002117781465860753135, 0.0002420274594459748011, 0.0002722905548971200711, 0.0002816827545175596553 ),
 .UNSPECIFIED. ) ;
#15949=B_SPLINE_CURVE_WITH_KNOTS ( 'NONE', 3,
 ( #13690, #20456, #17353, #29932, #13479, #26259, #14280, #26849, #5027, #39390, #7502, #32642, #23752, #8093, #5231, #36522, #27248, #5433, #27656, #27054, #24785, #40211, #12212, #21497, #5641, #20870, #18181, #17972, #30558, #39816, #11383 ),
 .UNSPECIFIED., .F., .F.,
 ( 4, 3, 3, 3, 3, 3, 3, 3, 3, 3, 4 ),
 ( 1.734723475976807094E-18, 2.999644130997484968E-05, 6.002588995694506797E-05, 8.960886084587879282E-05, 0.0001190604700446485644, 0.0001489538463052720186, 0.0001796139255493970147, 0.0002109707048517054523, 0.0002426195318110361155, 0.0002740640997890075935, 0.0002849778069099933643 ),
 .UNSPECIFIED. ) ;
#15950=ORIENTED_EDGE ( 'NONE', *, *, #35033, .T. ) ;
#15953=ORIENTED_EDGE ( 'NONE', *, *, #22949, .T. ) ;
#15957=CARTESIAN_POINT ( 'NONE',  ( -1.559432610588336932, -30.53614500623134376, 6.979335674598009298 ) ) ;
#15959=LINE ( 'NONE', #28521, #18020 ) ;
#15960=CARTESIAN_POINT ( 'NONE',  ( 5.199376495817195298, -29.65415698750913265, 6.865554069792298542 ) ) ;
#15961=CARTESIAN_POINT ( 'NONE',  ( 4.327845609297687801, -31.72781746291050098, 7.691066658568941783 ) ) ;
#15962=CARTESIAN_POINT ( 'NONE',  ( 3.481437286441587897, -32.58288071328335178, 7.695279973900954751 ) ) ;
#15963=AXIS2_PLACEMENT_3D ( 'NONE', #15466, #27619, #34034 ) ;
#15968=ORIENTED_EDGE ( 'NONE', *, *, #35812, .F. ) ;
#15976=CARTESIAN_POINT ( 'NONE',  ( 0.02590584277092264007, -32.52900140506991988, 7.661510568013096822 ) ) ;
#15977=ORIENTED_EDGE ( 'NONE', *, *, #6880, .F. ) ;
#15980=VERTEX_POINT ( 'NONE', #37426 ) ;
#15983=CARTESIAN_POINT ( 'NONE',  ( -1.699178655868960552, -29.51577928193538369, 7.785387725071490905 ) ) ;
#15987=ORIENTED_EDGE ( 'NONE', *, *, #31206, .T. ) ;
#15988=VERTEX_POINT ( 'NONE', #31073 ) ;
#15991=CARTESIAN_POINT ( 'NONE',  ( 4.104433119696450305, -25.16239669867571749, 7.754798119455333705 ) ) ;
#15992=CARTESIAN_POINT ( 'NONE',  ( 3.419158195859357097, -26.52102280379090971, 7.686927408461904143 ) ) ;
#15993=DIRECTION ( 'NONE',  ( -1.000000000000000000, 0.000000000000000000, 0.000000000000000000 ) ) ;
#15996=DIRECTION ( 'NONE',  ( -0.3420201433256725987, 0.9396926207859068736, -0.000000000000000000 ) ) ;
#15999=EDGE_CURVE ( 'NONE', #2110, #5237, #34483, .T. ) ;
#16000=CARTESIAN_POINT ( 'NONE',  ( -1.001222095928207656, -31.63424290415207096, 6.871394612369937427 ) ) ;
#16001=LINE ( 'NONE', #33392, #29382 ) ;
#16012=CARTESIAN_POINT ( 'NONE',  ( 2.474049714983522108, -26.25912200567108457, 7.013842709614101167 ) ) ;
#16015=CARTESIAN_POINT ( 'NONE',  ( 1.703254855081945740, -26.16993139028485871, 7.769368695748487319 ) ) ;
#16016=DIRECTION ( 'NONE',  ( -0.6834397476448871300, 0.000000000000000000, -0.7300069255418698555 ) ) ;
#16018=CARTESIAN_POINT ( 'NONE',  ( -1.003736583562488072, -27.34783681995375915, 7.686927408461907696 ) ) ;
#16027=ORIENTED_EDGE ( 'NONE', *, *, #9729, .T. ) ;
#16031=VERTEX_POINT ( 'NONE', #31276 ) ;
#16035=CARTESIAN_POINT ( 'NONE',  ( 5.166400672645620418, -29.08388956939788272, 7.753200566781577763 ) ) ;
#16039=VECTOR ( 'NONE', #16080, 1000.000000000000000 ) ;
#16040=CARTESIAN_POINT ( 'NONE',  ( 4.700406739381271848, -27.96996139531226433, 6.864276522220859711 ) ) ;
#16041=CARTESIAN_POINT ( 'NONE',  ( 4.554642986601973753, -31.41742589940882269, 6.882085323592685988 ) ) ;
#16042=CARTESIAN_POINT ( 'NONE',  ( 3.960473582032317363, -32.24238647371081612, 7.635761828346576685 ) ) ;
#16043=CARTESIAN_POINT ( 'NONE',  ( 5.144846875551112753, -28.94886861257825572, 7.635761828346576685 ) ) ;
#16045=ORIENTED_EDGE ( 'NONE', *, *, #7396, .F. ) ;
#16047=ORIENTED_EDGE ( 'NONE', *, *, #34232, .T. ) ;
#16050=DIRECTION ( 'NONE',  ( -1.000000000000000000, 0.000000000000000000, 0.000000000000000000 ) ) ;
#16052=CARTESIAN_POINT ( 'NONE',  ( -1.266401589527426763, -27.89466816046029862, 7.257242401810563237 ) ) ;
#16057=ORIENTED_EDGE ( 'NONE', *, *, #23460, .T. ) ;
#16062=CARTESIAN_POINT ( 'NONE',  ( 5.100338292692609521, -29.55116209899513180, 7.748216051605116839 ) ) ;
#16070=ORIENTED_EDGE ( 'NONE', *, *, #21656, .F. ) ;
#16071=ORIENTED_EDGE ( 'NONE', *, *, #30204, .F. ) ;
#16073=CARTESIAN_POINT ( 'NONE',  ( 1.691556635064260350, -33.06436417196861299, 7.773839561854632763 ) ) ;
#16074=CARTESIAN_POINT ( 'NONE',  ( 1.754226040725147096, -26.17035530198076643, 6.889465824494257262 ) ) ;
#16078=CARTESIAN_POINT ( 'NONE',  ( -0.5138166168388553778, -26.87613091215975913, 7.783750581861601070 ) ) ;
#16079=VERTEX_POINT ( 'NONE', #8101 ) ;
#16080=DIRECTION ( 'NONE',  ( -0.9396926207859104263, 0.3420201433256631063, -0.000000000000000000 ) ) ;
#16081=CARTESIAN_POINT ( 'NONE',  ( 4.945111664236113924, -28.55411654084933204, 6.871394612369935651 ) ) ;
#16083=CARTESIAN_POINT ( 'NONE',  ( 3.804543977483544559, -32.36680995045413312, 6.921725064902950031 ) ) ;
#16091=ORIENTED_EDGE ( 'NONE', *, *, #8585, .F. ) ;
#16099=AXIS2_PLACEMENT_3D ( 'NONE', #23175, #757, #20077 ) ;
#16100=DIRECTION ( 'NONE',  ( 0.8660254037844380415, 0.5000000000000009992, -0.000000000000000000 ) ) ;
#16104=( BOUNDED_CURVE ( )  B_SPLINE_CURVE ( 3, ( #26706, #39240, #39651, #33511 ),
 .UNSPECIFIED., .F., .F. ) 
 B_SPLINE_CURVE_WITH_KNOTS ( ( 4, 4 ),
 ( 1.381924640371167579, 1.574767692156076038 ),
 .UNSPECIFIED. ) 
 CURVE ( )  GEOMETRIC_REPRESENTATION_ITEM ( )  RATIONAL_B_SPLINE_CURVE ( ( 1.000000000000000000, 0.9969033633783032089, 0.9969033633783032089, 1.000000000000000000 ) ) 
 REPRESENTATION_ITEM ( '' )  );
#16105=CARTESIAN_POINT ( 'NONE',  ( -0.2133591888346773602, -32.50038470195961082, 6.951256099901593544 ) ) ;
#16109=CARTESIAN_POINT ( 'NONE',  ( -1.265720463714046895, -27.71192368072266277, 7.750000000000000888 ) ) ;
#16110=CARTESIAN_POINT ( 'NONE',  ( 4.707770054155486328, -31.33846319669150660, 7.781480525794719938 ) ) ;
#16116=CARTESIAN_POINT ( 'NONE',  ( -0.8817401311824972776, -31.78185462018515750, 7.712764235869105534 ) ) ;
#16117=CARTESIAN_POINT ( 'NONE',  ( 1.720554196122513257, -32.96987691609166404, 7.643333865083956624 ) ) ;
#16118=DIRECTION ( 'NONE',  ( -0.5751513419797880111, -0.4826092789263689564, 0.6605219282605377940 ) ) ;
#16125=ORIENTED_EDGE ( 'NONE', *, *, #28206, .T. ) ;
#16126=CARTESIAN_POINT ( 'NONE',  ( 2.884763386751913572, -26.27641232226080703, 7.635761828346579350 ) ) ;
#16129=ORIENTED_EDGE ( 'NONE', *, *, #7442, .F. ) ;
#16133=CARTESIAN_POINT ( 'NONE',  ( -1.431314549547642256, -28.24613789213861281, 6.882085323592685100 ) ) ;
#16136=CARTESIAN_POINT ( 'NONE',  ( 3.608934358494904515, -26.63608308657048340, 6.921725064902951807 ) ) ;
#16137=CARTESIAN_POINT ( 'NONE',  ( 1.123253381486050140, -26.11784194350818211, 6.894806418505347700 ) ) ;
#16139=ADVANCED_FACE ( 'NONE', ( #40221 ), #12004, .T. ) ;
#16142=CARTESIAN_POINT ( 'NONE',  ( 0.8902999215273917910, -32.98191326122828571, 7.387053503561886281 ) ) ;
#16143=EDGE_LOOP ( 'NONE', ( #17978, #31862, #17755, #35006 ) ) ;
#16146=CARTESIAN_POINT ( 'NONE',  ( -1.658561354524213716, -30.09671981084580850, 6.880147297696979969 ) ) ;
#16154=VERTEX_POINT ( 'NONE', #14690 ) ;
#16157=ORIENTED_EDGE ( 'NONE', *, *, #29614, .F. ) ;
#16159=CARTESIAN_POINT ( 'NONE',  ( 0.6211818808881177656, -26.24046902339169307, 7.751599049952197618 ) ) ;
#16160=CARTESIAN_POINT ( 'NONE',  ( -1.019135405902276581, -31.75353427597946165, 7.782861076432733505 ) ) ;
#16163=CARTESIAN_POINT ( 'NONE',  ( 3.757225787516494275, -32.27723424741392932, 6.876076431790008492 ) ) ;
#16173=EDGE_CURVE ( 'NONE', #15412, #40099, #6734, .T. ) ;
#16175=VECTOR ( 'NONE', #36045, 1000.000000000000000 ) ;
#16178=CARTESIAN_POINT ( 'NONE',  ( 1.646239191775039412, -25.86893018339335981, 7.695279973900954751 ) ) ;
#16184=ADVANCED_FACE ( 'NONE', ( #13239 ), #34291, .F. ) ;
#16187=CARTESIAN_POINT ( 'NONE',  ( 4.041943119853272037, -26.96886997397920638, 7.754798119455333705 ) ) ;
#16191=ADVANCED_FACE ( 'NONE', ( #34696 ), #25404, .T. ) ;
#16194=VERTEX_POINT ( 'NONE', #9135 ) ;
#16197=LINE ( 'NONE', #15991, #15755 ) ;
#16201=ORIENTED_EDGE ( 'NONE', *, *, #7066, .T. ) ;
#16203=CARTESIAN_POINT ( 'NONE',  ( -1.758549627899453682, -30.10456852828691865, 6.867280401193707640 ) ) ;
#16204=DIRECTION ( 'NONE',  ( -0.000000000000000000, -0.000000000000000000, -1.000000000000000000 ) ) ;
#16205=FACE_OUTER_BOUND ( 'NONE', #31585, .T. ) ;
#16210=CARTESIAN_POINT ( 'NONE',  ( -1.577145252566735767, -30.79784596747070680, 7.720710062488887360 ) ) ;
#16214=ADVANCED_FACE ( 'NONE', ( #25601 ), #18808, .F. ) ;
#16216=CARTESIAN_POINT ( 'NONE',  ( 6.064999797981664997, -27.09154098917056785, 7.695279973900954751 ) ) ;
#16217=CARTESIAN_POINT ( 'NONE',  ( 4.693152714189181118, -27.95640678116755851, 7.774064877406527074 ) ) ;
#16219=ORIENTED_EDGE ( 'NONE', *, *, #1916, .F. ) ;
#16222=ORIENTED_EDGE ( 'NONE', *, *, #11233, .F. ) ;
#16226=LINE ( 'NONE', #31281, #2074 ) ;
#16233=EDGE_CURVE ( 'NONE', #17469, #463, #3002, .T. ) ;
#16235=ORIENTED_EDGE ( 'NONE', *, *, #16721, .F. ) ;
#16242=CIRCLE ( 'NONE', #18197, 3.499999999999999556 ) ;
#16243=CARTESIAN_POINT ( 'NONE',  ( 4.690406051945708477, -27.95131943120609463, 6.866852738645442322 ) ) ;
#16244=CARTESIAN_POINT ( 'NONE',  ( 4.586012032047667830, -31.36803641669331455, 6.864276522220859711 ) ) ;
#16246=CARTESIAN_POINT ( 'NONE',  ( -2.639489883291917138, -27.04870784343005141, 7.635761828346577573 ) ) ;
#16262=CARTESIAN_POINT ( 'NONE',  ( 0.5651823463118889057, -32.77481760284047141, 7.661510568013097711 ) ) ;
#16263=DIRECTION ( 'NONE',  ( 0.1736481776669273613, 0.9848077530122086864, -0.000000000000000000 ) ) ;
#16266=VECTOR ( 'NONE', #7698, 1000.000000000000000 ) ;
#16270=ORIENTED_EDGE ( 'NONE', *, *, #2864, .F. ) ;
#16276=EDGE_LOOP ( 'NONE', ( #16865, #31950 ) ) ;
#16277=EDGE_CURVE ( 'NONE', #12271, #12509, #6263, .T. ) ;
#16279=B_SPLINE_CURVE_WITH_KNOTS ( 'NONE', 3,
 ( #29427, #1038, #38275, #13968 ),
 .UNSPECIFIED., .F., .F.,
 ( 4, 4 ),
 ( 0.000000000000000000, 6.391136169993976977E-06 ),
 .UNSPECIFIED. ) ;
#16283=VERTEX_POINT ( 'NONE', #9751 ) ;
#16286=VECTOR ( 'NONE', #24241, 1000.000000000000114 ) ;
#16299=CARTESIAN_POINT ( 'NONE',  ( 1.785524755912862194, -26.08120387293316256, 7.780491323090171996 ) ) ;
#16302=CARTESIAN_POINT ( 'NONE',  ( 3.915288987740546567, -32.15886406078164583, 7.257242401810560573 ) ) ;
#16306=DIRECTION ( 'NONE',  ( -0.3420201433256601642, -0.9396926207859115365, -0.000000000000000000 ) ) ;
#16308=CARTESIAN_POINT ( 'NONE',  ( 0.3263088656926940168, -26.34351183019633069, 7.139344958878410807 ) ) ;
#16309=ORIENTED_EDGE ( 'NONE', *, *, #35907, .F. ) ;
#16310=CARTESIAN_POINT ( 'NONE',  ( 2.277526804980155362, -33.02201842327861669, 6.894806418505347700 ) ) ;
#16313=LINE ( 'NONE', #10128, #32561 ) ;
#16314=CARTESIAN_POINT ( 'NONE',  ( 4.367281360980026506, -27.30327784999532525, 7.743886751744251562 ) ) ;
#16317=EDGE_CURVE ( 'NONE', #309, #320, #35095, .T. ) ;
#16318=CARTESIAN_POINT ( 'NONE',  ( -1.496426596291860811, -28.41215999167467743, 7.763628509615286610 ) ) ;
#16321=VERTEX_POINT ( 'NONE', #12629 ) ;
#16322=CARTESIAN_POINT ( 'NONE',  ( 5.401390093233090717, -28.86392406983564385, 6.954324564059724878 ) ) ;
#16326=CARTESIAN_POINT ( 'NONE',  ( 1.097341463758161773, -26.22383283646636087, 7.756377446753166538 ) ) ;
#16327=CARTESIAN_POINT ( 'NONE',  ( 4.392794304683587114, -31.80621346007680827, 7.640616322432098428 ) ) ;
#16328=ORIENTED_EDGE ( 'NONE', *, *, #2641, .F. ) ;
#16333=CYLINDRICAL_SURFACE ( 'NONE', #10090, 3.399999999999999911 ) ;
#16334=VERTEX_POINT ( 'NONE', #19826 ) ;
#16336=( BOUNDED_CURVE ( )  B_SPLINE_CURVE ( 3, ( #708, #32406, #13655, #13044 ),
 .UNSPECIFIED., .F., .T. ) 
 B_SPLINE_CURVE_WITH_KNOTS ( ( 4, 4 ),
 ( 1.347909859412854239, 1.534781240595298968 ),
 .UNSPECIFIED. ) 
 CURVE ( )  GEOMETRIC_REPRESENTATION_ITEM ( )  RATIONAL_B_SPLINE_CURVE ( ( 1.000000000000000000, 0.9970920404276226723, 0.9970920404276226723, 1.000000000000000000 ) ) 
 REPRESENTATION_ITEM ( '' )  );
#16337=AXIS2_PLACEMENT_3D ( 'NONE', #37311, #15489, #24347 ) ;
#16339=CARTESIAN_POINT ( 'NONE',  ( -1.713032059046489142, -28.79627056164295595, 7.013842709614101167 ) ) ;
#16348=ADVANCED_FACE ( 'NONE', ( #29893 ), #29098, .F. ) ;
#16349=FACE_OUTER_BOUND ( 'NONE', #20013, .T. ) ;
#16354=LINE ( 'NONE', #36313, #38618 ) ;
#16358=CARTESIAN_POINT ( 'NONE',  ( 3.402382127344176777, -32.62823414405891498, 6.875671892026064214 ) ) ;
#16360=CYLINDRICAL_SURFACE ( 'NONE', #20597, 0.09010775117052903516 ) ;
#16361=CARTESIAN_POINT ( 'NONE',  ( -0.5596933955661176352, -26.89747389307597203, 7.635761828346574909 ) ) ;
#16366=FACE_OUTER_BOUND ( 'NONE', #7519, .T. ) ;
#16369=PLANE ( 'NONE',  #32830 ) ;
#16370=ORIENTED_EDGE ( 'NONE', *, *, #14439, .F. ) ;
#16378=DIRECTION ( 'NONE',  ( 0.1736481776669193677, 0.9848077530122099077, 0.000000000000000000 ) ) ;
#16381=ORIENTED_EDGE ( 'NONE', *, *, #15481, .T. ) ;
#16385=CARTESIAN_POINT ( 'NONE',  ( -1.721720316595480860, -28.87059949175516849, 7.776484688137387025 ) ) ;
#16387=CARTESIAN_POINT ( 'NONE',  ( -1.699493400058616821, -29.53742913049718766, 6.912949926530957967 ) ) ;
#16392=CARTESIAN_POINT ( 'NONE',  ( 1.056572603559534418, -33.01021068541466263, 6.888594555015730592 ) ) ;
#16396=ORIENTED_EDGE ( 'NONE', *, *, #23923, .T. ) ;
#16397=CARTESIAN_POINT ( 'NONE',  ( 5.200213681912021713, -29.53468019335948824, 7.680160680325413658 ) ) ;
#16399=CARTESIAN_POINT ( 'NONE',  ( -1.011899981717923724, -31.62016981556380202, 6.882085323592687764 ) ) ;
#16400=CARTESIAN_POINT ( 'NONE',  ( 4.281747078493526537, -27.35710481417712003, 7.691066658568948000 ) ) ;
#16402=CARTESIAN_POINT ( 'NONE',  ( 4.716878747747901279, -27.79488195948977136, 7.730015791551948290 ) ) ;
#16403=CARTESIAN_POINT ( 'NONE',  ( 4.256814889047467076, -33.88948601255670212, 7.695279973900954751 ) ) ;
#16406=CARTESIAN_POINT ( 'NONE',  ( -0.01837800939314764015, -32.61883756299590686, 7.697032948437509070 ) ) ;
#16407=CARTESIAN_POINT ( 'NONE',  ( -1.287675252634163270, -27.77617148390492474, 7.785593909369613819 ) ) ;
#16411=ADVANCED_FACE ( 'NONE', ( #23321 ), #26014, .F. ) ;
#16414=DIRECTION ( 'NONE',  ( -0.8660254037844344888, -0.5000000000000069944, -0.000000000000000000 ) ) ;
#16424=CARTESIAN_POINT ( 'NONE',  ( 1.312110113526856914, -26.18508844559277549, 7.386948897581449458 ) ) ;
#16428=ORIENTED_EDGE ( 'NONE', *, *, #32842, .T. ) ;
#16430=ORIENTED_EDGE ( 'NONE', *, *, #29933, .F. ) ;
#16432=B_SPLINE_CURVE_WITH_KNOTS ( 'NONE', 3,
 ( #33880, #2176, #30368, #23575 ),
 .UNSPECIFIED., .F., .F.,
 ( 4, 4 ),
 ( 8.940560153363745023E-19, 2.475319317933450300E-05 ),
 .UNSPECIFIED. ) ;
#16435=ORIENTED_EDGE ( 'NONE', *, *, #25527, .F. ) ;
#16436=ORIENTED_EDGE ( 'NONE', *, *, #20897, .F. ) ;
#16438=CARTESIAN_POINT ( 'NONE',  ( -0.009267658575196100618, -32.50883118978046582, 7.775108481317163367 ) ) ;
#16439=CARTESIAN_POINT ( 'NONE',  ( 4.540213033195567682, -31.43953463181986407, 6.997764925645181933 ) ) ;
#16444=VERTEX_POINT ( 'NONE', #38945 ) ;
#16450=EDGE_CURVE ( 'NONE', #11806, #15412, #38411, .T. ) ;
#16453=CARTESIAN_POINT ( 'NONE',  ( 0.3928816666250639633, -32.70848353550643139, 6.871394612369935651 ) ) ;
#16456=ORIENTED_EDGE ( 'NONE', *, *, #22474, .T. ) ;
#16457=ADVANCED_FACE ( 'NONE', ( #23122 ), #16921, .F. ) ;
#16458=CARTESIAN_POINT ( 'NONE',  ( 0.5607539575979699764, -32.77325105075146894, 7.740055089680399902 ) ) ;
#16459=DIRECTION ( 'NONE',  ( -0.7126435865141264037, 0.000000000000000000, -0.7015262779114428415 ) ) ;
#16461=CARTESIAN_POINT ( 'NONE',  ( 5.075416774377466744, -29.15851806602221785, 6.887945620086119547 ) ) ;
#16467=CARTESIAN_POINT ( 'NONE',  ( 2.908998754795610875, -32.85463590341955609, 7.756742906098588186 ) ) ;
#16469=CARTESIAN_POINT ( 'NONE',  ( 3.431434570054124222, -32.49627346798381211, 7.695279973900954751 ) ) ;
#16471=ORIENTED_EDGE ( 'NONE', *, *, #28207, .F. ) ;
#16472=ORIENTED_EDGE ( 'NONE', *, *, #15201, .F. ) ;
#16474=CARTESIAN_POINT ( 'NONE',  ( -1.613120284615923605, -28.77710995882498324, 7.386948897581451234 ) ) ;
#16479=CARTESIAN_POINT ( 'NONE',  ( 5.401390093233090717, -29.51577928193538369, 7.785387725071483800 ) ) ;
#16482=CARTESIAN_POINT ( 'NONE',  ( 3.844330250123625170, -32.33644520256172683, 6.870724624169666228 ) ) ;
#16491=FACE_OUTER_BOUND ( 'NONE', #18408, .T. ) ;
#16493=CARTESIAN_POINT ( 'NONE',  ( 4.339220620109727200, -27.42596629983610512, 6.889465824494258150 ) ) ;
#16494=CARTESIAN_POINT ( 'NONE',  ( 1.803259918365761605, -26.07610587814439285, 7.771081512783698741 ) ) ;
#16497=CARTESIAN_POINT ( 'NONE',  ( -0.2049548994135422797, -32.50585849072293598, 6.912143950357353184 ) ) ;
#16499=CARTESIAN_POINT ( 'NONE',  ( -1.699556639465169106, -29.59009428628278471, 7.643333865083955736 ) ) ;
#16501=EDGE_CURVE ( 'NONE', #28513, #13346, #38935, .T. ) ;
#16504=CARTESIAN_POINT ( 'NONE',  ( 0.7269655568601173234, -26.31225054053048140, 6.911401339314956260 ) ) ;
#16509=CARTESIAN_POINT ( 'NONE',  ( 1.134318422345943267, -32.92248114710984197, 7.740055089680399014 ) ) ;
#16510=DIRECTION ( 'NONE',  ( -0.9396926207859104263, 0.3420201433256631063, -0.000000000000000000 ) ) ;
#16511=B_SPLINE_CURVE_WITH_KNOTS ( 'NONE', 3,
 ( #14973, #40086, #11660, #21160, #6127, #15172, #2448, #24235, #40695, #37000, #5923, #12287, #33727, #36796, #3071, #18255, #2653, #34355, #11865, #18663, #24440, #27730, #33939, #31250, #37200, #18461, #5714, #30846, #31047, #2855, #15376 ),
 .UNSPECIFIED., .F., .F.,
 ( 4, 3, 3, 3, 3, 3, 3, 3, 3, 3, 4 ),
 ( 8.673617379884035472E-19, 3.077658087705409682E-05, 6.152638666998541184E-05, 9.267501192706129737E-05, 0.0001241882240135219902, 0.0001556618703051623547, 0.0001866161554452190510, 0.0002167966385860956805, 0.0002463805737537764053, 0.0002758761370306536285, 0.0002847094172290138311 ),
 .UNSPECIFIED. ) ;
#16512=CARTESIAN_POINT ( 'NONE',  ( 3.339037877594524417, -32.54901303308319171, 7.784476445165072533 ) ) ;
#16513=CARTESIAN_POINT ( 'NONE',  ( -1.551693178343154012, -28.31429354101616269, 7.784725160561910329 ) ) ;
#16516=ORIENTED_EDGE ( 'NONE', *, *, #24074, .F. ) ;
#16518=DIRECTION ( 'NONE',  ( 0.4999999999999979461, 0.8660254037844397068, -0.000000000000000000 ) ) ;
#16525=CARTESIAN_POINT ( 'NONE',  ( 0.9145606489677439166, -32.87787577969059782, 6.911401339314955372 ) ) ;
#16526=CARTESIAN_POINT ( 'NONE',  ( 1.230319205269136518, -26.20258206353872765, 7.754798119455333705 ) ) ;
#16533=CARTESIAN_POINT ( 'NONE',  ( 0.4788954889883382249, -26.28999729831613053, 7.737115613922530777 ) ) ;
#16534=VERTEX_POINT ( 'NONE', #32602 ) ;
#16541=CARTESIAN_POINT ( 'NONE',  ( -1.627984416835427162, -30.65173788820889200, 7.754798119455333705 ) ) ;
#16545=CARTESIAN_POINT ( 'NONE',  ( 5.085231831033718564, -29.18165020368717322, 7.386948897581451234 ) ) ;
#16552=EDGE_CURVE ( 'NONE', #22181, #32450, #12619, .T. ) ;
#16554=CARTESIAN_POINT ( 'NONE',  ( 1.700390093233090871, -29.56993018339339940, -8.199999999999999289 ) ) ;
#16556=DIRECTION ( 'NONE',  ( -0.9848077530122149037, 0.1736481776668921395, 0.000000000000000000 ) ) ;
#16557=LINE ( 'NONE', #29136, #39113 ) ;
#16558=CARTESIAN_POINT ( 'NONE',  ( 3.475438317136747113, -32.58641883790819094, 7.730015791551950954 ) ) ;
#16568=( BOUNDED_CURVE ( )  B_SPLINE_CURVE ( 3, ( #25033, #12662, #15758, #34727 ),
 .UNSPECIFIED., .F., .T. ) 
 B_SPLINE_CURVE_WITH_KNOTS ( ( 4, 4 ),
 ( 4.708531083176466403, 4.712388980384689674 ),
 .UNSPECIFIED. ) 
 CURVE ( )  GEOMETRIC_REPRESENTATION_ITEM ( )  RATIONAL_B_SPLINE_CURVE ( ( 1.000000000000000000, 0.9999987597194787137, 0.9999987597194787137, 1.000000000000000000 ) ) 
 REPRESENTATION_ITEM ( '' )  );
#16572=CARTESIAN_POINT ( 'NONE',  ( 2.911470930621151698, -26.29543661044079528, 7.778495531946298058 ) ) ;
#16574=EDGE_LOOP ( 'NONE', ( #12862, #2638, #20760, #24010 ) ) ;
#16575=CARTESIAN_POINT ( 'NONE',  ( 4.008117074447018702, -26.95213428602776773, 7.780491323090171107 ) ) ;
#16580=ORIENTED_EDGE ( 'NONE', *, *, #25748, .T. ) ;
#16581=ADVANCED_FACE ( 'NONE', ( #4986 ), #39555, .T. ) ;
#16584=CARTESIAN_POINT ( 'NONE',  ( 0.9649312406235903694, -32.99179965756316335, 6.868546646838339598 ) ) ;
#16585=CARTESIAN_POINT ( 'NONE',  ( 3.578684702212876712, -26.72740941926953440, 7.386948897581451234 ) ) ;
#16587=VERTEX_POINT ( 'NONE', #17930 ) ;
#16589=AXIS2_PLACEMENT_3D ( 'NONE', #960, #13704, #16378 ) ;
#16590=CARTESIAN_POINT ( 'NONE',  ( -1.021081023829336187, -31.60797530386227905, 6.895222827070024429 ) ) ;
#16591=CARTESIAN_POINT ( 'NONE',  ( -0.5635009794871607136, -32.22451875026029455, 7.781480525794719050 ) ) ;
#16593=ADVANCED_FACE ( 'NONE', ( #24320 ), #27613, .F. ) ;
#16599=CARTESIAN_POINT ( 'NONE',  ( 2.931137878888503856, -32.84640083007458600, 7.698786668945013290 ) ) ;
#16600=CARTESIAN_POINT ( 'NONE',  ( -0.4574210171174859507, -32.19744825413003753, 7.695279973900954751 ) ) ;
#16611=CARTESIAN_POINT ( 'NONE',  ( 4.359062294607612742, -27.29364649790398190, 7.678495282201406091 ) ) ;
#16615=EDGE_LOOP ( 'NONE', ( #39678, #8625, #4634, #38466, #33740 ) ) ;
#16621=EDGE_CURVE ( 'NONE', #32349, #16283, #30805, .T. ) ;
#16622=CARTESIAN_POINT ( 'NONE',  ( 4.927610109650206738, -30.92457071343696384, 7.013842709614101167 ) ) ;
#16625=ORIENTED_EDGE ( 'NONE', *, *, #28207, .T. ) ;
#16626=ORIENTED_EDGE ( 'NONE', *, *, #3064, .T. ) ;
#16628=AXIS2_PLACEMENT_3D ( 'NONE', #15302, #2572, #21700 ) ;
#16629=CARTESIAN_POINT ( 'NONE',  ( 5.038969279218838970, -30.21327822487392112, 6.889465824494254598 ) ) ;
#16631=DIRECTION ( 'NONE',  ( 1.000000000000000000, -8.921435019309294079E-15, 0.000000000000000000 ) ) ;
#16640=CARTESIAN_POINT ( 'NONE',  ( 0.3523192157778118339, -32.69126323727760308, 6.997764925645181933 ) ) ;
#16643=CARTESIAN_POINT ( 'NONE',  ( -1.784963795961492350, -29.52657984859756723, 7.785096263473211486 ) ) ;
#16645=VECTOR ( 'NONE', #18591, 1000.000000000000227 ) ;
#16650=DIRECTION ( 'NONE',  ( 1.000000000000000000, 0.000000000000000000, 0.000000000000000000 ) ) ;
#16653=ADVANCED_FACE ( 'NONE', ( #39767 ), #24112, .F. ) ;
#16654=CARTESIAN_POINT ( 'NONE',  ( 5.585000075404096265, -26.15135101585522293, 7.754798119455333705 ) ) ;
#16658=ORIENTED_EDGE ( 'NONE', *, *, #19766, .T. ) ;
#16660=CARTESIAN_POINT ( 'NONE',  ( 1.672485556746682533, -33.05866413503350287, 7.781480525794718162 ) ) ;
#16661=CARTESIAN_POINT ( 'NONE',  ( 2.183653651549320340, -33.03640625185305879, 7.750000000000000888 ) ) ;
#16662=EDGE_CURVE ( 'NONE', #39861, #33383, #7235, .T. ) ;
#16665=B_SPLINE_CURVE_WITH_KNOTS ( 'NONE', 3,
 ( #17080, #17475, #867, #32362 ),
 .UNSPECIFIED., .F., .F.,
 ( 4, 4 ),
 ( 8.673617379884035472E-19, 6.391136169900847399E-06 ),
 .UNSPECIFIED. ) ;
#16666=EDGE_CURVE ( 'NONE', #28306, #31466, #7917, .T. ) ;
#16669=ORIENTED_EDGE ( 'NONE', *, *, #16277, .F. ) ;
#16672=VERTEX_POINT ( 'NONE', #32202 ) ;
#16678=CARTESIAN_POINT ( 'NONE',  ( 2.470422062425372545, -26.15568784190358542, 6.890920332093119605 ) ) ;
#16679=CARTESIAN_POINT ( 'NONE',  ( 4.394189364466743797, -27.35572347332146848, 7.783750581861601070 ) ) ;
#16682=B_SPLINE_CURVE_WITH_KNOTS ( 'NONE', 3,
 ( #10728, #23310, #20009, #4386, #13837, #16911, #29492, #21732, #14927, #18214, #6083, #24606, #30806, #34314, #12655, #9156 ),
 .UNSPECIFIED., .F., .F.,
 ( 4, 3, 3, 3, 3, 4 ),
 ( 2.455293198023857654E-05, 3.025503081355709683E-05, 6.050996021720427811E-05, 9.076574948361131121E-05, 0.0001210199690674203720, 0.0001477826154599604504 ),
 .UNSPECIFIED. ) ;
#16686=DIRECTION ( 'NONE',  ( 0.7126435865141282910, 0.000000000000000000, 0.7015262779114409541 ) ) ;
#16689=CARTESIAN_POINT ( 'NONE',  ( -0.07645708395594488782, -32.58535952412007930, 6.894806418505347700 ) ) ;
#16691=CARTESIAN_POINT ( 'NONE',  ( 2.408319516247223735, -26.24444671129270290, 7.757178535559534183 ) ) ;
#16693=AXIS2_PLACEMENT_3D ( 'NONE', #8925, #21508, #34086 ) ;
#16695=CARTESIAN_POINT ( 'NONE',  ( 0.7311680052080280490, -26.31100152636673783, 6.920489980334479263 ) ) ;
#16699=CARTESIAN_POINT ( 'NONE',  ( 1.040749578662133024, -32.90534253841714474, 7.784476445165072533 ) ) ;
#16701=CARTESIAN_POINT ( 'NONE',  ( 3.411503134503389933, -32.50797839004665946, 7.756377446753164762 ) ) ;
#16704=DIRECTION ( 'NONE',  ( 0.9848077530122103518, -0.1736481776669172583, -0.000000000000000000 ) ) ;
#16707=DIRECTION ( 'NONE',  ( 0.7660444431189857850, -0.6427876096865299260, -0.000000000000000000 ) ) ;
#16710=ORIENTED_EDGE ( 'NONE', *, *, #10067, .F. ) ;
#16715=CARTESIAN_POINT ( 'NONE',  ( 0.9049783971971742114, -32.87558106357499810, 6.939395833800440450 ) ) ;
#16716=CARTESIAN_POINT ( 'NONE',  ( 0.4482788600987206995, -32.83830765075952485, 6.873189335546979528 ) ) ;
#16721=EDGE_CURVE ( 'NONE', #17641, #14737, #38648, .T. ) ;
#16724=EDGE_CURVE ( 'NONE', #29197, #27494, #7462, .T. ) ;
#16729=CARTESIAN_POINT ( 'NONE',  ( -0.4747269484695719743, -32.18314005917732601, 7.635761828346577573 ) ) ;
#16731=( BOUNDED_CURVE ( )  B_SPLINE_CURVE ( 3, ( #18379, #27450, #24153, #24566 ),
 .UNSPECIFIED., .F., .T. ) 
 B_SPLINE_CURVE_WITH_KNOTS ( ( 4, 4 ),
 ( 4.886921905584129533, 4.895802057644188743 ),
 .UNSPECIFIED. ) 
 CURVE ( )  GEOMETRIC_REPRESENTATION_ITEM ( )  RATIONAL_B_SPLINE_CURVE ( ( 1.000000000000000000, 0.9999934285857451366, 0.9999934285857451366, 1.000000000000000000 ) ) 
 REPRESENTATION_ITEM ( '' )  );
#16743=CARTESIAN_POINT ( 'NONE',  ( -0.8809027425463855643, -31.78283038357269419, 7.695279973900954751 ) ) ;
#16751=AXIS2_PLACEMENT_3D ( 'NONE', #10130, #22717, #34887 ) ;
#16752=CARTESIAN_POINT ( 'NONE',  ( 3.349526715458713610, -32.65705642007926457, 6.865482280155368322 ) ) ;
#16753=CARTESIAN_POINT ( 'NONE',  ( 5.109224889810624504, -30.36356686813360994, 6.931070083220555844 ) ) ;
#16754=CYLINDRICAL_SURFACE ( 'NONE', #27832, 0.09010775117053204664 ) ;
#16755=CARTESIAN_POINT ( 'NONE',  ( -0.7727839574033206205, -27.22657253935856048, 7.386948897581452123 ) ) ;
#16758=CARTESIAN_POINT ( 'NONE',  ( 4.740160921379847458, -31.30480577326951064, 7.750000000000000000 ) ) ;
#16759=CARTESIAN_POINT ( 'NONE',  ( -1.265720463714046895, -27.71192368072266277, 7.750000000000000888 ) ) ;
#16761=VERTEX_POINT ( 'NONE', #29500 ) ;
#16763=B_SPLINE_CURVE_WITH_KNOTS ( 'NONE', 3,
 ( #22359, #37972, #16159, #22557 ),
 .UNSPECIFIED., .F., .F.,
 ( 4, 4 ),
 ( 2.168404344971008868E-19, 6.391136169993524662E-06 ),
 .UNSPECIFIED. ) ;
#16764=CARTESIAN_POINT ( 'NONE',  ( 2.287364877874435987, -26.11950075324752518, 7.744938106820261403 ) ) ;
#16772=ORIENTED_EDGE ( 'NONE', *, *, #33535, .T. ) ;
#16773=EDGE_CURVE ( 'NONE', #17495, #11431, #15105, .T. ) ;
#16781=CARTESIAN_POINT ( 'NONE',  ( -1.699609906766908818, -29.56993018339339940, 7.222147233343546802 ) ) ;
#16782=ORIENTED_EDGE ( 'NONE', *, *, #32161, .T. ) ;
#16784=DIRECTION ( 'NONE',  ( -0.4999999999999918954, -0.8660254037844432595, -0.000000000000000000 ) ) ;
#16785=CARTESIAN_POINT ( 'NONE',  ( -2.619165735930222727, -32.12635497920775407, 7.695279973900954751 ) ) ;
#16790=ORIENTED_EDGE ( 'NONE', *, *, #25313, .T. ) ;
#16791=CARTESIAN_POINT ( 'NONE',  ( -0.5438121010353070828, -32.25394735576643512, 7.762796336881262249 ) ) ;
#16793=CARTESIAN_POINT ( 'NONE',  ( -0.02825552051704444470, -26.64216676595851396, 7.670860738520325128 ) ) ;
#16794=DIRECTION ( 'NONE',  ( -0.000000000000000000, -0.000000000000000000, -1.000000000000000000 ) ) ;
#16796=LINE ( 'NONE', #30178, #15027 ) ;
#16797=CARTESIAN_POINT ( 'NONE',  ( 3.924182654612999421, -26.99799553805268459, 7.785868773668303433 ) ) ;
#16798=CARTESIAN_POINT ( 'NONE',  ( -1.576080553448099719, -30.80067796904879884, 7.698786668945008849 ) ) ;
#16800=DIRECTION ( 'NONE',  ( 0.9848077530122103518, -0.1736481776669172583, -0.000000000000000000 ) ) ;
#16804=AXIS2_PLACEMENT_3D ( 'NONE', #13043, #28698, #3607 ) ;
#16806=LINE ( 'NONE', #16216, #29202 ) ;
#16808=( BOUNDED_CURVE ( )  B_SPLINE_CURVE ( 3, ( #17626, #36384, #24434, #18040 ),
 .UNSPECIFIED., .F., .T. ) 
 B_SPLINE_CURVE_WITH_KNOTS ( ( 4, 4 ),
 ( 1.381924640371167579, 1.570796326794896780 ),
 .UNSPECIFIED. ) 
 CURVE ( )  GEOMETRIC_REPRESENTATION_ITEM ( )  RATIONAL_B_SPLINE_CURVE ( ( 1.000000000000000000, 0.9970294990994144069, 0.9970294990994144069, 1.000000000000000000 ) ) 
 REPRESENTATION_ITEM ( '' )  );
#16817=CARTESIAN_POINT ( 'NONE',  ( -0.5068137670456340782, -26.85363654698906188, 6.875671892026065990 ) ) ;
#16818=CARTESIAN_POINT ( 'NONE',  ( -1.246051523623666668, -27.68087481465684263, 6.887547729233689076 ) ) ;
#16821=CARTESIAN_POINT ( 'NONE',  ( 1.277039614466915829, -32.95056463638093192, 7.139196562012274150 ) ) ;
#16823=EDGE_LOOP ( 'NONE', ( #10195, #7463, #39364, #32220, #37390 ) ) ;
#16824=VERTEX_POINT ( 'NONE', #18338 ) ;
#16831=CARTESIAN_POINT ( 'NONE',  ( -0.05162664538871142295, -32.48376568794560626, 7.785172627573962778 ) ) ;
#16841=VERTEX_POINT ( 'NONE', #39553 ) ;
#16851=ORIENTED_EDGE ( 'NONE', *, *, #4310, .T. ) ;
#16856=CARTESIAN_POINT ( 'NONE',  ( -0.06469087068677582819, -26.54759843608177761, 7.750000000000000888 ) ) ;
#16857=CARTESIAN_POINT ( 'NONE',  ( 5.152478333118308385, -28.99279347164636889, 6.894806418505347700 ) ) ;
#16858=EDGE_CURVE ( 'NONE', #1323, #36841, #39110, .T. ) ;
#16862=CARTESIAN_POINT ( 'NONE',  ( -1.642747097704066128, -30.18915717881909444, 7.730758795053805699 ) ) ;
#16863=CARTESIAN_POINT ( 'NONE',  ( 4.983308922979784228, -28.35648716565642857, 7.750000000000000000 ) ) ;
#16865=ORIENTED_EDGE ( 'NONE', *, *, #32551, .T. ) ;
#16867=CARTESIAN_POINT ( 'NONE',  ( -0.5374033828380346822, -32.26107951187057665, 7.638132480492516585 ) ) ;
#16874=CARTESIAN_POINT ( 'NONE',  ( 4.914263057417876723, -28.46041651962800501, 6.887041543973313473 ) ) ;
#16878=CARTESIAN_POINT ( 'NONE',  ( 3.860546469805519187, -32.32378646663576660, 6.865482280155369210 ) ) ;
#16884=CARTESIAN_POINT ( 'NONE',  ( 2.474049714983521664, -26.15650803111381606, 7.013842709614101167 ) ) ;
#16890=EDGE_CURVE ( 'NONE', #19590, #38247, #21978, .T. ) ;
#16893=FACE_OUTER_BOUND ( 'NONE', #25688, .T. ) ;
#16894=CARTESIAN_POINT ( 'NONE',  ( 1.669512530038368414, -26.07006638945924948, 7.665454363767879364 ) ) ;
#16896=CARTESIAN_POINT ( 'NONE',  ( -0.2112746087012261631, -32.50174735455220798, 6.931070083220562061 ) ) ;
#16899=CARTESIAN_POINT ( 'NONE',  ( 2.330147284786646456, -26.22874769739361511, 7.784838882742139532 ) ) ;
#16903=DIRECTION ( 'NONE',  ( 0.7660444431189790127, 0.6427876096865381417, 0.000000000000000000 ) ) ;
#16905=PLANE ( 'NONE',  #40192 ) ;
#16907=EDGE_CURVE ( 'NONE', #22737, #5985, #33195, .T. ) ;
#16910=CARTESIAN_POINT ( 'NONE',  ( 4.693750549451069176, -31.38373704560598654, 6.867280401193709416 ) ) ;
#16911=CARTESIAN_POINT ( 'NONE',  ( -1.799476894543866612, -29.60054653561284965, 7.727461116072927183 ) ) ;
#16912=CARTESIAN_POINT ( 'NONE',  ( 2.242723711017451382, -32.92639770848892766, 6.894806418505347700 ) ) ;
#16913=ADVANCED_FACE ( 'NONE', ( #8249 ), #8662, .F. ) ;
#16917=CYLINDRICAL_SURFACE ( 'NONE', #25136, 3.399999999999999911 ) ;
#16919=CARTESIAN_POINT ( 'NONE',  ( 4.723655388576528225, -27.80644746340955464, 7.638132480492515697 ) ) ;
#16920=ORIENTED_EDGE ( 'NONE', *, *, #13622, .F. ) ;
#16921=CYLINDRICAL_SURFACE ( 'NONE', #25943, 0.09010775117052932659 ) ;
#16922=CARTESIAN_POINT ( 'NONE',  ( 5.067143666762728316, -33.49802700238250708, 7.695279973900954751 ) ) ;
#16924=CARTESIAN_POINT ( 'NONE',  ( 0.9038683196620087568, -32.87531266959080511, 6.949473656533217358 ) ) ;
#16925=( BOUNDED_CURVE ( )  B_SPLINE_CURVE ( 3, ( #25089, #9417, #38037, #40716 ),
 .UNSPECIFIED., .F., .F. ) 
 B_SPLINE_CURVE_WITH_KNOTS ( ( 4, 4 ),
 ( 1.347909859412852907, 1.534781240595298080 ),
 .UNSPECIFIED. ) 
 CURVE ( )  GEOMETRIC_REPRESENTATION_ITEM ( )  RATIONAL_B_SPLINE_CURVE ( ( 1.000000000000000000, 0.9970920404276226723, 0.9970920404276226723, 1.000000000000000000 ) ) 
 REPRESENTATION_ITEM ( '' )  );
#16927=CARTESIAN_POINT ( 'NONE',  ( 3.594851464545667952, -26.62696974998548782, 7.013842709614101167 ) ) ;
#16939=CARTESIAN_POINT ( 'NONE',  ( -1.656886121102593368, -30.10724210791205380, 6.889465824494254598 ) ) ;
#16942=DIRECTION ( 'NONE',  ( -0.8660254037844271613, 0.5000000000000200950, 0.000000000000000000 ) ) ;
#16952=ADVANCED_FACE ( 'NONE', ( #27611 ), #33416, .F. ) ;
#16954=CIRCLE ( 'NONE', #5774, 0.04999999999999991257 ) ;
#16959=FACE_OUTER_BOUND ( 'NONE', #26658, .T. ) ;
#16961=CARTESIAN_POINT ( 'NONE',  ( 5.108889948331447606, -30.36500087965021422, 6.971170733404099984 ) ) ;
#16965=EDGE_CURVE ( 'NONE', #25596, #34797, #35760, .T. ) ;
#16968=ORIENTED_EDGE ( 'NONE', *, *, #6880, .T. ) ;
#16972=CARTESIAN_POINT ( 'NONE',  ( 2.276779695690628547, -26.11771647328293255, 7.724038915126859806 ) ) ;
#16978=DIRECTION ( 'NONE',  ( 0.000000000000000000, -0.6834397476448842434, 0.7300069255418724090 ) ) ;
#16979=CARTESIAN_POINT ( 'NONE',  ( 1.137856487652708637, -26.12999894468477535, 7.785096263473212375 ) ) ;
#16981=EDGE_LOOP ( 'NONE', ( #22340, #35351, #6680, #14645, #24135 ) ) ;
#16985=CARTESIAN_POINT ( 'NONE',  ( -1.275819131918839666, -31.21377956460290548, 6.880147297696980857 ) ) ;
#16989=FACE_OUTER_BOUND ( 'NONE', #29052, .T. ) ;
#16996=CARTESIAN_POINT ( 'NONE',  ( 5.144126537964561763, -28.94488408058296613, 7.640616322432098428 ) ) ;
#17001=CARTESIAN_POINT ( 'NONE',  ( -1.278368187136755374, -27.75183824754000028, 7.780491323090174660 ) ) ;
#17014=CARTESIAN_POINT ( 'NONE',  ( -0.4435500636574273292, -26.80341516422506132, 6.870724624169666228 ) ) ;
#17015=CARTESIAN_POINT ( 'NONE',  ( -1.242570340174825594, -27.67546881208082965, 7.013842709614101167 ) ) ;
#17018=CARTESIAN_POINT ( 'NONE',  ( 1.062037487868057184, -32.90946697031814949, 6.894806418505346812 ) ) ;
#17022=ORIENTED_EDGE ( 'NONE', *, *, #22441, .T. ) ;
#17030=CARTESIAN_POINT ( 'NONE',  ( -0.9352292415849461360, -31.71783863626873767, 6.894806418505345924 ) ) ;
#17036=CARTESIAN_POINT ( 'NONE',  ( 5.123750824668761972, -30.29724448404768111, 7.754798119455333705 ) ) ;
#17040=CARTESIAN_POINT ( 'NONE',  ( 3.340113934647170435, -32.66206629357650115, 7.750000000000000888 ) ) ;
#17041=ORIENTED_EDGE ( 'NONE', *, *, #39068, .T. ) ;
#17042=CARTESIAN_POINT ( 'NONE',  ( 0.4844891494406461940, -32.74508134434379514, 6.887041543973317026 ) ) ;
#17045=( BOUNDED_CURVE ( )  B_SPLINE_CURVE ( 3, ( #9732, #29486, #38529, #35279 ),
 .UNSPECIFIED., .F., .T. ) 
 B_SPLINE_CURVE_WITH_KNOTS ( ( 4, 4 ),
 ( 1.347909859412853573, 1.534781240595298746 ),
 .UNSPECIFIED. ) 
 CURVE ( )  GEOMETRIC_REPRESENTATION_ITEM ( )  RATIONAL_B_SPLINE_CURVE ( ( 1.000000000000000000, 0.9970920404276226723, 0.9970920404276226723, 1.000000000000000000 ) ) 
 REPRESENTATION_ITEM ( '' )  );
#17046=CARTESIAN_POINT ( 'NONE',  ( -0.5103942914760696281, -26.98682223157766202, 7.670860738520326016 ) ) ;
#17047=VERTEX_POINT ( 'NONE', #16622 ) ;
#17050=CARTESIAN_POINT ( 'NONE',  ( 6.136079629878683050, -27.96984039756584295, 7.635761828346577573 ) ) ;
#17056=CARTESIAN_POINT ( 'NONE',  ( -1.808702272108716258, -33.43603381987017542, 6.954324564059724878 ) ) ;
#17058=CARTESIAN_POINT ( 'NONE',  ( 3.858201203583684791, -26.94241211265677194, 7.695279973900954751 ) ) ;
#17060=CARTESIAN_POINT ( 'NONE',  ( 5.002744721522525140, -28.44814603186448565, 7.782861076432730840 ) ) ;
#17064=CARTESIAN_POINT ( 'NONE',  ( -1.599034431228576247, -30.73774772367137942, 6.894806418505347700 ) ) ;
#17072=CARTESIAN_POINT ( 'NONE',  ( 6.143759433280234994, -27.99094048399745205, 7.695279973900954751 ) ) ;
#17074=CARTESIAN_POINT ( 'NONE',  ( 4.822813956501135202, -27.98864294135706032, 6.941203072598473689 ) ) ;
#17076=ORIENTED_EDGE ( 'NONE', *, *, #18319, .T. ) ;
#17080=CARTESIAN_POINT ( 'NONE',  ( 4.458039033310292609, -27.41499233908904287, 7.754798119455333705 ) ) ;
#17081=ORIENTED_EDGE ( 'NONE', *, *, #5532, .F. ) ;
#17082=B_SPLINE_CURVE_WITH_KNOTS ( 'NONE', 3,
 ( #29153, #10600, #961, #7318, #4454, #19876, #13706, #29551, #16979, #32449, #4247, #25457, #9802, #28750, #560, #13095, #9999, #22582, #6920 ),
 .UNSPECIFIED., .F., .F.,
 ( 4, 3, 3, 3, 3, 3, 4 ),
 ( 0.000000000000000000, 2.546128104244798653E-05, 5.711050680484043828E-05, 8.113074941675955595E-05, 0.0001053129305727074305, 0.0001360598016347138838, 0.0001612931755713711509 ),
 .UNSPECIFIED. ) ;
#17084=CARTESIAN_POINT ( 'NONE',  ( 4.413844959242510413, -27.38136177617460021, 7.784725160561910329 ) ) ;
#17087=VERTEX_POINT ( 'NONE', #39254 ) ;
#17094=CARTESIAN_POINT ( 'NONE',  ( -0.01837800939314739035, -32.61883756299590686, 7.695279973900954751 ) ) ;
#17098=CARTESIAN_POINT ( 'NONE',  ( -1.699515553723242700, -29.59554030218403398, 7.652160403243382980 ) ) ;
#17099=CARTESIAN_POINT ( 'NONE',  ( 3.442434176459446160, -26.65012155745640499, 6.894806418505343260 ) ) ;
#17101=ORIENTED_EDGE ( 'NONE', *, *, #816, .F. ) ;
#17107=CARTESIAN_POINT ( 'NONE',  ( 0.9924606702189815444, -32.89541365549410301, 7.757178535559533294 ) ) ;
#17108=CARTESIAN_POINT ( 'NONE',  ( -1.789478617146011086, -29.22571177910124263, 7.501983001166816045 ) ) ;
#17112=CARTESIAN_POINT ( 'NONE',  ( 4.325508966927646526, -31.73065943505188358, 7.721096864323899744 ) ) ;
#17118=CARTESIAN_POINT ( 'NONE',  ( 4.724705146729046845, -27.80824960587721506, 7.635761828346577573 ) ) ;
#17119=ORIENTED_EDGE ( 'NONE', *, *, #35408, .T. ) ;
#17123=CARTESIAN_POINT ( 'NONE',  ( 0.4906401998943609177, -26.28564864924214461, 7.635761828346577573 ) ) ;
#17124=CARTESIAN_POINT ( 'NONE',  ( 0.3423729883474129210, -32.79573922743291092, 6.898188844117810525 ) ) ;
#17125=CARTESIAN_POINT ( 'NONE',  ( -1.699561686978244612, -29.54937652563323169, 7.779495906702013741 ) ) ;
#17131=ORIENTED_EDGE ( 'NONE', *, *, #9542, .T. ) ;
#17133=B_SPLINE_CURVE_WITH_KNOTS ( 'NONE', 3,
 ( #35396, #25906, #16611, #35592, #29787, #1602, #20311, #20116, #32302, #7362 ),
 .UNSPECIFIED., .F., .F.,
 ( 4, 3, 3, 4 ),
 ( 0.0002170292169044786025, 0.0002420761345915961192, 0.0002723302478207003654, 0.0002816811360866758253 ),
 .UNSPECIFIED. ) ;
#17141=CARTESIAN_POINT ( 'NONE',  ( -0.9228924694586947419, -27.40696995593466312, 7.730758795053799481 ) ) ;
#17147=ORIENTED_EDGE ( 'NONE', *, *, #15308, .T. ) ;
#17151=CARTESIAN_POINT ( 'NONE',  ( 5.160844861227617208, -29.04528478060791485, 6.865554069792297653 ) ) ;
#17152=ORIENTED_EDGE ( 'NONE', *, *, #33915, .F. ) ;
#17154=DIRECTION ( 'NONE',  ( -0.8660254037844415942, 0.4999999999999950040, -0.000000000000000000 ) ) ;
#17155=CARTESIAN_POINT ( 'NONE',  ( 3.298377662289942336, -32.68384072543286578, 7.009310105710484073 ) ) ;
#17156=CARTESIAN_POINT ( 'NONE',  ( -1.100009487556019350, -31.66939733285032688, 6.941203072598479018 ) ) ;
#17159=CARTESIAN_POINT ( 'NONE',  ( 2.745177312916512236, -32.80544076198930270, 6.863904403958575706 ) ) ;
#17162=CARTESIAN_POINT ( 'NONE',  ( 1.826114730284481347, -26.07217366336726982, 6.867199677474202346 ) ) ;
#17164=ORIENTED_EDGE ( 'NONE', *, *, #16724, .F. ) ;
#17173=CARTESIAN_POINT ( 'NONE',  ( 2.872971158482682696, -26.27219422606927424, 7.737115613922530777 ) ) ;
#17176=CARTESIAN_POINT ( 'NONE',  ( 2.270544122507286211, -32.92179816162761341, 7.779495906702013741 ) ) ;
#17178=CARTESIAN_POINT ( 'NONE',  ( -1.751114083487925521, -28.98930116072738628, 7.655937882338901268 ) ) ;
#17180=ORIENTED_EDGE ( 'NONE', *, *, #26380, .T. ) ;
#17192=ORIENTED_EDGE ( 'NONE', *, *, #28966, .F. ) ;
#17198=CARTESIAN_POINT ( 'NONE',  ( 1.489942920397620885, -32.96341103692402186, 6.949473656533217358 ) ) ;
#17199=CARTESIAN_POINT ( 'NONE',  ( 2.433491429741967416, -26.24990572107254394, 6.868387053540520704 ) ) ;
#17203=CARTESIAN_POINT ( 'NONE',  ( -2.327064883976697640, -32.63228849572541890, 6.894806418505347700 ) ) ;
#17204=DIRECTION ( 'NONE',  ( 0.9848077530122083534, -0.1736481776669292765, 0.000000000000000000 ) ) ;
#17206=CARTESIAN_POINT ( 'NONE',  ( 3.963477911421234623, -32.23984282750152630, 7.750000000000001776 ) ) ;
#17207=CARTESIAN_POINT ( 'NONE',  ( 1.114803370050245102, -33.02060082531637164, 7.646866513072557048 ) ) ;
#17209=DIRECTION ( 'NONE',  ( -0.7660444431189818992, 0.6427876096865345890, 0.000000000000000000 ) ) ;
#17215=CARTESIAN_POINT ( 'NONE',  ( -0.5137931472823115131, -26.85930784658432202, 6.880608371227953768 ) ) ;
#17216=CARTESIAN_POINT ( 'NONE',  ( -1.315039247493585250, -27.79308300620435901, 6.894806418505347700 ) ) ;
#17217=CARTESIAN_POINT ( 'NONE',  ( 2.422160802983875261, -26.14601410332325315, 7.761113333117551250 ) ) ;
#17219=CARTESIAN_POINT ( 'NONE',  ( 0.6527267737179240914, -26.33536660093865578, 7.754798119455333705 ) ) ;
#17220=CARTESIAN_POINT ( 'NONE',  ( 3.739317481034212243, -32.29073431218959911, 7.013842709614101167 ) ) ;
#17222=LINE ( 'NONE', #23226, #7714 ) ;
#17223=EDGE_LOOP ( 'NONE', ( #10834, #39512, #9762, #19637, #38918, #12376, #34353, #1413, #29508, #11957, #8207, #8945, #16129, #23618, #17414, #18876, #14489, #15796, #16471, #3234, #15893, #17152, #29097, #20162, #2680, #35324, #7804, #21519, #20356, #6314, #38336, #9693, #31876, #33438, #6478, #36753, #1451, #7933, #36645, #25215, #11451, #7256, #2445, #31596, #32809, #31469, #19783, #4053, #23550, #7618, #16219, #8066, #20362, #24265, #15259, #19454, #37991, #35025 ) ) ;
#17232=CARTESIAN_POINT ( 'NONE',  ( -0.09205880772810777490, -32.45907920833084859, 7.768425012602593327 ) ) ;
#17239=VERTEX_POINT ( 'NONE', #2023 ) ;
#17257=ORIENTED_EDGE ( 'NONE', *, *, #32930, .T. ) ;
#17258=CARTESIAN_POINT ( 'NONE',  ( 3.858201203583684791, -26.94241211265676839, 7.693875151218752428 ) ) ;
#17259=VECTOR ( 'NONE', #23765, 1000.000000000000114 ) ;
#17262=VERTEX_POINT ( 'NONE', #33933 ) ;
#17265=CARTESIAN_POINT ( 'NONE',  ( -1.629426256325140487, -30.64809085600286664, 6.867199677474202346 ) ) ;
#17268=EDGE_LOOP ( 'NONE', ( #17681, #16222, #4715, #12059 ) ) ;
#17269=CARTESIAN_POINT ( 'NONE',  ( 5.142064470514565500, -28.93363034780944076, 7.730015791551945625 ) ) ;
#17272=CARTESIAN_POINT ( 'NONE',  ( 4.801435222562028926, -27.94711808525471852, 6.875780273367530171 ) ) ;
#17279=ORIENTED_EDGE ( 'NONE', *, *, #37581, .T. ) ;
#17280=B_SPLINE_CURVE_WITH_KNOTS ( 'NONE', 3,
 ( #7145, #4270, #13919, #16402, #35172, #19899, #19507, #29176, #32673, #10819 ),
 .UNSPECIFIED., .F., .F.,
 ( 4, 3, 3, 4 ),
 ( 0.0001585009270395757776, 0.0001815657551981876637, 0.0002118214035944180620, 0.0002170292169044793886 ),
 .UNSPECIFIED. ) ;
#17288=CYLINDRICAL_SURFACE ( 'NONE', #33330, 3.399999999999999911 ) ;
#17291=CARTESIAN_POINT ( 'NONE',  ( 1.672850645881087894, -26.07003693891804019, 7.655937882338900380 ) ) ;
#17298=CARTESIAN_POINT ( 'NONE',  ( 0.5983277861368044848, -26.35348481447137203, 6.880147297696980857 ) ) ;
#17301=CARTESIAN_POINT ( 'NONE',  ( 0.1024025241762535204, -26.45601964135392592, 7.009310105710488514 ) ) ;
#17303=CARTESIAN_POINT ( 'NONE',  ( 5.401390093233090717, -29.44812577374269580, 7.754798119455333705 ) ) ;
#17304=CARTESIAN_POINT ( 'NONE',  ( 4.976842733950423536, -28.33913446795707358, 7.695279973900954751 ) ) ;
#17305=CARTESIAN_POINT ( 'NONE',  ( -1.592719143486283517, -28.38440999418950739, 7.756742906098588186 ) ) ;
#17306=EDGE_CURVE ( 'NONE', #4710, #4303, #16808, .T. ) ;
#17312=CARTESIAN_POINT ( 'NONE',  ( 3.032804972883730521, -26.33347060717657584, 6.875780273367530171 ) ) ;
#17313=ADVANCED_FACE ( 'NONE', ( #2222 ), #30205, .F. ) ;
#17315=CARTESIAN_POINT ( 'NONE',  ( -1.642550015356792681, -30.60663237321507069, 7.013842709614101167 ) ) ;
#17318=CARTESIAN_POINT ( 'NONE',  ( 1.057042051752609346, -32.90850936937915350, 6.889465824494256374 ) ) ;
#17319=CARTESIAN_POINT ( 'NONE',  ( 3.599609112215594209, -26.63003781836791362, 7.006908160621414083 ) ) ;
#17321=ORIENTED_EDGE ( 'NONE', *, *, #20115, .T. ) ;
#17327=EDGE_CURVE ( 'NONE', #26935, #19421, #36077, .T. ) ;
#17346=CARTESIAN_POINT ( 'NONE',  ( 5.173490979662657807, -29.13678236134181887, 6.903112506833891437 ) ) ;
#17348=CARTESIAN_POINT ( 'NONE',  ( 5.026281758278582146, -30.27593629695115496, 6.864216812889196717 ) ) ;
#17349=CARTESIAN_POINT ( 'NONE',  ( 3.284898187062045061, -32.69072080446853334, 6.980586498568963627 ) ) ;
#17353=CARTESIAN_POINT ( 'NONE',  ( 5.094551125703637773, -29.76914366077792451, 6.997764925645186374 ) ) ;
#17354=CARTESIAN_POINT ( 'NONE',  ( 1.873447534517880264, -26.07421076434662410, 7.009310105710485850 ) ) ;
#17356=ORIENTED_EDGE ( 'NONE', *, *, #13870, .F. ) ;
#17357=EDGE_CURVE ( 'NONE', #19595, #11405, #9684, .T. ) ;
#17363=AXIS2_PLACEMENT_3D ( 'NONE', #1492, #14025, #20206 ) ;
#17364=ORIENTED_EDGE ( 'NONE', *, *, #17, .F. ) ;
#17371=CARTESIAN_POINT ( 'NONE',  ( 5.180766528530944548, -29.99759455875544489, 7.134293011406493079 ) ) ;
#17377=CARTESIAN_POINT ( 'NONE',  ( 0.4238093638620683556, -32.72117464255529029, 7.754798119455333705 ) ) ;
#17378=VECTOR ( 'NONE', #21282, 1000.000000000000114 ) ;
#17382=CARTESIAN_POINT ( 'NONE',  ( 4.042062268558281879, -27.10485839313172107, 6.939395833800443114 ) ) ;
#17383=CYLINDRICAL_SURFACE ( 'NONE', #18269, 0.09010775117052950700 ) ;
#17390=CARTESIAN_POINT ( 'NONE',  ( 1.700390093233090871, -29.56993018339339940, 7.750000000000000888 ) ) ;
#17392=CARTESIAN_POINT ( 'NONE',  ( -1.484429692467435391, -30.76027941025985513, 7.730758795053808363 ) ) ;
#17393=( BOUNDED_CURVE ( )  B_SPLINE_CURVE ( 3, ( #20741, #33329, #9000, #36602 ),
 .UNSPECIFIED., .F., .F. ) 
 B_SPLINE_CURVE_WITH_KNOTS ( ( 4, 4 ),
 ( 1.347909859412854239, 1.534781240595299190 ),
 .UNSPECIFIED. ) 
 CURVE ( )  GEOMETRIC_REPRESENTATION_ITEM ( )  RATIONAL_B_SPLINE_CURVE ( ( 1.000000000000000000, 0.9970920404276226723, 0.9970920404276226723, 1.000000000000000000 ) ) 
 REPRESENTATION_ITEM ( '' )  );
#17394=CARTESIAN_POINT ( 'NONE',  ( 3.863350320691840700, -26.94664762070162567, 7.730758795053802146 ) ) ;
#17395=CARTESIAN_POINT ( 'NONE',  ( -1.020414035563122601, -31.60885757119451256, 7.013842709614101167 ) ) ;
#17400=CARTESIAN_POINT ( 'NONE',  ( 1.107728911050566145, -33.01938716874131075, 7.637894019485640840 ) ) ;
#17405=CARTESIAN_POINT ( 'NONE',  ( 2.262923698813503748, -33.00986142210201990, 7.785096263473211486 ) ) ;
#17410=CARTESIAN_POINT ( 'NONE',  ( -1.638189092752657006, -28.92658214191287769, 6.889465824494254598 ) ) ;
#17413=CARTESIAN_POINT ( 'NONE',  ( -0.6767161412783136987, -32.13885329431887072, 6.895394898881668233 ) ) ;
#17414=ORIENTED_EDGE ( 'NONE', *, *, #15481, .F. ) ;
#17417=CARTESIAN_POINT ( 'NONE',  ( -1.523348320565749203, -28.20702496313861474, 7.002103980607166989 ) ) ;
#17421=EDGE_LOOP ( 'NONE', ( #24491, #12628, #22785, #11614 ) ) ;
#17423=LINE ( 'NONE', #2232, #18641 ) ;
#17429=ORIENTED_EDGE ( 'NONE', *, *, #35988, .F. ) ;
#17430=CARTESIAN_POINT ( 'NONE',  ( 5.123514540229139769, -30.22567137187272124, 7.785344483711591934 ) ) ;
#17431=EDGE_CURVE ( 'NONE', #20650, #19304, #36544, .T. ) ;
#17434=AXIS2_PLACEMENT_3D ( 'NONE', #29102, #13443, #26018 ) ;
#17440=CARTESIAN_POINT ( 'NONE',  ( -0.1940712780794633940, -32.51289061680132875, 7.013842709614101167 ) ) ;
#17448=CARTESIAN_POINT ( 'NONE',  ( -0.4949140130731182752, -26.97364919215634771, 7.756377446753162985 ) ) ;
#17450=CARTESIAN_POINT ( 'NONE',  ( 2.867385692375432171, -32.85781164720339120, 7.781480525794718162 ) ) ;
#17452=EDGE_CURVE ( 'NONE', #10191, #26363, #25009, .T. ) ;
#17454=EDGE_CURVE ( 'NONE', #18413, #4851, #5308, .T. ) ;
#17455=CARTESIAN_POINT ( 'NONE',  ( 5.026473753875771777, -28.48304391371080158, 7.761113333116787416 ) ) ;
#17462=CARTESIAN_POINT ( 'NONE',  ( 3.442434176459446160, -26.65012155745640499, 6.894806418505343260 ) ) ;
#17463=ORIENTED_EDGE ( 'NONE', *, *, #2067, .F. ) ;
#17466=CARTESIAN_POINT ( 'NONE',  ( -0.1391297599626309944, -34.30339127416094414, 7.013842709614101167 ) ) ;
#17467=ORIENTED_EDGE ( 'NONE', *, *, #27237, .F. ) ;
#17468=LINE ( 'NONE', #17072, #34606 ) ;
#17469=VERTEX_POINT ( 'NONE', #566 ) ;
#17470=CARTESIAN_POINT ( 'NONE',  ( 4.324299927142673639, -27.40773287891062182, 7.782167645815905033 ) ) ;
#17475=CARTESIAN_POINT ( 'NONE',  ( 4.459022997797871035, -27.41600137469124832, 7.753200566781599079 ) ) ;
#17476=ORIENTED_EDGE ( 'NONE', *, *, #40064, .F. ) ;
#17478=CARTESIAN_POINT ( 'NONE',  ( 1.081065130916230466, -26.22681238842248064, 7.661510568013099487 ) ) ;
#17479=CARTESIAN_POINT ( 'NONE',  ( -1.798349965106823989, -29.47546963991379698, 6.863805608295730387 ) ) ;
#17483=LINE ( 'NONE', #38719, #35944 ) ;
#17486=CARTESIAN_POINT ( 'NONE',  ( 5.198039085808181525, -29.69173459304409946, 7.754798119455333705 ) ) ;
#17487=CARTESIAN_POINT ( 'NONE',  ( 1.700390093233090871, -29.56993018339339940, 7.800000000000000711 ) ) ;
#17495=VERTEX_POINT ( 'NONE', #34553 ) ;
#17497=CARTESIAN_POINT ( 'NONE',  ( 0.1007194770999123301, -26.45688377920343015, 7.011627023500184741 ) ) ;
#17500=CARTESIAN_POINT ( 'NONE',  ( 6.126843302897349020, -31.19539656904077418, 7.635761828346577573 ) ) ;
#17506=EDGE_CURVE ( 'NONE', #32438, #31847, #17525, .T. ) ;
#17512=VERTEX_POINT ( 'NONE', #10005 ) ;
#17515=CARTESIAN_POINT ( 'NONE',  ( 0.9770400785565759305, -32.89210785486953625, 6.865312560952602894 ) ) ;
#17516=CARTESIAN_POINT ( 'NONE',  ( -1.475752358162186084, -28.35661785261500967, 6.889465824494256374 ) ) ;
#17517=CARTESIAN_POINT ( 'NONE',  ( -1.699475091297747653, -29.53965268324751747, 7.782167645815905033 ) ) ;
#17525=B_SPLINE_CURVE_WITH_KNOTS ( 'NONE', 3,
 ( #37594, #15369, #12280, #6732, #6325, #31849, #18873, #31445, #3267, #3869, #28959, #22588, #6928, #13293, #16385, #19490, #762, #32064, #25866 ),
 .UNSPECIFIED., .F., .F.,
 ( 4, 3, 3, 3, 3, 3, 4 ),
 ( 2.168404344971008868E-19, 2.546128104244468310E-05, 5.711050680484036374E-05, 8.113074941675828202E-05, 0.0001053129305727062515, 0.0001360598016347037195, 0.0001612931755713731025 ),
 .UNSPECIFIED. ) ;
#17531=AXIS2_PLACEMENT_3D ( 'NONE', #39740, #15031, #34771 ) ;
#17532=ORIENTED_EDGE ( 'NONE', *, *, #32486, .F. ) ;
#17533=ORIENTED_EDGE ( 'NONE', *, *, #15727, .T. ) ;
#17537=CARTESIAN_POINT ( 'NONE',  ( -0.8255983619643308957, -27.29410358292636118, 7.757178535559533294 ) ) ;
#17542=CARTESIAN_POINT ( 'NONE',  ( -1.767452271763144012, -30.04337931387000893, 6.870724624169667116 ) ) ;
#17544=VERTEX_POINT ( 'NONE', #30881 ) ;
#17545=DIRECTION ( 'NONE',  ( -0.9848077530122069101, -0.1736481776669374644, -0.000000000000000000 ) ) ;
#17549=VERTEX_POINT ( 'NONE', #8200 ) ;
#17550=CARTESIAN_POINT ( 'NONE',  ( 0.9719320429316903320, -25.36088087325603624, 7.635761828346577573 ) ) ;
#17555=CARTESIAN_POINT ( 'NONE',  ( 3.340387623678102713, -32.66193850451435310, 6.867199677474201458 ) ) ;
#17556=CARTESIAN_POINT ( 'NONE',  ( -1.096077277123481686, -31.67463417101835077, 6.989977667959449192 ) ) ;
#17557=CARTESIAN_POINT ( 'NONE',  ( 1.700390093233090871, -29.56993018339339940, 7.750000000000000888 ) ) ;
#17558=CARTESIAN_POINT ( 'NONE',  ( -2.716326236424497775, -26.78549066711456916, 6.954324564059724878 ) ) ;
#17559=CARTESIAN_POINT ( 'NONE',  ( -2.496911308493820147, -30.36501393308138574, 7.695279973900954751 ) ) ;
#17560=EDGE_CURVE ( 'NONE', #9646, #11704, #10, .T. ) ;
#17566=CARTESIAN_POINT ( 'NONE',  ( 3.977772666037320715, -27.04534534285276592, 7.754798119455333705 ) ) ;
#17567=VERTEX_POINT ( 'NONE', #8615 ) ;
#17569=CARTESIAN_POINT ( 'NONE',  ( 0.1449207719380061765, -26.54659038131189774, 6.876076431790004939 ) ) ;
#17570=CARTESIAN_POINT ( 'NONE',  ( 3.055600241130194572, -26.45169019916221131, 6.979335674598005745 ) ) ;
#17571=CARTESIAN_POINT ( 'NONE',  ( -0.8610712181068592708, -27.18477818879997088, 6.998987538705433664 ) ) ;
#17573=DIRECTION ( 'NONE',  ( -0.9848077530122092416, 0.1736481776669241694, -0.000000000000000000 ) ) ;
#17575=CARTESIAN_POINT ( 'NONE',  ( 5.200390093233090205, -29.56993018339339940, 7.620413589471895399 ) ) ;
#17582=CARTESIAN_POINT ( 'NONE',  ( 0.02512807029999888919, -32.53672186615392548, 7.257242401810563237 ) ) ;
#17595=CARTESIAN_POINT ( 'NONE',  ( 1.535796139241240255, -32.96595391691614196, 6.876076431790004939 ) ) ;
#17596=CARTESIAN_POINT ( 'NONE',  ( 2.354198823195432055, -26.23337563047396870, 6.880147297696980857 ) ) ;
#17598=CARTESIAN_POINT ( 'NONE',  ( -1.532840524546014160, -30.62170260317305903, 7.759451378593097637 ) ) ;
#17599=LINE ( 'NONE', #36163, #32562 ) ;
#17601=CARTESIAN_POINT ( 'NONE',  ( 0.6746755240984175783, -26.22359730851838933, 6.998987538705434552 ) ) ;
#17603=CARTESIAN_POINT ( 'NONE',  ( 4.428600589446192615, -27.37744993431208940, 6.867280401193706751 ) ) ;
#17606=EDGE_CURVE ( 'NONE', #26569, #22022, #4216, .T. ) ;
#17616=DIRECTION ( 'NONE',  ( -0.6427876096865327016, -0.7660444431189835646, -0.000000000000000000 ) ) ;
#17617=CARTESIAN_POINT ( 'NONE',  ( -1.608892841364319759, -28.78974341809173509, 7.006423389747791219 ) ) ;
#17618=CARTESIAN_POINT ( 'NONE',  ( 2.348307190418675638, -26.14505435796186461, 7.785096263473211486 ) ) ;
#17619=CARTESIAN_POINT ( 'NONE',  ( -0.5782875761460892772, -32.22655866202281061, 6.887161170156908874 ) ) ;
#17620=AXIS2_PLACEMENT_3D ( 'NONE', #11380, #15300, #14475 ) ;
#17622=ORIENTED_EDGE ( 'NONE', *, *, #6144, .F. ) ;
#17626=CARTESIAN_POINT ( 'NONE',  ( -1.639146693691649892, -28.93157757802832819, 6.894806418505346812 ) ) ;
#17629=CARTESIAN_POINT ( 'NONE',  ( 4.732935735574231195, -27.83999033440608883, 7.778495531946297170 ) ) ;
#17634=( BOUNDED_CURVE ( )  B_SPLINE_CURVE ( 3, ( #31052, #8589, #39471, #39893 ),
 .UNSPECIFIED., .F., .F. ) 
 B_SPLINE_CURVE_WITH_KNOTS ( ( 4, 4 ),
 ( 1.347909859412853795, 1.396263401595463360 ),
 .UNSPECIFIED. ) 
 CURVE ( )  GEOMETRIC_REPRESENTATION_ITEM ( )  RATIONAL_B_SPLINE_CURVE ( ( 1.000000000000000000, 0.9998051707368829089, 0.9998051707368829089, 1.000000000000000000 ) ) 
 REPRESENTATION_ITEM ( '' )  );
#17636=CARTESIAN_POINT ( 'NONE',  ( 3.554700302571109916, -26.60177950712765593, 7.754798119455333705 ) ) ;
#17639=FACE_OUTER_BOUND ( 'NONE', #15281, .T. ) ;
#17641=VERTEX_POINT ( 'NONE', #20564 ) ;
#17643=EDGE_CURVE ( 'NONE', #23554, #25871, #20036, .T. ) ;
#17646=CARTESIAN_POINT ( 'NONE',  ( -0.9695225508750403565, -31.83301800158153227, 7.749999999999998224 ) ) ;
#17651=CARTESIAN_POINT ( 'NONE',  ( 2.778259044425222868, -32.89982485500929954, 7.750000000000000888 ) ) ;
#17652=VERTEX_POINT ( 'NONE', #17462 ) ;
#17653=FACE_OUTER_BOUND ( 'NONE', #5546, .T. ) ;
#17654=CARTESIAN_POINT ( 'NONE',  ( 5.056857618328627346, -29.02759656560906976, 6.894806418505346812 ) ) ;
#17660=VERTEX_POINT ( 'NONE', #14584 ) ;
#17662=CARTESIAN_POINT ( 'NONE',  ( -1.211329843465634326, -27.81438207803897456, 6.880147297696979969 ) ) ;
#17679=CARTESIAN_POINT ( 'NONE',  ( 4.822972847261124407, -27.98895676671407173, 6.951256099901587326 ) ) ;
#17681=ORIENTED_EDGE ( 'NONE', *, *, #28547, .F. ) ;
#17687=DIRECTION ( 'NONE',  ( 0.3420201433256662704, 0.9396926207859093161, -0.000000000000000000 ) ) ;
#17688=VERTEX_POINT ( 'NONE', #36630 ) ;
#17698=AXIS2_PLACEMENT_3D ( 'NONE', #32179, #13821, #16686 ) ;
#17699=CARTESIAN_POINT ( 'NONE',  ( -2.217539137252236614, -26.10432465486971054, 7.013842709614101167 ) ) ;
#17700=CARTESIAN_POINT ( 'NONE',  ( -1.250824363190944588, -27.88163718980674233, 7.635761828346577573 ) ) ;
#17704=CARTESIAN_POINT ( 'NONE',  ( 2.868207633511080434, -32.86935470785505231, 6.894806418505347700 ) ) ;
#17706=CARTESIAN_POINT ( 'NONE',  ( 5.916497905674401814, -30.25835747790444330, 7.695279973900954751 ) ) ;
#17708=CARTESIAN_POINT ( 'NONE',  ( -0.8241947473075555974, -27.29254761058917822, 7.754798119455333705 ) ) ;
#17717=LINE ( 'NONE', #11739, #13249 ) ;
#17721=VECTOR ( 'NONE', #22565, 1000.000000000000114 ) ;
#17722=CARTESIAN_POINT ( 'NONE',  ( 3.839274798992386550, -32.21287782106406183, 7.785172627573962778 ) ) ;
#17725=CARTESIAN_POINT ( 'NONE',  ( -1.699178655868960552, -29.51577928193538369, 7.785387725071490905 ) ) ;
#17726=CARTESIAN_POINT ( 'NONE',  ( -1.321941654078521378, -31.33501114731328130, 7.749999999999999112 ) ) ;
#17731=CARTESIAN_POINT ( 'NONE',  ( -0.09771614006683670972, -32.45555212220796193, 6.864276522220859711 ) ) ;
#17735=CARTESIAN_POINT ( 'NONE',  ( 2.255912809263124874, -26.21562030886189731, 7.680992449362118890 ) ) ;
#17743=EDGE_CURVE ( 'NONE', #24264, #15530, #881, .T. ) ;
#17748=CARTESIAN_POINT ( 'NONE',  ( 4.326629237392442207, -31.88355676469063837, 6.865554069792296765 ) ) ;
#17755=ORIENTED_EDGE ( 'NONE', *, *, #38021, .T. ) ;
#17756=CARTESIAN_POINT ( 'NONE',  ( 4.995237956833183723, -30.75059844998224179, 7.750000000000001776 ) ) ;
#17757=CARTESIAN_POINT ( 'NONE',  ( 5.170673138964259508, -29.11471587363884339, 6.880828092187099010 ) ) ;
#17765=FACE_OUTER_BOUND ( 'NONE', #30486, .T. ) ;
#17766=CARTESIAN_POINT ( 'NONE',  ( 1.905780558339014386, -26.16908768638748839, 7.386948897581449458 ) ) ;
#17768=CARTESIAN_POINT ( 'NONE',  ( 2.850561110411099275, -26.37038230420113649, 7.635761828346577573 ) ) ;
#17775=ORIENTED_EDGE ( 'NONE', *, *, #33482, .F. ) ;
#17780=CARTESIAN_POINT ( 'NONE',  ( -0.8574700402111025133, -27.18092379207987719, 6.921725064902947366 ) ) ;
#17784=CARTESIAN_POINT ( 'NONE',  ( -1.749609906766908640, -29.56993018339339940, 7.750000000000000888 ) ) ;
#17787=VECTOR ( 'NONE', #3305, 1000.000000000000114 ) ;
#17790=CARTESIAN_POINT ( 'NONE',  ( 2.431875535358183793, -26.14722233025152676, 7.750000000000000888 ) ) ;
#17791=B_SPLINE_CURVE_WITH_KNOTS ( 'NONE', 3,
 ( #6129, #15992, #31657, #28561, #369, #12904, #22397, #2655, #15174, #27732 ),
 .UNSPECIFIED., .F., .F.,
 ( 4, 3, 3, 4 ),
 ( 0.0002170292169044748620, 0.0002420761345916006457, 0.0002723302478207037807, 0.0002816811360866676396 ),
 .UNSPECIFIED. ) ;
#17799=ORIENTED_EDGE ( 'NONE', *, *, #1204, .F. ) ;
#17804=CARTESIAN_POINT ( 'NONE',  ( 0.01209709964644558461, -32.52114463981743597, 7.635761828346577573 ) ) ;
#17806=CARTESIAN_POINT ( 'NONE',  ( -1.740944944166762820, -30.15835019865512834, 7.778495531946297170 ) ) ;
#17810=CARTESIAN_POINT ( 'NONE',  ( 0.6636879034114320230, -26.22699007480350986, 7.013842709614101167 ) ) ;
#17812=CARTESIAN_POINT ( 'NONE',  ( 0.05705130999228511662, -26.47997509747052192, 7.754798119455333705 ) ) ;
#17814=CARTESIAN_POINT ( 'NONE',  ( -0.4456138174198727153, -26.93275873432113343, 6.892063359921933419 ) ) ;
#17816=ORIENTED_EDGE ( 'NONE', *, *, #2166, .T. ) ;
#17823=CARTESIAN_POINT ( 'NONE',  ( 1.096693473209699121, -26.22395493079927320, 7.635761828346577573 ) ) ;
#17824=CARTESIAN_POINT ( 'NONE',  ( -1.624037871885951390, -28.85698716789056206, 6.863904403958575706 ) ) ;
#17827=EDGE_LOOP ( 'NONE', ( #498, #7458, #11051, #27676, #38455 ) ) ;
#17835=CYLINDRICAL_SURFACE ( 'NONE', #1332, 0.09010775117052864658 ) ;
#17843=CARTESIAN_POINT ( 'NONE',  ( 3.817924346030161509, -32.35669330361569962, 7.013842709614101167 ) ) ;
#17845=CARTESIAN_POINT ( 'NONE',  ( -1.587491370576900040, -30.73692578253573160, 7.781480525794717273 ) ) ;
#17848=CARTESIAN_POINT ( 'NONE',  ( 5.100363281305461349, -29.55642757665872722, 7.635761828346577573 ) ) ;
#17857=CARTESIAN_POINT ( 'NONE',  ( -1.578737010731859902, -28.64489982150178449, 7.505001789837627335 ) ) ;
#17861=CARTESIAN_POINT ( 'NONE',  ( 4.791866717558907141, -27.92896270571450756, 7.751599049952199394 ) ) ;
#17862=DIRECTION ( 'NONE',  ( -0.7394003126383911217, -0.1303762246624254051, -0.6605219282605404585 ) ) ;
#17864=CARTESIAN_POINT ( 'NONE',  ( -0.4155616643037752800, -26.90858688352082595, 7.778050822775633755 ) ) ;
#17881=VERTEX_POINT ( 'NONE', #17220 ) ;
#17883=LINE ( 'NONE', #152, #22700 ) ;
#17885=( BOUNDED_CURVE ( )  B_SPLINE_CURVE ( 3, ( #33022, #22954, #10969, #7288 ),
 .UNSPECIFIED., .F., .T. ) 
 B_SPLINE_CURVE_WITH_KNOTS ( ( 4, 4 ),
 ( 4.708531083176467291, 4.895802057644188743 ),
 .UNSPECIFIED. ) 
 CURVE ( )  GEOMETRIC_REPRESENTATION_ITEM ( )  RATIONAL_B_SPLINE_CURVE ( ( 1.000000000000000000, 0.9970795998553221295, 0.9970795998553221295, 1.000000000000000000 ) ) 
 REPRESENTATION_ITEM ( '' )  );
#17888=CARTESIAN_POINT ( 'NONE',  ( 4.814300635272573459, -27.97194261433657658, 7.009310105710484073 ) ) ;
#17889=CARTESIAN_POINT ( 'NONE',  ( 4.284140121002783630, -27.35989946098248637, 7.721096864323904185 ) ) ;
#17896=CARTESIAN_POINT ( 'NONE',  ( 0.08686669100723981574, -26.57716756243731382, 7.774064877406531515 ) ) ;
#17897=CARTESIAN_POINT ( 'NONE',  ( 1.074608721727911664, -26.22801491291194864, 7.693875151218754205 ) ) ;
#17900=VERTEX_POINT ( 'NONE', #38651 ) ;
#17902=CARTESIAN_POINT ( 'NONE',  ( 4.421194222029321885, -27.53100279559231112, 7.013842709614101167 ) ) ;
#17904=ORIENTED_EDGE ( 'NONE', *, *, #9059, .T. ) ;
#17908=CARTESIAN_POINT ( 'NONE',  ( 5.130566331936590174, -30.26557237595616812, 6.864665094830451508 ) ) ;
#17909=DIRECTION ( 'NONE',  ( 0.8660254037844449249, -0.4999999999999888423, -0.000000000000000000 ) ) ;
#17911=CARTESIAN_POINT ( 'NONE',  ( 2.760057193591220148, -32.90566183273490708, 6.875780273367530171 ) ) ;
#17914=CARTESIAN_POINT ( 'NONE',  ( 0.09894228122565373873, -26.45779829264445482, 7.013842709614101167 ) ) ;
#17916=CARTESIAN_POINT ( 'NONE',  ( 5.100363281305461349, -29.55642757665872722, 7.635761828346577573 ) ) ;
#17921=CARTESIAN_POINT ( 'NONE',  ( 3.495976636161775009, -32.58216173033495977, 7.255881584735162981 ) ) ;
#17930=CARTESIAN_POINT ( 'NONE',  ( 4.722721840544713778, -27.80484921947353527, 7.750000000000000888 ) ) ;
#17933=CARTESIAN_POINT ( 'NONE',  ( 1.037538140294150812, -32.90470487196093785, 6.874555630061442102 ) ) ;
#17950=CARTESIAN_POINT ( 'NONE',  ( -0.8394110418630301718, -27.30951073800569162, 7.774064877406532403 ) ) ;
#17951=ORIENTED_EDGE ( 'NONE', *, *, #22649, .F. ) ;
#17959=CARTESIAN_POINT ( 'NONE',  ( -1.583399485992929234, -33.56764205940365997, 7.695279973900954751 ) ) ;
#17962=EDGE_CURVE ( 'NONE', #33357, #9291, #13620, .T. ) ;
#17964=CARTESIAN_POINT ( 'NONE',  ( 5.172631060824327776, -29.12999534392161038, 6.895394898881670009 ) ) ;
#17965=CARTESIAN_POINT ( 'NONE',  ( -0.1940712780794633940, -32.51289061680132875, 7.013842709614101167 ) ) ;
#17967=CARTESIAN_POINT ( 'NONE',  ( 3.371584782127380553, -26.60899745902780111, 7.670860738520336675 ) ) ;
#17968=CARTESIAN_POINT ( 'NONE',  ( 1.145397458645855071, -32.92432777161535284, 7.692469944509197077 ) ) ;
#17969=CARTESIAN_POINT ( 'NONE',  ( 5.046365345827218185, -28.96623356337001809, 7.635761828346577573 ) ) ;
#17971=CARTESIAN_POINT ( 'NONE',  ( 2.669612181258177674, -32.82885884042005387, 6.920489980334475710 ) ) ;
#17972=CARTESIAN_POINT ( 'NONE',  ( 5.099918824123694350, -29.62653767273290484, 6.887041543973313473 ) ) ;
#17973=CARTESIAN_POINT ( 'NONE',  ( 5.051054751933684805, -30.14703185982037681, 7.635761828346577573 ) ) ;
#17977=CARTESIAN_POINT ( 'NONE',  ( 2.204354934003065480, -33.03347235908793067, 6.863784140767622333 ) ) ;
#17978=ORIENTED_EDGE ( 'NONE', *, *, #10083, .F. ) ;
#17981=EDGE_CURVE ( 'NONE', #19029, #5035, #35732, .T. ) ;
#17983=AXIS2_PLACEMENT_3D ( 'NONE', #16322, #37340, #19223 ) ;
#17984=ORIENTED_EDGE ( 'NONE', *, *, #32563, .F. ) ;
#17987=CARTESIAN_POINT ( 'NONE',  ( 0.1594620532245137889, -26.53915374751568734, 6.887945620086119547 ) ) ;
#17990=CARTESIAN_POINT ( 'NONE',  ( 1.233316054836066877, -26.20214888389141095, 6.863904403958575706 ) ) ;
#17992=CARTESIAN_POINT ( 'NONE',  ( 6.089801904741589667, -27.84269339272794852, 7.754798119455333705 ) ) ;
#17993=ORIENTED_EDGE ( 'NONE', *, *, #4554, .T. ) ;
#17996=AXIS2_PLACEMENT_3D ( 'NONE', #29894, #30109, #32803 ) ;
#18008=CARTESIAN_POINT ( 'NONE',  ( 2.140846989427893643, -33.04210496623404225, 7.013842709614101167 ) ) ;
#18015=CARTESIAN_POINT ( 'NONE',  ( -1.744286257805016227, -30.18979420120317769, 7.756742906098588186 ) ) ;
#18018=CARTESIAN_POINT ( 'NONE',  ( 0.6222294206236387293, -26.24011383383516360, 6.867199677474202346 ) ) ;
#18019=CARTESIAN_POINT ( 'NONE',  ( 5.063156877882684093, -29.06813385812045425, 7.778050822775631978 ) ) ;
#18020=VECTOR ( 'NONE', #331, 1000.000000000000000 ) ;
#18035=CARTESIAN_POINT ( 'NONE',  ( -0.6886162980804276801, -32.12779031683759712, 6.921725064902948255 ) ) ;
#18040=CARTESIAN_POINT ( 'NONE',  ( -1.699609906766908818, -29.56993018339339940, 7.620413589471895399 ) ) ;
#18044=VERTEX_POINT ( 'NONE', #38148 ) ;
#18047=CARTESIAN_POINT ( 'NONE',  ( 3.336167888981159013, -32.55058882503006146, 6.874555630061441214 ) ) ;
#18057=CARTESIAN_POINT ( 'NONE',  ( 3.074471320773512595, -32.79634853659045746, 7.139344958878411695 ) ) ;
#18058=CARTESIAN_POINT ( 'NONE',  ( 1.084888741049048200, -33.00974195381812848, 7.773839561854631874 ) ) ;
#18061=LINE ( 'NONE', #24661, #11476 ) ;
#18062=EDGE_LOOP ( 'NONE', ( #15642, #10589, #15874, #10204, #4898 ) ) ;
#18065=EDGE_CURVE ( 'NONE', #23718, #40022, #25445, .T. ) ;
#18071=CARTESIAN_POINT ( 'NONE',  ( 2.455443087130759761, -25.36557027936252950, 7.635761828346577573 ) ) ;
#18073=CARTESIAN_POINT ( 'NONE',  ( 1.894216096139698768, -26.17545946167590998, 6.903372536218456368 ) ) ;
#18077=EDGE_CURVE ( 'NONE', #18814, #27830, #3210, .T. ) ;
#18078=ORIENTED_EDGE ( 'NONE', *, *, #31863, .T. ) ;
#18079=ORIENTED_EDGE ( 'NONE', *, *, #26217, .F. ) ;
#18083=CARTESIAN_POINT ( 'NONE',  ( 3.467144142116896255, -32.59128420613762245, 7.643192810543821381 ) ) ;
#18084=CARTESIAN_POINT ( 'NONE',  ( 4.769070051701195467, -31.05032170149767978, 7.505001789837629111 ) ) ;
#18101=CARTESIAN_POINT ( 'NONE',  ( -1.796599816117110171, -29.42480412128576717, 6.875780273367531059 ) ) ;
#18104=CARTESIAN_POINT ( 'NONE',  ( 4.812521983982041895, -27.96848237138598137, 7.013842709614101167 ) ) ;
#18108=CYLINDRICAL_SURFACE ( 'NONE', #24101, 0.09010775117053039518 ) ;
#18111=DIRECTION ( 'NONE',  ( -3.491481338843133750E-15, 1.000000000000000000, -0.000000000000000000 ) ) ;
#18112=EDGE_CURVE ( 'NONE', #39610, #30637, #22102, .T. ) ;
#18113=FACE_OUTER_BOUND ( 'NONE', #21728, .T. ) ;
#18114=EDGE_CURVE ( 'NONE', #26363, #2075, #27333, .T. ) ;
#18115=CARTESIAN_POINT ( 'NONE',  ( 2.715450815169567100, -32.91950506007766819, 6.941203072598474577 ) ) ;
#18119=CARTESIAN_POINT ( 'NONE',  ( 0.5160167997142889318, -32.86344804452599533, 7.635761828346576685 ) ) ;
#18120=CARTESIAN_POINT ( 'NONE',  ( 4.631402061531082026, -31.48282785863527167, 6.971170733404096431 ) ) ;
#18122=CARTESIAN_POINT ( 'NONE',  ( 1.577180237285443098, -33.06768434091362963, 7.753200566781576875 ) ) ;
#18123=VECTOR ( 'NONE', #31214, 1000.000000000000000 ) ;
#18126=EDGE_CURVE ( 'NONE', #38094, #38896, #30849, .T. ) ;
#18127=EDGE_LOOP ( 'NONE', ( #5249, #23639, #1063, #11687 ) ) ;
#18132=DIRECTION ( 'NONE',  ( 0.000000000000000000, -0.7508067542896647018, 0.6605219282605379050 ) ) ;
#18135=DIRECTION ( 'NONE',  ( 0.6427876096865369204, -0.7660444431189800119, 0.000000000000000000 ) ) ;
#18144=EDGE_LOOP ( 'NONE', ( #17993, #22211, #31456, #36934, #11397 ) ) ;
#18149=CARTESIAN_POINT ( 'NONE',  ( -0.1401643189945547263, -32.42867603148304312, 6.876076431790004051 ) ) ;
#18157=ORIENTED_EDGE ( 'NONE', *, *, #32300, .T. ) ;
#18161=CARTESIAN_POINT ( 'NONE',  ( -1.695633640289647914, -29.40533622940153791, 6.876076431790004939 ) ) ;
#18165=CARTESIAN_POINT ( 'NONE',  ( -1.774602633087123627, -29.98757303562673826, 6.951256099901590879 ) ) ;
#18167=CARTESIAN_POINT ( 'NONE',  ( 1.662469596549258855, -33.06973143922542135, 6.887161170156904433 ) ) ;
#18169=EDGE_CURVE ( 'NONE', #13356, #9646, #28872, .T. ) ;
#18170=DIRECTION ( 'NONE',  ( -0.000000000000000000, -0.000000000000000000, 1.000000000000000000 ) ) ;
#18172=CARTESIAN_POINT ( 'NONE',  ( 0.5198276744376743030, -32.86481647987437782, 7.640616322432098428 ) ) ;
#18178=CARTESIAN_POINT ( 'NONE',  ( -0.08065709997537935660, -26.55697965350343281, 7.697032948437506406 ) ) ;
#18180=CARTESIAN_POINT ( 'NONE',  ( 1.967410481810895506, -33.06655284499420588, 7.501983001166817822 ) ) ;
#18181=CARTESIAN_POINT ( 'NONE',  ( 5.099787579797017578, -29.63441947184663405, 6.880147297696980857 ) ) ;
#18186=DIRECTION ( 'NONE',  ( -0.9396926207859104263, 0.3420201433256631063, -0.000000000000000000 ) ) ;
#18193=CARTESIAN_POINT ( 'NONE',  ( 2.941320696289306813, -26.40447741350430633, 6.870716933885664623 ) ) ;
#18194=CARTESIAN_POINT ( 'NONE',  ( 4.899719713945094313, -30.72072342401420997, 7.756377446753166538 ) ) ;
#18197=AXIS2_PLACEMENT_3D ( 'NONE', #17390, #14932, #14515 ) ;
#18201=ORIENTED_EDGE ( 'NONE', *, *, #11406, .T. ) ;
#18206=EDGE_CURVE ( 'NONE', #29262, #12828, #36283, .T. ) ;
#18207=B_SPLINE_CURVE_WITH_KNOTS ( 'NONE', 3,
 ( #1394, #10229, #991, #1585, #10626, #22812, #35382, #20102, #26496, #20296 ),
 .UNSPECIFIED., .F., .F.,
 ( 4, 3, 3, 4 ),
 ( 8.673617379884035472E-19, 3.025570593003174677E-05, 6.051145698344189566E-05, 6.468151674593709615E-05 ),
 .UNSPECIFIED. ) ;
#18210=CARTESIAN_POINT ( 'NONE',  ( 2.860566172189516809, -32.76586376621662566, 7.769368695748487319 ) ) ;
#18214=CARTESIAN_POINT ( 'NONE',  ( -1.799428607678825287, -29.60555406228417041, 7.687540746915169976 ) ) ;
#18215=ADVANCED_FACE ( 'NONE', ( #33205 ), #13853, .F. ) ;
#18220=CARTESIAN_POINT ( 'NONE',  ( 3.739317481034212243, -32.29073431218959911, 7.013842709614101167 ) ) ;
#18221=CARTESIAN_POINT ( 'NONE',  ( 3.977772666037320715, -27.04534534285276592, 7.754798119455333705 ) ) ;
#18223=CARTESIAN_POINT ( 'NONE',  ( 4.323735235430704371, -31.73281258077615519, 7.661510568013093270 ) ) ;
#18234=CARTESIAN_POINT ( 'NONE',  ( -1.649885511253406545, -30.14934551598626911, 7.775108481317161591 ) ) ;
#18235=CARTESIAN_POINT ( 'NONE',  ( 2.320254111042885370, -33.01460653443150761, 7.756742906098588186 ) ) ;
#18237=CARTESIAN_POINT ( 'NONE',  ( -0.6444488087166562185, -32.16833941288422238, 7.750000000000000888 ) ) ;
#18238=CARTESIAN_POINT ( 'NONE',  ( 4.850511272190507484, -30.84932285044435218, 6.863904403958575706 ) ) ;
#18242=ORIENTED_EDGE ( 'NONE', *, *, #27188, .T. ) ;
#18248=CARTESIAN_POINT ( 'NONE',  ( -1.522997566795316615, -28.20618826020304226, 6.906857269533148269 ) ) ;
#18251=CARTESIAN_POINT ( 'NONE',  ( -1.343674119598266214, -31.08441801232856605, 6.949473656533214694 ) ) ;
#18255=CARTESIAN_POINT ( 'NONE',  ( 4.927406398964075507, -30.92505592019657001, 6.895394898881661128 ) ) ;
#18256=CARTESIAN_POINT ( 'NONE',  ( -1.183594904732484521, -27.76919811496597745, 7.759451378593095860 ) ) ;
#18264=CARTESIAN_POINT ( 'NONE',  ( 4.977259614314325731, -28.34024264869372445, 7.678495282201406091 ) ) ;
#18268=ORIENTED_EDGE ( 'NONE', *, *, #13628, .F. ) ;
#18269=AXIS2_PLACEMENT_3D ( 'NONE', #39419, #23774, #36351 ) ;
#18273=CARTESIAN_POINT ( 'NONE',  ( 4.082517674496584981, -27.00565348427343082, 6.903112506833890549 ) ) ;
#18277=CARTESIAN_POINT ( 'NONE',  ( -0.4765361063777948658, -26.95821406652526164, 7.775108481317161591 ) ) ;
#18283=ORIENTED_EDGE ( 'NONE', *, *, #33249, .F. ) ;
#18288=CARTESIAN_POINT ( 'NONE',  ( 1.230319205269136518, -26.20258206353872765, 7.754798119455333705 ) ) ;
#18291=CARTESIAN_POINT ( 'NONE',  ( -1.743346351498375801, -30.19497628620385754, 7.640616322432101981 ) ) ;
#18293=ORIENTED_EDGE ( 'NONE', *, *, #30942, .T. ) ;
#18294=CARTESIAN_POINT ( 'NONE',  ( 5.897691494960017877, -28.77484643370537754, 7.695279973900954751 ) ) ;
#18301=ORIENTED_EDGE ( 'NONE', *, *, #4293, .T. ) ;
#18304=ORIENTED_EDGE ( 'NONE', *, *, #4450, .T. ) ;
#18305=CARTESIAN_POINT ( 'NONE',  ( 4.315404545797473013, -33.85565925846036350, 7.754798119455333705 ) ) ;
#18307=CARTESIAN_POINT ( 'NONE',  ( 5.772750116865767112, -28.06626866760150563, 7.013842709614101167 ) ) ;
#18310=CARTESIAN_POINT ( 'NONE',  ( 0.5037982502477859059, -26.38745190989316214, 7.693875151218754205 ) ) ;
#18319=EDGE_CURVE ( 'NONE', #29803, #17239, #1700, .T. ) ;
#18320=CARTESIAN_POINT ( 'NONE',  ( 2.751297001641176632, -32.90844469663947791, 6.880828092187096345 ) ) ;
#18325=CARTESIAN_POINT ( 'NONE',  ( -1.583891440918162585, -30.77968007673214146, 7.635761828346579350 ) ) ;
#18326=CARTESIAN_POINT ( 'NONE',  ( 4.641243193987799387, -31.46766203338331636, 7.009310105710484073 ) ) ;
#18327=CARTESIAN_POINT ( 'NONE',  ( 4.899937972425366439, -30.72010120057137073, 7.635761828346577573 ) ) ;
#18329=CARTESIAN_POINT ( 'NONE',  ( 1.513399906207050449, -32.96478432900200062, 7.013842709614101167 ) ) ;
#18330=ORIENTED_EDGE ( 'NONE', *, *, #29195, .T. ) ;
#18333=ORIENTED_EDGE ( 'NONE', *, *, #7540, .T. ) ;
#18336=DIRECTION ( 'NONE',  ( -0.000000000000000000, -0.000000000000000000, -1.000000000000000000 ) ) ;
#18338=CARTESIAN_POINT ( 'NONE',  ( 0.01209709964644558461, -32.52114463981743597, 7.635761828346577573 ) ) ;
#18340=CARTESIAN_POINT ( 'NONE',  ( 4.269670580072574495, -31.94665014585129725, 7.013842709614101167 ) ) ;
#18341=LINE ( 'NONE', #21455, #31189 ) ;
#18346=DIRECTION ( 'NONE',  ( 0.7541618601367554575, 0.000000000000000000, -0.6566885781822834334 ) ) ;
#18354=CARTESIAN_POINT ( 'NONE',  ( -0.08877474292672410394, -32.46112373979092069, 6.864651958020304257 ) ) ;
#18357=CARTESIAN_POINT ( 'NONE',  ( 3.947630499704354090, -32.24896051801510310, 7.767720160662275219 ) ) ;
#18362=VERTEX_POINT ( 'NONE', #2327 ) ;
#18364=CARTESIAN_POINT ( 'NONE',  ( 1.688104973690869537, -26.06994794917929781, 7.756742906098588186 ) ) ;
#18365=ADVANCED_FACE ( 'NONE', ( #24532 ), #2741, .T. ) ;
#18369=CARTESIAN_POINT ( 'NONE',  ( -1.577286183139641418, -30.79746357491616138, 7.670465701733744979 ) ) ;
#18375=AXIS2_PLACEMENT_3D ( 'NONE', #28063, #35825, #7600 ) ;
#18377=FACE_OUTER_BOUND ( 'NONE', #29446, .T. ) ;
#18379=CARTESIAN_POINT ( 'NONE',  ( -1.799609906766908685, -29.56993018339339940, 6.929570838012926615 ) ) ;
#18381=CARTESIAN_POINT ( 'NONE',  ( 4.458039033310292609, -27.41499233908904287, 7.754798119455333705 ) ) ;
#18384=( BOUNDED_CURVE ( )  B_SPLINE_CURVE ( 3, ( #7797, #20349, #1637, #36210 ),
 .UNSPECIFIED., .F., .T. ) 
 B_SPLINE_CURVE_WITH_KNOTS ( ( 4, 4 ),
 ( 4.748221474220560623, 4.941946782021394924 ),
 .UNSPECIFIED. ) 
 CURVE ( )  GEOMETRIC_REPRESENTATION_ITEM ( )  RATIONAL_B_SPLINE_CURVE ( ( 1.000000000000000000, 0.9968749865767494445, 0.9968749865767494445, 1.000000000000000000 ) ) 
 REPRESENTATION_ITEM ( '' )  );
#18385=CARTESIAN_POINT ( 'NONE',  ( 0.5148699040292038509, -32.86303942011277712, 7.756742906098588186 ) ) ;
#18397=CARTESIAN_POINT ( 'NONE',  ( -1.654012860102806570, -29.01496998062980381, 7.695279973900954751 ) ) ;
#18398=CARTESIAN_POINT ( 'NONE',  ( 3.052721860142450172, -26.45044204593990145, 6.920489980334479263 ) ) ;
#18401=CARTESIAN_POINT ( 'NONE',  ( 1.307444196246471124, -26.19270861743451206, 6.911401339314954484 ) ) ;
#18407=VERTEX_POINT ( 'NONE', #21049 ) ;
#18408=EDGE_LOOP ( 'NONE', ( #11460, #10097, #31099, #5721 ) ) ;
#18413=VERTEX_POINT ( 'NONE', #17725 ) ;
#18414=DIRECTION ( 'NONE',  ( -0.8660254037844415942, 0.4999999999999950040, -0.000000000000000000 ) ) ;
#18415=CARTESIAN_POINT ( 'NONE',  ( 4.899937972425366439, -30.72010120057137073, 7.635761828346577573 ) ) ;
#18417=VERTEX_POINT ( 'NONE', #8669 ) ;
#18424=CARTESIAN_POINT ( 'NONE',  ( 5.141684319425215755, -30.20828278875847062, 6.894806418505347700 ) ) ;
#18429=VECTOR ( 'NONE', #10030, 1000.000000000000000 ) ;
#18431=CARTESIAN_POINT ( 'NONE',  ( 3.901280325574687957, -32.16147924937965996, 7.643333865083956624 ) ) ;
#18437=CARTESIAN_POINT ( 'NONE',  ( -1.663744362731840676, -30.06256111737130965, 7.774064877406527962 ) ) ;
#18445=VERTEX_POINT ( 'NONE', #9703 ) ;
#18447=CARTESIAN_POINT ( 'NONE',  ( 5.200390093233090205, -29.56993018339339940, 7.620413589471895399 ) ) ;
#18455=CARTESIAN_POINT ( 'NONE',  ( 4.978659405551939088, -28.32469115355010914, 7.255881584735162981 ) ) ;
#18457=CARTESIAN_POINT ( 'NONE',  ( -0.8361945232212143475, -27.30589628897558896, 6.864651958020303368 ) ) ;
#18460=CARTESIAN_POINT ( 'NONE',  ( 0.05705130999228511662, -26.47997509747052192, 7.754798119455333705 ) ) ;
#18461=CARTESIAN_POINT ( 'NONE',  ( 4.921350899141003765, -30.93938997316396566, 6.989977667959438534 ) ) ;
#18467=DIRECTION ( 'NONE',  ( 1.224646799147353207E-16, 1.000000000000000000, -0.000000000000000000 ) ) ;
#18470=CARTESIAN_POINT ( 'NONE',  ( 5.006037652185061582, -30.36535116702205883, 6.969307238440507923 ) ) ;
#18473=FACE_OUTER_BOUND ( 'NONE', #7768, .T. ) ;
#18476=CARTESIAN_POINT ( 'NONE',  ( 3.498496326533036882, -26.68430824457884398, 6.864276522220859711 ) ) ;
#18477=CARTESIAN_POINT ( 'NONE',  ( 3.992140197745001728, -26.92457926934255141, 6.875671892026062437 ) ) ;
#18480=CARTESIAN_POINT ( 'NONE',  ( 1.825221044428271044, -26.17220649359113338, 6.863904403958575706 ) ) ;
#18487=( BOUNDED_CURVE ( )  B_SPLINE_CURVE ( 3, ( #26510, #26710, #10842, #39244 ),
 .UNSPECIFIED., .F., .F. ) 
 B_SPLINE_CURVE_WITH_KNOTS ( ( 4, 4 ),
 ( 1.347909859412853795, 1.534781240595298746 ),
 .UNSPECIFIED. ) 
 CURVE ( )  GEOMETRIC_REPRESENTATION_ITEM ( )  RATIONAL_B_SPLINE_CURVE ( ( 1.000000000000000000, 0.9970920404276226723, 0.9970920404276226723, 1.000000000000000000 ) ) 
 REPRESENTATION_ITEM ( '' )  );
#18494=EDGE_CURVE ( 'NONE', #20325, #21904, #660, .T. ) ;
#18500=ORIENTED_EDGE ( 'NONE', *, *, #17506, .T. ) ;
#18508=CARTESIAN_POINT ( 'NONE',  ( 4.668948836787977896, -27.91232378075620701, 6.894806418505348589 ) ) ;
#18511=DIRECTION ( 'NONE',  ( 0.3754033771448229140, 0.6502177225477935307, -0.6605219282605403475 ) ) ;
#18512=CARTESIAN_POINT ( 'NONE',  ( 0.5718647330646855487, -26.27158218865373129, 7.784725160561909441 ) ) ;
#18516=CARTESIAN_POINT ( 'NONE',  ( 4.460814650971867579, -27.41817363093848314, 7.750000000000000888 ) ) ;
#18520=ORIENTED_EDGE ( 'NONE', *, *, #39068, .F. ) ;
#18527=CARTESIAN_POINT ( 'NONE',  ( 1.075343990422650275, -26.12619373866192873, 7.640616322432101093 ) ) ;
#18528=AXIS2_PLACEMENT_3D ( 'NONE', #12748, #12341, #25325 ) ;
#18530=CARTESIAN_POINT ( 'NONE',  ( 5.140967908914694462, -28.99159849420241741, 7.781480525794719938 ) ) ;
#18535=CARTESIAN_POINT ( 'NONE',  ( 1.719724692003898658, -33.06987729247488517, 7.747520101777647383 ) ) ;
#18544=EDGE_CURVE ( 'NONE', #6683, #2116, #17468, .T. ) ;
#18548=CARTESIAN_POINT ( 'NONE',  ( -1.744066689084928345, -30.19099175420856440, 7.635761828346576685 ) ) ;
#18553=CARTESIAN_POINT ( 'NONE',  ( -0.05515801212132670495, -32.48165012009213370, 6.880147297696981745 ) ) ;
#18556=CYLINDRICAL_SURFACE ( 'NONE', #22643, 0.09010775117053000660 ) ;
#18563=CARTESIAN_POINT ( 'NONE',  ( 4.748716522672954632, -31.28972995975264837, 7.678495282201404315 ) ) ;
#18567=CARTESIAN_POINT ( 'NONE',  ( -1.693306178808691609, -29.36295009413090540, 6.979335674598003969 ) ) ;
#18574=DIRECTION ( 'NONE',  ( 0.3420201433256790380, -0.9396926207859046531, -0.000000000000000000 ) ) ;
#18576=CARTESIAN_POINT ( 'NONE',  ( 5.198171123944452354, -29.69454897310232155, 7.751599049952198506 ) ) ;
#18580=DIRECTION ( 'NONE',  ( -0.9848077530122092416, 0.1736481776669241694, -0.000000000000000000 ) ) ;
#18581=CARTESIAN_POINT ( 'NONE',  ( -0.9113260236350476662, -31.74685638300427826, 7.775108481317166031 ) ) ;
#18584=B_SPLINE_CURVE_WITH_KNOTS ( 'NONE', 3,
 ( #26097, #25287, #19511, #6555, #25484, #13314, #6348, #382, #16406, #19100 ),
 .UNSPECIFIED., .F., .F.,
 ( 4, 3, 3, 4 ),
 ( 0.0001585009270395775123, 0.0001815657551981816192, 0.0002118214035944121802, 0.0002170292169044816383 ),
 .UNSPECIFIED. ) ;
#18588=CARTESIAN_POINT ( 'NONE',  ( -1.535120485362819753, -30.61471740307679568, 6.863904403958576594 ) ) ;
#18591=DIRECTION ( 'NONE',  ( 0.9848077530122103518, -0.1736481776669172583, -0.000000000000000000 ) ) ;
#18596=FACE_OUTER_BOUND ( 'NONE', #18062, .T. ) ;
#18598=CARTESIAN_POINT ( 'NONE',  ( 5.023800704533929462, -28.47218391387568204, 6.863784140767622333 ) ) ;
#18600=CARTESIAN_POINT ( 'NONE',  ( 5.052941056949534548, -30.13600185428053635, 7.740055089680399902 ) ) ;
#18601=VERTEX_POINT ( 'NONE', #37242 ) ;
#18604=ORIENTED_EDGE ( 'NONE', *, *, #25900, .F. ) ;
#18606=CARTESIAN_POINT ( 'NONE',  ( -1.482088180267138622, -30.76652202637871625, 7.695279973900954751 ) ) ;
#18610=CARTESIAN_POINT ( 'NONE',  ( 4.421861210295527478, -27.53188506292452686, 6.895222827070019989 ) ) ;
#18611=( BOUNDED_CURVE ( )  B_SPLINE_CURVE ( 3, ( #24658, #30855, #36605, #11669 ),
 .UNSPECIFIED., .F., .T. ) 
 B_SPLINE_CURVE_WITH_KNOTS ( ( 4, 4 ),
 ( 1.381924640371166690, 1.574767692156074483 ),
 .UNSPECIFIED. ) 
 CURVE ( )  GEOMETRIC_REPRESENTATION_ITEM ( )  RATIONAL_B_SPLINE_CURVE ( ( 1.000000000000000000, 0.9969033633783033199, 0.9969033633783033199, 1.000000000000000000 ) ) 
 REPRESENTATION_ITEM ( '' )  );
#18612=B_SPLINE_CURVE_WITH_KNOTS ( 'NONE', 3,
 ( #35529, #5025, #20658, #1959, #30351, #36520, #35927, #27245, #8091, #36321 ),
 .UNSPECIFIED., .F., .F.,
 ( 4, 3, 3, 4 ),
 ( 0.0002170292169044774099, 0.0002420761345915964716, 0.0002723302478207020459, 0.0002816811360866753916 ),
 .UNSPECIFIED. ) ;
#18613=CARTESIAN_POINT ( 'NONE',  ( 2.761442704594925246, -32.80013489931718595, 7.768425012602591551 ) ) ;
#18619=CARTESIAN_POINT ( 'NONE',  ( -0.1551898507743131317, -32.53746921202473175, 7.753200566781576875 ) ) ;
#18620=CARTESIAN_POINT ( 'NONE',  ( 1.629959277500286685, -32.96921550338401374, 7.784476445165072533 ) ) ;
#18621=CARTESIAN_POINT ( 'NONE',  ( 3.421838780265678004, -26.52253300979309003, 7.720710062488887360 ) ) ;
#18623=CARTESIAN_POINT ( 'NONE',  ( 3.723586923686467376, -32.30245183660008479, 6.929923840112067523 ) ) ;
#18625=LINE ( 'NONE', #25035, #18123 ) ;
#18629=DIRECTION ( 'NONE',  ( 0.000000000000000000, 0.000000000000000000, 1.000000000000000000 ) ) ;
#18631=AXIS2_PLACEMENT_3D ( 'NONE', #24364, #5431, #8706 ) ;
#18633=AXIS2_PLACEMENT_3D ( 'NONE', #29182, #13925, #10434 ) ;
#18641=VECTOR ( 'NONE', #39885, 1000.000000000000000 ) ;
#18644=EDGE_CURVE ( 'NONE', #14367, #24859, #8823, .T. ) ;
#18650=ORIENTED_EDGE ( 'NONE', *, *, #34789, .F. ) ;
#18652=ORIENTED_EDGE ( 'NONE', *, *, #16773, .F. ) ;
#18654=CARTESIAN_POINT ( 'NONE',  ( -1.697427395360086244, -29.44812577374269580, 7.754798119455333705 ) ) ;
#18655=B_SPLINE_CURVE_WITH_KNOTS ( 'NONE', 3,
 ( #30337, #33846, #2764, #8898 ),
 .UNSPECIFIED., .F., .F.,
 ( 4, 4 ),
 ( 0.000000000000000000, 6.391136169994862974E-06 ),
 .UNSPECIFIED. ) ;
#18662=CARTESIAN_POINT ( 'NONE',  ( -1.784512137809761700, -29.51577928193536593, 7.785387725071483800 ) ) ;
#18663=CARTESIAN_POINT ( 'NONE',  ( 4.919623465605695856, -30.94344769399372908, 6.931070083220548739 ) ) ;
#18665=CARTESIAN_POINT ( 'NONE',  ( 0.9053063435450576790, -25.37262878166647084, 7.695279973900954751 ) ) ;
#18669=CYLINDRICAL_SURFACE ( 'NONE', #12348, 0.09010775117053039518 ) ;
#18670=EDGE_CURVE ( 'NONE', #24849, #19674, #23386, .T. ) ;
#18678=B_SPLINE_CURVE_WITH_KNOTS ( 'NONE', 3,
 ( #23823, #33733, #21167, #30645 ),
 .UNSPECIFIED., .F., .F.,
 ( 4, 4 ),
 ( 0.000000000000000000, 6.391136169994469103E-06 ),
 .UNSPECIFIED. ) ;
#18682=CARTESIAN_POINT ( 'NONE',  ( 2.913833110970087681, -32.85284901314008010, 7.750000000000001776 ) ) ;
#18685=CARTESIAN_POINT ( 'NONE',  ( 4.066175018403209940, -26.99056084707641290, 6.880828092187096345 ) ) ;
#18686=DIRECTION ( 'NONE',  ( 1.000000000000000000, 0.000000000000000000, 0.000000000000000000 ) ) ;
#18687=CARTESIAN_POINT ( 'NONE',  ( 4.792526203416204389, -27.93020634197934982, 7.750000000000000888 ) ) ;
#18689=CARTESIAN_POINT ( 'NONE',  ( 1.910276347359660898, -26.17641463748400810, 6.959317978105163505 ) ) ;
#18692=AXIS2_PLACEMENT_3D ( 'NONE', #8664, #23905, #30930 ) ;
#18693=AXIS2_PLACEMENT_3D ( 'NONE', #9771, #37966, #31202 ) ;
#18694=DIRECTION ( 'NONE',  ( 1.000000000000000000, 0.000000000000000000, 0.000000000000000000 ) ) ;
#18701=CARTESIAN_POINT ( 'NONE',  ( 5.928245814084836418, -30.19173177851781276, 7.754798119455333705 ) ) ;
#18706=ORIENTED_EDGE ( 'NONE', *, *, #4988, .T. ) ;
#18712=ORIENTED_EDGE ( 'NONE', *, *, #3078, .T. ) ;
#18714=CARTESIAN_POINT ( 'NONE',  ( 6.029042948269167645, -32.11059846819836139, 7.695279973900954751 ) ) ;
#18719=CARTESIAN_POINT ( 'NONE',  ( 0.8302441911734864677, -26.17279668076718835, 7.501983001166816933 ) ) ;
#18727=EDGE_CURVE ( 'NONE', #651, #38473, #799, .T. ) ;
#18729=ORIENTED_EDGE ( 'NONE', *, *, #30165, .T. ) ;
#18730=CARTESIAN_POINT ( 'NONE',  ( 3.939786388318850641, -26.88011527646091992, 7.635761828346575797 ) ) ;
#18737=CARTESIAN_POINT ( 'NONE',  ( 0.5502190760550982329, -32.76947806258566231, 7.635761828346577573 ) ) ;
#18739=CARTESIAN_POINT ( 'NONE',  ( 1.073548286649947725, -26.12652063041838346, 7.643192810543820492 ) ) ;
#18742=CARTESIAN_POINT ( 'NONE',  ( 5.098207581826219581, -29.69173459304409946, 7.754798119455333705 ) ) ;
#18744=( BOUNDED_CURVE ( )  B_SPLINE_CURVE ( 3, ( #37210, #31870, #40294, #34571 ),
 .UNSPECIFIED., .F., .F. ) 
 B_SPLINE_CURVE_WITH_KNOTS ( ( 4, 4 ),
 ( 4.748221474220558846, 4.941946782021394036 ),
 .UNSPECIFIED. ) 
 CURVE ( )  GEOMETRIC_REPRESENTATION_ITEM ( )  RATIONAL_B_SPLINE_CURVE ( ( 1.000000000000000000, 0.9968749865767494445, 0.9968749865767494445, 1.000000000000000000 ) ) 
 REPRESENTATION_ITEM ( '' )  );
#18747=EDGE_LOOP ( 'NONE', ( #13942, #30953, #6799, #18268 ) ) ;
#18750=CYLINDRICAL_SURFACE ( 'NONE', #29078, 0.09010775117052798044 ) ;
#18754=ORIENTED_EDGE ( 'NONE', *, *, #4346, .F. ) ;
#18758=CARTESIAN_POINT ( 'NONE',  ( 4.960212797054523115, -28.60371536055546926, 6.979335674598003969 ) ) ;
#18759=CARTESIAN_POINT ( 'NONE',  ( -0.8532251611581016526, -27.17638696620667105, 6.951256099901587326 ) ) ;
#18767=CARTESIAN_POINT ( 'NONE',  ( -1.749422520758312505, -28.97934324792513294, 7.750000000000000000 ) ) ;
#18768=VERTEX_POINT ( 'NONE', #11425 ) ;
#18775=ORIENTED_EDGE ( 'NONE', *, *, #38118, .F. ) ;
#18779=CARTESIAN_POINT ( 'NONE',  ( 4.254702208415469755, -31.96273153170552916, 6.971170733404099984 ) ) ;
#18780=CARTESIAN_POINT ( 'NONE',  ( -1.693494594903330652, -29.36608178104888722, 6.920489980334477487 ) ) ;
#18782=CARTESIAN_POINT ( 'NONE',  ( -1.420400527842048843, -31.15443827722234360, 6.980586498568969844 ) ) ;
#18784=CARTESIAN_POINT ( 'NONE',  ( 1.519733255401420458, -33.06526953655340861, 6.998987538705437217 ) ) ;
#18788=AXIS2_PLACEMENT_3D ( 'NONE', #26305, #38838, #32687 ) ;
#18789=CARTESIAN_POINT ( 'NONE',  ( -0.6412820820920860365, -32.03500197365509194, 6.939395833800439561 ) ) ;
#18791=CARTESIAN_POINT ( 'NONE',  ( -0.03065438358791758300, -26.64358689880297248, 7.695279973900954751 ) ) ;
#18797=CARTESIAN_POINT ( 'NONE',  ( 0.4893092558450570229, -32.84442375634601063, 7.778495531946294506 ) ) ;
#18799=CARTESIAN_POINT ( 'NONE',  ( 2.128010023882844326, -32.94294212574573777, 6.876076431790006716 ) ) ;
#18800=AXIS2_PLACEMENT_3D ( 'NONE', #29278, #16306, #32183 ) ;
#18803=VERTEX_POINT ( 'NONE', #24412 ) ;
#18806=CARTESIAN_POINT ( 'NONE',  ( 2.933026231274471485, -26.29416234278157916, 6.887161170156907986 ) ) ;
#18808=CYLINDRICAL_SURFACE ( 'NONE', #23267, 0.09010775117052854943 ) ;
#18809=CARTESIAN_POINT ( 'NONE',  ( 0.09112544421487976665, -26.57487120552241322, 6.864651958020304257 ) ) ;
#18810=CARTESIAN_POINT ( 'NONE',  ( 5.038904606479174042, -28.51902327498534362, 6.880828092187097234 ) ) ;
#18812=CARTESIAN_POINT ( 'NONE',  ( 1.317809913116059883, -26.19152339826795739, 6.959317978105164393 ) ) ;
#18813=CARTESIAN_POINT ( 'NONE',  ( 5.031981677282425736, -30.24852985705353348, 7.778050822775632867 ) ) ;
#18814=VERTEX_POINT ( 'NONE', #2199 ) ;
#18816=FACE_OUTER_BOUND ( 'NONE', #20954, .T. ) ;
#18819=ORIENTED_EDGE ( 'NONE', *, *, #22386, .T. ) ;
#18822=CARTESIAN_POINT ( 'NONE',  ( -1.673641830192087676, -29.98934475122311838, 6.882085323592687764 ) ) ;
#18827=CARTESIAN_POINT ( 'NONE',  ( 4.434886103410926594, -27.54940263586490801, 6.959317978105159952 ) ) ;
#18829=CARTESIAN_POINT ( 'NONE',  ( -1.591993232420714444, -30.71360387936050529, 7.785344483711591934 ) ) ;
#18830=CARTESIAN_POINT ( 'NONE',  ( 2.815854552281536805, -32.78175835696561791, 7.785868773668302545 ) ) ;
#18840=EDGE_CURVE ( 'NONE', #5389, #20836, #12061, .T. ) ;
#18843=B_SPLINE_CURVE_WITH_KNOTS ( 'NONE', 3,
 ( #24929, #24092, #39954, #27189, #2719, #37265, #9061, #39747, #30910, #21840 ),
 .UNSPECIFIED., .F., .F.,
 ( 4, 3, 3, 4 ),
 ( 1.817454023025239628E-18, 3.025570593003134020E-05, 6.051145698344051330E-05, 6.468151674594376400E-05 ),
 .UNSPECIFIED. ) ;
#18844=DIRECTION ( 'NONE',  ( -0.000000000000000000, -0.000000000000000000, -1.000000000000000000 ) ) ;
#18847=CARTESIAN_POINT ( 'NONE',  ( 4.327546298727369845, -31.72818190512046499, 7.680992449362112673 ) ) ;
#18854=AXIS2_PLACEMENT_3D ( 'NONE', #19433, #22338, #25211 ) ;
#18864=EDGE_CURVE ( 'NONE', #37836, #5603, #39856, .T. ) ;
#18872=ADVANCED_FACE ( 'NONE', ( #21949 ), #12465, .F. ) ;
#18873=CARTESIAN_POINT ( 'NONE',  ( -1.730496578629491689, -28.93663728645029920, 7.781480525794718162 ) ) ;
#18876=ORIENTED_EDGE ( 'NONE', *, *, #16890, .F. ) ;
#18877=ORIENTED_EDGE ( 'NONE', *, *, #25768, .F. ) ;
#18883=( GEOMETRIC_REPRESENTATION_CONTEXT ( 3 ) GLOBAL_UNCERTAINTY_ASSIGNED_CONTEXT ( ( #6531 ) ) GLOBAL_UNIT_ASSIGNED_CONTEXT ( ( #39307, #19973, #1460 ) ) REPRESENTATION_CONTEXT ( 'NONE', 'WORKASPACE' ) );
#18885=AXIS2_PLACEMENT_3D ( 'NONE', #5628, #18170, #5835 ) ;
#18889=VECTOR ( 'NONE', #15175, 1000.000000000000000 ) ;
#18891=CARTESIAN_POINT ( 'NONE',  ( -0.9451523768770455636, -31.70561910709598052, 6.880147297696979969 ) ) ;
#18892=DIRECTION ( 'NONE',  ( 0.3420201433256662704, 0.9396926207859093161, -0.000000000000000000 ) ) ;
#18902=CARTESIAN_POINT ( 'NONE',  ( 4.093191441545242171, -27.01561806821104739, 6.971170733404101760 ) ) ;
#18903=PLANE ( 'NONE',  #28495 ) ;
#18906=VERTEX_POINT ( 'NONE', #25036 ) ;
#18913=CARTESIAN_POINT ( 'NONE',  ( 6.053772676492744864, -27.07209504432901070, 7.635761828346577573 ) ) ;
#18919=EDGE_LOOP ( 'NONE', ( #18650, #16047, #35346, #29959, #14192 ) ) ;
#18921=ORIENTED_EDGE ( 'NONE', *, *, #19481, .F. ) ;
#18923=EDGE_CURVE ( 'NONE', #21155, #29030, #6298, .T. ) ;
#18928=VERTEX_POINT ( 'NONE', #36969 ) ;
#18929=EDGE_CURVE ( 'NONE', #37836, #2601, #9167, .T. ) ;
#18940=VERTEX_POINT ( 'NONE', #31215 ) ;
#18945=CARTESIAN_POINT ( 'NONE',  ( -1.368289865235002178, -28.08953866528909415, 7.505001789837628223 ) ) ;
#18950=CARTESIAN_POINT ( 'NONE',  ( 0.4535750661203729606, -32.73306980853894999, 7.778050822775633755 ) ) ;
#18956=CARTESIAN_POINT ( 'NONE',  ( -0.07645708395594488782, -32.58535952412007930, 6.894806418505347700 ) ) ;
#18957=CARTESIAN_POINT ( 'NONE',  ( -1.273818662545060709, -31.21737738347374602, 7.785172627573962778 ) ) ;
#18963=CARTESIAN_POINT ( 'NONE',  ( -1.135875017054286618, -33.94315967623287378, 6.894806418505347700 ) ) ;
#18967=CARTESIAN_POINT ( 'NONE',  ( -0.5067439190362983403, -26.87212914619025739, 7.785096263473212375 ) ) ;
#18973=CARTESIAN_POINT ( 'NONE',  ( 5.904749997263966321, -30.32498317729107740, 7.635761828346577573 ) ) ;
#18974=CARTESIAN_POINT ( 'NONE',  ( 2.272716057154847924, -26.11704110451741556, 7.685194954629195330 ) ) ;
#18978=ORIENTED_EDGE ( 'NONE', *, *, #19993, .T. ) ;
#18984=CARTESIAN_POINT ( 'NONE',  ( -1.752170693794088185, -28.99562711716245644, 7.714178352335857802 ) ) ;
#18988=CARTESIAN_POINT ( 'NONE',  ( 3.930644293244915044, -32.25600374108427104, 7.778495531946298058 ) ) ;
#18996=CARTESIAN_POINT ( 'NONE',  ( 3.438683469850188690, -26.53211252316276259, 7.635761828346582014 ) ) ;
#18998=( BOUNDED_CURVE ( )  B_SPLINE_CURVE ( 3, ( #7440, #7648, #681, #16109 ),
 .UNSPECIFIED., .F., .F. ) 
 B_SPLINE_CURVE_WITH_KNOTS ( ( 4, 4 ),
 ( 1.347909859412855793, 1.534781240595299856 ),
 .UNSPECIFIED. ) 
 CURVE ( )  GEOMETRIC_REPRESENTATION_ITEM ( )  RATIONAL_B_SPLINE_CURVE ( ( 1.000000000000000000, 0.9970920404276226723, 0.9970920404276226723, 1.000000000000000000 ) ) 
 REPRESENTATION_ITEM ( '' )  );
#19000=CARTESIAN_POINT ( 'NONE',  ( -1.699260392630454364, -29.52118006577551412, 6.894806418505346812 ) ) ;
#19002=CARTESIAN_POINT ( 'NONE',  ( -1.414328007069049375, -31.16634214640615141, 7.006908160621414083 ) ) ;
#19004=CARTESIAN_POINT ( 'NONE',  ( 1.527332651948331899, -33.06564960244016760, 7.009310105710487626 ) ) ;
#19010=CARTESIAN_POINT ( 'NONE',  ( 3.056550635926903237, -26.44443126081507600, 7.386948897581450346 ) ) ;
#19011=CARTESIAN_POINT ( 'NONE',  ( 4.358774179341475374, -27.29331111184919934, 7.710604733652631992 ) ) ;
#19013=CARTESIAN_POINT ( 'NONE',  ( 1.075454873741154005, -26.12617409861640638, 7.750000000000000888 ) ) ;
#19014=CARTESIAN_POINT ( 'NONE',  ( 2.156915105547790645, -32.93915630191352761, 6.865312560952603782 ) ) ;
#19017=CARTESIAN_POINT ( 'NONE',  ( -1.473412216555795018, -28.35051274117816789, 7.785172627573962778 ) ) ;
#19019=ORIENTED_EDGE ( 'NONE', *, *, #17981, .F. ) ;
#19020=CARTESIAN_POINT ( 'NONE',  ( 5.067143666762728316, -33.49802700238250708, 7.695279973900954751 ) ) ;
#19024=CARTESIAN_POINT ( 'NONE',  ( 0.04964925160023719169, -26.59754819687732308, 6.887041543973313473 ) ) ;
#19026=CARTESIAN_POINT ( 'NONE',  ( 1.139827216511555052, -26.21645895774650370, 7.782167645815905033 ) ) ;
#19029=VERTEX_POINT ( 'NONE', #1353 ) ;
#19030=B_SPLINE_CURVE_WITH_KNOTS ( 'NONE', 3,
 ( #3876, #16392, #29363, #573, #6738, #13110, #34766, #973, #35363, #38014, #7330, #16584, #25670, #25470, #13510, #29165, #28963, #768, #13300, #19886, #25873, #38413, #22793, #32461, #13718, #26284, #38818, #33485, #35952, #1774, #8117 ),
 .UNSPECIFIED., .F., .F.,
 ( 4, 3, 3, 3, 3, 3, 3, 3, 3, 3, 4 ),
 ( 6.484403375994738403E-05, 8.983333709522376971E-05, 0.0001203539973219378077, 0.0001514144607149686141, 0.0001828916862241615547, 0.0002144221682127263285, 0.0002455195857862215369, 0.0002758614570916280775, 0.0003055381793602579294, 0.0003350143730643711853, 0.0003497271997307910231 ),
 .UNSPECIFIED. ) ;
#19034=EDGE_CURVE ( 'NONE', #17047, #32358, #21037, .T. ) ;
#19035=CARTESIAN_POINT ( 'NONE',  ( -0.5217032702065468319, -32.27405686018897768, 7.695279973900954751 ) ) ;
#19036=ORIENTED_EDGE ( 'NONE', *, *, #36767, .F. ) ;
#19039=CARTESIAN_POINT ( 'NONE',  ( -1.675359094926574866, -29.97529103330290212, 7.013842709614101167 ) ) ;
#19046=ORIENTED_EDGE ( 'NONE', *, *, #1576, .F. ) ;
#19049=VERTEX_POINT ( 'NONE', #37982 ) ;
#19051=DIRECTION ( 'NONE',  ( -0.000000000000000000, 0.7508067542896647018, 0.6605219282605379050 ) ) ;
#19063=DIRECTION ( 'NONE',  ( -0.6427876096865327016, -0.7660444431189835646, -0.000000000000000000 ) ) ;
#19074=CARTESIAN_POINT ( 'NONE',  ( 0.6874672402166666085, -34.21933100612760370, 6.894806418505347700 ) ) ;
#19076=CARTESIAN_POINT ( 'NONE',  ( 3.985769669582015062, -26.93874319361661662, 7.785593909369613819 ) ) ;
#19077=AXIS2_PLACEMENT_3D ( 'NONE', #19259, #25845, #31828 ) ;
#19083=CARTESIAN_POINT ( 'NONE',  ( -1.340386146056437688, -31.09100870292229857, 6.988553391373219625 ) ) ;
#19093=CARTESIAN_POINT ( 'NONE',  ( -1.033767024100737508, -31.59091637407721009, 6.969307238440508812 ) ) ;
#19100=CARTESIAN_POINT ( 'NONE',  ( -0.01837800939314739035, -32.61883756299590686, 7.695279973900954751 ) ) ;
#19101=ORIENTED_EDGE ( 'NONE', *, *, #1590, .F. ) ;
#19102=CARTESIAN_POINT ( 'NONE',  ( 2.866894658930008610, -26.27004123098783950, 7.670465701733748531 ) ) ;
#19105=CARTESIAN_POINT ( 'NONE',  ( 1.790155505744531084, -26.17111536485493772, 7.778050822775631978 ) ) ;
#19106=VECTOR ( 'NONE', #14075, 1000.000000000000227 ) ;
#19107=DIRECTION ( 'NONE',  ( -0.7126435865141306225, 0.000000000000000000, -0.7015262779114384006 ) ) ;
#19108=CARTESIAN_POINT ( 'NONE',  ( 4.632456985502078517, -27.84858802096400510, 7.740055089680403455 ) ) ;
#19110=ORIENTED_EDGE ( 'NONE', *, *, #30891, .T. ) ;
#19112=EDGE_CURVE ( 'NONE', #10847, #4150, #16557, .T. ) ;
#19117=CARTESIAN_POINT ( 'NONE',  ( -1.334894404175721805, -31.29013112173537792, 7.781480525794719050 ) ) ;
#19121=ORIENTED_EDGE ( 'NONE', *, *, #2208, .T. ) ;
#19134=CARTESIAN_POINT ( 'NONE',  ( 4.714904839365606115, -27.99744780023306134, 6.868387053540519815 ) ) ;
#19143=EDGE_CURVE ( 'NONE', #40099, #23269, #19463, .T. ) ;
#19149=ORIENTED_EDGE ( 'NONE', *, *, #17560, .F. ) ;
#19150=AXIS2_PLACEMENT_3D ( 'NONE', #8759, #15355, #12477 ) ;
#19151=CARTESIAN_POINT ( 'NONE',  ( 0.4299795134041287659, -32.72366716650702756, 7.761597726988851420 ) ) ;
#19155=CARTESIAN_POINT ( 'NONE',  ( 5.099854031935251442, -29.63030343461936411, 7.785172627573962778 ) ) ;
#19158=EDGE_CURVE ( 'NONE', #32112, #16761, #1100, .T. ) ;
#19159=EDGE_CURVE ( 'NONE', #19681, #36032, #19957, .T. ) ;
#19160=CARTESIAN_POINT ( 'NONE',  ( 0.5160167997142889318, -32.86344804452599533, 7.635761828346576685 ) ) ;
#19164=VERTEX_POINT ( 'NONE', #35725 ) ;
#19167=CARTESIAN_POINT ( 'NONE',  ( 1.712675212775339517, -33.06991241760749745, 7.756742906098588186 ) ) ;
#19172=CARTESIAN_POINT ( 'NONE',  ( 4.957993191292200841, -28.59625817525675018, 6.997764925645181044 ) ) ;
#19174=CARTESIAN_POINT ( 'NONE',  ( 2.292186059008701093, -26.12032476611858911, 7.638991368224661294 ) ) ;
#19177=CARTESIAN_POINT ( 'NONE',  ( 3.829758772512354970, -32.34767630444171971, 6.880828092187096345 ) ) ;
#19178=ORIENTED_EDGE ( 'NONE', *, *, #3064, .F. ) ;
#19183=ORIENTED_EDGE ( 'NONE', *, *, #40605, .F. ) ;
#19192=VERTEX_POINT ( 'NONE', #8295 ) ;
#19193=EDGE_CURVE ( 'NONE', #19421, #18407, #34730, .T. ) ;
#19194=CARTESIAN_POINT ( 'NONE',  ( 1.718491058161632168, -26.07869869449652001, 7.778495531946298058 ) ) ;
#19200=CARTESIAN_POINT ( 'NONE',  ( -1.367092955110547514, -31.25535295005563796, 6.867280401193707640 ) ) ;
#19202=ADVANCED_FACE ( 'NONE', ( #33461 ), #33656, .F. ) ;
#19204=CARTESIAN_POINT ( 'NONE',  ( -0.6017143941908295046, -32.07201138884889247, 6.871394612369935651 ) ) ;
#19211=CARTESIAN_POINT ( 'NONE',  ( -0.9781255058339732855, -31.66410296430423443, 7.759451378593094084 ) ) ;
#19213=CARTESIAN_POINT ( 'NONE',  ( -1.577774374486538678, -28.34370111728035013, 6.894806418505347700 ) ) ;
#19215=ADVANCED_FACE ( 'NONE', ( #17765 ), #20255, .F. ) ;
#19218=ORIENTED_EDGE ( 'NONE', *, *, #4776, .F. ) ;
#19220=CYLINDRICAL_SURFACE ( 'NONE', #8037, 0.09010775117052882699 ) ;
#19223=DIRECTION ( 'NONE',  ( 0.000000000000000000, 0.000000000000000000, 1.000000000000000000 ) ) ;
#19224=CARTESIAN_POINT ( 'NONE',  ( -1.600658481268678823, -28.40671124064021669, 7.697032948437508182 ) ) ;
#19226=CARTESIAN_POINT ( 'NONE',  ( 3.601045828089646239, -26.63095849577496566, 6.903112506833891437 ) ) ;
#19228=CARTESIAN_POINT ( 'NONE',  ( -1.268168650321787716, -31.22753658603060956, 6.894806418505346812 ) ) ;
#19229=EDGE_LOOP ( 'NONE', ( #27441, #23580, #37938, #7192 ) ) ;
#19230=CYLINDRICAL_SURFACE ( 'NONE', #18854, 0.09010775117053149152 ) ;
#19234=ORIENTED_EDGE ( 'NONE', *, *, #23641, .F. ) ;
#19236=( BOUNDED_CURVE ( )  B_SPLINE_CURVE ( 3, ( #26936, #17857, #4908, #36208 ),
 .UNSPECIFIED., .F., .T. ) 
 B_SPLINE_CURVE_WITH_KNOTS ( ( 4, 4 ),
 ( 4.748221474220560623, 4.941946782021394924 ),
 .UNSPECIFIED. ) 
 CURVE ( )  GEOMETRIC_REPRESENTATION_ITEM ( )  RATIONAL_B_SPLINE_CURVE ( ( 1.000000000000000000, 0.9968749865767494445, 0.9968749865767494445, 1.000000000000000000 ) ) 
 REPRESENTATION_ITEM ( '' )  );
#19238=DIRECTION ( 'NONE',  ( -0.000000000000000000, -0.000000000000000000, -1.000000000000000000 ) ) ;
#19250=EDGE_LOOP ( 'NONE', ( #38409, #10560, #16782, #40121 ) ) ;
#19251=CARTESIAN_POINT ( 'NONE',  ( -1.543298022821887328, -28.25521066738867049, 7.750000000000000888 ) ) ;
#19252=CARTESIAN_POINT ( 'NONE',  ( 1.697525331384263314, -32.96992897650194720, 7.769368695748486431 ) ) ;
#19255=CARTESIAN_POINT ( 'NONE',  ( 3.821287304908778548, -32.22733399491815476, 6.870716933885664623 ) ) ;
#19257=CARTESIAN_POINT ( 'NONE',  ( 5.195093854244484000, -29.76240288740631357, 6.961115707816230902 ) ) ;
#19259=CARTESIAN_POINT ( 'NONE',  ( 5.150390093233091271, -29.56993018339339940, 7.750000000000000888 ) ) ;
#19263=CARTESIAN_POINT ( 'NONE',  ( 1.731470216958145070, -26.07006818241261215, 6.894806418505347700 ) ) ;
#19267=CARTESIAN_POINT ( 'NONE',  ( 1.822194502883806022, -33.27093018339341768, 7.754798119455333705 ) ) ;
#19268=VERTEX_POINT ( 'NONE', #23751 ) ;
#19270=B_SPLINE_CURVE_WITH_KNOTS ( 'NONE', 3,
 ( #19580, #19167, #1058, #13382, #16073, #7012, #16660, #22872, #25553, #28846, #7212, #38093, #22473, #35242, #34637, #10294, #31941, #35041, #35442 ),
 .UNSPECIFIED., .F., .F.,
 ( 4, 3, 3, 3, 3, 3, 4 ),
 ( 0.000000000000000000, 2.546128104244783067E-05, 5.711050680484007236E-05, 8.113074941675932556E-05, 0.0001053129305727076745, 0.0001360598016347103331, 0.0001612931755702044952 ),
 .UNSPECIFIED. ) ;
#19279=CARTESIAN_POINT ( 'NONE',  ( 4.017083442752244160, -26.95596097974580729, 7.776484688137382584 ) ) ;
#19286=ORIENTED_EDGE ( 'NONE', *, *, #21256, .F. ) ;
#19287=VERTEX_POINT ( 'NONE', #19013 ) ;
#19288=CARTESIAN_POINT ( 'NONE',  ( -0.06024024948605010560, -26.54499921554088360, 7.756742906098588186 ) ) ;
#19292=ORIENTED_EDGE ( 'NONE', *, *, #28989, .T. ) ;
#19295=CARTESIAN_POINT ( 'NONE',  ( -1.754169330766808699, -30.13215794990895091, 6.880608371227949327 ) ) ;
#19296=CARTESIAN_POINT ( 'NONE',  ( -0.6073368879808319631, -32.18772608075904174, 7.780491323090166667 ) ) ;
#19297=CIRCLE ( 'NONE', #35103, 3.449999999999999734 ) ;
#19300=CARTESIAN_POINT ( 'NONE',  ( 5.137206238981461226, -30.23196853600094158, 6.875671892026062437 ) ) ;
#19304=VERTEX_POINT ( 'NONE', #34281 ) ;
#19306=CARTESIAN_POINT ( 'NONE',  ( 4.594123659639434365, -31.35497693952491005, 7.774064877406528851 ) ) ;
#19308=CARTESIAN_POINT ( 'NONE',  ( 1.711546634882549212, -26.16993837675040524, 7.775108481317162479 ) ) ;
#19311=CARTESIAN_POINT ( 'NONE',  ( 4.684314823655713944, -27.94012068505428559, 7.782034975670475418 ) ) ;
#19312=CARTESIAN_POINT ( 'NONE',  ( -0.9997577495568453765, -27.34300195364327735, 7.660770905198786451 ) ) ;
#19320=CARTESIAN_POINT ( 'NONE',  ( -0.04165398999324298329, -32.48973880933039737, 6.894806418505347700 ) ) ;
#19321=DIRECTION ( 'NONE',  ( 0.6662082868431827842, 0.000000000000000000, 0.7457657263118703250 ) ) ;
#19325=FACE_OUTER_BOUND ( 'NONE', #4502, .T. ) ;
#19326=AXIS2_PLACEMENT_3D ( 'NONE', #20416, #1312, #29502 ) ;
#19327=AXIS2_PLACEMENT_3D ( 'NONE', #9040, #15018, #5965 ) ;
#19331=CARTESIAN_POINT ( 'NONE',  ( 5.152603803343559719, -30.14631978585090621, 7.724038915126860694 ) ) ;
#19332=ADVANCED_FACE ( 'NONE', ( #11784 ), #8707, .F. ) ;
#19338=CARTESIAN_POINT ( 'NONE',  ( 4.543259257677775054, -31.43490735317836027, 7.006423389747791219 ) ) ;
#19346=ORIENTED_EDGE ( 'NONE', *, *, #8566, .F. ) ;
#19347=EDGE_CURVE ( 'NONE', #33823, #15769, #25257, .T. ) ;
#19354=CARTESIAN_POINT ( 'NONE',  ( 2.733375749414411082, -32.91402105668144884, 7.009310105710485850 ) ) ;
#19364=CARTESIAN_POINT ( 'NONE',  ( 0.9689046511080217083, -32.99263803653528271, 7.750000000000000888 ) ) ;
#19366=CARTESIAN_POINT ( 'NONE',  ( 2.863609035986291573, -26.26888160889163615, 7.695279973900954751 ) ) ;
#19367=AXIS2_PLACEMENT_3D ( 'NONE', #17500, #1906, #14426 ) ;
#19373=CARTESIAN_POINT ( 'NONE',  ( -1.650274565467498622, -28.99282850696639713, 7.635761828346577573 ) ) ;
#19377=CARTESIAN_POINT ( 'NONE',  ( 4.947902983373059449, -28.56308938330872849, 6.876076431790004939 ) ) ;
#19378=CARTESIAN_POINT ( 'NONE',  ( 2.274434078087634870, -26.11732469660939415, 7.674970859709602244 ) ) ;
#19387=CARTESIAN_POINT ( 'NONE',  ( 2.919807535448344815, -26.39612787360452373, 7.785172627573962778 ) ) ;
#19390=CARTESIAN_POINT ( 'NONE',  ( -1.594496203247892208, -28.38936776459798139, 7.640616322432101093 ) ) ;
#19397=VECTOR ( 'NONE', #13389, 1000.000000000000000 ) ;
#19398=FACE_OUTER_BOUND ( 'NONE', #28429, .T. ) ;
#19401=CARTESIAN_POINT ( 'NONE',  ( -0.1660129358314331172, -32.53077879159856423, 6.870724624169668004 ) ) ;
#19404=CARTESIAN_POINT ( 'NONE',  ( -1.699457623340715040, -29.60210943304089071, 7.721096864323900633 ) ) ;
#19405=CARTESIAN_POINT ( 'NONE',  ( 3.554655459890166735, -26.72005913740336069, 6.887945620086118659 ) ) ;
#19406=CARTESIAN_POINT ( 'NONE',  ( -0.06129048428309483154, -26.54561512989744188, 7.635761828346575797 ) ) ;
#19407=CARTESIAN_POINT ( 'NONE',  ( 2.322191688357494677, -25.34207446254166385, 7.754798119455333705 ) ) ;
#19413=DIRECTION ( 'NONE',  ( 1.000000000000000000, -2.973811673103098158E-15, 0.000000000000000000 ) ) ;
#19414=CARTESIAN_POINT ( 'NONE',  ( 1.686887486498408029, -26.16995699532097319, 7.635761828346577573 ) ) ;
#19420=VECTOR ( 'NONE', #8912, 1000.000000000000227 ) ;
#19421=VERTEX_POINT ( 'NONE', #12621 ) ;
#19424=EDGE_CURVE ( 'NONE', #18044, #28636, #37328, .T. ) ;
#19426=CARTESIAN_POINT ( 'NONE',  ( -0.9479511760676456733, -27.30154873620575984, 7.783750581861600182 ) ) ;
#19429=CARTESIAN_POINT ( 'NONE',  ( 1.074608721727911442, -26.22801491291194864, 7.695279973900954751 ) ) ;
#19430=CARTESIAN_POINT ( 'NONE',  ( 1.165751748339587168, -26.11099046226085107, 6.867280401193707640 ) ) ;
#19431=EDGE_LOOP ( 'NONE', ( #28117, #36587, #6896, #14943, #15026 ) ) ;
#19433=CARTESIAN_POINT ( 'NONE',  ( 5.698101969243359655, -32.85371976261941285, 7.695279973900954751 ) ) ;
#19435=CARTESIAN_POINT ( 'NONE',  ( -0.9807834779648342272, -31.66069757387703731, 7.754798119455333705 ) ) ;
#19439=CARTESIAN_POINT ( 'NONE',  ( -1.489921458977837565, -30.74547780039133116, 7.635761828346577573 ) ) ;
#19454=ORIENTED_EDGE ( 'NONE', *, *, #21772, .F. ) ;
#19457=DIRECTION ( 'NONE',  ( -1.000000000000000000, 0.000000000000000000, 0.000000000000000000 ) ) ;
#19462=CARTESIAN_POINT ( 'NONE',  ( 5.195651087393625467, -29.75204319633411743, 6.912143950357338085 ) ) ;
#19463=B_SPLINE_CURVE_WITH_KNOTS ( 'NONE', 3,
 ( #22367, #7301, #9985, #32433 ),
 .UNSPECIFIED., .F., .F.,
 ( 4, 4 ),
 ( 1.084202172485504434E-19, 6.391136169993539061E-06 ),
 .UNSPECIFIED. ) ;
#19464=CARTESIAN_POINT ( 'NONE',  ( -0.5741452863692977360, -26.90976311966657164, 7.670465701733756525 ) ) ;
#19465=CARTESIAN_POINT ( 'NONE',  ( 3.465471057152984091, -32.59226193070500699, 7.750000000000000000 ) ) ;
#19477=CYLINDRICAL_SURFACE ( 'NONE', #5750, 0.09010775117052950700 ) ;
#19478=( BOUNDED_CURVE ( )  B_SPLINE_CURVE ( 3, ( #39136, #29086, #17108, #3989 ),
 .UNSPECIFIED., .F., .T. ) 
 B_SPLINE_CURVE_WITH_KNOTS ( ( 4, 4 ),
 ( 1.347909859412854017, 1.534781240595298746 ),
 .UNSPECIFIED. ) 
 CURVE ( )  GEOMETRIC_REPRESENTATION_ITEM ( )  RATIONAL_B_SPLINE_CURVE ( ( 1.000000000000000000, 0.9970920404276226723, 0.9970920404276226723, 1.000000000000000000 ) ) 
 REPRESENTATION_ITEM ( '' )  );
#19481=EDGE_CURVE ( 'NONE', #19773, #33743, #27654, .T. ) ;
#19483=CARTESIAN_POINT ( 'NONE',  ( 2.999143718241246148, -26.32260591150095763, 7.766640943994346458 ) ) ;
#19487=EDGE_CURVE ( 'NONE', #16824, #2431, #11993, .T. ) ;
#19488=ORIENTED_EDGE ( 'NONE', *, *, #3107, .F. ) ;
#19490=CARTESIAN_POINT ( 'NONE',  ( -1.722492012567419239, -28.86192695835683253, 7.771081512783704071 ) ) ;
#19492=CARTESIAN_POINT ( 'NONE',  ( -1.699260392630454364, -29.52118006577551412, 6.894806418505346812 ) ) ;
#19497=CARTESIAN_POINT ( 'NONE',  ( -0.5217428287191434588, -32.27402435476302145, 7.698786668945014178 ) ) ;
#19498=DIRECTION ( 'NONE',  ( 0.8660254037844380415, 0.5000000000000009992, -0.000000000000000000 ) ) ;
#19504=DIRECTION ( 'NONE',  ( -0.7660444431189725734, -0.6427876096865456912, -0.000000000000000000 ) ) ;
#19507=CARTESIAN_POINT ( 'NONE',  ( 4.713418716757639793, -27.78901510573760092, 7.700536657684214248 ) ) ;
#19511=CARTESIAN_POINT ( 'NONE',  ( -0.02702267027603847890, -32.61394955640600557, 7.737115613922536106 ) ) ;
#19512=CARTESIAN_POINT ( 'NONE',  ( -1.579542791844172900, -30.79142478763816371, 7.737115613922529000 ) ) ;
#19514=CARTESIAN_POINT ( 'NONE',  ( 1.668210843585588687, -26.17008246681959349, 7.721096864323904185 ) ) ;
#19517=DIRECTION ( 'NONE',  ( -0.6427876096865327016, -0.7660444431189835646, -0.000000000000000000 ) ) ;
#19523=VERTEX_POINT ( 'NONE', #23112 ) ;
#19526=CARTESIAN_POINT ( 'NONE',  ( -1.343377678608602688, -31.26794527077870356, 7.785344483711591934 ) ) ;
#19528=VERTEX_POINT ( 'NONE', #13635 ) ;
#19530=ORIENTED_EDGE ( 'NONE', *, *, #8857, .T. ) ;
#19531=CYLINDRICAL_SURFACE ( 'NONE', #9689, 0.09010775117052841066 ) ;
#19533=ORIENTED_EDGE ( 'NONE', *, *, #36136, .F. ) ;
#19542=ADVANCED_FACE ( 'NONE', ( #38533 ), #35479, .F. ) ;
#19545=ADVANCED_FACE ( 'NONE', ( #31987 ), #889, .F. ) ;
#19546=FACE_OUTER_BOUND ( 'NONE', #31884, .T. ) ;
#19547=EDGE_CURVE ( 'NONE', #17567, #26935, #34895, .T. ) ;
#19548=CARTESIAN_POINT ( 'NONE',  ( 4.534632712474313543, -31.44797946402438171, 6.969307238440503482 ) ) ;
#19560=CARTESIAN_POINT ( 'NONE',  ( 0.3842138451641537999, -32.70485417806369810, 6.876076431790004939 ) ) ;
#19563=ORIENTED_EDGE ( 'NONE', *, *, #26058, .T. ) ;
#19564=CARTESIAN_POINT ( 'NONE',  ( 0.4621924864893861007, -32.73646653789152339, 7.782034975670476307 ) ) ;
#19567=CARTESIAN_POINT ( 'NONE',  ( 5.077611659191977544, -29.17698428640678543, 6.911401339314954484 ) ) ;
#19569=CARTESIAN_POINT ( 'NONE',  ( 5.150898290942641289, -29.04796049306044026, 7.780491323090170219 ) ) ;
#19573=CARTESIAN_POINT ( 'NONE',  ( 2.887256171390399029, -32.85664523690996219, 7.773839561854631874 ) ) ;
#19577=ORIENTED_EDGE ( 'NONE', *, *, #38192, .T. ) ;
#19580=CARTESIAN_POINT ( 'NONE',  ( 1.717829174068238984, -33.06988673718940674, 7.750000000000000888 ) ) ;
#19585=CARTESIAN_POINT ( 'NONE',  ( 2.285976816415960400, -26.11925954147043072, 7.646866513072557048 ) ) ;
#19587=ORIENTED_EDGE ( 'NONE', *, *, #24736, .T. ) ;
#19590=VERTEX_POINT ( 'NONE', #281 ) ;
#19593=CARTESIAN_POINT ( 'NONE',  ( 1.079328522417935421, -26.12547340107537863, 7.635761828346579350 ) ) ;
#19595=VERTEX_POINT ( 'NONE', #19213 ) ;
#19597=( BOUNDED_CURVE ( )  B_SPLINE_CURVE ( 3, ( #2173, #5655, #27067, #21509 ),
 .UNSPECIFIED., .F., .F. ) 
 B_SPLINE_CURVE_WITH_KNOTS ( ( 4, 4 ),
 ( 4.748221474220558846, 4.941946782021393147 ),
 .UNSPECIFIED. ) 
 CURVE ( )  GEOMETRIC_REPRESENTATION_ITEM ( )  RATIONAL_B_SPLINE_CURVE ( ( 1.000000000000000000, 0.9968749865767494445, 0.9968749865767494445, 1.000000000000000000 ) ) 
 REPRESENTATION_ITEM ( '' )  );
#19599=CARTESIAN_POINT ( 'NONE',  ( 4.458039033310292609, -27.41499233908904287, 7.754798119455333705 ) ) ;
#19604=DIRECTION ( 'NONE',  ( 0.6502177225477889788, 0.3754033771448354040, 0.6605219282605379050 ) ) ;
#19609=CARTESIAN_POINT ( 'NONE',  ( 2.301779523252329263, -26.22352920515988828, 7.775108481317162479 ) ) ;
#19616=DIRECTION ( 'NONE',  ( -0.000000000000000000, -0.000000000000000000, -1.000000000000000000 ) ) ;
#19617=CARTESIAN_POINT ( 'NONE',  ( 6.029691375358208205, -29.61640541118720193, 6.954324564059724878 ) ) ;
#19619=DIRECTION ( 'NONE',  ( 0.000000000000000000, -0.7541618601367526820, -0.6566885781822866530 ) ) ;
#19621=EDGE_CURVE ( 'NONE', #15830, #9639, #22045, .T. ) ;
#19623=CARTESIAN_POINT ( 'NONE',  ( -1.493583877073865862, -28.40437011329764871, 7.769368695748486431 ) ) ;
#19624=ORIENTED_EDGE ( 'NONE', *, *, #20377, .F. ) ;
#19625=CARTESIAN_POINT ( 'NONE',  ( 2.410368835147195021, -26.24488429107400478, 7.754798119455333705 ) ) ;
#19628=CARTESIAN_POINT ( 'NONE',  ( 3.069849883003687552, -26.34896937748550272, 6.989977667959442975 ) ) ;
#19629=EDGE_CURVE ( 'NONE', #29197, #24455, #28002, .T. ) ;
#19631=CARTESIAN_POINT ( 'NONE',  ( -1.391746016950013320, -31.20965402480746320, 7.750000000000000888 ) ) ;
#19634=CARTESIAN_POINT ( 'NONE',  ( 0.4754575822783353445, -26.29127984263010731, 7.660770905198778458 ) ) ;
#19635=CARTESIAN_POINT ( 'NONE',  ( 1.130236063958923509, -26.21806220515917474, 7.779495906702013741 ) ) ;
#19636=CARTESIAN_POINT ( 'NONE',  ( 1.206567936595640100, -26.10494249544789369, 6.865482280155369210 ) ) ;
#19637=ORIENTED_EDGE ( 'NONE', *, *, #22115, .F. ) ;
#19641=CARTESIAN_POINT ( 'NONE',  ( 4.826555071938813946, -30.90675198375193844, 7.013842709614101167 ) ) ;
#19646=CARTESIAN_POINT ( 'NONE',  ( -1.656469331124993616, -30.10983836210348485, 6.892063359921931642 ) ) ;
#19650=LINE ( 'NONE', #20043, #1072 ) ;
#19659=EDGE_CURVE ( 'NONE', #28877, #19681, #38936, .T. ) ;
#19660=CARTESIAN_POINT ( 'NONE',  ( -1.053369181053855463, -31.72885680097385475, 7.761113333116790969 ) ) ;
#19664=CARTESIAN_POINT ( 'NONE',  ( 3.842201187575565502, -32.21050686967832632, 6.887041543973314361 ) ) ;
#19666=CARTESIAN_POINT ( 'NONE',  ( -89.20959394718985891, -30.34358980514384285, 7.013842709614101167 ) ) ;
#19674=VERTEX_POINT ( 'NONE', #32589 ) ;
#19675=EDGE_CURVE ( 'NONE', #31513, #1511, #16682, .T. ) ;
#19681=VERTEX_POINT ( 'NONE', #15545 ) ;
#19684=CARTESIAN_POINT ( 'NONE',  ( 2.891262396755087671, -26.28021669631634438, 7.762796336881261361 ) ) ;
#19692=B_SPLINE_CURVE_WITH_KNOTS ( 'NONE', 3,
 ( #39336, #2304, #14826, #7850, #35873, #21026, #33600, #29676, #1903, #20203, #11527, #1488, #4970, #7652, #14022, #5374, #14423, #26992, #32787, #10930, #39538, #8442, #26595, #10724, #23509, #4578, #36073, #32980, #17301, #17497, #17914 ),
 .UNSPECIFIED., .F., .F.,
 ( 4, 3, 3, 3, 3, 3, 3, 3, 3, 3, 4 ),
 ( 3.049318610115481221E-20, 3.077658087705713937E-05, 6.152638666999062957E-05, 9.267501192706755864E-05, 0.0001241882240135204452, 0.0001556618703051673963, 0.0001866161554452218428, 0.0002167966385860980115, 0.0002463805737537775979, 0.0002758761370306525985, 0.0002847094172290031517 ),
 .UNSPECIFIED. ) ;
#19695=CARTESIAN_POINT ( 'NONE',  ( 1.700390093233090871, -29.56993018339339940, 7.750000000000000888 ) ) ;
#19701=ORIENTED_EDGE ( 'NONE', *, *, #37455, .T. ) ;
#19702=CARTESIAN_POINT ( 'NONE',  ( -0.9384404336435322458, -31.71389406695070790, 6.889465824494253710 ) ) ;
#19703=CARTESIAN_POINT ( 'NONE',  ( 4.283498045048843572, -27.35914579868425278, 7.670860738520329569 ) ) ;
#19705=CARTESIAN_POINT ( 'NONE',  ( 5.141430038532381452, -28.93020829471468858, 7.670465701733746755 ) ) ;
#19711=CARTESIAN_POINT ( 'NONE',  ( 3.936759689487521641, -26.87759828911498516, 7.750000000000000888 ) ) ;
#19713=AXIS2_PLACEMENT_3D ( 'NONE', #17050, #11073, #11271 ) ;
#19714=CARTESIAN_POINT ( 'NONE',  ( 1.730667593378961477, -26.17006499886255710, 7.782167645815905033 ) ) ;
#19715=EDGE_CURVE ( 'NONE', #40540, #39495, #33678, .T. ) ;
#19716=CARTESIAN_POINT ( 'NONE',  ( -0.3639226275255784682, -26.86831799423209688, 6.871394612369935651 ) ) ;
#19717=CARTESIAN_POINT ( 'NONE',  ( 4.679472942922894063, -27.93128239903199628, 7.784476445165072533 ) ) ;
#19719=( BOUNDED_CURVE ( )  B_SPLINE_CURVE ( 3, ( #10714, #33173, #33391, #20588 ),
 .UNSPECIFIED., .F., .T. ) 
 B_SPLINE_CURVE_WITH_KNOTS ( ( 4, 4 ),
 ( 1.381924640371166690, 1.574767692156075372 ),
 .UNSPECIFIED. ) 
 CURVE ( )  GEOMETRIC_REPRESENTATION_ITEM ( )  RATIONAL_B_SPLINE_CURVE ( ( 1.000000000000000000, 0.9969033633783032089, 0.9969033633783032089, 1.000000000000000000 ) ) 
 REPRESENTATION_ITEM ( '' )  );
#19723=CARTESIAN_POINT ( 'NONE',  ( 4.229427455569045868, -31.84236720560299005, 7.761597726988855861 ) ) ;
#19727=CARTESIAN_POINT ( 'NONE',  ( -0.4126339070069648951, -26.77974567795123662, 7.006908160621408754 ) ) ;
#19728=CARTESIAN_POINT ( 'NONE',  ( -1.271367234268484081, -27.72096874884677931, 6.865482280155368322 ) ) ;
#19729=ORIENTED_EDGE ( 'NONE', *, *, #26681, .T. ) ;
#19731=VERTEX_POINT ( 'NONE', #8947 ) ;
#19733=EDGE_LOOP ( 'NONE', ( #27784, #36629, #13507, #13451, #25357, #31526 ) ) ;
#19734=ADVANCED_FACE ( 'NONE', ( #33898 ), #2612, .F. ) ;
#19738=VERTEX_POINT ( 'NONE', #32027 ) ;
#19740=CARTESIAN_POINT ( 'NONE',  ( -0.03413980529548706760, -32.49422506527100296, 7.784838882742139532 ) ) ;
#19741=CARTESIAN_POINT ( 'NONE',  ( 4.597156102822266277, -31.35005458526572752, 6.866852738645444987 ) ) ;
#19748=DIRECTION ( 'NONE',  ( 1.000000000000000000, -1.189524669241239263E-14, 0.000000000000000000 ) ) ;
#19753=CARTESIAN_POINT ( 'NONE',  ( 0.3572758658287483180, -32.69339687477079082, 6.903372536218454592 ) ) ;
#19756=CARTESIAN_POINT ( 'NONE',  ( -1.786444507892435585, -29.53457013502913497, 7.783750581861600182 ) ) ;
#19759=FACE_OUTER_BOUND ( 'NONE', #30792, .T. ) ;
#19761=DIRECTION ( 'NONE',  ( -0.000000000000000000, -0.000000000000000000, -1.000000000000000000 ) ) ;
#19766=EDGE_CURVE ( 'NONE', #20836, #2808, #37855, .T. ) ;
#19770=CARTESIAN_POINT ( 'NONE',  ( 3.429035706983251774, -32.49769360082827063, 7.670860738520329569 ) ) ;
#19773=VERTEX_POINT ( 'NONE', #35520 ) ;
#19776=CYLINDRICAL_SURFACE ( 'NONE', #9336, 0.09010775117052885475 ) ;
#19779=ORIENTED_EDGE ( 'NONE', *, *, #16662, .F. ) ;
#19781=CARTESIAN_POINT ( 'NONE',  ( 5.143311846931861275, -28.94039731499685786, 7.743886751744253338 ) ) ;
#19783=ORIENTED_EDGE ( 'NONE', *, *, #29069, .F. ) ;
#19785=DIRECTION ( 'NONE',  ( -0.3420201433256601087, -0.9396926207859114255, -0.000000000000000000 ) ) ;
#19786=ORIENTED_EDGE ( 'NONE', *, *, #35268, .T. ) ;
#19792=CARTESIAN_POINT ( 'NONE',  ( -1.600265505308078318, -28.40559435941229438, 7.678495282201406980 ) ) ;
#19793=CARTESIAN_POINT ( 'NONE',  ( 4.390852040715039983, -27.34879134089963415, 7.781480525794719050 ) ) ;
#19804=CARTESIAN_POINT ( 'NONE',  ( -0.1945137394687337096, -32.51260574566864392, 6.895394898881673562 ) ) ;
#19806=CARTESIAN_POINT ( 'NONE',  ( -1.699587041002557086, -29.58345656395455592, 7.755436452974803885 ) ) ;
#19809=CARTESIAN_POINT ( 'NONE',  ( 0.7267180850964402028, -26.31232708533429232, 6.997764925645182821 ) ) ;
#19814=CARTESIAN_POINT ( 'NONE',  ( 3.374101601209122059, -32.52943855271229268, 7.782167645815905033 ) ) ;
#19817=CARTESIAN_POINT ( 'NONE',  ( -0.4595759649632789601, -32.19567977424306093, 7.670860738520322464 ) ) ;
#19820=VERTEX_POINT ( 'NONE', #16743 ) ;
#19822=CARTESIAN_POINT ( 'NONE',  ( 2.835023152515760980, -26.35730453524175942, 7.257242401810562349 ) ) ;
#19824=CARTESIAN_POINT ( 'NONE',  ( 4.718801410692444520, -27.79814376769215301, 7.651421919295145813 ) ) ;
#19826=CARTESIAN_POINT ( 'NONE',  ( 4.733915118986097958, -28.03444136281207832, 7.013842709614101167 ) ) ;
#19829=CARTESIAN_POINT ( 'NONE',  ( 0.9267304714826859469, -32.88073836111571779, 7.013842709614101167 ) ) ;
#19832=CARTESIAN_POINT ( 'NONE',  ( 4.404516770028685357, -31.79202354683301834, 7.686927408461905031 ) ) ;
#19833=VERTEX_POINT ( 'NONE', #726 ) ;
#19849=ORIENTED_EDGE ( 'NONE', *, *, #37936, .T. ) ;
#19854=CARTESIAN_POINT ( 'NONE',  ( 0.2535576206106768815, -26.37550602218658469, 7.501983001166817822 ) ) ;
#19855=CARTESIAN_POINT ( 'NONE',  ( -0.1539201161049026934, -32.53808085965915353, 7.754798119455333705 ) ) ;
#19856=DIRECTION ( 'NONE',  ( 1.047444401652940007E-14, -1.000000000000000000, -0.000000000000000000 ) ) ;
#19859=CARTESIAN_POINT ( 'NONE',  ( -1.015903543171244650, -31.77713404367212746, 6.875671892026059773 ) ) ;
#19862=CARTESIAN_POINT ( 'NONE',  ( 2.748053412748273860, -32.80449376584813592, 7.754798119455333705 ) ) ;
#19864=DIRECTION ( 'NONE',  ( -0.9396926207859005453, -0.3420201433256903067, 0.000000000000000000 ) ) ;
#19866=CARTESIAN_POINT ( 'NONE',  ( 2.225035496018605841, -33.03038495138792285, 6.865554069792297653 ) ) ;
#19876=CARTESIAN_POINT ( 'NONE',  ( 1.111970077971375481, -26.12859514599353972, 7.778495531946297170 ) ) ;
#19882=B_SPLINE_CURVE_WITH_KNOTS ( 'NONE', 3,
 ( #9530, #38139, #9745, #29090, #28478, #28687, #26004, #13233, #16318, #19623, #34689, #31992, #6465, #13032, #25799, #19017, #10134, #892, #31578, #38333, #32197, #9325, #3404, #15917, #285 ),
 .UNSPECIFIED., .F., .F.,
 ( 4, 3, 3, 3, 3, 3, 3, 3, 4 ),
 ( 6.468151674593778733E-05, 9.076621574722025119E-05, 0.0001210204262068008668, 0.0001512763324577457336, 0.0001815301820994240595, 0.0002117781465860724675, 0.0002420274594459785687, 0.0002722905548971212095, 0.0002816827545175671905 ),
 .UNSPECIFIED. ) ;
#19884=CARTESIAN_POINT ( 'NONE',  ( 2.294856720451861953, -26.12078399496891734, 7.635761828346576685 ) ) ;
#19886=CARTESIAN_POINT ( 'NONE',  ( 0.9084830412599044225, -32.97916797363021857, 6.925313231306333250 ) ) ;
#19888=ADVANCED_FACE ( 'NONE', ( #26877 ), #29759, .T. ) ;
#19891=CARTESIAN_POINT ( 'NONE',  ( 3.369155479471896530, -26.60763004909045293, 7.695279973900954751 ) ) ;
#19895=ADVANCED_FACE ( 'NONE', ( #16349 ), #28922, .F. ) ;
#19897=CARTESIAN_POINT ( 'NONE',  ( -0.6366397171544941891, -32.17424313428438865, 7.761113333116783863 ) ) ;
#19899=CARTESIAN_POINT ( 'NONE',  ( 4.713718104732327774, -27.78952162317270691, 7.710604733652627552 ) ) ;
#19903=CARTESIAN_POINT ( 'NONE',  ( 3.871457482660439986, -26.95335486619629606, 7.748216051605115950 ) ) ;
#19904=CARTESIAN_POINT ( 'NONE',  ( -0.8827178585826440660, -31.78071456810256734, 7.670860738520331346 ) ) ;
#19905=CYLINDRICAL_SURFACE ( 'NONE', #14021, 0.09010775117053081151 ) ;
#19909=CARTESIAN_POINT ( 'NONE',  ( 4.934953675687837382, -28.52226686387824373, 7.754798119455333705 ) ) ;
#19910=CYLINDRICAL_SURFACE ( 'NONE', #4976, 0.09010775117052882699 ) ;
#19919=CARTESIAN_POINT ( 'NONE',  ( -0.4362586782667852714, -26.79779526112715615, 6.875780273367529283 ) ) ;
#19930=ORIENTED_EDGE ( 'NONE', *, *, #27893, .T. ) ;
#19931=CIRCLE ( 'NONE', #6164, 3.499999999999999556 ) ;
#19932=EDGE_CURVE ( 'NONE', #22200, #33808, #2290, .T. ) ;
#19933=PLANE ( 'NONE',  #28556 ) ;
#19934=CARTESIAN_POINT ( 'NONE',  ( 4.534639009953071564, -31.44797187246948411, 6.939395833800439561 ) ) ;
#19936=CARTESIAN_POINT ( 'NONE',  ( 6.173121028034443292, -31.06824956420287975, 7.754798119455333705 ) ) ;
#19941=CARTESIAN_POINT ( 'NONE',  ( 1.700390093233090871, -29.56993018339339940, 7.750000000000000888 ) ) ;
#19945=CARTESIAN_POINT ( 'NONE',  ( 0.3691700977291238472, -32.69849508640032099, 6.887945620086118659 ) ) ;
#19948=( BOUNDED_CURVE ( )  B_SPLINE_CURVE ( 3, ( #24161, #30972, #17766, #1961 ),
 .UNSPECIFIED., .F., .T. ) 
 B_SPLINE_CURVE_WITH_KNOTS ( ( 4, 4 ),
 ( 1.381924640371167579, 1.574767692156076260 ),
 .UNSPECIFIED. ) 
 CURVE ( )  GEOMETRIC_REPRESENTATION_ITEM ( )  RATIONAL_B_SPLINE_CURVE ( ( 1.000000000000000000, 0.9969033633783032089, 0.9969033633783032089, 1.000000000000000000 ) ) 
 REPRESENTATION_ITEM ( '' )  );
#19956=FACE_OUTER_BOUND ( 'NONE', #14958, .T. ) ;
#19957=B_SPLINE_CURVE_WITH_KNOTS ( 'NONE', 3,
 ( #35130, #6907, #10389, #19464, #10180, #1155, #23158, #32037, #3844, #16361 ),
 .UNSPECIFIED., .F., .F.,
 ( 4, 3, 3, 4 ),
 ( 0.0002170292169044849180, 0.0002420761345915980437, 0.0002723302478207024254, 0.0002816811360866880226 ),
 .UNSPECIFIED. ) ;
#19958=CARTESIAN_POINT ( 'NONE',  ( 3.743426330989782169, -26.71972442647873081, 7.501983001166817822 ) ) ;
#19963=CARTESIAN_POINT ( 'NONE',  ( -1.146144745493847150, -27.71056485836612637, 7.013842709614101167 ) ) ;
#19965=VERTEX_POINT ( 'NONE', #15542 ) ;
#19967=CARTESIAN_POINT ( 'NONE',  ( -1.643700780054958566, -30.60291583957470607, 7.009310105710485850 ) ) ;
#19968=CARTESIAN_POINT ( 'NONE',  ( 2.187796539937281182, -33.03559314236433408, 7.754798119455333705 ) ) ;
#19973=( NAMED_UNIT ( * ) PLANE_ANGLE_UNIT ( ) SI_UNIT ( $, .RADIAN. ) );
#19976=ORIENTED_EDGE ( 'NONE', *, *, #29566, .T. ) ;
#19981=CARTESIAN_POINT ( 'NONE',  ( -1.319585150783705307, -31.33904616602695015, 7.743886751744247121 ) ) ;
#19982=VERTEX_POINT ( 'NONE', #40650 ) ;
#19984=CARTESIAN_POINT ( 'NONE',  ( 2.415456923980280557, -26.14375455631804712, 6.864673517077424236 ) ) ;
#19985=CARTESIAN_POINT ( 'NONE',  ( 4.407950444472939822, -27.37556883494658777, 7.785593909369613819 ) ) ;
#19986=CARTESIAN_POINT ( 'NONE',  ( 4.542910857356968535, -31.44822479237316415, 7.386948897581447682 ) ) ;
#19993=EDGE_CURVE ( 'NONE', #35883, #32059, #9474, .T. ) ;
#19999=CARTESIAN_POINT ( 'NONE',  ( 2.256618981523600631, -26.21573644513852841, 7.712764235869103757 ) ) ;
#20002=LINE ( 'NONE', #35673, #30085 ) ;
#20003=DIRECTION ( 'NONE',  ( -0.6427876096865328126, -0.7660444431189835646, -0.000000000000000000 ) ) ;
#20004=CARTESIAN_POINT ( 'NONE',  ( 3.939786388318850641, -26.88011527646091992, 7.635761828346575797 ) ) ;
#20007=CARTESIAN_POINT ( 'NONE',  ( 1.138852870224363656, -32.92323963771860207, 7.730758795053805699 ) ) ;
#20008=CARTESIAN_POINT ( 'NONE',  ( 4.708129185550455453, -31.35978672175994930, 6.880608371227951992 ) ) ;
#20009=CARTESIAN_POINT ( 'NONE',  ( -1.799554507848646789, -29.58965135258283041, 7.746913345081743785 ) ) ;
#20013=EDGE_LOOP ( 'NONE', ( #9803, #37290, #32457, #24919 ) ) ;
#20021=CARTESIAN_POINT ( 'NONE',  ( -1.494034067973715851, -31.01676265601582827, 7.501983001166817822 ) ) ;
#20022=CARTESIAN_POINT ( 'NONE',  ( -1.596034042910392747, -28.39366076309272202, 7.743886751744253338 ) ) ;
#20024=CARTESIAN_POINT ( 'NONE',  ( 0.4886831474300012412, -26.28636952045412301, 7.638132480492516585 ) ) ;
#20025=CARTESIAN_POINT ( 'NONE',  ( -1.465062676656003982, -28.32899958033718590, 6.870716933885663735 ) ) ;
#20026=CARTESIAN_POINT ( 'NONE',  ( 0.3427083762866449668, -32.79587364754041090, 7.010186378901971160 ) ) ;
#20027=CARTESIAN_POINT ( 'NONE',  ( 4.400537936023037666, -31.79685841314351080, 7.660770905198780234 ) ) ;
#20036=B_SPLINE_CURVE_WITH_KNOTS ( 'NONE', 3,
 ( #40122, #27567, #39503, #24474, #37031, #33977, #5752, #18291, #33147, #4931 ),
 .UNSPECIFIED., .F., .F.,
 ( 4, 3, 3, 4 ),
 ( 0.0002170292169044788736, 0.0002420761345915969052, 0.0002723302478206991186, 0.0002816811360866808668 ),
 .UNSPECIFIED. ) ;
#20038=CARTESIAN_POINT ( 'NONE',  ( -1.721192392427412843, -28.83312752697541015, 6.869019495930281494 ) ) ;
#20043=CARTESIAN_POINT ( 'NONE',  ( 6.366197675807956813, -31.52662935008911660, 6.894806418505347700 ) ) ;
#20051=ORIENTED_EDGE ( 'NONE', *, *, #27237, .T. ) ;
#20062=CARTESIAN_POINT ( 'NONE',  ( -2.995288454638185272, -28.68415433521490954, 7.013842709614101167 ) ) ;
#20076=CARTESIAN_POINT ( 'NONE',  ( 3.005752271882382587, -26.32336525051885090, 7.761113333116789192 ) ) ;
#20077=DIRECTION ( 'NONE',  ( 0.4999999999999927836, 0.8660254037844429265, 0.000000000000000000 ) ) ;
#20079=CARTESIAN_POINT ( 'NONE',  ( -1.749215324041719422, -28.97813421761779296, 7.638991368224663958 ) ) ;
#20089=CARTESIAN_POINT ( 'NONE',  ( 3.995286705358532586, -27.06125532609220485, 6.868387053540521592 ) ) ;
#20090=CYLINDRICAL_SURFACE ( 'NONE', #32757, 0.09010775117052950700 ) ;
#20092=VERTEX_POINT ( 'NONE', #12452 ) ;
#20096=CARTESIAN_POINT ( 'NONE',  ( -0.03065438358791758300, -26.64358689880297248, 7.695279973900954751 ) ) ;
#20099=CARTESIAN_POINT ( 'NONE',  ( -1.486040044270929616, -30.75597321790062821, 7.740055089680402567 ) ) ;
#20101=CARTESIAN_POINT ( 'NONE',  ( -1.281659060280029294, -27.76124872452957604, 7.782861076432732617 ) ) ;
#20102=CARTESIAN_POINT ( 'NONE',  ( -1.641531228027346412, -30.19567924397617631, 7.692469944509197965 ) ) ;
#20104=B_SPLINE_CURVE_WITH_KNOTS ( 'NONE', 3,
 ( #14203, #38507, #10308, #8020, #20182, #4555, #23484, #36051, #4745, #35851 ),
 .UNSPECIFIED., .F., .F.,
 ( 4, 3, 3, 4 ),
 ( 8.940560153363745023E-19, 3.025570593003372205E-05, 6.051145698343924614E-05, 6.468151674593483288E-05 ),
 .UNSPECIFIED. ) ;
#20107=CARTESIAN_POINT ( 'NONE',  ( 5.013900471082111565, -30.36275040796179425, 7.386948897581450346 ) ) ;
#20108=CARTESIAN_POINT ( 'NONE',  ( -1.003736583562490070, -27.34783681995376270, 7.695279973900954751 ) ) ;
#20115=EDGE_CURVE ( 'NONE', #486, #9636, #9738, .T. ) ;
#20116=CARTESIAN_POINT ( 'NONE',  ( 4.370230286903631800, -27.30675615745736806, 7.640616322432101981 ) ) ;
#20122=CARTESIAN_POINT ( 'NONE',  ( 5.628486912222185445, -26.20317660986373909, 7.695279973900954751 ) ) ;
#20123=EDGE_CURVE ( 'NONE', #31083, #28028, #10790, .T. ) ;
#20124=ORIENTED_EDGE ( 'NONE', *, *, #32336, .T. ) ;
#20125=EDGE_LOOP ( 'NONE', ( #34254, #29653, #3337, #29341, #37871 ) ) ;
#20131=CARTESIAN_POINT ( 'NONE',  ( -1.614537886288068158, -25.59834652758622653, 7.635761828346577573 ) ) ;
#20132=CARTESIAN_POINT ( 'NONE',  ( 0.02181676014757850252, -32.52668967079699769, 7.740055089680399902 ) ) ;
#20136=CARTESIAN_POINT ( 'NONE',  ( 0.04278369059588756074, -26.60137143983851615, 6.894806418505345924 ) ) ;
#20141=CARTESIAN_POINT ( 'NONE',  ( 5.122500503061667487, -30.26926087503160190, 7.776484688137387025 ) ) ;
#20142=AXIS2_PLACEMENT_3D ( 'NONE', #5161, #14606, #26786 ) ;
#20146=CARTESIAN_POINT ( 'NONE',  ( 0.3487507780706524674, -32.68971722127069768, 6.988553391373221402 ) ) ;
#20149=CARTESIAN_POINT ( 'NONE',  ( -0.5005001391084890061, -26.97838111740712463, 7.643333865083954848 ) ) ;
#20160=AXIS2_PLACEMENT_3D ( 'NONE', #14514, #27088, #1580 ) ;
#20161=CARTESIAN_POINT ( 'NONE',  ( -1.133858823486877165, -27.69188849431729693, 6.939395833800444002 ) ) ;
#20162=ORIENTED_EDGE ( 'NONE', *, *, #34538, .F. ) ;
#20166=EDGE_CURVE ( 'NONE', #7424, #20092, #17885, .T. ) ;
#20178=CARTESIAN_POINT ( 'NONE',  ( 1.700390093233090871, -29.56993018339339940, 7.750000000000000888 ) ) ;
#20182=CARTESIAN_POINT ( 'NONE',  ( -1.227373324201784355, -31.29857579714354898, 7.670860738520331346 ) ) ;
#20191=LINE ( 'NONE', #26583, #40668 ) ;
#20202=CARTESIAN_POINT ( 'NONE',  ( 0.6935492931484148471, -26.32241729325343016, 6.876076431790004939 ) ) ;
#20203=CARTESIAN_POINT ( 'NONE',  ( 0.05125347100749116230, -26.48280394670751647, 6.865482280155369210 ) ) ;
#20205=CARTESIAN_POINT ( 'NONE',  ( 1.060496565001608493, -32.90918720382173746, 7.785868773668302545 ) ) ;
#20206=DIRECTION ( 'NONE',  ( 1.000000000000000000, 0.000000000000000000, 0.000000000000000000 ) ) ;
#20209=CARTESIAN_POINT ( 'NONE',  ( -0.4654086415465331639, -32.19087087841436556, 7.652160403243379427 ) ) ;
#20212=B_SPLINE_CURVE_WITH_KNOTS ( 'NONE', 3,
 ( #29944, #38598, #27068, #21301, #20886, #30366, #11193, #15112, #37138, #8927, #21510, #37342, #3004, #21914, #22333, #16133, #25605, #40631, #34490, #13851, #22928, #4785, #7267, #10549, #20025, #38348, #32806, #33203, #17516, #36888, #39559 ),
 .UNSPECIFIED., .F., .F.,
 ( 4, 3, 3, 3, 3, 3, 3, 3, 3, 3, 4 ),
 ( 0.000000000000000000, 2.999644130997770587E-05, 6.002588995694883557E-05, 8.960886084588016163E-05, 0.0001190604700446482121, 0.0001489538463052730757, 0.0001796139255493973941, 0.0002109707048517075394, 0.0002426195318110314805, 0.0002740640997890032566, 0.0002849778069099877806 ),
 .UNSPECIFIED. ) ;
#20217=CARTESIAN_POINT ( 'NONE',  ( 3.072552236484260124, -26.35012101938563944, 6.980586498568965403 ) ) ;
#20222=CARTESIAN_POINT ( 'NONE',  ( 5.043330201822981529, -28.53322799357174588, 7.013842709614101167 ) ) ;
#20223=DIRECTION ( 'NONE',  ( -0.6834397476448853537, 0.000000000000000000, 0.7300069255418715208 ) ) ;
#20226=DIRECTION ( 'NONE',  ( 1.000000000000000000, 4.956352788505163465E-15, 0.000000000000000000 ) ) ;
#20227=ORIENTED_EDGE ( 'NONE', *, *, #14160, .F. ) ;
#20237=DIRECTION ( 'NONE',  ( 0.4999999999999980016, 0.8660254037844398178, -0.000000000000000000 ) ) ;
#20248=CARTESIAN_POINT ( 'NONE',  ( -0.9695225508750403565, -31.83301800158153227, 7.749999999999998224 ) ) ;
#20249=ORIENTED_EDGE ( 'NONE', *, *, #29961, .T. ) ;
#20252=CARTESIAN_POINT ( 'NONE',  ( 3.286904077270082603, -32.68970154976867803, 6.921725064902947366 ) ) ;
#20253=CARTESIAN_POINT ( 'NONE',  ( 5.110221463921440055, -30.35927082751544859, 6.989977667959444751 ) ) ;
#20255=CYLINDRICAL_SURFACE ( 'NONE', #31923, 0.09010775117052841066 ) ;
#20262=EDGE_CURVE ( 'NONE', #2057, #16321, #29213, .T. ) ;
#20267=CARTESIAN_POINT ( 'NONE',  ( 4.715819433959782536, -31.34677736058242559, 6.894806418505347700 ) ) ;
#20270=CARTESIAN_POINT ( 'NONE',  ( 2.315096682381391435, -32.91390549881585059, 7.740055089680399902 ) ) ;
#20272=CARTESIAN_POINT ( 'NONE',  ( 2.853712549240934315, -26.25820597416272051, 7.255881584735163869 ) ) ;
#20277=DIRECTION ( 'NONE',  ( 0.3754033771448366252, -0.6502177225477857592, -0.6605219282605403475 ) ) ;
#20281=CARTESIAN_POINT ( 'NONE',  ( 2.908949165453299734, -26.39197723079101010, 6.894806418505348589 ) ) ;
#20293=( BOUNDED_CURVE ( )  B_SPLINE_CURVE ( 3, ( #23884, #11524, #4965, #14823 ),
 .UNSPECIFIED., .F., .F. ) 
 B_SPLINE_CURVE_WITH_KNOTS ( ( 4, 4 ),
 ( 1.396263401595456477, 1.534781240595298524 ),
 .UNSPECIFIED. ) 
 CURVE ( )  GEOMETRIC_REPRESENTATION_ITEM ( )  RATIONAL_B_SPLINE_CURVE ( ( 1.000000000000000000, 0.9984017064007808528, 0.9984017064007808528, 1.000000000000000000 ) ) 
 REPRESENTATION_ITEM ( '' )  );
#20294=FACE_OUTER_BOUND ( 'NONE', #14297, .T. ) ;
#20295=DIRECTION ( 'NONE',  ( -0.000000000000000000, -0.000000000000000000, -1.000000000000000000 ) ) ;
#20296=CARTESIAN_POINT ( 'NONE',  ( -1.641525177248355227, -30.19571155489859393, 7.695279973900954751 ) ) ;
#20298=CARTESIAN_POINT ( 'NONE',  ( 4.441298539795110578, -27.39334439880510530, 6.863805608295729499 ) ) ;
#20301=CARTESIAN_POINT ( 'NONE',  ( 4.190466207346752903, -31.88499410171630188, 6.882085323592687764 ) ) ;
#20304=ORIENTED_EDGE ( 'NONE', *, *, #27883, .F. ) ;
#20309=CARTESIAN_POINT ( 'NONE',  ( 4.820177131110392921, -30.92156949855583292, 6.988553391373219625 ) ) ;
#20311=CARTESIAN_POINT ( 'NONE',  ( 4.369049338451901576, -27.30536447825076252, 7.643192810543822269 ) ) ;
#20312=CARTESIAN_POINT ( 'NONE',  ( 2.408393318269669514, -26.14704807759288840, 7.771081512783700518 ) ) ;
#20313=ORIENTED_EDGE ( 'NONE', *, *, #21544, .T. ) ;
#20319=ORIENTED_EDGE ( 'NONE', *, *, #21407, .T. ) ;
#20325=VERTEX_POINT ( 'NONE', #39799 ) ;
#20326=CARTESIAN_POINT ( 'NONE',  ( -0.02576358332172043811, -32.49916105256644983, 7.782167645815905033 ) ) ;
#20329=DIRECTION ( 'NONE',  ( -0.5000000000000039968, 0.8660254037844363761, -0.000000000000000000 ) ) ;
#20330=CARTESIAN_POINT ( 'NONE',  ( 4.657599813362783614, -31.24770399340489746, 7.652160403243380316 ) ) ;
#20331=EDGE_CURVE ( 'NONE', #3667, #11806, #18655, .T. ) ;
#20335=ORIENTED_EDGE ( 'NONE', *, *, #12467, .F. ) ;
#20340=VERTEX_POINT ( 'NONE', #40000 ) ;
#20344=DIRECTION ( 'NONE',  ( -0.000000000000000000, -0.000000000000000000, -1.000000000000000000 ) ) ;
#20349=CARTESIAN_POINT ( 'NONE',  ( 4.516786734692483485, -27.65257114232802493, 7.505001789837628223 ) ) ;
#20356=ORIENTED_EDGE ( 'NONE', *, *, #27216, .F. ) ;
#20359=CARTESIAN_POINT ( 'NONE',  ( -1.201486998515826743, -27.79817699957155597, 6.870716933885664623 ) ) ;
#20362=ORIENTED_EDGE ( 'NONE', *, *, #34488, .F. ) ;
#20364=CARTESIAN_POINT ( 'NONE',  ( -0.5265381365170317407, -32.27007802618333443, 7.660770905198784675 ) ) ;
#20367=ORIENTED_EDGE ( 'NONE', *, *, #14400, .T. ) ;
#20368=CARTESIAN_POINT ( 'NONE',  ( 5.140791489254627145, -28.92678305073006584, 7.695279973900954751 ) ) ;
#20376=LINE ( 'NONE', #1272, #545 ) ;
#20377=EDGE_CURVE ( 'NONE', #38144, #3709, #13929, .T. ) ;
#20380=VERTEX_POINT ( 'NONE', #2560 ) ;
#20397=CARTESIAN_POINT ( 'NONE',  ( 4.662690227536057996, -31.23869556963216354, 7.695279973900954751 ) ) ;
#20410=VERTEX_POINT ( 'NONE', #28463 ) ;
#20412=FACE_OUTER_BOUND ( 'NONE', #27163, .T. ) ;
#20414=CARTESIAN_POINT ( 'NONE',  ( 3.049102248865016129, -26.34022061302200868, 6.887547729233688187 ) ) ;
#20416=CARTESIAN_POINT ( 'NONE',  ( 1.686887486498432676, -33.27093018339341768, 7.635761828346577573 ) ) ;
#20417=CARTESIAN_POINT ( 'NONE',  ( 3.908224997449445848, -32.15555842136866005, 7.730758795053810140 ) ) ;
#20419=CARTESIAN_POINT ( 'NONE',  ( 5.050066951568335405, -28.55520611019255028, 6.951256099901589103 ) ) ;
#20420=CARTESIAN_POINT ( 'NONE',  ( 0.3240269795377119233, -32.78794596868797839, 6.955226052476382925 ) ) ;
#20421=CARTESIAN_POINT ( 'NONE',  ( 1.282397997787059651, -26.09497943095427175, 6.941203072598478130 ) ) ;
#20435=ADVANCED_FACE ( 'NONE', ( #26145 ), #7394, .T. ) ;
#20437=EDGE_CURVE ( 'NONE', #4122, #33687, #34817, .T. ) ;
#20445=LINE ( 'NONE', #1736, #6464 ) ;
#20454=DIRECTION ( 'NONE',  ( -0.9396926207859104263, 0.3420201433256631063, -0.000000000000000000 ) ) ;
#20456=CARTESIAN_POINT ( 'NONE',  ( 5.094875594170104272, -29.76361320768288365, 7.006423389747792108 ) ) ;
#20457=CARTESIAN_POINT ( 'NONE',  ( 1.794850636712705283, -26.07119012505348721, 6.863805608295729499 ) ) ;
#20458=CARTESIAN_POINT ( 'NONE',  ( 2.133537915284704045, -33.04303106982295901, 6.903112506833890549 ) ) ;
#20462=B_SPLINE_CURVE_WITH_KNOTS ( 'NONE', 3,
 ( #12350, #28194, #426, #15647, #23, #37458, #5776, #15849, #28619, #37867, #34619, #37260, #6393, #34411, #6184, #15435, #27787, #3130, #9671 ),
 .UNSPECIFIED., .F., .F.,
 ( 4, 3, 3, 3, 3, 3, 4 ),
 ( 0.000000000000000000, 2.546128104244751558E-05, 5.711050680484040440E-05, 8.113074941675670992E-05, 0.0001053129305727009795, 0.0001360598016347053458, 0.0001612931755701967431 ),
 .UNSPECIFIED. ) ;
#20463=ORIENTED_EDGE ( 'NONE', *, *, #36430, .T. ) ;
#20465=CIRCLE ( 'NONE', #23133, 3.499999999999999556 ) ;
#20466=CARTESIAN_POINT ( 'NONE',  ( 0.1793115737041967861, -26.52915394410386796, 6.988553391373222290 ) ) ;
#20467=CARTESIAN_POINT ( 'NONE',  ( 4.746899557684813864, -27.84691535960167030, 6.894806418505347700 ) ) ;
#20469=CARTESIAN_POINT ( 'NONE',  ( 0.2020707124235944507, -34.04266111819475782, 7.754798119455333705 ) ) ;
#20471=CARTESIAN_POINT ( 'NONE',  ( -1.749066892114814253, -28.97726900121085336, 7.637894019485643504 ) ) ;
#20473=ORIENTED_EDGE ( 'NONE', *, *, #3117, .T. ) ;
#20490=CARTESIAN_POINT ( 'NONE',  ( 1.501176615848605289, -32.96409121586394519, 6.997764925645181933 ) ) ;
#20496=CARTESIAN_POINT ( 'NONE',  ( 0.6832822253045948147, -26.22097430988279498, 6.931070083220555844 ) ) ;
#20502=CARTESIAN_POINT ( 'NONE',  ( 2.271049717768559351, -33.00993214001371712, 7.783750581861600182 ) ) ;
#20506=CARTESIAN_POINT ( 'NONE',  ( -1.386427062873444971, -31.21787257485771860, 7.761113333116786528 ) ) ;
#20507=B_SPLINE_CURVE_WITH_KNOTS ( 'NONE', 3,
 ( #3960, #6625, #19172, #29050, #18758, #453, #6823, #31738, #12580, #34644, #31536, #3552, #3360, #15877, #28434, #242, #19377, #16081, #28645, #12781, #25356, #12992, #38299, #29254, #4737, #7621, #35843, #16874, #29648, #26962, #23475 ),
 .UNSPECIFIED., .F., .F.,
 ( 4, 3, 3, 3, 3, 3, 3, 3, 3, 3, 4 ),
 ( 8.673617379884035472E-19, 2.999644130997489372E-05, 6.002588995694583369E-05, 8.960886084587896901E-05, 0.0001190604700446460436, 0.0001489538463052678444, 0.0001796139255493967978, 0.0002109707048517057775, 0.0002426195318110350042, 0.0002740640997890026061, 0.0002849778069099786191 ),
 .UNSPECIFIED. ) ;
#20508=CARTESIAN_POINT ( 'NONE',  ( -1.606535956885630778, -28.77983680501876051, 6.920489980334479263 ) ) ;
#20512=EDGE_LOOP ( 'NONE', ( #36621, #29423, #3754, #10066, #31749, #34549, #17463, #6913, #23661, #9913, #807, #22234, #21609, #39515, #37809, #39448, #30653, #21818, #3370, #18520, #30029, #8521, #32494, #15403, #10765, #7699, #9614, #1075, #32251, #36248, #32092, #15450, #37306, #26199, #32148, #40228, #36987, #21095, #30420, #4556, #6340, #13306, #31082, #39010, #16070, #9821, #23619, #25125, #27100, #4059, #27016, #40413, #29105, #29967, #30882, #26556, #11201, #9041, #13141 ) ) ;
#20513=ORIENTED_EDGE ( 'NONE', *, *, #1780, .F. ) ;
#20521=CARTESIAN_POINT ( 'NONE',  ( 4.747863368183087296, -27.87906903544868342, 7.785593909369613819 ) ) ;
#20524=CARTESIAN_POINT ( 'NONE',  ( 3.351130934865960587, -32.54231216990946507, 6.887041543973314361 ) ) ;
#20525=( BOUNDED_CURVE ( )  B_SPLINE_CURVE ( 3, ( #34894, #13036, #26009, #38540 ),
 .UNSPECIFIED., .F., .T. ) 
 B_SPLINE_CURVE_WITH_KNOTS ( ( 4, 4 ),
 ( 1.381924640371167801, 1.574767692156076482 ),
 .UNSPECIFIED. ) 
 CURVE ( )  GEOMETRIC_REPRESENTATION_ITEM ( )  RATIONAL_B_SPLINE_CURVE ( ( 1.000000000000000000, 0.9969033633783032089, 0.9969033633783032089, 1.000000000000000000 ) ) 
 REPRESENTATION_ITEM ( '' )  );
#20528=CARTESIAN_POINT ( 'NONE',  ( -1.218628611532051265, -27.82653379209746092, 7.785868773668303433 ) ) ;
#20531=ORIENTED_EDGE ( 'NONE', *, *, #19487, .T. ) ;
#20549=DIRECTION ( 'NONE',  ( 0.1736481776669127897, 0.9848077530122111289, 0.000000000000000000 ) ) ;
#20551=CARTESIAN_POINT ( 'NONE',  ( -0.5039490865542369802, -26.98131590518362088, 7.740055089680398126 ) ) ;
#20556=CARTESIAN_POINT ( 'NONE',  ( -1.174035473898453752, -27.75395182900487612, 6.865312560952603782 ) ) ;
#20560=CARTESIAN_POINT ( 'NONE',  ( -0.5300021044395021308, -32.26722227524986408, 7.651421919295148477 ) ) ;
#20564=CARTESIAN_POINT ( 'NONE',  ( 4.713340623123058570, -27.78888299018493058, 7.695279973900954751 ) ) ;
#20573=LINE ( 'NONE', #23864, #31420 ) ;
#20574=EDGE_CURVE ( 'NONE', #40124, #39495, #3401, .T. ) ;
#20579=CARTESIAN_POINT ( 'NONE',  ( -1.794389567730132695, -29.37881818594272687, 6.971170733404102648 ) ) ;
#20583=ORIENTED_EDGE ( 'NONE', *, *, #16662, .T. ) ;
#20584=DIRECTION ( 'NONE',  ( -1.000000000000000000, 0.000000000000000000, 0.000000000000000000 ) ) ;
#20588=CARTESIAN_POINT ( 'NONE',  ( 4.313599969017027469, -31.74504722509605159, 7.635761828346577573 ) ) ;
#20589=DIRECTION ( 'NONE',  ( -1.000000000000000000, 0.000000000000000000, 0.000000000000000000 ) ) ;
#20593=LINE ( 'NONE', #33178, #2397 ) ;
#20594=CYLINDRICAL_SURFACE ( 'NONE', #7731, 0.09010775117052938210 ) ;
#20596=CARTESIAN_POINT ( 'NONE',  ( 0.5857718112008674094, -26.35782306785393203, 6.892063359921932530 ) ) ;
#20597=AXIS2_PLACEMENT_3D ( 'NONE', #28934, #735, #16556 ) ;
#20601=CARTESIAN_POINT ( 'NONE',  ( 4.656309160454404683, -31.44410799460488448, 6.875780273367530171 ) ) ;
#20602=DIRECTION ( 'NONE',  ( -0.6427876096865328126, -0.7660444431189835646, -0.000000000000000000 ) ) ;
#20603=CARTESIAN_POINT ( 'NONE',  ( 1.574364539997139767, -33.06766052747819629, 7.750000000000000888 ) ) ;
#20607=DIRECTION ( 'NONE',  ( 0.8660254037844380415, 0.5000000000000009992, -0.000000000000000000 ) ) ;
#20610=B_SPLINE_CURVE_WITH_KNOTS ( 'NONE', 3,
 ( #20248, #1147, #3838, #6901, #35719, #13682, #38372, #26251, #10171, #10580, #22763, #3635, #16160, #35329, #23151, #28724, #7098, #19660, #7494 ),
 .UNSPECIFIED., .F., .F.,
 ( 4, 3, 3, 3, 3, 3, 4 ),
 ( 1.893477691975264912E-18, 2.546128104244556401E-05, 5.711050680483675877E-05, 8.113074941675210206E-05, 0.0001053129305726940135, 0.0001360598016346985153, 0.0001612931755713739156 ),
 .UNSPECIFIED. ) ;
#20611=CARTESIAN_POINT ( 'NONE',  ( -0.6444488087166562185, -32.16833941288422238, 7.750000000000000888 ) ) ;
#20612=VERTEX_POINT ( 'NONE', #23830 ) ;
#20614=CARTESIAN_POINT ( 'NONE',  ( 2.259918937511053105, -26.20908457450270745, 7.257242401810562349 ) ) ;
#20616=CARTESIAN_POINT ( 'NONE',  ( 0.9874470777302929436, -32.89435814851245254, 6.863904403958575706 ) ) ;
#20621=EDGE_CURVE ( 'NONE', #22624, #32358, #37755, .T. ) ;
#20624=EDGE_CURVE ( 'NONE', #31321, #35289, #22379, .T. ) ;
#20630=CARTESIAN_POINT ( 'NONE',  ( 2.265556469525966232, -26.21722959230298144, 7.652160403243383868 ) ) ;
#20635=CARTESIAN_POINT ( 'NONE',  ( -0.9271279775035500270, -27.41211907304282036, 7.695279973900954751 ) ) ;
#20636=ADVANCED_FACE ( 'NONE', ( #35819 ), #33339, .T. ) ;
#20638=B_SPLINE_CURVE_WITH_KNOTS ( 'NONE', 3,
 ( #5112, #8593, #18264, #37008, #2043, #2243, #8790, #39683, #40095, #5318 ),
 .UNSPECIFIED., .F., .F.,
 ( 4, 3, 3, 4 ),
 ( 0.0002170292169044841320, 0.0002420761345916009981, 0.0002723302478207072501, 0.0002816811360866829810 ),
 .UNSPECIFIED. ) ;
#20640=CARTESIAN_POINT ( 'NONE',  ( 3.485436849364648815, -26.67619661698708100, 7.774064877406524410 ) ) ;
#20644=CARTESIAN_POINT ( 'NONE',  ( -1.774127509761148858, -29.99150749123047532, 6.980586498568968956 ) ) ;
#20650=VERTEX_POINT ( 'NONE', #4714 ) ;
#20652=CARTESIAN_POINT ( 'NONE',  ( 5.173052788776492328, -29.13333318653474890, 7.009310105710487626 ) ) ;
#20656=CARTESIAN_POINT ( 'NONE',  ( 0.3896649785617538608, -32.81498557016907114, 7.754798119455333705 ) ) ;
#20657=CARTESIAN_POINT ( 'NONE',  ( -1.096489673827657274, -31.67408406764383955, 6.921725064902951807 ) ) ;
#20658=CARTESIAN_POINT ( 'NONE',  ( 5.001045691774267610, -30.73426600737448311, 7.678495282201405203 ) ) ;
#20659=CARTESIAN_POINT ( 'NONE',  ( 2.793730807323614229, -32.78935575605969888, 6.874555630061442990 ) ) ;
#20660=CARTESIAN_POINT ( 'NONE',  ( 2.875937710231030398, -32.76024173560432473, 7.635761828346577573 ) ) ;
#20661=EDGE_CURVE ( 'NONE', #422, #28877, #3904, .T. ) ;
#20667=EDGE_LOOP ( 'NONE', ( #14495, #28234, #37624, #6223, #21808 ) ) ;
#20669=CARTESIAN_POINT ( 'NONE',  ( 0.1760639294348596007, -26.53077541110940629, 6.911401339314955372 ) ) ;
#20670=CARTESIAN_POINT ( 'NONE',  ( 3.016566341302053811, -26.43500618872311492, 6.876076431790005827 ) ) ;
#20672=CARTESIAN_POINT ( 'NONE',  ( -0.8789792430839086235, -27.20414525822329566, 6.880828092187095457 ) ) ;
#20675=EDGE_CURVE ( 'NONE', #31321, #6597, #26742, .T. ) ;
#20676=DIRECTION ( 'NONE',  ( 1.000000000000000000, 0.000000000000000000, 0.000000000000000000 ) ) ;
#20677=CARTESIAN_POINT ( 'NONE',  ( -1.752215393550915268, -28.99588619853886229, 7.674970859709603133 ) ) ;
#20683=CARTESIAN_POINT ( 'NONE',  ( 0.5324193565422453700, -26.37682618861159511, 7.763628509615287498 ) ) ;
#20684=VECTOR ( 'NONE', #10726, 1000.000000000000114 ) ;
#20695=VECTOR ( 'NONE', #32162, 1000.000000000000114 ) ;
#20698=CARTESIAN_POINT ( 'NONE',  ( 1.496541690888591569, -32.96381487152982004, 6.920489980334477487 ) ) ;
#20699=CARTESIAN_POINT ( 'NONE',  ( 2.495801789269033399, -26.26427930321180071, 6.939395833800443114 ) ) ;
#20701=CARTESIAN_POINT ( 'NONE',  ( -1.521215565022806082, -30.65682612155753262, 7.782034975670475418 ) ) ;
#20707=CARTESIAN_POINT ( 'NONE',  ( -1.751698146652124866, -30.14706689514045479, 6.894806418505347700 ) ) ;
#20716=ADVANCED_FACE ( 'NONE', ( #18473 ), #15601, .F. ) ;
#20720=CARTESIAN_POINT ( 'NONE',  ( 2.333682990176194849, -26.13904351153081507, 7.781480525794718162 ) ) ;
#20722=CARTESIAN_POINT ( 'NONE',  ( -0.1483345642761195737, -26.70808950415996463, 7.139196562012273262 ) ) ;
#20728=CARTESIAN_POINT ( 'NONE',  ( -1.553388381126008744, -28.28034428687672985, 6.863654226668488789 ) ) ;
#20731=CARTESIAN_POINT ( 'NONE',  ( -0.8016911122223995267, -27.26782569596947070, 6.871394612369936539 ) ) ;
#20732=EDGE_LOOP ( 'NONE', ( #31001, #29325, #24634, #31122, #6359 ) ) ;
#20738=DIRECTION ( 'NONE',  ( -1.000000000000000000, 0.000000000000000000, 0.000000000000000000 ) ) ;
#20740=VERTEX_POINT ( 'NONE', #9006 ) ;
#20741=CARTESIAN_POINT ( 'NONE',  ( 2.474049714983521664, -26.15650803111381606, 7.013842709614101167 ) ) ;
#20742=AXIS2_PLACEMENT_3D ( 'NONE', #11472, #8598, #39688 ) ;
#20750=CARTESIAN_POINT ( 'NONE',  ( 5.123750824668761972, -30.29724448404768111, 7.754798119455333705 ) ) ;
#20752=CARTESIAN_POINT ( 'NONE',  ( -0.1576164094376339420, -32.53604074034053895, 7.750000000000000888 ) ) ;
#20757=DIRECTION ( 'NONE',  ( -0.6662082868431848937, 0.000000000000000000, 0.7457657263118685487 ) ) ;
#20760=ORIENTED_EDGE ( 'NONE', *, *, #23859, .T. ) ;
#20762=CARTESIAN_POINT ( 'NONE',  ( -1.142394782723454405, -27.70483658010354588, 6.903372536218457256 ) ) ;
#20764=VERTEX_POINT ( 'NONE', #40297 ) ;
#20766=CARTESIAN_POINT ( 'NONE',  ( -1.638124420012986970, -30.62083709180146940, 6.880828092187095457 ) ) ;
#20769=EDGE_CURVE ( 'NONE', #19421, #11999, #18061, .T. ) ;
#20770=ORIENTED_EDGE ( 'NONE', *, *, #38625, .T. ) ;
#20771=CARTESIAN_POINT ( 'NONE',  ( 0.7553917981025534134, -32.94700704774471944, 7.501983001166816933 ) ) ;
#20777=FACE_OUTER_BOUND ( 'NONE', #16981, .T. ) ;
#20779=( BOUNDED_CURVE ( )  B_SPLINE_CURVE ( 3, ( #30393, #11220, #27290, #17395 ),
 .UNSPECIFIED., .F., .T. ) 
 B_SPLINE_CURVE_WITH_KNOTS ( ( 4, 4 ),
 ( 4.748221474220559735, 4.941946782021394036 ),
 .UNSPECIFIED. ) 
 CURVE ( )  GEOMETRIC_REPRESENTATION_ITEM ( )  RATIONAL_B_SPLINE_CURVE ( ( 1.000000000000000000, 0.9968749865767494445, 0.9968749865767494445, 1.000000000000000000 ) ) 
 REPRESENTATION_ITEM ( '' )  );
#20783=CARTESIAN_POINT ( 'NONE',  ( 4.822514058981756335, -27.98804819767207874, 6.971170733404099096 ) ) ;
#20784=VERTEX_POINT ( 'NONE', #14985 ) ;
#20787=CARTESIAN_POINT ( 'NONE',  ( 0.07492370758569941169, -33.99638339305766266, 7.635761828346577573 ) ) ;
#20789=CARTESIAN_POINT ( 'NONE',  ( 0.002871653215719630579, -26.62401247480054067, 7.769368695748484654 ) ) ;
#20791=CARTESIAN_POINT ( 'NONE',  ( -1.795161916675976466, -29.39339987696827805, 6.903112506833889661 ) ) ;
#20808=CARTESIAN_POINT ( 'NONE',  ( 4.631036947150836802, -31.48338494934807485, 6.941203072598471024 ) ) ;
#20821=ORIENTED_EDGE ( 'NONE', *, *, #4310, .F. ) ;
#20822=CARTESIAN_POINT ( 'NONE',  ( -0.4809337148280844465, -32.17797450963541195, 7.763628509615282169 ) ) ;
#20828=EDGE_CURVE ( 'NONE', #12896, #15980, #37414, .T. ) ;
#20830=VERTEX_POINT ( 'NONE', #9210 ) ;
#20835=CARTESIAN_POINT ( 'NONE',  ( -0.1589752317941719728, -32.41646502212034875, 7.013842709614101167 ) ) ;
#20836=VERTEX_POINT ( 'NONE', #6138 ) ;
#20846=CARTESIAN_POINT ( 'NONE',  ( -0.8516922296151283600, -27.32338581145017997, 7.782034975670478971 ) ) ;
#20860=EDGE_LOOP ( 'NONE', ( #6081, #31996, #1059, #21247, #9962 ) ) ;
#20862=CARTESIAN_POINT ( 'NONE',  ( 5.157792374610187913, -29.02545772698320903, 6.870737987065013819 ) ) ;
#20865=CARTESIAN_POINT ( 'NONE',  ( 3.378163903244623345, -26.61272046326372376, 7.652160403243390974 ) ) ;
#20869=CARTESIAN_POINT ( 'NONE',  ( 2.679370002084180857, -32.82594665571590298, 7.006423389747790331 ) ) ;
#20870=CARTESIAN_POINT ( 'NONE',  ( 5.099605094774092073, -29.64363437814743207, 6.874555630061440326 ) ) ;
#20878=AXIS2_PLACEMENT_3D ( 'NONE', #6039, #18574, #2977 ) ;
#20883=DIRECTION ( 'NONE',  ( 0.000000000000000000, 0.7541618601367583441, 0.6566885781822799917 ) ) ;
#20885=CARTESIAN_POINT ( 'NONE',  ( 3.057737949672496125, -26.45262135935053749, 6.939395833800443114 ) ) ;
#20886=CARTESIAN_POINT ( 'NONE',  ( -1.417849890998097440, -28.21472003549629903, 6.979335674598003969 ) ) ;
#20887=LINE ( 'NONE', #14693, #37273 ) ;
#20897=EDGE_CURVE ( 'NONE', #25596, #19681, #35322, .T. ) ;
#20899=DIRECTION ( 'NONE',  ( 0.3420201433256578882, 0.9396926207859123137, 0.000000000000000000 ) ) ;
#20904=CIRCLE ( 'NONE', #24171, 3.499999999999999556 ) ;
#20910=CARTESIAN_POINT ( 'NONE',  ( 2.475127768148066565, -26.25936912986495386, 6.895222827070022653 ) ) ;
#20911=CARTESIAN_POINT ( 'NONE',  ( -1.740571384909186170, -30.12451254141716106, 7.785344483711591934 ) ) ;
#20914=CARTESIAN_POINT ( 'NONE',  ( 0.6674044370517944191, -26.22583931010534641, 7.009310105710485850 ) ) ;
#20916=EDGE_CURVE ( 'NONE', #14526, #27830, #18584, .T. ) ;
#20918=CARTESIAN_POINT ( 'NONE',  ( 4.490574598675256546, -27.45690618315335030, 7.006908160621416748 ) ) ;
#20926=DIRECTION ( 'NONE',  ( -0.9396926207858983249, -0.3420201433256965240, 0.000000000000000000 ) ) ;
#20927=CARTESIAN_POINT ( 'NONE',  ( -0.1040043641139408170, -32.45162424111279620, 7.754798119455333705 ) ) ;
#20928=CARTESIAN_POINT ( 'NONE',  ( 4.832094736013836211, -30.89372247464815757, 6.882085323592682435 ) ) ;
#20929=DIRECTION ( 'NONE',  ( 0.7660444431189840087, -0.6427876096865322575, 0.000000000000000000 ) ) ;
#20932=CARTESIAN_POINT ( 'NONE',  ( -0.6913368354159359352, -32.12524937216382170, 6.931070083220554956 ) ) ;
#20936=ORIENTED_EDGE ( 'NONE', *, *, #20661, .T. ) ;
#20938=CARTESIAN_POINT ( 'NONE',  ( -1.518426245678387021, -28.19544030114832012, 6.935328752148349984 ) ) ;
#20952=( BOUNDED_CURVE ( )  B_SPLINE_CURVE ( 3, ( #29756, #15896, #37701, #12603 ),
 .UNSPECIFIED., .F., .T. ) 
 B_SPLINE_CURVE_WITH_KNOTS ( ( 4, 4 ),
 ( 4.708531083176469068, 4.895802057644189631 ),
 .UNSPECIFIED. ) 
 CURVE ( )  GEOMETRIC_REPRESENTATION_ITEM ( )  RATIONAL_B_SPLINE_CURVE ( ( 1.000000000000000000, 0.9970795998553221295, 0.9970795998553221295, 1.000000000000000000 ) ) 
 REPRESENTATION_ITEM ( '' )  );
#20954=EDGE_LOOP ( 'NONE', ( #19218, #33591, #10785, #24689, #7197, #38168, #155, #34779, #17279, #16396, #35473, #38386, #18301, #35021, #39179, #39000, #35564, #22432, #30055, #20463, #29229, #38810, #22020, #35402, #35553, #24467, #17180, #22692, #33340, #4877, #7295, #1055, #2964, #18201, #32400, #34084, #894, #36996, #1419, #40135, #33192, #36783, #23669, #38759, #2935, #3083, #22459, #31645, #32451, #28902, #31520, #28394, #40712, #27084, #21587, #25813, #12243, #35400, #17321, #4300, #9342, #17533, #31315, #3001, #11762, #35151, #25022, #18333, #25952, #12003, #10813, #27607, #6328, #33510, #34959, #11011, #22676, #37842, #12985, #32198, #2650, #28085, #22240, #16381, #569, #4200, #13012, #6467, #31673, #21321, #27524, #25199, #9184, #24048, #33820, #23854, #37335, #38368, #21007, #23656, #35052, #32203, #3459, #15546, #30311, #21234, #21761, #13091, #27991, #21447, #31449 ) ) ;
#20961=CARTESIAN_POINT ( 'NONE',  ( 1.060084769145667405, -32.99765172409238545, 7.783750581861601070 ) ) ;
#20965=CARTESIAN_POINT ( 'NONE',  ( 2.780913079066563487, -32.89888420713570838, 7.753200566781599079 ) ) ;
#20966=ORIENTED_EDGE ( 'NONE', *, *, #29248, .T. ) ;
#20968=FACE_OUTER_BOUND ( 'NONE', #27349, .T. ) ;
#20974=CARTESIAN_POINT ( 'NONE',  ( 3.960473582032317363, -32.24238647371081612, 7.635761828346576685 ) ) ;
#20976=CARTESIAN_POINT ( 'NONE',  ( 2.787276362915718231, -32.89601384403606943, 7.761113333116785640 ) ) ;
#20979=ORIENTED_EDGE ( 'NONE', *, *, #31861, .T. ) ;
#20990=CARTESIAN_POINT ( 'NONE',  ( 4.662690227536057996, -31.23869556963216354, 7.695279973900954751 ) ) ;
#21001=CARTESIAN_POINT ( 'NONE',  ( 4.742907322181076246, -28.05233206275141811, 6.979335674598003969 ) ) ;
#21003=CARTESIAN_POINT ( 'NONE',  ( -0.02095206919630761971, -26.63786329112441820, 7.740055089680397238 ) ) ;
#21007=ORIENTED_EDGE ( 'NONE', *, *, #13033, .T. ) ;
#21010=CARTESIAN_POINT ( 'NONE',  ( 0.5134882369223120469, -26.38382311207955411, 7.652160403243385645 ) ) ;
#21011=DIRECTION ( 'NONE',  ( -0.000000000000000000, -0.000000000000000000, -1.000000000000000000 ) ) ;
#21014=ORIENTED_EDGE ( 'NONE', *, *, #35802, .T. ) ;
#21022=ADVANCED_FACE ( 'NONE', ( #20294 ), #7545, .F. ) ;
#21023=DIRECTION ( 'NONE',  ( -0.1736481776669206722, -0.9848077530122096857, -0.000000000000000000 ) ) ;
#21026=CARTESIAN_POINT ( 'NONE',  ( 0.01496732657086547076, -26.50244713504975635, 6.867280401193706751 ) ) ;
#21029=CARTESIAN_POINT ( 'NONE',  ( 6.112940767310136359, -27.90626689514689218, 7.695279973900954751 ) ) ;
#21030=CARTESIAN_POINT ( 'NONE',  ( 4.651387254527720394, -31.45187073487890217, 6.880828092187094569 ) ) ;
#21034=DIRECTION ( 'NONE',  ( 0.8660254037844380415, 0.5000000000000009992, -0.000000000000000000 ) ) ;
#21035=EDGE_LOOP ( 'NONE', ( #9490, #6149, #37791, #18293, #40572 ) ) ;
#21037=( BOUNDED_CURVE ( )  B_SPLINE_CURVE ( 3, ( #6711, #38583, #29539, #542 ),
 .UNSPECIFIED., .F., .T. ) 
 B_SPLINE_CURVE_WITH_KNOTS ( ( 4, 4 ),
 ( 1.347909859412854239, 1.534781240595298968 ),
 .UNSPECIFIED. ) 
 CURVE ( )  GEOMETRIC_REPRESENTATION_ITEM ( )  RATIONAL_B_SPLINE_CURVE ( ( 1.000000000000000000, 0.9970920404276226723, 0.9970920404276226723, 1.000000000000000000 ) ) 
 REPRESENTATION_ITEM ( '' )  );
#21040=CARTESIAN_POINT ( 'NONE',  ( -0.6434037460695107846, -32.16928249125778194, 7.751599049952175413 ) ) ;
#21041=EDGE_LOOP ( 'NONE', ( #28693, #37071, #12680, #10000, #5999 ) ) ;
#21042=CARTESIAN_POINT ( 'NONE',  ( -0.5155868758681084740, -32.14860049917209750, 7.784838882742138644 ) ) ;
#21044=CARTESIAN_POINT ( 'NONE',  ( 3.847093746412449722, -32.20655010317304345, 7.785868773668303433 ) ) ;
#21049=CARTESIAN_POINT ( 'NONE',  ( 2.817328913877361618, -32.78123018042540338, 6.894806418505346812 ) ) ;
#21055=CARTESIAN_POINT ( 'NONE',  ( -0.04165398999324298329, -32.48973880933039737, 6.894806418505347700 ) ) ;
#21063=ADVANCED_BREP_SHAPE_REPRESENTATION ( '', ( #12876, #30744 ), #18883 ) ;
#21066=CARTESIAN_POINT ( 'NONE',  ( 3.410047845041411563, -26.63102917700635430, 7.775108481317166031 ) ) ;
#21069=CARTESIAN_POINT ( 'NONE',  ( -1.769892952498073768, -30.02514449314797673, 6.880828092187097234 ) ) ;
#21076=CARTESIAN_POINT ( 'NONE',  ( -1.060034464505671403, -31.72168673584834053, 7.750000000000000888 ) ) ;
#21077=AXIS2_PLACEMENT_3D ( 'NONE', #35726, #1156, #10982 ) ;
#21078=EDGE_CURVE ( 'NONE', #17881, #5880, #39229, .T. ) ;
#21081=CARTESIAN_POINT ( 'NONE',  ( 3.391251241177835940, -32.61740345834337518, 7.785593909369613819 ) ) ;
#21082=CARTESIAN_POINT ( 'NONE',  ( 0.9689046511080217083, -32.99263803653528271, 7.750000000000000888 ) ) ;
#21085=CARTESIAN_POINT ( 'NONE',  ( 2.670334759559959803, -32.82864271202553397, 6.988553391373221402 ) ) ;
#21086=CARTESIAN_POINT ( 'NONE',  ( 4.626750114682200987, -27.83891399941946077, 7.692469944509199742 ) ) ;
#21087=CARTESIAN_POINT ( 'NONE',  ( 4.888877264403690859, -28.38944318249906118, 7.748216051605119503 ) ) ;
#21095=ORIENTED_EDGE ( 'NONE', *, *, #37936, .F. ) ;
#21097=CARTESIAN_POINT ( 'NONE',  ( 0.1859022642979256124, -26.52586597056204099, 6.949473656533218247 ) ) ;
#21101=CARTESIAN_POINT ( 'NONE',  ( 1.318368334477774573, -26.19146016107992025, 6.949473656533216470 ) ) ;
#21102=EDGE_CURVE ( 'NONE', #26823, #19049, #17599, .T. ) ;
#21118=EDGE_LOOP ( 'NONE', ( #17467, #27764, #12115, #38490 ) ) ;
#21124=CARTESIAN_POINT ( 'NONE',  ( -0.1779045157466759008, -32.41245094751727862, 7.386948897581450346 ) ) ;
#21125=CARTESIAN_POINT ( 'NONE',  ( 2.403116422957143783, -26.24334398948340663, 6.864276522220859711 ) ) ;
#21126=CARTESIAN_POINT ( 'NONE',  ( -1.746590121550728236, -30.10122404981289534, 7.782861076432730840 ) ) ;
#21128=CARTESIAN_POINT ( 'NONE',  ( -1.391746016950013320, -31.20965402480746320, 7.750000000000000888 ) ) ;
#21129=CARTESIAN_POINT ( 'NONE',  ( 0.6641905360584041684, -26.22683424134941177, 6.895394898881668233 ) ) ;
#21130=CARTESIAN_POINT ( 'NONE',  ( -0.4067295501017070269, -32.37312860990524399, 7.139344958878410807 ) ) ;
#21136=ORIENTED_EDGE ( 'NONE', *, *, #23953, .T. ) ;
#21145=CARTESIAN_POINT ( 'NONE',  ( -0.6518040451976112593, -32.16169936346016556, 6.870724624169667116 ) ) ;
#21152=CARTESIAN_POINT ( 'NONE',  ( 4.932354078450567059, -25.52873147056503811, 7.754798119455333705 ) ) ;
#21155=VERTEX_POINT ( 'NONE', #7942 ) ;
#21160=CARTESIAN_POINT ( 'NONE',  ( 4.970031525767722336, -30.81870754651817990, 6.875671892026065102 ) ) ;
#21161=CARTESIAN_POINT ( 'NONE',  ( 1.700390093233090871, -29.56993018339339940, 7.800000000000000711 ) ) ;
#21164=CARTESIAN_POINT ( 'NONE',  ( -1.584315626793068921, -30.77853884495590719, 7.756742906098588186 ) ) ;
#21167=CARTESIAN_POINT ( 'NONE',  ( -1.797390937478270612, -29.44531139368447725, 7.751599049952198506 ) ) ;
#21170=EDGE_CURVE ( 'NONE', #27620, #36238, #22036, .T. ) ;
#21177=CARTESIAN_POINT ( 'NONE',  ( 4.079964913973585183, -27.00329292675143478, 7.009310105710486738 ) ) ;
#21181=CARTESIAN_POINT ( 'NONE',  ( -0.4618072112497045301, -26.94602034948383107, 7.782167645815904145 ) ) ;
#21182=ORIENTED_EDGE ( 'NONE', *, *, #14061, .T. ) ;
#21183=CARTESIAN_POINT ( 'NONE',  ( 2.844063789200206749, -32.86231350904720472, 7.785344483711591934 ) ) ;
#21194=VERTEX_POINT ( 'NONE', #24201 ) ;
#21198=CARTESIAN_POINT ( 'NONE',  ( 0.03112795225476835265, -32.53195046136271174, 7.680992449362118890 ) ) ;
#21204=ORIENTED_EDGE ( 'NONE', *, *, #22298, .T. ) ;
#21217=VERTEX_POINT ( 'NONE', #9363 ) ;
#21222=LINE ( 'NONE', #14613, #21451 ) ;
#21229=( LENGTH_UNIT ( ) NAMED_UNIT ( * ) SI_UNIT ( .MILLI., .METRE. ) );
#21230=CARTESIAN_POINT ( 'NONE',  ( 5.197197318687171830, -29.57030403941794461, 7.767581361668585593 ) ) ;
#21234=ORIENTED_EDGE ( 'NONE', *, *, #22574, .T. ) ;
#21239=FACE_OUTER_BOUND ( 'NONE', #3923, .T. ) ;
#21247=ORIENTED_EDGE ( 'NONE', *, *, #30090, .T. ) ;
#21250=PLANE ( 'NONE',  #9393 ) ;
#21251=ORIENTED_EDGE ( 'NONE', *, *, #18544, .T. ) ;
#21253=EDGE_CURVE ( 'NONE', #33252, #40099, #15959, .T. ) ;
#21256=EDGE_CURVE ( 'NONE', #6532, #27165, #13713, .T. ) ;
#21261=CARTESIAN_POINT ( 'NONE',  ( 2.270926882672761771, -26.21813482148259311, 7.643333865083956624 ) ) ;
#21265=CIRCLE ( 'NONE', #31798, 3.499999999999999556 ) ;
#21267=VECTOR ( 'NONE', #38764, 1000.000000000000000 ) ;
#21269=FACE_OUTER_BOUND ( 'NONE', #14925, .T. ) ;
#21273=CARTESIAN_POINT ( 'NONE',  ( -1.774560659206035451, -29.98792227883944150, 6.941203072598477242 ) ) ;
#21275=CARTESIAN_POINT ( 'NONE',  ( 1.555264031125473068, -33.06692009274359378, 6.875780273367531947 ) ) ;
#21278=CARTESIAN_POINT ( 'NONE',  ( 4.998126050557230471, -30.74251124864294837, 7.737115613922533441 ) ) ;
#21279=CARTESIAN_POINT ( 'NONE',  ( 5.198144250753316875, -29.69314003934108470, 7.753200566781576875 ) ) ;
#21282=DIRECTION ( 'NONE',  ( -0.5000000000000039968, 0.8660254037844363761, -0.000000000000000000 ) ) ;
#21283=CARTESIAN_POINT ( 'NONE',  ( 5.200344093257736056, -29.59065050415977538, 6.906385212079477753 ) ) ;
#21285=( BOUNDED_CURVE ( )  B_SPLINE_CURVE ( 3, ( #40548, #15038, #12360, #39956 ),
 .UNSPECIFIED., .F., .T. ) 
 B_SPLINE_CURVE_WITH_KNOTS ( ( 4, 4 ),
 ( 1.396263401595456699, 1.574767692156075594 ),
 .UNSPECIFIED. ) 
 CURVE ( )  GEOMETRIC_REPRESENTATION_ITEM ( )  RATIONAL_B_SPLINE_CURVE ( ( 1.000000000000000000, 0.9973464470609390009, 0.9973464470609390009, 1.000000000000000000 ) ) 
 REPRESENTATION_ITEM ( '' )  );
#21286=DIRECTION ( 'NONE',  ( 0.3420201433256790380, -0.9396926207859046531, -0.000000000000000000 ) ) ;
#21301=CARTESIAN_POINT ( 'NONE',  ( -1.419396944644200298, -28.21829086823094102, 6.988553391373221402 ) ) ;
#21303=CARTESIAN_POINT ( 'NONE',  ( 1.317243270070298511, -26.19158756650236342, 6.969307238440505259 ) ) ;
#21304=CARTESIAN_POINT ( 'NONE',  ( 2.170460981197068762, -32.93727830324805694, 7.754798119455333705 ) ) ;
#21310=EDGE_CURVE ( 'NONE', #12509, #14835, #14629, .T. ) ;
#21311=VECTOR ( 'NONE', #1764, 1000.000000000000227 ) ;
#21318=CARTESIAN_POINT ( 'NONE',  ( -1.389564992689783951, -31.21326896663422090, 7.754798119455333705 ) ) ;
#21321=ORIENTED_EDGE ( 'NONE', *, *, #5799, .T. ) ;
#21324=CARTESIAN_POINT ( 'NONE',  ( 5.039926880157825195, -30.20828278875847062, 6.894806418505346812 ) ) ;
#21334=DIRECTION ( 'NONE',  ( -0.7660444431189761261, -0.6427876096865416944, 0.000000000000000000 ) ) ;
#21337=CARTESIAN_POINT ( 'NONE',  ( 1.128064129311358244, -33.02281926226938680, 7.695279973900954751 ) ) ;
#21358=CARTESIAN_POINT ( 'NONE',  ( -1.528267587133116612, -28.21871976935260662, 6.890920332093122269 ) ) ;
#21362=ORIENTED_EDGE ( 'NONE', *, *, #33535, .F. ) ;
#21364=CARTESIAN_POINT ( 'NONE',  ( -1.799609906766908685, -29.56993018339339940, 7.202408869016148074 ) ) ;
#21366=FACE_OUTER_BOUND ( 'NONE', #10489, .T. ) ;
#21369=EDGE_LOOP ( 'NONE', ( #14140, #31381, #1254, #7408 ) ) ;
#21371=CARTESIAN_POINT ( 'NONE',  ( 2.896981936218417264, -32.75240845689362601, 7.695279973900954751 ) ) ;
#21378=CARTESIAN_POINT ( 'NONE',  ( 3.533038598990357215, -26.70610496455467953, 6.871394612369934762 ) ) ;
#21380=VERTEX_POINT ( 'NONE', #30350 ) ;
#21388=CARTESIAN_POINT ( 'NONE',  ( 1.845837775478998077, -26.17304264157967708, 6.868387053540520704 ) ) ;
#21390=CARTESIAN_POINT ( 'NONE',  ( 2.877452244276258231, -32.85680554558438615, 7.778495531946297170 ) ) ;
#21391=EDGE_CURVE ( 'NONE', #28028, #20325, #35821, .T. ) ;
#21397=( BOUNDED_CURVE ( )  B_SPLINE_CURVE ( 3, ( #15408, #12938, #24896, #34993 ),
 .UNSPECIFIED., .F., .F. ) 
 B_SPLINE_CURVE_WITH_KNOTS ( ( 4, 4 ),
 ( 1.381924640371167357, 1.574767692156076038 ),
 .UNSPECIFIED. ) 
 CURVE ( )  GEOMETRIC_REPRESENTATION_ITEM ( )  RATIONAL_B_SPLINE_CURVE ( ( 1.000000000000000000, 0.9969033633783032089, 0.9969033633783032089, 1.000000000000000000 ) ) 
 REPRESENTATION_ITEM ( '' )  );
#21399=CARTESIAN_POINT ( 'NONE',  ( 3.463872813216964275, -32.59319547873680989, 7.638132480492515697 ) ) ;
#21404=VERTEX_POINT ( 'NONE', #8704 ) ;
#21405=LINE ( 'NONE', #19074, #9538 ) ;
#21406=EDGE_CURVE ( 'NONE', #13175, #17512, #33860, .T. ) ;
#21407=EDGE_CURVE ( 'NONE', #28306, #11301, #36717, .T. ) ;
#21419=CARTESIAN_POINT ( 'NONE',  ( -1.796981532764649003, -29.43400205062587816, 6.870724624169667116 ) ) ;
#21426=B_SPLINE_CURVE_WITH_KNOTS ( 'NONE', 3,
 ( #9102, #18364, #2755, #25984, #10517, #19194, #3573, #32177, #10712, #674, #29272, #38516, #13213, #16299, #25779, #16494, #7432, #38119, #22896 ),
 .UNSPECIFIED., .F., .F.,
 ( 4, 3, 3, 3, 3, 3, 4 ),
 ( 0.000000000000000000, 2.546128104244783745E-05, 5.711050680484153604E-05, 8.113074941675923069E-05, 0.0001053129305727060346, 0.0001360598016347114444, 0.0001612931755702003752 ),
 .UNSPECIFIED. ) ;
#21429=CARTESIAN_POINT ( 'NONE',  ( 3.896194328649233984, -32.16578144256224903, 7.635761828346577573 ) ) ;
#21432=DIRECTION ( 'NONE',  ( -1.000000000000000000, 0.000000000000000000, 0.000000000000000000 ) ) ;
#21438=CARTESIAN_POINT ( 'NONE',  ( 5.166053052204034657, -29.08252373668924307, 7.754798119455333705 ) ) ;
#21442=EDGE_CURVE ( 'NONE', #12108, #25231, #2156, .T. ) ;
#21444=CIRCLE ( 'NONE', #37207, 3.499999999999999556 ) ;
#21445=CARTESIAN_POINT ( 'NONE',  ( 1.952673410241816176, -32.96768074256310399, 7.505001789837626447 ) ) ;
#21447=ORIENTED_EDGE ( 'NONE', *, *, #14880, .T. ) ;
#21451=VECTOR ( 'NONE', #17909, 1000.000000000000114 ) ;
#21452=CARTESIAN_POINT ( 'NONE',  ( 1.700390093233090871, -29.56993018339339940, 7.750000000000000888 ) ) ;
#21455=CARTESIAN_POINT ( 'NONE',  ( 5.866854291671645960, -27.23014986009699712, 7.013842709614101167 ) ) ;
#21460=ORIENTED_EDGE ( 'NONE', *, *, #25355, .F. ) ;
#21464=CARTESIAN_POINT ( 'NONE',  ( -0.1322584125241582920, -32.43375540223212994, 6.871394612369934762 ) ) ;
#21467=CARTESIAN_POINT ( 'NONE',  ( 3.859316710813556206, -32.32368945768034507, 7.761113333116784752 ) ) ;
#21469=CARTESIAN_POINT ( 'NONE',  ( 0.5037982502477859059, -26.38745190989316214, 7.703977250142848732 ) ) ;
#21472=ORIENTED_EDGE ( 'NONE', *, *, #17606, .F. ) ;
#21474=CARTESIAN_POINT ( 'NONE',  ( 4.747584925568015812, -31.29173262670428102, 7.670465701733750308 ) ) ;
#21476=CARTESIAN_POINT ( 'NONE',  ( 4.258250226677295913, -31.95893657470690741, 6.921725064902953584 ) ) ;
#21477=DIRECTION ( 'NONE',  ( 0.4999999999999999445, -0.8660254037844387076, 0.000000000000000000 ) ) ;
#21478=ORIENTED_EDGE ( 'NONE', *, *, #21548, .T. ) ;
#21486=CARTESIAN_POINT ( 'NONE',  ( -1.593127767899503722, -28.38555688987459291, 7.635761828346575797 ) ) ;
#21487=DIRECTION ( 'NONE',  ( -0.6662082868431850047, 0.000000000000000000, -0.7457657263118683266 ) ) ;
#21488=CARTESIAN_POINT ( 'NONE',  ( 0.5179793559627476895, -32.86415379421544714, 7.638132480492514809 ) ) ;
#21493=CARTESIAN_POINT ( 'NONE',  ( 1.123288416806107026, -32.92059484209399045, 7.635761828346577573 ) ) ;
#21494=CARTESIAN_POINT ( 'NONE',  ( -0.07210163165322443224, -26.55193716086669653, 7.737115613922529889 ) ) ;
#21495=DIRECTION ( 'NONE',  ( -0.000000000000000000, -0.000000000000000000, -1.000000000000000000 ) ) ;
#21497=CARTESIAN_POINT ( 'NONE',  ( 5.099125247292754182, -29.66318013251687447, 6.866852738645440546 ) ) ;
#21503=CARTESIAN_POINT ( 'NONE',  ( 4.738207753463742122, -31.30822356001046458, 7.635761828346574021 ) ) ;
#21508=DIRECTION ( 'NONE',  ( 0.5000000000000101030, -0.8660254037844328234, -0.000000000000000000 ) ) ;
#21509=CARTESIAN_POINT ( 'NONE',  ( 4.954463893073100422, -28.58453498085037836, 7.013842709614101167 ) ) ;
#21510=CARTESIAN_POINT ( 'NONE',  ( -1.419098044220405974, -28.21759841648404432, 6.920489980334477487 ) ) ;
#21512=CARTESIAN_POINT ( 'NONE',  ( 1.301684415825685726, -26.19338184037020767, 7.006423389747789443 ) ) ;
#21519=ORIENTED_EDGE ( 'NONE', *, *, #12062, .F. ) ;
#21524=B_SPLINE_CURVE_WITH_KNOTS ( 'NONE', 3,
 ( #15659, #24937, #225, #19364 ),
 .UNSPECIFIED., .F., .F.,
 ( 4, 4 ),
 ( 0.000000000000000000, 6.391136169993434029E-06 ),
 .UNSPECIFIED. ) ;
#21527=CARTESIAN_POINT ( 'NONE',  ( 4.389962996808223217, -27.48995486600581728, 6.865312560952602006 ) ) ;
#21528=CARTESIAN_POINT ( 'NONE',  ( 2.895778614782184679, -32.75286161408205743, 7.712764235869103757 ) ) ;
#21533=CARTESIAN_POINT ( 'NONE',  ( -1.312560436656866392, -31.35097737660188244, 7.695279973900954751 ) ) ;
#21535=FACE_OUTER_BOUND ( 'NONE', #10093, .T. ) ;
#21536=CARTESIAN_POINT ( 'NONE',  ( 3.465471057152984091, -32.59226193070500699, 7.750000000000000000 ) ) ;
#21538=CARTESIAN_POINT ( 'NONE',  ( -1.758218327909825129, -30.07531940574666507, 7.771081512783698741 ) ) ;
#21539=DIRECTION ( 'NONE',  ( 0.000000000000000000, 0.000000000000000000, -1.000000000000000000 ) ) ;
#21544=EDGE_CURVE ( 'NONE', #30375, #320, #28885, .T. ) ;
#21545=ADVANCED_FACE ( 'NONE', ( #37930 ), #3790, .F. ) ;
#21548=EDGE_CURVE ( 'NONE', #19820, #24741, #32321, .T. ) ;
#21550=ORIENTED_EDGE ( 'NONE', *, *, #21613, .F. ) ;
#21553=CARTESIAN_POINT ( 'NONE',  ( 4.948327458862285866, -30.86155448860804285, 7.771081512783703182 ) ) ;
#21559=CARTESIAN_POINT ( 'NONE',  ( -1.551921384529348691, -30.56115925902171071, 6.887945620086122211 ) ) ;
#21571=CARTESIAN_POINT ( 'NONE',  ( -1.343423704725136059, -31.08492112836934496, 6.959317978105162616 ) ) ;
#21572=ORIENTED_EDGE ( 'NONE', *, *, #33298, .F. ) ;
#21576=DIRECTION ( 'NONE',  ( 0.7394003126383932312, 0.1303762246624257659, 0.6605219282605379050 ) ) ;
#21583=CARTESIAN_POINT ( 'NONE',  ( 5.005772579430486147, -30.36645195696452149, 6.949473656533219135 ) ) ;
#21587=ORIENTED_EDGE ( 'NONE', *, *, #10120, .T. ) ;
#21588=CARTESIAN_POINT ( 'NONE',  ( 2.884763386751913572, -26.27641232226080703, 7.635761828346579350 ) ) ;
#21589=CARTESIAN_POINT ( 'NONE',  ( 4.609042127190076776, -31.33056771902256088, 7.784476445165074310 ) ) ;
#21596=ORIENTED_EDGE ( 'NONE', *, *, #22115, .T. ) ;
#21605=CARTESIAN_POINT ( 'NONE',  ( 3.462070670749302970, -32.59424523688933562, 7.635761828346575797 ) ) ;
#21606=ORIENTED_EDGE ( 'NONE', *, *, #31317, .F. ) ;
#21609=ORIENTED_EDGE ( 'NONE', *, *, #37330, .F. ) ;
#21613=EDGE_CURVE ( 'NONE', #19192, #27494, #28411, .T. ) ;
#21618=LINE ( 'NONE', #2084, #23916 ) ;
#21623=CARTESIAN_POINT ( 'NONE',  ( 0.5644051061537491698, -26.27513991809672333, 7.785593909369612931 ) ) ;
#21626=ORIENTED_EDGE ( 'NONE', *, *, #8014, .F. ) ;
#21640=EDGE_CURVE ( 'NONE', #34783, #29061, #12769, .T. ) ;
#21642=CARTESIAN_POINT ( 'NONE',  ( 5.100388886341633565, -29.57279494524226138, 7.769368695748485543 ) ) ;
#21644=( BOUNDED_CURVE ( )  B_SPLINE_CURVE ( 3, ( #14314, #11014, #11823, #26690 ),
 .UNSPECIFIED., .F., .F. ) 
 B_SPLINE_CURVE_WITH_KNOTS ( ( 4, 4 ),
 ( 4.748221474220558846, 4.941946782021393147 ),
 .UNSPECIFIED. ) 
 CURVE ( )  GEOMETRIC_REPRESENTATION_ITEM ( )  RATIONAL_B_SPLINE_CURVE ( ( 1.000000000000000000, 0.9968749865767494445, 0.9968749865767494445, 1.000000000000000000 ) ) 
 REPRESENTATION_ITEM ( '' )  );
#21648=ORIENTED_EDGE ( 'NONE', *, *, #32563, .T. ) ;
#21656=EDGE_CURVE ( 'NONE', #23269, #25596, #25279, .T. ) ;
#21657=VERTEX_POINT ( 'NONE', #32790 ) ;
#21662=CARTESIAN_POINT ( 'NONE',  ( 5.030284764849001000, -28.49206123220129783, 7.750000000000000888 ) ) ;
#21663=VERTEX_POINT ( 'NONE', #29490 ) ;
#21668=CARTESIAN_POINT ( 'NONE',  ( -0.06304711255985051555, -32.47688463027607497, 6.874555630061442990 ) ) ;
#21673=CARTESIAN_POINT ( 'NONE',  ( 0.5143470587258708315, -26.38350004588937381, 7.740055089680401679 ) ) ;
#21679=EDGE_CURVE ( 'NONE', #2075, #17900, #8732, .T. ) ;
#21695=ADVANCED_FACE ( 'NONE', ( #14229 ), #29882, .F. ) ;
#21700=DIRECTION ( 'NONE',  ( 0.8660254037844252739, 0.5000000000000230926, 0.000000000000000000 ) ) ;
#21701=CARTESIAN_POINT ( 'NONE',  ( -0.7974450458313169232, -25.21654760013375451, 7.635761828346577573 ) ) ;
#21704=CARTESIAN_POINT ( 'NONE',  ( 2.829436171004394041, -26.36286689144161954, 7.692469944509199742 ) ) ;
#21708=EDGE_LOOP ( 'NONE', ( #30471, #34380, #4148, #21869 ) ) ;
#21709=DIRECTION ( 'NONE',  ( 0.9396926207859126468, -0.3420201433256568890, -0.000000000000000000 ) ) ;
#21710=LINE ( 'NONE', #8719, #28505 ) ;
#21711=CARTESIAN_POINT ( 'NONE',  ( 1.280975525403379889, -26.19589825996822086, 6.882085323592684212 ) ) ;
#21712=EDGE_CURVE ( 'NONE', #25728, #33766, #19478, .T. ) ;
#21713=CARTESIAN_POINT ( 'NONE',  ( 5.028355742328307620, -30.26613402516411355, 7.768425012602594215 ) ) ;
#21718=EDGE_CURVE ( 'NONE', #18768, #20340, #25998, .T. ) ;
#21721=CARTESIAN_POINT ( 'NONE',  ( -1.483070179901938568, -30.76391300394762141, 7.670860738520329569 ) ) ;
#21724=EDGE_CURVE ( 'NONE', #4303, #37042, #26566, .T. ) ;
#21725=CARTESIAN_POINT ( 'NONE',  ( 4.345932563343239075, -27.43424125969082894, 6.880147297696982633 ) ) ;
#21726=AXIS2_PLACEMENT_3D ( 'NONE', #28238, #15275, #40585 ) ;
#21727=CARTESIAN_POINT ( 'NONE',  ( -1.064602432027077050, -27.57915845623975670, 7.505001789837630000 ) ) ;
#21728=EDGE_LOOP ( 'NONE', ( #37620, #18078 ) ) ;
#21732=CARTESIAN_POINT ( 'NONE',  ( -1.799429409603024332, -29.60556360950435817, 7.707924859530665529 ) ) ;
#21735=CARTESIAN_POINT ( 'NONE',  ( 1.592658322483926137, -32.96823108478886866, 7.768425012602593327 ) ) ;
#21736=CARTESIAN_POINT ( 'NONE',  ( 1.649183331817654086, -32.96954544161381762, 6.892063359921931642 ) ) ;
#21738=CARTESIAN_POINT ( 'NONE',  ( 4.907431569743298638, -30.69903822425716911, 7.691066658568948888 ) ) ;
#21742=CARTESIAN_POINT ( 'NONE',  ( 1.700390093233090871, -29.56993018339339940, 6.850000000000000533 ) ) ;
#21747=VERTEX_POINT ( 'NONE', #38532 ) ;
#21750=CARTESIAN_POINT ( 'NONE',  ( -1.657912054741428554, -30.10078485551160554, 7.785172627573962778 ) ) ;
#21761=ORIENTED_EDGE ( 'NONE', *, *, #21640, .T. ) ;
#21764=EDGE_CURVE ( 'NONE', #24059, #30463, #39650, .T. ) ;
#21765=ORIENTED_EDGE ( 'NONE', *, *, #2249, .F. ) ;
#21769=CARTESIAN_POINT ( 'NONE',  ( -0.8709512122991237559, -27.34547296267558281, 6.892063359921930754 ) ) ;
#21772=EDGE_CURVE ( 'NONE', #17549, #347, #30381, .T. ) ;
#21774=EDGE_CURVE ( 'NONE', #38484, #13794, #36268, .T. ) ;
#21779=VECTOR ( 'NONE', #31102, 1000.000000000000000 ) ;
#21787=LINE ( 'NONE', #9828, #30737 ) ;
#21790=CARTESIAN_POINT ( 'NONE',  ( -0.8560347025813198618, -25.25037435423009669, 7.695279973900954751 ) ) ;
#21792=DIRECTION ( 'NONE',  ( -1.000000000000000000, 0.000000000000000000, 0.000000000000000000 ) ) ;
#21795=CARTESIAN_POINT ( 'NONE',  ( 4.037301893384181994, -26.96438931088447433, 6.865482280155368322 ) ) ;
#21807=CARTESIAN_POINT ( 'NONE',  ( 0.8386806441584250260, -25.38437669007690900, 7.754798119455333705 ) ) ;
#21808=ORIENTED_EDGE ( 'NONE', *, *, #28605, .F. ) ;
#21809=CARTESIAN_POINT ( 'NONE',  ( -1.644339674572252052, -28.95929335108931468, 7.779495906702011965 ) ) ;
#21810=VERTEX_POINT ( 'NONE', #21438 ) ;
#21818=ORIENTED_EDGE ( 'NONE', *, *, #25714, .F. ) ;
#21820=CARTESIAN_POINT ( 'NONE',  ( 4.739544865517091310, -28.04560401959518501, 6.911401339314954484 ) ) ;
#21821=ADVANCED_FACE ( 'NONE', ( #24097 ), #11327, .F. ) ;
#21824=CARTESIAN_POINT ( 'NONE',  ( 3.613857606807241218, -32.50872529095400409, 7.139344958878409919 ) ) ;
#21840=CARTESIAN_POINT ( 'NONE',  ( -0.9271279775035500270, -27.41211907304282036, 7.695279973900954751 ) ) ;
#21841=ORIENTED_EDGE ( 'NONE', *, *, #27383, .T. ) ;
#21845=CARTESIAN_POINT ( 'NONE',  ( 5.100032641329620198, -29.62024639473925092, 7.785868773668302545 ) ) ;
#21860=ORIENTED_EDGE ( 'NONE', *, *, #21718, .F. ) ;
#21863=ORIENTED_EDGE ( 'NONE', *, *, #28790, .F. ) ;
#21867=CARTESIAN_POINT ( 'NONE',  ( 2.882556208928725550, -26.38205034947389649, 7.779495906702015517 ) ) ;
#21869=ORIENTED_EDGE ( 'NONE', *, *, #35802, .F. ) ;
#21871=CARTESIAN_POINT ( 'NONE',  ( 2.375388416495339605, -26.13562163180044706, 6.869132338375688818 ) ) ;
#21879=CARTESIAN_POINT ( 'NONE',  ( 0.5197218266442334977, -32.86477804699348582, 7.750000000000000888 ) ) ;
#21881=( BOUNDED_CURVE ( )  B_SPLINE_CURVE ( 3, ( #37005, #15178, #2659, #11258 ),
 .UNSPECIFIED., .F., .F. ) 
 B_SPLINE_CURVE_WITH_KNOTS ( ( 4, 4 ),
 ( 4.708531083176467291, 4.895802057644188743 ),
 .UNSPECIFIED. ) 
 CURVE ( )  GEOMETRIC_REPRESENTATION_ITEM ( )  RATIONAL_B_SPLINE_CURVE ( ( 1.000000000000000000, 0.9970795998553221295, 0.9970795998553221295, 1.000000000000000000 ) ) 
 REPRESENTATION_ITEM ( '' )  );
#21882=CARTESIAN_POINT ( 'NONE',  ( 4.260855366779333409, -31.95614730464330933, 6.912143950357351407 ) ) ;
#21883=CARTESIAN_POINT ( 'NONE',  ( -1.581856393934390814, -30.78519064826367568, 7.643192810543816051 ) ) ;
#21895=FACE_OUTER_BOUND ( 'NONE', #35165, .T. ) ;
#21897=CARTESIAN_POINT ( 'NONE',  ( 0.5095177897111177190, -32.85964367047046153, 7.762796336881260473 ) ) ;
#21898=CARTESIAN_POINT ( 'NONE',  ( 1.531218635892081847, -33.06583936671340496, 7.013842709614101167 ) ) ;
#21899=CARTESIAN_POINT ( 'NONE',  ( 1.680225990343694908, -26.16998345069513832, 7.643333865083956624 ) ) ;
#21904=VERTEX_POINT ( 'NONE', #25544 ) ;
#21910=ORIENTED_EDGE ( 'NONE', *, *, #38624, .F. ) ;
#21913=CARTESIAN_POINT ( 'NONE',  ( 5.017169059587130775, -28.45235365878695077, 6.865554069792297653 ) ) ;
#21914=CARTESIAN_POINT ( 'NONE',  ( -1.425344313683088782, -28.23208962058615512, 6.895222827070020877 ) ) ;
#21915=CARTESIAN_POINT ( 'NONE',  ( 4.884862803864217895, -30.76120410455747844, 7.782167645815905033 ) ) ;
#21916=CARTESIAN_POINT ( 'NONE',  ( 5.043346053430708409, -30.19012809388586760, 7.782167645815904145 ) ) ;
#21919=DIRECTION ( 'NONE',  ( 0.6834397476448837994, 0.000000000000000000, -0.7300069255418729641 ) ) ;
#21926=CARTESIAN_POINT ( 'NONE',  ( -1.677641490061642759, -29.95580920881881681, 6.929923840112066635 ) ) ;
#21929=CARTESIAN_POINT ( 'NONE',  ( 4.402002282394398058, -27.50561746263473495, 6.871394612369932986 ) ) ;
#21939=EDGE_CURVE ( 'NONE', #39722, #11704, #21524, .T. ) ;
#21941=ADVANCED_FACE ( 'NONE', ( #12564 ), #3142, .F. ) ;
#21942=CARTESIAN_POINT ( 'NONE',  ( 1.729679958306010068, -32.96980524772960308, 7.730758795053805699 ) ) ;
#21943=CARTESIAN_POINT ( 'NONE',  ( 1.635900804779897300, -32.96932766995732322, 6.880147297696981745 ) ) ;
#21945=CARTESIAN_POINT ( 'NONE',  ( -1.555626379089409372, -30.54891009224447629, 7.006423389747794772 ) ) ;
#21946=CARTESIAN_POINT ( 'NONE',  ( 3.828902690058404445, -32.22125608946033992, 6.874555630061442102 ) ) ;
#21949=FACE_OUTER_BOUND ( 'NONE', #5097, .T. ) ;
#21952=CARTESIAN_POINT ( 'NONE',  ( 3.913290293412393872, -32.15122301917286762, 7.695279973900954751 ) ) ;
#21960=EDGE_CURVE ( 'NONE', #14737, #37640, #22135, .T. ) ;
#21962=CARTESIAN_POINT ( 'NONE',  ( -1.666668308769183815, -30.04207646230481998, 7.757178535559534183 ) ) ;
#21963=EDGE_CURVE ( 'NONE', #1128, #29803, #37876, .T. ) ;
#21968=ORIENTED_EDGE ( 'NONE', *, *, #27658, .T. ) ;
#21976=CARTESIAN_POINT ( 'NONE',  ( 4.487153213455422396, -27.45239593059636363, 7.013842709614101167 ) ) ;
#21978=B_SPLINE_CURVE_WITH_KNOTS ( 'NONE', 3,
 ( #36881, #8052, #21040, #20611 ),
 .UNSPECIFIED., .F., .F.,
 ( 4, 4 ),
 ( 0.000000000000000000, 6.391136169897297484E-06 ),
 .UNSPECIFIED. ) ;
#21979=DIRECTION ( 'NONE',  ( 0.7055275666422172742, -0.2567910337120293818, 0.6605219282605377940 ) ) ;
#21984=CARTESIAN_POINT ( 'NONE',  ( 0.03641831304798801017, -26.49892041654603503, 7.776484688137387025 ) ) ;
#21987=CARTESIAN_POINT ( 'NONE',  ( -1.425774885472621767, -28.23310838303483550, 7.013842709614101167 ) ) ;
#21990=DIRECTION ( 'NONE',  ( -0.9396926207859007674, 0.3420201433256899737, 0.000000000000000000 ) ) ;
#21994=CARTESIAN_POINT ( 'NONE',  ( -89.20959394718985891, -29.55642757665872722, 7.635761828346577573 ) ) ;
#22000=CARTESIAN_POINT ( 'NONE',  ( 4.583196249787880205, -31.37254857199200231, 7.757178535559535071 ) ) ;
#22001=EDGE_CURVE ( 'NONE', #16672, #17495, #11680, .T. ) ;
#22006=CARTESIAN_POINT ( 'NONE',  ( 4.702906489365862974, -27.97465601193010798, 7.757178535559532406 ) ) ;
#22013=LINE ( 'NONE', #18913, #17787 ) ;
#22014=CARTESIAN_POINT ( 'NONE',  ( -1.351882211874637418, -31.25406282615607267, 7.784725160561909441 ) ) ;
#22015=FACE_OUTER_BOUND ( 'NONE', #28858, .T. ) ;
#22017=VERTEX_POINT ( 'NONE', #34631 ) ;
#22020=ORIENTED_EDGE ( 'NONE', *, *, #16552, .T. ) ;
#22022=VERTEX_POINT ( 'NONE', #12975 ) ;
#22030=CARTESIAN_POINT ( 'NONE',  ( 3.055030623276686619, -26.34271016697629619, 7.013842709614101167 ) ) ;
#22036=B_SPLINE_CURVE_WITH_KNOTS ( 'NONE', 3,
 ( #23599, #1392, #4860, #14519, #17394, #11423, #19903, #26298, #4274, #32677, #38830, #13923, #32876, #27091, #16797, #29378, #29974, #4666, #10624, #33499, #9165, #5267, #37369, #8337, #18221 ),
 .UNSPECIFIED., .F., .F.,
 ( 4, 3, 3, 3, 3, 3, 3, 3, 4 ),
 ( 6.468151674593845140E-05, 9.076621574721758135E-05, 0.0001210204262067946055, 0.0001512763324577414510, 0.0001815301820994176898, 0.0002117781465860678054, 0.0002420274594459698408, 0.0002722905548971106386, 0.0002816827545175582459 ),
 .UNSPECIFIED. ) ;
#22038=ORIENTED_EDGE ( 'NONE', *, *, #7217, .T. ) ;
#22039=VECTOR ( 'NONE', #29535, 1000.000000000000227 ) ;
#22043=CARTESIAN_POINT ( 'NONE',  ( -1.450854365928797352, -28.29334945402236556, 7.754798119455333705 ) ) ;
#22045=CIRCLE ( 'NONE', #4292, 3.499999999999999556 ) ;
#22048=CIRCLE ( 'NONE', #14782, 3.499999999999999556 ) ;
#22049=CARTESIAN_POINT ( 'NONE',  ( 0.5182239775374835045, -32.75781001731291298, 7.779495906702013741 ) ) ;
#22052=CARTESIAN_POINT ( 'NONE',  ( 5.100395873294749194, -29.56450258678017562, 7.763628509615285722 ) ) ;
#22053=B_SPLINE_CURVE_WITH_KNOTS ( 'NONE', 3,
 ( #14247, #26425, #4408, #32811, #38552, #7273, #7876, #38762, #10555, #39359 ),
 .UNSPECIFIED., .F., .F.,
 ( 4, 3, 3, 4 ),
 ( 0.0001585009270395749373, 0.0001815657551981825679, 0.0002118214035944122073, 0.0002170292169044788736 ),
 .UNSPECIFIED. ) ;
#22060=VERTEX_POINT ( 'NONE', #1446 ) ;
#22063=DIRECTION ( 'NONE',  ( -0.8660254037844415942, 0.4999999999999950040, -0.000000000000000000 ) ) ;
#22064=CARTESIAN_POINT ( 'NONE',  ( 1.764879381686311977, -26.17053269682947203, 6.880147297696981745 ) ) ;
#22065=ORIENTED_EDGE ( 'NONE', *, *, #1576, .T. ) ;
#22067=CARTESIAN_POINT ( 'NONE',  ( -0.5298641067787194237, -26.88385662570251711, 7.778495531946298058 ) ) ;
#22073=ORIENTED_EDGE ( 'NONE', *, *, #10098, .F. ) ;
#22078=AXIS2_PLACEMENT_3D ( 'NONE', #9589, #145, #12479 ) ;
#22081=CARTESIAN_POINT ( 'NONE',  ( 2.832967893104934465, -26.36411242075662642, 7.721096864323907738 ) ) ;
#22084=CARTESIAN_POINT ( 'NONE',  ( 3.921528935726882992, -32.26039213087532431, 7.781480525794719050 ) ) ;
#22085=CYLINDRICAL_SURFACE ( 'NONE', #11173, 3.399999999999999911 ) ;
#22090=CARTESIAN_POINT ( 'NONE',  ( 4.749297472835600331, -31.28869828601962766, 7.695279973900954751 ) ) ;
#22093=CARTESIAN_POINT ( 'NONE',  ( 4.269313204158568631, -31.94703641790479764, 6.895394898881674450 ) ) ;
#22094=CARTESIAN_POINT ( 'NONE',  ( -1.698345060826572883, -29.47668023426995632, 6.866852738645442322 ) ) ;
#22096=CARTESIAN_POINT ( 'NONE',  ( -1.404916813412772525, -31.18459841582754422, 6.880828092187095457 ) ) ;
#22099=CARTESIAN_POINT ( 'NONE',  ( 4.679148373602942890, -31.38802211924678787, 7.780491323090170219 ) ) ;
#22102=CIRCLE ( 'NONE', #16804, 3.499999999999999556 ) ;
#22109=DIRECTION ( 'NONE',  ( 1.000000000000000000, -0.000000000000000000, -0.000000000000000000 ) ) ;
#22110=CARTESIAN_POINT ( 'NONE',  ( 2.083536916395903660, -32.94827280028442829, 6.969307238440508812 ) ) ;
#22111=AXIS2_PLACEMENT_3D ( 'NONE', #4420, #20237, #16942 ) ;
#22115=EDGE_CURVE ( 'NONE', #17544, #22827, #8256, .T. ) ;
#22117=EDGE_LOOP ( 'NONE', ( #38097, #22426, #32557, #31080, #24579 ) ) ;
#22119=ADVANCED_FACE ( 'NONE', ( #19956 ), #29632, .F. ) ;
#22122=CARTESIAN_POINT ( 'NONE',  ( -0.9099111520310427803, -27.24534035165016377, 7.771081512783699630 ) ) ;
#22125=CARTESIAN_POINT ( 'NONE',  ( 5.020437716722687682, -28.46205448284394990, 6.863805608295730387 ) ) ;
#22126=CARTESIAN_POINT ( 'NONE',  ( 3.514196955445712867, -26.57656972717544264, 6.867280401193707640 ) ) ;
#22131=CARTESIAN_POINT ( 'NONE',  ( 0.4695943777967593880, -26.29347754267606874, 7.695279973900954751 ) ) ;
#22132=VERTEX_POINT ( 'NONE', #16857 ) ;
#22134=B_SPLINE_CURVE_WITH_KNOTS ( 'NONE', 3,
 ( #26222, #13850, #32404, #7467, #19634, #22927, #29694, #38347, #20024, #17123 ),
 .UNSPECIFIED., .F., .F.,
 ( 4, 3, 3, 4 ),
 ( 0.0002170292169044726665, 0.0002420761345915957668, 0.0002723302478206989560, 0.0002816811360866700248 ),
 .UNSPECIFIED. ) ;
#22135=( BOUNDED_CURVE ( )  B_SPLINE_CURVE ( 3, ( #34424, #25134, #31115, #6808 ),
 .UNSPECIFIED., .F., .T. ) 
 B_SPLINE_CURVE_WITH_KNOTS ( ( 4, 4 ),
 ( 4.708531083176466403, 4.895802057644187855 ),
 .UNSPECIFIED. ) 
 CURVE ( )  GEOMETRIC_REPRESENTATION_ITEM ( )  RATIONAL_B_SPLINE_CURVE ( ( 1.000000000000000000, 0.9970795998553221295, 0.9970795998553221295, 1.000000000000000000 ) ) 
 REPRESENTATION_ITEM ( '' )  );
#22137=DIRECTION ( 'NONE',  ( -1.000000000000000000, 0.000000000000000000, 0.000000000000000000 ) ) ;
#22138=AXIS2_PLACEMENT_3D ( 'NONE', #20122, #23423, #33097 ) ;
#22143=CARTESIAN_POINT ( 'NONE',  ( 2.893445099977317359, -32.75373604287706542, 7.721096864323904185 ) ) ;
#22145=CARTESIAN_POINT ( 'NONE',  ( 1.356171688940976727, -33.05979889377250913, 7.501983001166816933 ) ) ;
#22151=CARTESIAN_POINT ( 'NONE',  ( -0.1539201161049026934, -32.53808085965915353, 7.754798119455333705 ) ) ;
#22152=PLANE ( 'NONE',  #36774 ) ;
#22155=DIRECTION ( 'NONE',  ( 1.000000000000000000, 0.000000000000000000, 0.000000000000000000 ) ) ;
#22164=CYLINDRICAL_SURFACE ( 'NONE', #13068, 0.09010775117052947925 ) ;
#22165=EDGE_CURVE ( 'NONE', #24264, #39701, #10945, .T. ) ;
#22172=AXIS2_PLACEMENT_3D ( 'NONE', #12622, #30773, #25190 ) ;
#22178=CARTESIAN_POINT ( 'NONE',  ( 0.4918310210129015481, -32.74788313599579936, 6.894806418505344148 ) ) ;
#22181=VERTEX_POINT ( 'NONE', #39353 ) ;
#22182=CARTESIAN_POINT ( 'NONE',  ( 4.024979924976341827, -26.95962893812927774, 7.771081512783698741 ) ) ;
#22184=ORIENTED_EDGE ( 'NONE', *, *, #22623, .T. ) ;
#22189=ORIENTED_EDGE ( 'NONE', *, *, #12827, .F. ) ;
#22193=CARTESIAN_POINT ( 'NONE',  ( -0.5217032702065468319, -32.27405686018897768, 7.695279973900954751 ) ) ;
#22194=CARTESIAN_POINT ( 'NONE',  ( -1.629504578382812818, -30.64779913458552230, 7.750000000000000888 ) ) ;
#22200=VERTEX_POINT ( 'NONE', #39150 ) ;
#22201=FACE_OUTER_BOUND ( 'NONE', #15655, .T. ) ;
#22205=CARTESIAN_POINT ( 'NONE',  ( -1.651405268677713423, -28.99939339395372784, 7.643333865083954848 ) ) ;
#22210=CARTESIAN_POINT ( 'NONE',  ( -0.5762289783111216313, -26.91154609728502578, 7.710604733652636433 ) ) ;
#22211=ORIENTED_EDGE ( 'NONE', *, *, #16890, .T. ) ;
#22214=CARTESIAN_POINT ( 'NONE',  ( 1.815543965490744593, -26.17188080386636528, 7.761597726988850532 ) ) ;
#22215=DIRECTION ( 'NONE',  ( 0.7055275666422118341, 0.2567910337120383746, -0.6605219282605402364 ) ) ;
#22216=CARTESIAN_POINT ( 'NONE',  ( 4.635447563317058872, -27.85370244579436516, 7.748216051605121280 ) ) ;
#22221=ORIENTED_EDGE ( 'NONE', *, *, #12981, .T. ) ;
#22228=ORIENTED_EDGE ( 'NONE', *, *, #25527, .T. ) ;
#22229=CARTESIAN_POINT ( 'NONE',  ( -1.638866927195242296, -28.93003665516189926, 7.785868773668302545 ) ) ;
#22231=EDGE_LOOP ( 'NONE', ( #3103, #353, #31794, #39619, #34016 ) ) ;
#22234=ORIENTED_EDGE ( 'NONE', *, *, #18114, .F. ) ;
#22240=ORIENTED_EDGE ( 'NONE', *, *, #30022, .T. ) ;
#22244=CARTESIAN_POINT ( 'NONE',  ( 2.868207633511080434, -32.86935470785505231, 6.894806418505347700 ) ) ;
#22249=CARTESIAN_POINT ( 'NONE',  ( 0.5490648462263181262, -26.27994216516969672, 7.785096263473212375 ) ) ;
#22262=CARTESIAN_POINT ( 'NONE',  ( 0.5701619414054610591, -32.77657804911444117, 7.712764235869103757 ) ) ;
#22265=CARTESIAN_POINT ( 'NONE',  ( 5.100230395877511924, -29.53676087646269366, 7.670860738520326905 ) ) ;
#22267=ORIENTED_EDGE ( 'NONE', *, *, #29916, .T. ) ;
#22269=CARTESIAN_POINT ( 'NONE',  ( -1.299983928880091399, -31.16922869443764910, 7.761597726988848756 ) ) ;
#22291=CARTESIAN_POINT ( 'NONE',  ( 3.894751441679935144, -32.27749053463322326, 7.785593909369612931 ) ) ;
#22296=VERTEX_POINT ( 'NONE', #40173 ) ;
#22298=EDGE_CURVE ( 'NONE', #27620, #18445, #11543, .T. ) ;
#22299=CARTESIAN_POINT ( 'NONE',  ( 4.738207753463742122, -31.30822356001046458, 7.635761828346574021 ) ) ;
#22304=CARTESIAN_POINT ( 'NONE',  ( 4.255709282003521388, -31.96165711204241333, 6.931070083220559397 ) ) ;
#22307=CARTESIAN_POINT ( 'NONE',  ( -1.411982544752807600, -31.17091005906851109, 6.895394898881667345 ) ) ;
#22308=CARTESIAN_POINT ( 'NONE',  ( -1.788343858407013265, -29.54202564690695354, 7.781480525794717273 ) ) ;
#22310=DIRECTION ( 'NONE',  ( -0.000000000000000000, -0.000000000000000000, -1.000000000000000000 ) ) ;
#22316=CARTESIAN_POINT ( 'NONE',  ( -0.9794948794710025552, -31.66235005623412135, 7.757178535559534183 ) ) ;
#22320=B_SPLINE_CURVE_WITH_KNOTS ( 'NONE', 3,
 ( #23024, #26509, #798, #20309, #38442, #35590, #10246, #22825, #1006, #13541, #26114, #38645, #10443, #7361, #40069, #20928, #27305, #33922, #5286, #2430, #18238, #5698, #2213, #39653, #14950, #23800, #30623, #14531, #30828, #39445, #5488 ),
 .UNSPECIFIED., .F., .F.,
 ( 4, 3, 3, 3, 3, 3, 3, 3, 3, 3, 4 ),
 ( 0.000000000000000000, 2.999644130997945415E-05, 6.002588995695307074E-05, 8.960886084588327871E-05, 0.0001190604700446532943, 0.0001489538463052769788, 0.0001796139255494003486, 0.0002109707048517106293, 0.0002426195318110385007, 0.0002740640997890078645, 0.0002849778069099876180 ),
 .UNSPECIFIED. ) ;
#22323=CARTESIAN_POINT ( 'NONE',  ( 1.720540564825900454, -33.91097937392895290, 7.013842709614101167 ) ) ;
#22328=CARTESIAN_POINT ( 'NONE',  ( 2.957564255009486942, -26.30349574841345728, 6.870737987065013819 ) ) ;
#22330=CARTESIAN_POINT ( 'NONE',  ( -0.9261155348575771384, -27.27773970951159654, 7.784725160561909441 ) ) ;
#22331=CARTESIAN_POINT ( 'NONE',  ( -1.599636697286329401, -28.40380913581408606, 7.720710062488896241 ) ) ;
#22333=CARTESIAN_POINT ( 'NONE',  ( -1.428174809773816500, -28.23871018788941356, 6.887945620086119547 ) ) ;
#22334=CARTESIAN_POINT ( 'NONE',  ( 1.207759159255195724, -26.20579572742846608, 7.774064877406527074 ) ) ;
#22335=DIRECTION ( 'NONE',  ( -0.6502177225477943079, 0.3754033771448263557, 0.6605219282605377940 ) ) ;
#22338=DIRECTION ( 'NONE',  ( -0.7660444431189813441, 0.6427876096865353661, -0.000000000000000000 ) ) ;
#22340=ORIENTED_EDGE ( 'NONE', *, *, #10590, .F. ) ;
#22342=EDGE_LOOP ( 'NONE', ( #4442, #6528, #12993, #11666 ) ) ;
#22345=CARTESIAN_POINT ( 'NONE',  ( -1.670147819023525271, -30.01655550963544172, 6.868387053540520704 ) ) ;
#22348=VECTOR ( 'NONE', #30964, 1000.000000000000114 ) ;
#22349=EDGE_CURVE ( 'NONE', #18413, #33687, #9484, .T. ) ;
#22359=CARTESIAN_POINT ( 'NONE',  ( 0.6185823884176052667, -26.24155567332487493, 7.754798119455333705 ) ) ;
#22366=CARTESIAN_POINT ( 'NONE',  ( 5.200252094213874798, -29.60101030711846448, 6.894806418505347700 ) ) ;
#22367=CARTESIAN_POINT ( 'NONE',  ( -0.9006701161811203615, -27.22837715677322379, 7.754798119455333705 ) ) ;
#22368=CARTESIAN_POINT ( 'NONE',  ( 1.700390093233090871, -29.56993018339339940, 7.750000000000000888 ) ) ;
#22377=DIRECTION ( 'NONE',  ( -0.3420201433256725987, 0.9396926207859068736, -0.000000000000000000 ) ) ;
#22379=( BOUNDED_CURVE ( )  B_SPLINE_CURVE ( 3, ( #13780, #26348, #38881, #10673 ),
 .UNSPECIFIED., .F., .T. ) 
 B_SPLINE_CURVE_WITH_KNOTS ( ( 4, 4 ),
 ( 4.748221474220560623, 4.941946782021394924 ),
 .UNSPECIFIED. ) 
 CURVE ( )  GEOMETRIC_REPRESENTATION_ITEM ( )  RATIONAL_B_SPLINE_CURVE ( ( 1.000000000000000000, 0.9968749865767494445, 0.9968749865767494445, 1.000000000000000000 ) ) 
 REPRESENTATION_ITEM ( '' )  );
#22385=CARTESIAN_POINT ( 'NONE',  ( 3.953335785500533994, -26.89871648206090171, 7.773839561854631874 ) ) ;
#22386=EDGE_CURVE ( 'NONE', #35661, #6366, #2839, .T. ) ;
#22394=CARTESIAN_POINT ( 'NONE',  ( 0.01625745047043060387, -26.51765787828566445, 7.784725160561910329 ) ) ;
#22397=CARTESIAN_POINT ( 'NONE',  ( 3.433582406314023228, -26.52919928344892142, 7.643192810543816940 ) ) ;
#22401=CARTESIAN_POINT ( 'NONE',  ( -1.751698146652124866, -30.14706689514045479, 6.894806418505347700 ) ) ;
#22402=CARTESIAN_POINT ( 'NONE',  ( -1.565604181971737008, -30.54008291720758095, 7.386948897581447682 ) ) ;
#22404=CARTESIAN_POINT ( 'NONE',  ( 1.700390093233090871, -29.56993018339339940, 7.800000000000000711 ) ) ;
#22408=CARTESIAN_POINT ( 'NONE',  ( -0.5714989174472279165, -26.90750265890564208, 7.730015791551954507 ) ) ;
#22410=CARTESIAN_POINT ( 'NONE',  ( -1.332552448688619329, -27.82589715396020225, 7.762796336881261361 ) ) ;
#22412=CARTESIAN_POINT ( 'NONE',  ( 1.770820908965922591, -26.17064486340278862, 7.784476445165072533 ) ) ;
#22415=LINE ( 'NONE', #25895, #32683 ) ;
#22416=CARTESIAN_POINT ( 'NONE',  ( -0.1576164094376339420, -32.53604074034053895, 7.750000000000000888 ) ) ;
#22423=EDGE_CURVE ( 'NONE', #35515, #15871, #20507, .T. ) ;
#22426=ORIENTED_EDGE ( 'NONE', *, *, #32993, .T. ) ;
#22430=VERTEX_POINT ( 'NONE', #10696 ) ;
#22432=ORIENTED_EDGE ( 'NONE', *, *, #19621, .T. ) ;
#22436=EDGE_LOOP ( 'NONE', ( #19183, #14911, #3958, #4689 ) ) ;
#22440=CARTESIAN_POINT ( 'NONE',  ( 4.731166529110806707, -28.02900214338483664, 6.887945620086118659 ) ) ;
#22441=EDGE_CURVE ( 'NONE', #14269, #39459, #33151, .T. ) ;
#22445=CARTESIAN_POINT ( 'NONE',  ( 0.5333944940907733301, -26.28204871958340050, 7.781480525794718162 ) ) ;
#22449=ORIENTED_EDGE ( 'NONE', *, *, #18065, .F. ) ;
#22456=ORIENTED_EDGE ( 'NONE', *, *, #31430, .T. ) ;
#22458=CARTESIAN_POINT ( 'NONE',  ( 0.4257515640715447969, -32.72196143500892163, 7.757178535559534183 ) ) ;
#22459=ORIENTED_EDGE ( 'NONE', *, *, #19715, .T. ) ;
#22462=CARTESIAN_POINT ( 'NONE',  ( 5.162032219521623944, -29.07102167996093911, 7.766640943994643997 ) ) ;
#22463=DIRECTION ( 'NONE',  ( -0.9848077530122142376, 0.1736481776668952204, 0.000000000000000000 ) ) ;
#22464=PRODUCT ( 'Ruler Clamping Screw', 'Ruler Clamping Screw', '', ( #4641 ) ) ;
#22465=VERTEX_POINT ( 'NONE', #30057 ) ;
#22470=ORIENTED_EDGE ( 'NONE', *, *, #26829, .F. ) ;
#22473=CARTESIAN_POINT ( 'NONE',  ( 1.625050579259687433, -33.05680123510155255, 7.782861076432730840 ) ) ;
#22474=EDGE_CURVE ( 'NONE', #23718, #16154, #7415, .T. ) ;
#22476=DIRECTION ( 'NONE',  ( -0.000000000000000000, -0.000000000000000000, -1.000000000000000000 ) ) ;
#22480=CARTESIAN_POINT ( 'NONE',  ( 3.015109609237833332, -26.32624206733842698, 7.750000000000000888 ) ) ;
#22481=CARTESIAN_POINT ( 'NONE',  ( -0.07645708395594488782, -32.58535952412007930, 6.894806418505347700 ) ) ;
#22483=EDGE_LOOP ( 'NONE', ( #16125, #5664, #22972, #37143, #23735 ) ) ;
#22486=EDGE_CURVE ( 'NONE', #16194, #20410, #23666, .T. ) ;
#22493=ORIENTED_EDGE ( 'NONE', *, *, #33249, .T. ) ;
#22497=CARTESIAN_POINT ( 'NONE',  ( -0.9606818258635283492, -27.29645349747919170, 6.894806418505347700 ) ) ;
#22505=CARTESIAN_POINT ( 'NONE',  ( 0.5371711504799139281, -32.87097875789517332, 7.695279973900954751 ) ) ;
#22507=CARTESIAN_POINT ( 'NONE',  ( -0.1988289257493946471, -32.50982254841889585, 7.006908160621415860 ) ) ;
#22510=CARTESIAN_POINT ( 'NONE',  ( -1.699415837186460942, -29.60626003165447173, 7.701140543647732706 ) ) ;
#22511=CARTESIAN_POINT ( 'NONE',  ( 3.565483696522954826, -26.72714530743686012, 6.903372536218455480 ) ) ;
#22512=FACE_OUTER_BOUND ( 'NONE', #25091, .T. ) ;
#22513=PLANE ( 'NONE',  #38835 ) ;
#22517=CARTESIAN_POINT ( 'NONE',  ( 1.716602532315689267, -33.06989263416611635, 7.638991368224661294 ) ) ;
#22518=CARTESIAN_POINT ( 'NONE',  ( 1.736346942945643512, -32.96974004645320377, 7.693875151218753317 ) ) ;
#22519=CARTESIAN_POINT ( 'NONE',  ( 2.089729628487263735, -32.94756467017376167, 6.988553391373224066 ) ) ;
#22523=EDGE_CURVE ( 'NONE', #37904, #21904, #39185, .T. ) ;
#22528=EDGE_CURVE ( 'NONE', #14780, #18906, #29848, .T. ) ;
#22534=CARTESIAN_POINT ( 'NONE',  ( 1.078322358366002653, -26.22732166111063989, 7.721096864323905962 ) ) ;
#22543=EDGE_LOOP ( 'NONE', ( #27434, #3467, #13552, #33308, #30043 ) ) ;
#22546=CARTESIAN_POINT ( 'NONE',  ( -1.664445652997000646, -30.05777379808717242, 6.864651958020303368 ) ) ;
#22557=CARTESIAN_POINT ( 'NONE',  ( 0.6225211420409756391, -26.24003551177748861, 7.750000000000000888 ) ) ;
#22561=CARTESIAN_POINT ( 'NONE',  ( 3.744196778873498666, -32.28708296902909325, 6.887945620086123100 ) ) ;
#22564=CARTESIAN_POINT ( 'NONE',  ( -0.9128197825508301833, -27.39481314169073300, 7.635761828346577573 ) ) ;
#22565=DIRECTION ( 'NONE',  ( -0.3420201433256601087, -0.9396926207859114255, -0.000000000000000000 ) ) ;
#22567=CYLINDRICAL_SURFACE ( 'NONE', #11161, 0.09010775117052825800 ) ;
#22574=EDGE_CURVE ( 'NONE', #7218, #34783, #32755, .T. ) ;
#22581=CARTESIAN_POINT ( 'NONE',  ( 2.319617088658799453, -32.91306737433055929, 7.730758795053806587 ) ) ;
#22582=CARTESIAN_POINT ( 'NONE',  ( 1.207584434645498028, -26.10564138716367211, 7.761113333116787416 ) ) ;
#22584=CARTESIAN_POINT ( 'NONE',  ( 3.973940671657854029, -26.92785926235529104, 7.785096263473212375 ) ) ;
#22586=ORIENTED_EDGE ( 'NONE', *, *, #34112, .T. ) ;
#22588=CARTESIAN_POINT ( 'NONE',  ( -1.720325740817129301, -28.89808781674439686, 7.784725160561909441 ) ) ;
#22591=ORIENTED_EDGE ( 'NONE', *, *, #4776, .T. ) ;
#22592=VERTEX_POINT ( 'NONE', #2076 ) ;
#22598=LINE ( 'NONE', #25073, #30106 ) ;
#22600=CARTESIAN_POINT ( 'NONE',  ( -1.034105916944730863, -31.59045773092190856, 6.959317978105167946 ) ) ;
#22605=CARTESIAN_POINT ( 'NONE',  ( -1.799609906766908685, -29.56993018339339940, 7.620413589471895399 ) ) ;
#22609=CARTESIAN_POINT ( 'NONE',  ( -1.306989867689303697, -27.80139717009528511, 7.781480525794717273 ) ) ;
#22613=CARTESIAN_POINT ( 'NONE',  ( -0.3206046116097268639, -26.83577804592309590, 6.939395833800441338 ) ) ;
#22614=CARTESIAN_POINT ( 'NONE',  ( 4.701862308883337782, -27.97269194523573432, 7.759451378593094972 ) ) ;
#22615=CARTESIAN_POINT ( 'NONE',  ( -0.9931795851432037026, -27.33505157645927142, 7.643192810543826710 ) ) ;
#22616=( BOUNDED_CURVE ( )  B_SPLINE_CURVE ( 3, ( #4894, #14353, #33532, #27323 ),
 .UNSPECIFIED., .F., .T. ) 
 B_SPLINE_CURVE_WITH_KNOTS ( ( 4, 4 ),
 ( 4.708531083176465515, 4.895802057644186966 ),
 .UNSPECIFIED. ) 
 CURVE ( )  GEOMETRIC_REPRESENTATION_ITEM ( )  RATIONAL_B_SPLINE_CURVE ( ( 1.000000000000000000, 0.9970795998553221295, 0.9970795998553221295, 1.000000000000000000 ) ) 
 REPRESENTATION_ITEM ( '' )  );
#22617=ORIENTED_EDGE ( 'NONE', *, *, #5120, .T. ) ;
#22623=EDGE_CURVE ( 'NONE', #16334, #13771, #12684, .T. ) ;
#22624=VERTEX_POINT ( 'NONE', #33371 ) ;
#22626=CARTESIAN_POINT ( 'NONE',  ( -0.4171441595639596156, -26.78316706317107787, 7.013842709614101167 ) ) ;
#22628=EDGE_CURVE ( 'NONE', #16824, #18814, #34279, .T. ) ;
#22637=CARTESIAN_POINT ( 'NONE',  ( 5.150522559231670350, -30.15864875804516032, 7.747520101777648271 ) ) ;
#22642=CARTESIAN_POINT ( 'NONE',  ( 4.741504651846523366, -28.04952573427642193, 6.920489980334477487 ) ) ;
#22643=AXIS2_PLACEMENT_3D ( 'NONE', #31141, #2959, #15475 ) ;
#22644=CARTESIAN_POINT ( 'NONE',  ( 4.569457157119717117, -31.39433534204675524, 6.868387053540519815 ) ) ;
#22645=CARTESIAN_POINT ( 'NONE',  ( 3.977572546501451978, -32.22783162523180778, 7.686927408461907696 ) ) ;
#22649=EDGE_CURVE ( 'NONE', #36238, #19982, #17883, .T. ) ;
#22655=CARTESIAN_POINT ( 'NONE',  ( 1.120206005321838783, -33.02151157302147055, 7.733670252284491120 ) ) ;
#22659=CARTESIAN_POINT ( 'NONE',  ( 0.4809726510178614634, -32.74373249318228574, 7.785172627573962778 ) ) ;
#22665=CARTESIAN_POINT ( 'NONE',  ( 5.078470208622237969, -29.18445660682317211, 6.979335674598004857 ) ) ;
#22667=CARTESIAN_POINT ( 'NONE',  ( 0.5708372184697405594, -32.77681504654623268, 7.680992449362118890 ) ) ;
#22671=CARTESIAN_POINT ( 'NONE',  ( -1.267760583032661037, -27.71561997405539302, 7.754798119455333705 ) ) ;
#22676=ORIENTED_EDGE ( 'NONE', *, *, #14160, .T. ) ;
#22682=ORIENTED_EDGE ( 'NONE', *, *, #31587, .T. ) ;
#22689=ADVANCED_FACE ( 'NONE', ( #34752 ), #2488, .F. ) ;
#22691=CARTESIAN_POINT ( 'NONE',  ( 2.972966256002666618, -26.41706555567719050, 7.759451378593095860 ) ) ;
#22692=ORIENTED_EDGE ( 'NONE', *, *, #26045, .T. ) ;
#22695=CARTESIAN_POINT ( 'NONE',  ( 2.491849584607222834, -26.16059047924537140, 6.984548363133216142 ) ) ;
#22699=CARTESIAN_POINT ( 'NONE',  ( 4.430837595856232269, -27.54393501177549908, 6.988553391373218737 ) ) ;
#22700=VECTOR ( 'NONE', #8618, 1000.000000000000114 ) ;
#22707=EDGE_CURVE ( 'NONE', #16761, #8120, #33980, .T. ) ;
#22708=CARTESIAN_POINT ( 'NONE',  ( 2.340283621464598340, -26.23067316296506846, 7.785868773668302545 ) ) ;
#22709=CARTESIAN_POINT ( 'NONE',  ( 3.578439373864104045, -26.73568756415219738, 6.969307238440505259 ) ) ;
#22710=EDGE_CURVE ( 'NONE', #17652, #38094, #21405, .T. ) ;
#22712=CARTESIAN_POINT ( 'NONE',  ( 0.7341752703951600623, -26.31010747957196827, 6.979335674598004857 ) ) ;
#22716=CARTESIAN_POINT ( 'NONE',  ( -0.9060015222600810159, -31.75321274565758856, 7.769368695748492648 ) ) ;
#22717=DIRECTION ( 'NONE',  ( 0.8660254037844450359, -0.4999999999999888978, -0.000000000000000000 ) ) ;
#22719=ADVANCED_FACE ( 'NONE', ( #8821 ), #14587, .F. ) ;
#22728=CARTESIAN_POINT ( 'NONE',  ( 3.061823518957293100, -26.34556267481334757, 6.903112506833887885 ) ) ;
#22730=DIRECTION ( 'NONE',  ( -0.3754033771448240797, -0.6502177225477954181, 0.6605219282605377940 ) ) ;
#22733=CARTESIAN_POINT ( 'NONE',  ( 5.043922214925016689, -28.53513699343982779, 7.011627023500182077 ) ) ;
#22734=( BOUNDED_CURVE ( )  B_SPLINE_CURVE ( 3, ( #7550, #32885, #39030, #26304 ),
 .UNSPECIFIED., .F., .F. ) 
 B_SPLINE_CURVE_WITH_KNOTS ( ( 4, 4 ),
 ( 4.708531083176467291, 4.895802057644187855 ),
 .UNSPECIFIED. ) 
 CURVE ( )  GEOMETRIC_REPRESENTATION_ITEM ( )  RATIONAL_B_SPLINE_CURVE ( ( 1.000000000000000000, 0.9970795998553221295, 0.9970795998553221295, 1.000000000000000000 ) ) 
 REPRESENTATION_ITEM ( '' )  );
#22735=CARTESIAN_POINT ( 'NONE',  ( 1.091512329210375665, -26.22489388037982749, 7.748216051605120391 ) ) ;
#22736=CARTESIAN_POINT ( 'NONE',  ( 1.147042297102817354, -26.11394895998986598, 6.875671892026061549 ) ) ;
#22737=VERTEX_POINT ( 'NONE', #20990 ) ;
#22739=PLANE ( 'NONE',  #30013 ) ;
#22741=CARTESIAN_POINT ( 'NONE',  ( 0.4741610271200560334, -32.84809465111302984, 6.894806418505347700 ) ) ;
#22742=ORIENTED_EDGE ( 'NONE', *, *, #5627, .T. ) ;
#22751=ADVANCED_FACE ( 'NONE', ( #20777 ), #27160, .F. ) ;
#22753=CARTESIAN_POINT ( 'NONE',  ( -1.482088180267138622, -30.76652202637871625, 7.695279973900954751 ) ) ;
#22759=AXIS2_PLACEMENT_3D ( 'NONE', #38193, #1167, #9994 ) ;
#22760=EDGE_CURVE ( 'NONE', #22022, #13175, #22048, .T. ) ;
#22762=EDGE_LOOP ( 'NONE', ( #10345, #23759, #35923, #23706 ) ) ;
#22763=CARTESIAN_POINT ( 'NONE',  ( -1.007170258006738095, -31.76429153184023946, 7.785593909369613819 ) ) ;
#22765=CYLINDRICAL_SURFACE ( 'NONE', #13468, 0.09010775117053029803 ) ;
#22766=CARTESIAN_POINT ( 'NONE',  ( 3.848298546108438245, -32.20554951821143419, 6.894806418505343260 ) ) ;
#22768=CARTESIAN_POINT ( 'NONE',  ( 5.195486027961456088, -29.75516796582088475, 6.989977667959438534 ) ) ;
#22770=CARTESIAN_POINT ( 'NONE',  ( 3.469506075866656936, -32.58990542741018714, 7.743886751744251562 ) ) ;
#22774=FACE_OUTER_BOUND ( 'NONE', #9606, .T. ) ;
#22777=VECTOR ( 'NONE', #27769, 1000.000000000000114 ) ;
#22780=ORIENTED_EDGE ( 'NONE', *, *, #14619, .F. ) ;
#22781=CARTESIAN_POINT ( 'NONE',  ( 2.863753781421408462, -26.26893261765590282, 7.700536657684216024 ) ) ;
#22785=ORIENTED_EDGE ( 'NONE', *, *, #26729, .T. ) ;
#22790=CARTESIAN_POINT ( 'NONE',  ( -1.289625865479514744, -31.18854093558072904, 6.866852738645443210 ) ) ;
#22793=CARTESIAN_POINT ( 'NONE',  ( 0.9037396047256786025, -32.97806002456835017, 6.955226052476382925 ) ) ;
#22794=FACE_OUTER_BOUND ( 'NONE', #12385, .T. ) ;
#22798=CARTESIAN_POINT ( 'NONE',  ( 5.200364047366366371, -29.55642757665872722, 7.635761828346577573 ) ) ;
#22802=CARTESIAN_POINT ( 'NONE',  ( -1.032131559973606727, -31.59312701384676103, 6.929923840112067523 ) ) ;
#22811=CARTESIAN_POINT ( 'NONE',  ( 2.924663588294490246, -32.84882548658472246, 7.730015791551949178 ) ) ;
#22812=CARTESIAN_POINT ( 'NONE',  ( -1.641630102650725176, -30.19515113050700705, 7.680992449362118890 ) ) ;
#22815=CARTESIAN_POINT ( 'NONE',  ( -0.3498495389373063036, -26.85764010844238214, 6.882085323592685100 ) ) ;
#22825=CARTESIAN_POINT ( 'NONE',  ( 4.817241837858415643, -30.92832464666959780, 6.949473656533212917 ) ) ;
#22826=CARTESIAN_POINT ( 'NONE',  ( -1.230064425333113221, -27.65618090132562301, 6.951256099901589991 ) ) ;
#22827=VERTEX_POINT ( 'NONE', #31843 ) ;
#22831=ORIENTED_EDGE ( 'NONE', *, *, #10918, .T. ) ;
#22840=CARTESIAN_POINT ( 'NONE',  ( -0.06024744239608810503, -32.47858221735037887, 7.784476445165072533 ) ) ;
#22841=CARTESIAN_POINT ( 'NONE',  ( 4.620198719170100610, -31.31197426661971761, 6.894806418505346812 ) ) ;
#22842=CARTESIAN_POINT ( 'NONE',  ( 4.381563664431031846, -27.47916279290977570, 7.754798119455333705 ) ) ;
#22847=CARTESIAN_POINT ( 'NONE',  ( 2.333773081392421567, -33.01214383003427599, 7.737115613922531665 ) ) ;
#22851=ADVANCED_FACE ( 'NONE', ( #26271 ), #29353, .F. ) ;
#22855=ORIENTED_EDGE ( 'NONE', *, *, #32792, .T. ) ;
#22858=CARTESIAN_POINT ( 'NONE',  ( 5.078732710124126193, -29.18678336023061348, 6.969307238440507035 ) ) ;
#22865=VECTOR ( 'NONE', #30341, 999.9999999999998863 ) ;
#22872=CARTESIAN_POINT ( 'NONE',  ( 1.665030044868864634, -33.05676478451892564, 7.783750581861600182 ) ) ;
#22876=ORIENTED_EDGE ( 'NONE', *, *, #7526, .T. ) ;
#22878=CARTESIAN_POINT ( 'NONE',  ( 2.294856720451861953, -26.12078399496891734, 7.635761828346576685 ) ) ;
#22879=AXIS2_PLACEMENT_3D ( 'NONE', #18665, #12700, #28352 ) ;
#22882=CARTESIAN_POINT ( 'NONE',  ( 3.837038864732983612, -32.34206510565962844, 6.875780273367530171 ) ) ;
#22890=CARTESIAN_POINT ( 'NONE',  ( 2.425674012770692833, -26.14588693425077892, 6.865706122441728176 ) ) ;
#22894=CARTESIAN_POINT ( 'NONE',  ( 4.407694157253644107, -27.51309448911002065, 6.876076431790002275 ) ) ;
#22896=CARTESIAN_POINT ( 'NONE',  ( 1.822194502883780931, -26.07228119081829476, 7.754798119455333705 ) ) ;
#22897=CARTESIAN_POINT ( 'NONE',  ( -1.799583860900191734, -29.58343279012807159, 7.635761828346577573 ) ) ;
#22901=CARTESIAN_POINT ( 'NONE',  ( -0.1134167689795140821, -32.56329063961136683, 6.867280401193707640 ) ) ;
#22903=CARTESIAN_POINT ( 'NONE',  ( -1.699609906766908818, -29.57706174694755674, 7.761939382804113663 ) ) ;
#22904=CARTESIAN_POINT ( 'NONE',  ( 3.578914694166553723, -26.73600263956173606, 6.959317978105163505 ) ) ;
#22905=DIRECTION ( 'NONE',  ( -0.000000000000000000, -0.000000000000000000, -1.000000000000000000 ) ) ;
#22907=CARTESIAN_POINT ( 'NONE',  ( 3.935268700167234623, -26.87636050501711793, 7.643192810543824045 ) ) ;
#22909=CARTESIAN_POINT ( 'NONE',  ( 1.089753260929022360, -32.91465995119874322, 7.779495906702012853 ) ) ;
#22911=CARTESIAN_POINT ( 'NONE',  ( 3.313913495458963077, -32.56269280434947433, 7.774064877406527074 ) ) ;
#22922=CARTESIAN_POINT ( 'NONE',  ( 3.076197136650148156, -26.35167677831728383, 6.951256099901586438 ) ) ;
#22927=CARTESIAN_POINT ( 'NONE',  ( 0.4796627190948448138, -26.28970783387809007, 7.651421919295143148 ) ) ;
#22928=CARTESIAN_POINT ( 'NONE',  ( -1.449731085724313751, -28.29053751634241820, 6.863904403958575706 ) ) ;
#22932=CARTESIAN_POINT ( 'NONE',  ( 3.497962998608483698, -26.56680986448170501, 6.875671892026061549 ) ) ;
#22933=DIRECTION ( 'NONE',  ( -0.000000000000000000, -0.000000000000000000, -1.000000000000000000 ) ) ;
#22940=CLOSED_SHELL ( 'NONE', ( #34578, #2805, #2694, #11871, #32109, #21545, #10687, #26953, #22751, #10592, #5242, #36723, #12884, #16593, #15200, #22851, #4149, #6070, #32381, #28953, #6018, #27933, #4392, #8735, #14947, #6304, #3770, #27565, #32325, #12226, #24206, #7907, #13168, #12009, #31720, #26686, #36963, #32380, #23961, #22719, #19215, #31259, #27697, #38164, #39493, #36017, #11744, #4791, #38833, #29211, #19332, #14118, #16952, #37094, #8769, #9579, #2590, #26773, #16214, #40104, #34008, #36451, #1798, #25153, #14175, #13214, #34283, #36539, #11693, #18872, #3344, #2211, #8584, #2591, #26920, #24430, #32548, #6105, #8109, #13192, #35280, #3511, #39640, #35002, #19895, #12347, #11360, #5687, #26532, #21821, #27845, #20435, #5069, #21695, #30211, #19734, #16191, #39440, #34062, #6058, #39508, #8816, #26776, #27227, #5263, #21022, #15150, #22689, #22119, #24018, #14860, #36705, #25991, #5869, #33213, #31942, #33762, #4575, #26239, #29568, #30450, #2577, #13487, #6890, #36259, #26832, #26236, #4258, #21941, #33869, #4075, #1502, #11938, #36917, #16348, #8687, #16581, #5901, #35362, #34773, #36196, #33291, #8304, #37690, #18215, #31576, #284, #5111, #10615, #4169, #16457, #7302, #11349, #16653, #15431, #23244, #36991, #4331, #9385, #13299, #24665, #29146, #7172, #27007, #10259, #38334, #1136, #19545, #19202, #27471, #33715, #20636, #16411, #36535, #5563, #19542, #14292, #1549, #24261, #15385, #20716, #9479, #37744, #11506, #30300, #29121, #30314, #25191, #24475, #8830, #29071, #11190, #6276, #6939, #8626, #15189, #19888, #7163, #16184, #1048, #29846, #1812, #4707, #31868, #25254, #6334, #10875, #25437, #14076, #4658, #4612, #29048, #30374, #35762, #35231, #6492, #16139, #3030, #16913, #33488, #38967, #27793, #17313, #13726, #298, #30137, #18365, #688, #1201, #28926, #14623 ) ) ;
#22941=CARTESIAN_POINT ( 'NONE',  ( 0.4695943777967604427, -26.29347754267606874, 7.697032948437506406 ) ) ;
#22949=EDGE_CURVE ( 'NONE', #19287, #24258, #17082, .T. ) ;
#22951=CARTESIAN_POINT ( 'NONE',  ( 3.301837905240542881, -32.68206207414233688, 7.013842709614101167 ) ) ;
#22952=ORIENTED_EDGE ( 'NONE', *, *, #21391, .F. ) ;
#22954=CARTESIAN_POINT ( 'NONE',  ( -1.434056508659582674, -31.14254555582535389, 7.387053503561885393 ) ) ;
#22955=ORIENTED_EDGE ( 'NONE', *, *, #40511, .T. ) ;
#22957=CARTESIAN_POINT ( 'NONE',  ( -1.642550015356792681, -30.60663237321507069, 7.013842709614101167 ) ) ;
#22961=CARTESIAN_POINT ( 'NONE',  ( -1.749609906766908640, -29.56993018339339940, 7.800000000000000711 ) ) ;
#22963=CARTESIAN_POINT ( 'NONE',  ( 5.112182647635235000, -30.35077483426318778, 6.903112506833887885 ) ) ;
#22970=AXIS2_PLACEMENT_3D ( 'NONE', #15798, #34154, #2856 ) ;
#22971=CARTESIAN_POINT ( 'NONE',  ( 2.737092283054774811, -32.91287029198328185, 7.013842709614101167 ) ) ;
#22972=ORIENTED_EDGE ( 'NONE', *, *, #14119, .F. ) ;
#22981=CARTESIAN_POINT ( 'NONE',  ( 2.919829066420930541, -26.30113654672046408, 7.781480525794719050 ) ) ;
#22991=CARTESIAN_POINT ( 'NONE',  ( -1.271991893282980790, -31.22067102502625957, 6.887041543973314361 ) ) ;
#22996=CARTESIAN_POINT ( 'NONE',  ( 1.123288416806107026, -32.92059484209399045, 7.635761828346577573 ) ) ;
#22999=ORIENTED_EDGE ( 'NONE', *, *, #24548, .F. ) ;
#23002=CARTESIAN_POINT ( 'NONE',  ( 4.281682929012584182, -27.35702998321412593, 7.693875151218753317 ) ) ;
#23004=CARTESIAN_POINT ( 'NONE',  ( 5.144476794586663182, -28.94681611416600830, 7.638132480492515697 ) ) ;
#23005=CYLINDRICAL_SURFACE ( 'NONE', #12266, 3.399999999999999911 ) ;
#23009=CARTESIAN_POINT ( 'NONE',  ( 2.918216031185672410, -32.85122898407183101, 7.743886751744253338 ) ) ;
#23010=CARTESIAN_POINT ( 'NONE',  ( 5.123097946374971734, -30.30141562551846235, 7.750000000000000888 ) ) ;
#23013=CARTESIAN_POINT ( 'NONE',  ( 1.799419147782851391, -26.17136002503600523, 7.774064877406527962 ) ) ;
#23021=EDGE_CURVE ( 'NONE', #22465, #13345, #28627, .T. ) ;
#23024=CARTESIAN_POINT ( 'NONE',  ( 4.826555071938813946, -30.90675198375193844, 7.013842709614101167 ) ) ;
#23028=CARTESIAN_POINT ( 'NONE',  ( 4.907464300517769829, -30.69894525369553762, 7.695279973900954751 ) ) ;
#23032=EDGE_CURVE ( 'NONE', #4122, #12351, #35861, .T. ) ;
#23038=VERTEX_POINT ( 'NONE', #23964 ) ;
#23042=CARTESIAN_POINT ( 'NONE',  ( 3.974925472835492801, -32.23009724712022006, 7.670465701733754749 ) ) ;
#23048=CARTESIAN_POINT ( 'NONE',  ( 2.343537225896454856, -33.01033157941493101, 7.697032948437507294 ) ) ;
#23049=B_SPLINE_CURVE_WITH_KNOTS ( 'NONE', 3,
 ( #12469, #18431, #2417, #24618, #31422, #25039, #15142, #24830, #36768, #21952 ),
 .UNSPECIFIED., .F., .F.,
 ( 4, 3, 3, 4 ),
 ( 1.939479807224432123E-18, 3.025570593003372544E-05, 6.051145698344380657E-05, 6.468151674593654050E-05 ),
 .UNSPECIFIED. ) ;
#23050=ORIENTED_EDGE ( 'NONE', *, *, #32614, .F. ) ;
#23054=CARTESIAN_POINT ( 'NONE',  ( 1.124000490775577399, -33.02214389350386625, 7.724038915126860694 ) ) ;
#23057=CARTESIAN_POINT ( 'NONE',  ( -1.784597664094826008, -29.51857049915745890, 7.785344483711591934 ) ) ;
#23058=ORIENTED_EDGE ( 'NONE', *, *, #7396, .T. ) ;
#23059=DIRECTION ( 'NONE',  ( 0.6502177225477924205, -0.3754033771448251899, -0.6605219282605403475 ) ) ;
#23071=B_SPLINE_CURVE_WITH_KNOTS ( 'NONE', 3,
 ( #7125, #6922, #31845, #13290, #22385, #9387, #37792, #32260, #22584, #154, #19076, #4060, #12895, #16575, #19279, #22182, #13099, #37590, #16187 ),
 .UNSPECIFIED., .F., .F.,
 ( 4, 3, 3, 3, 3, 3, 4 ),
 ( 1.226634733346699349E-18, 2.546128104244621453E-05, 5.711050680483870356E-05, 8.113074941675817360E-05, 0.0001053129305727074034, 0.0001360598016347105499, 0.0001612931755701972581 ),
 .UNSPECIFIED. ) ;
#23084=CARTESIAN_POINT ( 'NONE',  ( 3.823044550204501402, -32.35280395774920237, 6.887547729233690852 ) ) ;
#23085=ORIENTED_EDGE ( 'NONE', *, *, #21442, .F. ) ;
#23091=CARTESIAN_POINT ( 'NONE',  ( 2.445140233331022372, -26.15008410077153300, 6.872971584836693459 ) ) ;
#23095=CARTESIAN_POINT ( 'NONE',  ( -1.666958026621576883, -30.04000107135736641, 7.754798119455333705 ) ) ;
#23096=AXIS2_PLACEMENT_3D ( 'NONE', #4262, #2348, #33640 ) ;
#23099=DIRECTION ( 'NONE',  ( -0.000000000000000000, -0.000000000000000000, -1.000000000000000000 ) ) ;
#23101=CARTESIAN_POINT ( 'NONE',  ( 3.739317481034212243, -32.29073431218959911, 7.013842709614101167 ) ) ;
#23103=CARTESIAN_POINT ( 'NONE',  ( 4.514135614585971013, -27.47691543170328643, 7.387053503561888057 ) ) ;
#23105=CARTESIAN_POINT ( 'NONE',  ( 4.674695785371929979, -31.40593021786562744, 7.771081512783701406 ) ) ;
#23106=CARTESIAN_POINT ( 'NONE',  ( 0.6657407460327561255, -26.33116491667136216, 6.865312560952602894 ) ) ;
#23110=CARTESIAN_POINT ( 'NONE',  ( 1.070632901679560378, -32.91111266939319080, 7.784838882742139532 ) ) ;
#23111=CARTESIAN_POINT ( 'NONE',  ( 4.712346640638399364, -31.35267092476172479, 6.887161170156907097 ) ) ;
#23112=CARTESIAN_POINT ( 'NONE',  ( 0.6225211420409756391, -26.24003551177748861, 7.750000000000000888 ) ) ;
#23113=CARTESIAN_POINT ( 'NONE',  ( -1.546174839641468735, -28.26456800474412034, 7.761113333116787416 ) ) ;
#23115=CARTESIAN_POINT ( 'NONE',  ( -0.4578616284939905356, -32.19708638888766217, 7.680992449362111785 ) ) ;
#23120=CARTESIAN_POINT ( 'NONE',  ( 4.722665460610376620, -27.80475174052855536, 7.640616322432100205 ) ) ;
#23122=FACE_OUTER_BOUND ( 'NONE', #12656, .T. ) ;
#23127=CARTESIAN_POINT ( 'NONE',  ( 0.4012375803829261178, -32.81988445204935800, 6.864673517077424236 ) ) ;
#23133=AXIS2_PLACEMENT_3D ( 'NONE', #2285, #8634, #15226 ) ;
#23138=CARTESIAN_POINT ( 'NONE',  ( -1.707939823346567021, -28.77413670247031519, 6.966757512882405301 ) ) ;
#23141=ORIENTED_EDGE ( 'NONE', *, *, #31294, .T. ) ;
#23146=EDGE_CURVE ( 'NONE', #9291, #34893, #30158, .T. ) ;
#23151=CARTESIAN_POINT ( 'NONE',  ( -1.035018467416049415, -31.74189774292361577, 7.776484688137389689 ) ) ;
#23155=CARTESIAN_POINT ( 'NONE',  ( 3.301369968908216990, -32.68230282137928810, 6.895394898881662016 ) ) ;
#23156=CARTESIAN_POINT ( 'NONE',  ( -1.090829593295360223, -31.68159764409877255, 6.903112506833894102 ) ) ;
#23157=CARTESIAN_POINT ( 'NONE',  ( 5.196611068567014158, -29.73267931344627613, 6.887547729233683746 ) ) ;
#23158=CARTESIAN_POINT ( 'NONE',  ( -0.5641756119095632238, -26.90127093817460135, 7.643192810543826710 ) ) ;
#23164=ORIENTED_EDGE ( 'NONE', *, *, #23953, .F. ) ;
#23171=ORIENTED_EDGE ( 'NONE', *, *, #8536, .T. ) ;
#23172=CARTESIAN_POINT ( 'NONE',  ( 2.863657326339113851, -26.26889862419239918, 7.698786668945012401 ) ) ;
#23175=CARTESIAN_POINT ( 'NONE',  ( -2.673316637388258865, -27.10729750018004935, 7.695279973900954751 ) ) ;
#23176=ORIENTED_EDGE ( 'NONE', *, *, #1328, .F. ) ;
#23177=ORIENTED_EDGE ( 'NONE', *, *, #4047, .T. ) ;
#23184=EDGE_CURVE ( 'NONE', #19049, #9920, #27374, .T. ) ;
#23186=CARTESIAN_POINT ( 'NONE',  ( 4.042889426911806972, -27.10564586790783892, 6.949473656533219135 ) ) ;
#23189=CARTESIAN_POINT ( 'NONE',  ( 3.384110555093582384, -26.61610462891116313, 7.748216051605124832 ) ) ;
#23193=CARTESIAN_POINT ( 'NONE',  ( -0.5399441734843601903, -32.25896884755352545, 7.756742906098588186 ) ) ;
#23195=CARTESIAN_POINT ( 'NONE',  ( -0.01704589846277644594, -26.63557199280749899, 7.643333865083955736 ) ) ;
#23199=( BOUNDED_CURVE ( )  B_SPLINE_CURVE ( 3, ( #28703, #32010, #9761, #13049 ),
 .UNSPECIFIED., .F., .F. ) 
 B_SPLINE_CURVE_WITH_KNOTS ( ( 4, 4 ),
 ( 1.347909859412852907, 1.534781240595298080 ),
 .UNSPECIFIED. ) 
 CURVE ( )  GEOMETRIC_REPRESENTATION_ITEM ( )  RATIONAL_B_SPLINE_CURVE ( ( 1.000000000000000000, 0.9970920404276226723, 0.9970920404276226723, 1.000000000000000000 ) ) 
 REPRESENTATION_ITEM ( '' )  );
#23200=CARTESIAN_POINT ( 'NONE',  ( -1.284247711295874561, -27.76865114928376599, 7.784725160561910329 ) ) ;
#23201=CARTESIAN_POINT ( 'NONE',  ( 2.388817387744127441, -25.35382237095210201, 7.695279973900954751 ) ) ;
#23204=EDGE_CURVE ( 'NONE', #10597, #13756, #10672, .T. ) ;
#23205=EDGE_CURVE ( 'NONE', #2658, #40515, #30945, .T. ) ;
#23206=CARTESIAN_POINT ( 'NONE',  ( 4.488362440207297688, -27.45398732327946334, 7.011627023500181188 ) ) ;
#23208=CARTESIAN_POINT ( 'NONE',  ( 4.890934407267558903, -28.39499951105307574, 7.756377446753164762 ) ) ;
#23218=CARTESIAN_POINT ( 'NONE',  ( -2.742979246814043925, -31.14891988278930413, 7.695279973900954751 ) ) ;
#23219=CARTESIAN_POINT ( 'NONE',  ( -1.232229479062399102, -27.65950027256457844, 6.980586498568968068 ) ) ;
#23226=CARTESIAN_POINT ( 'NONE',  ( 3.657089259928787417, -24.90412260081853546, 6.894806418505347700 ) ) ;
#23227=ORIENTED_EDGE ( 'NONE', *, *, #40215, .T. ) ;
#23234=VECTOR ( 'NONE', #20454, 1000.000000000000000 ) ;
#23235=CARTESIAN_POINT ( 'NONE',  ( -0.09836077524968195318, -32.45515033324894461, 7.761597726988851420 ) ) ;
#23237=CARTESIAN_POINT ( 'NONE',  ( 3.976673778722537023, -32.22860238476790329, 7.678495282201407868 ) ) ;
#23243=CARTESIAN_POINT ( 'NONE',  ( 5.150202707224498688, -30.16051711886163744, 7.750000000000001776 ) ) ;
#23244=ADVANCED_FACE ( 'NONE', ( #34249 ), #18556, .F. ) ;
#23247=EDGE_CURVE ( 'NONE', #29003, #7610, #14095, .T. ) ;
#23250=CARTESIAN_POINT ( 'NONE',  ( 0.4209974261821289865, -32.72005136235081579, 6.863904403958575706 ) ) ;
#23255=EDGE_CURVE ( 'NONE', #7785, #28942, #38166, .T. ) ;
#23267=AXIS2_PLACEMENT_3D ( 'NONE', #15519, #21709, #40628 ) ;
#23268=CARTESIAN_POINT ( 'NONE',  ( 4.988271557043087334, -28.40293458425108142, 7.781480525794716385 ) ) ;
#23269=VERTEX_POINT ( 'NONE', #13814 ) ;
#23272=CARTESIAN_POINT ( 'NONE',  ( 4.536655203520439272, -25.19670069055390016, 6.894806418505347700 ) ) ;
#23276=EDGE_LOOP ( 'NONE', ( #16435, #10244, #36052, #39832, #5906 ) ) ;
#23278=DIRECTION ( 'NONE',  ( -0.9396926207859057634, -0.3420201433256757073, -0.000000000000000000 ) ) ;
#23283=ORIENTED_EDGE ( 'NONE', *, *, #36793, .T. ) ;
#23284=CARTESIAN_POINT ( 'NONE',  ( 2.495056794208367013, -26.16133723403751432, 6.935328752148349096 ) ) ;
#23290=CARTESIAN_POINT ( 'NONE',  ( 2.338742698598176073, -33.27093018339341057, 6.894806418505347700 ) ) ;
#23296=CARTESIAN_POINT ( 'NONE',  ( -0.2081541720287059805, -32.50377728021632606, 6.921725064902957136 ) ) ;
#23298=CARTESIAN_POINT ( 'NONE',  ( -1.699583094839331787, -29.58343279012807159, 7.635761828346577573 ) ) ;
#23301=EDGE_CURVE ( 'NONE', #4851, #30829, #33441, .T. ) ;
#23303=CYLINDRICAL_SURFACE ( 'NONE', #37305, 0.09010775117052866046 ) ;
#23309=CARTESIAN_POINT ( 'NONE',  ( -1.699609906766908818, -29.56993018339339940, 7.620413589471895399 ) ) ;
#23310=CARTESIAN_POINT ( 'NONE',  ( -1.799560655197548487, -29.58853437876398118, 7.748475685504735644 ) ) ;
#23317=B_SPLINE_CURVE_WITH_KNOTS ( 'NONE', 3,
 ( #19465, #22770, #32243, #16558, #40664, #12466, #25037, #37571, #3446, #15962 ),
 .UNSPECIFIED., .F., .F.,
 ( 4, 3, 3, 4 ),
 ( 0.0001585009270395762383, 0.0001815657551981843026, 0.0002118214035944171133, 0.0002170292169044785754 ),
 .UNSPECIFIED. ) ;
#23318=CARTESIAN_POINT ( 'NONE',  ( -1.347936336206764008, -27.85013040703412912, 7.678495282201406091 ) ) ;
#23321=FACE_OUTER_BOUND ( 'NONE', #6438, .T. ) ;
#23324=CARTESIAN_POINT ( 'NONE',  ( 5.044480966521144971, -28.53694452721211050, 7.009310105710484073 ) ) ;
#23325=DIRECTION ( 'NONE',  ( -0.3420201433256601087, -0.9396926207859114255, -0.000000000000000000 ) ) ;
#23327=EDGE_LOOP ( 'NONE', ( #36668, #8725, #12283, #3922, #12653 ) ) ;
#23343=CARTESIAN_POINT ( 'NONE',  ( 5.046365345827218185, -28.96623356337001809, 7.635761828346577573 ) ) ;
#23347=CARTESIAN_POINT ( 'NONE',  ( -0.8688903936063803179, -27.19321022093548734, 7.013842709614101167 ) ) ;
#23357=CARTESIAN_POINT ( 'NONE',  ( 5.113695884919195578, -30.34410301451193703, 6.895394898881665569 ) ) ;
#23359=CARTESIAN_POINT ( 'NONE',  ( 2.802452400329403126, -32.78637555231541256, 6.880147297696982633 ) ) ;
#23361=AXIS2_PLACEMENT_3D ( 'NONE', #17784, #5245, #26667 ) ;
#23367=CARTESIAN_POINT ( 'NONE',  ( -0.8725572984338751947, -27.34733221711291051, 6.894806418505345036 ) ) ;
#23371=CARTESIAN_POINT ( 'NONE',  ( 2.940588421764992688, -26.31267895086665831, 7.785344483711591934 ) ) ;
#23373=CARTESIAN_POINT ( 'NONE',  ( 5.054699967764599400, -30.12545289942340077, 7.680992449362116226 ) ) ;
#23375=AXIS2_PLACEMENT_3D ( 'NONE', #21152, #39663, #14539 ) ;
#23376=ORIENTED_EDGE ( 'NONE', *, *, #33482, .T. ) ;
#23380=PLANE ( 'NONE',  #7886 ) ;
#23384=CARTESIAN_POINT ( 'NONE',  ( 3.922988059513587089, -26.99698279172644177, 6.894806418505345924 ) ) ;
#23386=B_SPLINE_CURVE_WITH_KNOTS ( 'NONE', 3,
 ( #15835, #22637, #34599, #34803, #32117, #19331, #9859, #28808, #6167, #12948 ),
 .UNSPECIFIED., .F., .F.,
 ( 4, 3, 3, 4 ),
 ( 0.0005050348086185349949, 0.0005143352185143347608, 0.0005445898203825249879, 0.0005634294782181770286 ),
 .UNSPECIFIED. ) ;
#23389=CARTESIAN_POINT ( 'NONE',  ( 5.200200943668277453, -29.53353846251400228, 7.690468881945117019 ) ) ;
#23391=ORIENTED_EDGE ( 'NONE', *, *, #20675, .T. ) ;
#23399=DIRECTION ( 'NONE',  ( -0.4999999999999999445, -0.8660254037844387076, 0.000000000000000000 ) ) ;
#23406=CARTESIAN_POINT ( 'NONE',  ( 4.250519439829707480, -31.81867212404081968, 6.870716933885661959 ) ) ;
#23407=CARTESIAN_POINT ( 'NONE',  ( -1.799609906766908685, -29.56993018339339940, 7.800000000000000711 ) ) ;
#23413=CARTESIAN_POINT ( 'NONE',  ( 4.226378548430531623, -31.84575678386042341, 7.757178535559535959 ) ) ;
#23416=CARTESIAN_POINT ( 'NONE',  ( -0.4007890326520501811, -26.77081244048443409, 6.931070083220551403 ) ) ;
#23418=CARTESIAN_POINT ( 'NONE',  ( 2.308148104750579854, -26.12639665259444044, 7.767720160662275219 ) ) ;
#23420=CARTESIAN_POINT ( 'NONE',  ( 1.713892699967800581, -32.96990337146582561, 7.635761828346577573 ) ) ;
#23423=DIRECTION ( 'NONE',  ( -0.7660444431189726844, -0.6427876096865458022, -0.000000000000000000 ) ) ;
#23430=CARTESIAN_POINT ( 'NONE',  ( -0.7800240848564992113, -27.24451720821412337, 7.013842709614101167 ) ) ;
#23433=CARTESIAN_POINT ( 'NONE',  ( 5.039926880157825195, -30.20828278875847062, 6.894806418505346812 ) ) ;
#23436=CARTESIAN_POINT ( 'NONE',  ( -1.250501372580467230, -27.88106231952350100, 7.756377446753163873 ) ) ;
#23438=CARTESIAN_POINT ( 'NONE',  ( 4.654912386708397243, -31.25244092439575994, 7.643333865083952183 ) ) ;
#23444=CARTESIAN_POINT ( 'NONE',  ( 3.147222565855531062, -32.76435434460020701, 7.501983001166816045 ) ) ;
#23449=CARTESIAN_POINT ( 'NONE',  ( 5.123392144880668297, -30.30003903553068767, 7.751599049952197618 ) ) ;
#23457=CARTESIAN_POINT ( 'NONE',  ( -0.5074448109832514486, -26.98430194541812099, 7.730758795053803922 ) ) ;
#23459=CARTESIAN_POINT ( 'NONE',  ( 2.277491769660097365, -26.21926552469281191, 7.635761828346577573 ) ) ;
#23460=EDGE_CURVE ( 'NONE', #7585, #22592, #26373, .T. ) ;
#23463=ORIENTED_EDGE ( 'NONE', *, *, #23927, .F. ) ;
#23466=CARTESIAN_POINT ( 'NONE',  ( -1.642550015356792681, -30.60663237321507069, 7.013842709614101167 ) ) ;
#23472=AXIS2_PLACEMENT_3D ( 'NONE', #4280, #29186, #29387 ) ;
#23473=ORIENTED_EDGE ( 'NONE', *, *, #24312, .F. ) ;
#23475=CARTESIAN_POINT ( 'NONE',  ( 4.911690090265110165, -28.45299136274915952, 6.894806418505345924 ) ) ;
#23478=CARTESIAN_POINT ( 'NONE',  ( 4.787516329918978464, -27.92079356116780886, 6.865482280155368322 ) ) ;
#23483=DIRECTION ( 'NONE',  ( -0.9848077530122067991, -0.1736481776669374644, -0.000000000000000000 ) ) ;
#23484=CARTESIAN_POINT ( 'NONE',  ( -1.226003372003152458, -31.30088982666143949, 7.691066658568947112 ) ) ;
#23493=VECTOR ( 'NONE', #174, 1000.000000000000114 ) ;
#23494=DIRECTION ( 'NONE',  ( -0.000000000000000000, -0.000000000000000000, -1.000000000000000000 ) ) ;
#23503=AXIS2_PLACEMENT_3D ( 'NONE', #6452, #22310, #37710 ) ;
#23505=VECTOR ( 'NONE', #37137, 1000.000000000000227 ) ;
#23509=CARTESIAN_POINT ( 'NONE',  ( 0.1158819994041509066, -26.44913956231825480, 6.980586498568971621 ) ) ;
#23512=CARTESIAN_POINT ( 'NONE',  ( 4.977103583311326851, -28.33982894766831606, 7.710604733652631992 ) ) ;
#23513=CARTESIAN_POINT ( 'NONE',  ( -1.594457770366995319, -28.38926191680453925, 7.750000000000000888 ) ) ;
#23520=CARTESIAN_POINT ( 'NONE',  ( 3.055030623276686619, -26.34271016697629619, 7.013842709614101167 ) ) ;
#23522=EDGE_LOOP ( 'NONE', ( #20821, #23058, #16968, #23171 ) ) ;
#23524=CARTESIAN_POINT ( 'NONE',  ( 3.816341850769968236, -32.23127348326596575, 7.778050822775631090 ) ) ;
#23525=CARTESIAN_POINT ( 'NONE',  ( 5.900850858889974404, -30.34709628986367846, 7.695279973900954751 ) ) ;
#23526=CARTESIAN_POINT ( 'NONE',  ( 5.048915835387577822, -28.55141393210982415, 6.980586498568967180 ) ) ;
#23529=VECTOR ( 'NONE', #6587, 1000.000000000000000 ) ;
#23530=CARTESIAN_POINT ( 'NONE',  ( 1.280274463769470294, -26.09523354690790242, 6.931070083220559397 ) ) ;
#23533=EDGE_CURVE ( 'NONE', #10351, #22200, #31776, .T. ) ;
#23534=DIRECTION ( 'NONE',  ( -3.491481338843133750E-15, 1.000000000000000000, -0.000000000000000000 ) ) ;
#23545=CARTESIAN_POINT ( 'NONE',  ( -0.8455530167579952128, -27.31644983497921331, 7.778050822775635531 ) ) ;
#23550=ORIENTED_EDGE ( 'NONE', *, *, #39719, .F. ) ;
#23554=VERTEX_POINT ( 'NONE', #15224 ) ;
#23555=CARTESIAN_POINT ( 'NONE',  ( 5.169453744383599059, -29.10560552944284396, 6.875780273367533724 ) ) ;
#23559=CARTESIAN_POINT ( 'NONE',  ( 3.281055722528557705, -32.69266877113672365, 6.961115707816233567 ) ) ;
#23563=VECTOR ( 'NONE', #32638, 1000.000000000000227 ) ;
#23568=EDGE_LOOP ( 'NONE', ( #5552, #23650 ) ) ;
#23573=CARTESIAN_POINT ( 'NONE',  ( -0.9325302353475311001, -27.26388753469717940, 6.867280401193709416 ) ) ;
#23575=CARTESIAN_POINT ( 'NONE',  ( -1.796521113867400654, -29.56993018341788826, 7.767301406056523305 ) ) ;
#23580=ORIENTED_EDGE ( 'NONE', *, *, #27271, .F. ) ;
#23585=ORIENTED_EDGE ( 'NONE', *, *, #36035, .T. ) ;
#23586=AXIS2_PLACEMENT_3D ( 'NONE', #549, #25645, #19864 ) ;
#23587=CARTESIAN_POINT ( 'NONE',  ( 0.3896649785617538608, -32.81498557016907114, 7.754798119455333705 ) ) ;
#23588=CARTESIAN_POINT ( 'NONE',  ( 3.949132033880527803, -27.01980083679679723, 6.870716933885664623 ) ) ;
#23591=ORIENTED_EDGE ( 'NONE', *, *, #9205, .F. ) ;
#23595=CARTESIAN_POINT ( 'NONE',  ( 1.527538316465248291, -32.96553355588380185, 6.882085323592685100 ) ) ;
#23596=CARTESIAN_POINT ( 'NONE',  ( 2.468116271650433902, -26.25773128481726459, 6.887945620086119547 ) ) ;
#23599=CARTESIAN_POINT ( 'NONE',  ( 3.858201203583684791, -26.94241211265677194, 7.695279973900954751 ) ) ;
#23601=CARTESIAN_POINT ( 'NONE',  ( 0.5732355268899250733, -26.25637850312180177, 6.867280401193708528 ) ) ;
#23603=CARTESIAN_POINT ( 'NONE',  ( 3.977009164777316919, -32.22831426950175882, 7.710604733652632881 ) ) ;
#23608=DIRECTION ( 'NONE',  ( 0.5000000000000101030, -0.8660254037844328234, -0.000000000000000000 ) ) ;
#23614=ORIENTED_EDGE ( 'NONE', *, *, #32002, .F. ) ;
#23616=CARTESIAN_POINT ( 'NONE',  ( 1.296126803379346715, -26.19404450011727548, 6.895222827070020877 ) ) ;
#23617=B_SPLINE_CURVE_WITH_KNOTS ( 'NONE', 3,
 ( #15296, #21279, #18576, #27848 ),
 .UNSPECIFIED., .F., .F.,
 ( 4, 4 ),
 ( 0.000000000000000000, 6.391136169994552113E-06 ),
 .UNSPECIFIED. ) ;
#23618=ORIENTED_EDGE ( 'NONE', *, *, #7385, .F. ) ;
#23619=ORIENTED_EDGE ( 'NONE', *, *, #16173, .F. ) ;
#23627=CARTESIAN_POINT ( 'NONE',  ( 5.039465595983135593, -30.21069599340067313, 6.892063359921932530 ) ) ;
#23629=CARTESIAN_POINT ( 'NONE',  ( -1.198187176124504205, -27.79278364650808442, 7.778050822775631978 ) ) ;
#23630=FACE_OUTER_BOUND ( 'NONE', #16615, .T. ) ;
#23632=ORIENTED_EDGE ( 'NONE', *, *, #30264, .F. ) ;
#23633=CARTESIAN_POINT ( 'NONE',  ( 2.342808000876349439, -33.01046787075163280, 7.710604733652627552 ) ) ;
#23639=ORIENTED_EDGE ( 'NONE', *, *, #5175, .F. ) ;
#23640=CARTESIAN_POINT ( 'NONE',  ( -1.699609906766908596, -29.56993018339339940, 7.767301406074262893 ) ) ;
#23641=EDGE_CURVE ( 'NONE', #20410, #4296, #39621, .T. ) ;
#23643=AXIS2_PLACEMENT_3D ( 'NONE', #20178, #7823, #29652 ) ;
#23650=ORIENTED_EDGE ( 'NONE', *, *, #18319, .F. ) ;
#23655=CARTESIAN_POINT ( 'NONE',  ( -1.133537450598582241, -27.69140558245994654, 6.959317978105168834 ) ) ;
#23656=ORIENTED_EDGE ( 'NONE', *, *, #35540, .T. ) ;
#23659=CARTESIAN_POINT ( 'NONE',  ( -1.644731256756654769, -30.59959515653206097, 6.903112506833887885 ) ) ;
#23661=ORIENTED_EDGE ( 'NONE', *, *, #36793, .F. ) ;
#23666=( BOUNDED_CURVE ( )  B_SPLINE_CURVE ( 3, ( #4936, #14392, #10897, #36041 ),
 .UNSPECIFIED., .F., .T. ) 
 B_SPLINE_CURVE_WITH_KNOTS ( ( 4, 4 ),
 ( 1.381924640371168245, 1.574767692156076482 ),
 .UNSPECIFIED. ) 
 CURVE ( )  GEOMETRIC_REPRESENTATION_ITEM ( )  RATIONAL_B_SPLINE_CURVE ( ( 1.000000000000000000, 0.9969033633783032089, 0.9969033633783032089, 1.000000000000000000 ) ) 
 REPRESENTATION_ITEM ( '' )  );
#23669=ORIENTED_EDGE ( 'NONE', *, *, #14340, .T. ) ;
#23670=CARTESIAN_POINT ( 'NONE',  ( 4.805696999878964704, -27.95526195095927591, 6.880828092187096345 ) ) ;
#23671=CARTESIAN_POINT ( 'NONE',  ( 4.306781708726275859, -27.38664762112922446, 7.769368695748487319 ) ) ;
#23677=ORIENTED_EDGE ( 'NONE', *, *, #28081, .T. ) ;
#23678=CARTESIAN_POINT ( 'NONE',  ( 0.03514138663457523626, -26.60563578670519291, 7.784838882742139532 ) ) ;
#23685=FACE_OUTER_BOUND ( 'NONE', #29657, .T. ) ;
#23686=DIRECTION ( 'NONE',  ( 0.6427876096865481337, -0.7660444431189707970, -0.000000000000000000 ) ) ;
#23692=CARTESIAN_POINT ( 'NONE',  ( 4.336009428051142756, -27.42202173051807890, 6.894806418505345924 ) ) ;
#23693=CARTESIAN_POINT ( 'NONE',  ( 4.654215647715354010, -31.25365064525384540, 7.748216051605115950 ) ) ;
#23695=CYLINDRICAL_SURFACE ( 'NONE', #31019, 0.09010775117052960415 ) ;
#23697=EDGE_CURVE ( 'NONE', #22592, #9154, #33992, .T. ) ;
#23700=CARTESIAN_POINT ( 'NONE',  ( 4.977925439032924615, -28.34201439931610977, 7.720710062488894465 ) ) ;
#23703=EDGE_CURVE ( 'NONE', #14078, #3561, #8620, .T. ) ;
#23704=DIRECTION ( 'NONE',  ( -0.7660444431189725734, -0.6427876096865456912, -0.000000000000000000 ) ) ;
#23706=ORIENTED_EDGE ( 'NONE', *, *, #19159, .F. ) ;
#23712=CARTESIAN_POINT ( 'NONE',  ( -0.4625701342256395288, -32.19321274608519445, 7.730758795053800370 ) ) ;
#23716=CARTESIAN_POINT ( 'NONE',  ( 3.604513180742714429, -26.63320592762521244, 6.998987538705435441 ) ) ;
#23718=VERTEX_POINT ( 'NONE', #4116 ) ;
#23723=CARTESIAN_POINT ( 'NONE',  ( -0.01940968312617183042, -32.61825661283325672, 7.678495282201406980 ) ) ;
#23731=FACE_OUTER_BOUND ( 'NONE', #19229, .T. ) ;
#23735=ORIENTED_EDGE ( 'NONE', *, *, #8639, .F. ) ;
#23739=FACE_OUTER_BOUND ( 'NONE', #31146, .T. ) ;
#23742=DIRECTION ( 'NONE',  ( 0.6662082868431817850, 0.000000000000000000, -0.7457657263118712132 ) ) ;
#23747=CARTESIAN_POINT ( 'NONE',  ( 3.384522735995777243, -32.62220248850111659, 7.784725160561910329 ) ) ;
#23749=CARTESIAN_POINT ( 'NONE',  ( -1.034128943104400067, -31.75451381418163166, 6.865554069792296765 ) ) ;
#23751=CARTESIAN_POINT ( 'NONE',  ( 0.9904113513190105911, -32.89497607571279758, 7.754798119455333705 ) ) ;
#23752=CARTESIAN_POINT ( 'NONE',  ( 5.094860814950578742, -29.76375618630001796, 6.903372536218460809 ) ) ;
#23759=ORIENTED_EDGE ( 'NONE', *, *, #20661, .F. ) ;
#23762=CARTESIAN_POINT ( 'NONE',  ( 0.1848886247971567864, -26.52637048718725765, 6.969307238440507035 ) ) ;
#23763=CARTESIAN_POINT ( 'NONE',  ( 2.932249383186227742, -26.40092124923403460, 6.874555630061442102 ) ) ;
#23765=DIRECTION ( 'NONE',  ( -0.9396926207859057634, -0.3420201433256757073, -0.000000000000000000 ) ) ;
#23770=DIRECTION ( 'NONE',  ( 0.000000000000000000, 0.7126435865141299564, -0.7015262779114391778 ) ) ;
#23772=SHAPE_REPRESENTATION ( 'Ruler Clamping Screw', ( #30744 ), #18883 ) ;
#23773=CARTESIAN_POINT ( 'NONE',  ( 4.009398355169389028, -27.07422402788343518, 6.876076431790005827 ) ) ;
#23774=DIRECTION ( 'NONE',  ( -0.3420201433256601642, -0.9396926207859115365, -0.000000000000000000 ) ) ;
#23776=VERTEX_POINT ( 'NONE', #11455 ) ;
#23784=CARTESIAN_POINT ( 'NONE',  ( -1.490154220801371387, -30.74486085573374083, 7.756377446753165650 ) ) ;
#23786=DIRECTION ( 'NONE',  ( 0.1736481776669404897, -0.9848077530122062440, -0.000000000000000000 ) ) ;
#23787=CARTESIAN_POINT ( 'NONE',  ( -1.390358791352311885, -31.21210439690994320, 7.753200566781599967 ) ) ;
#23788=CARTESIAN_POINT ( 'NONE',  ( 0.6707251200944375213, -26.22480883340364954, 6.903112506833889661 ) ) ;
#23793=EDGE_CURVE ( 'NONE', #1128, #12118, #6173, .T. ) ;
#23800=CARTESIAN_POINT ( 'NONE',  ( 4.869399027392470103, -30.80178947334650275, 6.874555630061443878 ) ) ;
#23801=CARTESIAN_POINT ( 'NONE',  ( -1.611808805343041051, -28.80220400497604416, 6.887945620086120435 ) ) ;
#23803=CARTESIAN_POINT ( 'NONE',  ( -0.6586047051253564044, -32.15549463652887852, 6.875780273367531059 ) ) ;
#23805=CARTESIAN_POINT ( 'NONE',  ( -1.722317759908783996, -28.83844474126830804, 7.750000000000000888 ) ) ;
#23806=PRODUCT_DEFINITION_CONTEXT ( 'detailed design', #1357, 'design' ) ;
#23808=CARTESIAN_POINT ( 'NONE',  ( -1.521248034093554136, -28.20206769887411724, 6.916197352289367828 ) ) ;
#23812=CARTESIAN_POINT ( 'NONE',  ( -0.7638942222524777170, -27.22743084971469330, 6.949473656533219135 ) ) ;
#23813=ORIENTED_EDGE ( 'NONE', *, *, #31306, .T. ) ;
#23818=CARTESIAN_POINT ( 'NONE',  ( -1.182416063321688693, -27.76731179479478229, 7.757178535559532406 ) ) ;
#23823=CARTESIAN_POINT ( 'NONE',  ( -1.797258899342013549, -29.44812577374269580, 7.754798119455333705 ) ) ;
#23830=CARTESIAN_POINT ( 'NONE',  ( 4.296241352401964697, -27.37412594797728715, 7.635761828346577573 ) ) ;
#23834=CARTESIAN_POINT ( 'NONE',  ( 5.063683507119011828, -29.07157929038318755, 6.866852738645444099 ) ) ;
#23842=DIRECTION ( 'NONE',  ( 0.9396926207859080948, 0.3420201433256694901, -0.000000000000000000 ) ) ;
#23844=CARTESIAN_POINT ( 'NONE',  ( -1.137290665474521401, -27.69707997270900179, 6.988553391373223178 ) ) ;
#23845=ORIENTED_EDGE ( 'NONE', *, *, #30942, .F. ) ;
#23848=CARTESIAN_POINT ( 'NONE',  ( -1.649386784634844894, -30.58432408495164623, 6.961115707816236231 ) ) ;
#23851=ORIENTED_EDGE ( 'NONE', *, *, #15119, .T. ) ;
#23854=ORIENTED_EDGE ( 'NONE', *, *, #4806, .T. ) ;
#23856=VERTEX_POINT ( 'NONE', #11251 ) ;
#23858=ORIENTED_EDGE ( 'NONE', *, *, #17743, .T. ) ;
#23859=EDGE_CURVE ( 'NONE', #37103, #4455, #17423, .T. ) ;
#23860=CARTESIAN_POINT ( 'NONE',  ( 4.818431413503324379, -27.98001418187951472, 6.912143950357346078 ) ) ;
#23864=CARTESIAN_POINT ( 'NONE',  ( 0.3299799762144463022, -25.47407434293985418, 6.894806418505347700 ) ) ;
#23865=CYLINDRICAL_SURFACE ( 'NONE', #293, 3.399999999999999911 ) ;
#23869=CARTESIAN_POINT ( 'NONE',  ( -1.799174846253356552, -29.51474654163957112, 6.875671892026061549 ) ) ;
#23878=CARTESIAN_POINT ( 'NONE',  ( -1.261910041069868260, -27.90116479715461750, 7.695279973900954751 ) ) ;
#23884=CARTESIAN_POINT ( 'NONE',  ( -1.799609906766908685, -29.56993018339339940, 7.202408869016148074 ) ) ;
#23885=DIRECTION ( 'NONE',  ( -0.1736481776669340227, 0.9848077530122073542, -0.000000000000000000 ) ) ;
#23891=CARTESIAN_POINT ( 'NONE',  ( -0.3385372945680173995, -26.84912605459717838, 7.013842709614101167 ) ) ;
#23894=CARTESIAN_POINT ( 'NONE',  ( 0.05705130999228511662, -26.47997509747052192, 7.754798119455333705 ) ) ;
#23899=( BOUNDED_CURVE ( )  B_SPLINE_CURVE ( 3, ( #8411, #25704, #34386, #401 ),
 .UNSPECIFIED., .F., .T. ) 
 B_SPLINE_CURVE_WITH_KNOTS ( ( 4, 4 ),
 ( 1.347909859412855127, 1.534781240595300078 ),
 .UNSPECIFIED. ) 
 CURVE ( )  GEOMETRIC_REPRESENTATION_ITEM ( )  RATIONAL_B_SPLINE_CURVE ( ( 1.000000000000000000, 0.9970920404276226723, 0.9970920404276226723, 1.000000000000000000 ) ) 
 REPRESENTATION_ITEM ( '' )  );
#23900=DIRECTION ( 'NONE',  ( -0.000000000000000000, -0.000000000000000000, -1.000000000000000000 ) ) ;
#23903=CARTESIAN_POINT ( 'NONE',  ( -2.628262761802994785, -27.02926189858848360, 7.695279973900954751 ) ) ;
#23905=DIRECTION ( 'NONE',  ( -0.000000000000000000, -0.000000000000000000, -1.000000000000000000 ) ) ;
#23906=FACE_OUTER_BOUND ( 'NONE', #14591, .T. ) ;
#23909=CARTESIAN_POINT ( 'NONE',  ( 0.3268026257083770925, -32.78913155470570473, 6.974994249511788702 ) ) ;
#23916=VECTOR ( 'NONE', #30268, 999.9999999999998863 ) ;
#23917=CARTESIAN_POINT ( 'NONE',  ( -0.07973430863924736711, -32.46669619298256748, 6.866852738645443210 ) ) ;
#23918=VERTEX_POINT ( 'NONE', #8780 ) ;
#23923=EDGE_CURVE ( 'NONE', #16534, #17047, #16511, .T. ) ;
#23927=EDGE_CURVE ( 'NONE', #14639, #9920, #24862, .T. ) ;
#23931=CARTESIAN_POINT ( 'NONE',  ( 3.434919991761703262, -26.64563530151581361, 7.784838882742140420 ) ) ;
#23936=ORIENTED_EDGE ( 'NONE', *, *, #3719, .T. ) ;
#23939=CARTESIAN_POINT ( 'NONE',  ( 0.3635682928745467835, -32.69609516209911959, 7.013842709614101167 ) ) ;
#23940=CARTESIAN_POINT ( 'NONE',  ( 5.001438667734867671, -30.73314912614656436, 7.695279973900954751 ) ) ;
#23947=CARTESIAN_POINT ( 'NONE',  ( 2.674062101369763855, -32.82753328145249583, 6.997764925645181933 ) ) ;
#23953=EDGE_CURVE ( 'NONE', #8120, #34664, #2421, .T. ) ;
#23955=CARTESIAN_POINT ( 'NONE',  ( 1.700390093233090871, -29.56993018339339940, 7.800000000000000711 ) ) ;
#23956=CARTESIAN_POINT ( 'NONE',  ( 0.1799856441161017395, -26.52881562477996980, 6.920489980334477487 ) ) ;
#23957=FACE_OUTER_BOUND ( 'NONE', #13983, .T. ) ;
#23961=ADVANCED_FACE ( 'NONE', ( #26663 ), #24378, .F. ) ;
#23964=CARTESIAN_POINT ( 'NONE',  ( 4.638101942922436827, -27.85824998890764448, 7.635761828346577573 ) ) ;
#23975=CARTESIAN_POINT ( 'NONE',  ( 4.015454011556017555, -27.07985406927975447, 6.882085323592685988 ) ) ;
#23979=VERTEX_POINT ( 'NONE', #36532 ) ;
#23990=CARTESIAN_POINT ( 'NONE',  ( 0.5638177912361027611, -26.25960026125660818, 6.870737987065013819 ) ) ;
#23991=CARTESIAN_POINT ( 'NONE',  ( 4.478136214281437155, -27.44056150411416795, 6.880828092187099010 ) ) ;
#23993=CARTESIAN_POINT ( 'NONE',  ( 4.184975392578208719, -31.89090000634120514, 6.887945620086122211 ) ) ;
#23995=CARTESIAN_POINT ( 'NONE',  ( 0.3012221886605330745, -26.46337503191243457, 7.505001789837628223 ) ) ;
#24003=CARTESIAN_POINT ( 'NONE',  ( -1.615458968787878868, -28.81812344876338017, 6.876076431790006716 ) ) ;
#24010=ORIENTED_EDGE ( 'NONE', *, *, #27522, .F. ) ;
#24013=CARTESIAN_POINT ( 'NONE',  ( -1.564531365849052946, -28.30882517984442615, 6.869132338375688818 ) ) ;
#24016=CARTESIAN_POINT ( 'NONE',  ( 3.137425909638337895, -33.65403811543650647, 6.954324564059724878 ) ) ;
#24018=ADVANCED_FACE ( 'NONE', ( #29739 ), #10991, .F. ) ;
#24021=CARTESIAN_POINT ( 'NONE',  ( 3.272872476393454910, -32.58444492952590110, 6.868387053540521592 ) ) ;
#24028=VERTEX_POINT ( 'NONE', #1758 ) ;
#24029=CARTESIAN_POINT ( 'NONE',  ( 5.026281758278582146, -30.27593629695115496, 6.864216812889196717 ) ) ;
#24034=VERTEX_POINT ( 'NONE', #14085 ) ;
#24035=CARTESIAN_POINT ( 'NONE',  ( 1.067097196290011318, -33.00081685525598374, 7.781480525794718162 ) ) ;
#24040=CYLINDRICAL_SURFACE ( 'NONE', #10865, 0.09010775117052811922 ) ;
#24042=DIRECTION ( 'NONE',  ( 0.000000000000000000, 0.6662082868431845606, 0.7457657263118687707 ) ) ;
#24048=ORIENTED_EDGE ( 'NONE', *, *, #27405, .T. ) ;
#24049=DIRECTION ( 'NONE',  ( -0.3420201433256706003, 0.9396926207859077618, 0.000000000000000000 ) ) ;
#24055=CARTESIAN_POINT ( 'NONE',  ( -1.330295241805246498, -31.30949717850352343, 7.773839561854631874 ) ) ;
#24058=CARTESIAN_POINT ( 'NONE',  ( 4.546924931960046656, -31.42929550842064756, 7.013842709614101167 ) ) ;
#24059=VERTEX_POINT ( 'NONE', #20267 ) ;
#24062=ORIENTED_EDGE ( 'NONE', *, *, #28605, .T. ) ;
#24063=DIRECTION ( 'NONE',  ( 0.1736481776669361321, -0.9848077530122070211, 0.000000000000000000 ) ) ;
#24070=CIRCLE ( 'NONE', #39865, 3.499999999999999556 ) ;
#24073=CARTESIAN_POINT ( 'NONE',  ( 4.736942281967229995, -28.04042185224137995, 7.006423389747790331 ) ) ;
#24074=EDGE_CURVE ( 'NONE', #30107, #5805, #24391, .T. ) ;
#24078=CARTESIAN_POINT ( 'NONE',  ( 1.090137774077392319, -26.22513774092466221, 7.643333865083958401 ) ) ;
#24082=ORIENTED_EDGE ( 'NONE', *, *, #34393, .F. ) ;
#24087=CARTESIAN_POINT ( 'NONE',  ( -1.653919781298413660, -29.01440746736336962, 7.680992449362115337 ) ) ;
#24092=CARTESIAN_POINT ( 'NONE',  ( -0.9170814437486904946, -27.39993314898963206, 7.643333865083951295 ) ) ;
#24097=FACE_OUTER_BOUND ( 'NONE', #14288, .T. ) ;
#24101=AXIS2_PLACEMENT_3D ( 'NONE', #30701, #18892, #2508 ) ;
#24103=CARTESIAN_POINT ( 'NONE',  ( 4.392721987511531978, -31.80629977964779442, 7.749999999999998224 ) ) ;
#24109=CARTESIAN_POINT ( 'NONE',  ( -0.5587660686011224342, -26.89668496448380353, 7.756742906098588186 ) ) ;
#24110=EDGE_CURVE ( 'NONE', #27683, #6019, #21710, .T. ) ;
#24111=ORIENTED_EDGE ( 'NONE', *, *, #38575, .F. ) ;
#24112=CYLINDRICAL_SURFACE ( 'NONE', #9464, 0.09010775117052736982 ) ;
#24113=CARTESIAN_POINT ( 'NONE',  ( 3.913290293412393872, -32.15122301917286762, 7.695279973900954751 ) ) ;
#24124=AXIS2_PLACEMENT_3D ( 'NONE', #18973, #6626, #38099 ) ;
#24127=EDGE_LOOP ( 'NONE', ( #32078, #26960, #34656, #30437 ) ) ;
#24135=ORIENTED_EDGE ( 'NONE', *, *, #29843, .F. ) ;
#24137=CARTESIAN_POINT ( 'NONE',  ( -0.8241947473075555974, -27.29254761058917822, 7.754798119455333705 ) ) ;
#24140=CARTESIAN_POINT ( 'NONE',  ( 3.452406831854927471, -26.65609467884121031, 7.785172627573961890 ) ) ;
#24150=CYLINDRICAL_SURFACE ( 'NONE', #29013, 0.09010775117052882699 ) ;
#24152=CARTESIAN_POINT ( 'NONE',  ( -0.06129048428309483154, -26.54561512989744188, 7.635761828346575797 ) ) ;
#24153=CARTESIAN_POINT ( 'NONE',  ( -1.799563906791552315, -29.54920986262704119, 6.906385212079471536 ) ) ;
#24157=CARTESIAN_POINT ( 'NONE',  ( 5.042410289116912026, -28.94470923627980952, 7.680992449362118002 ) ) ;
#24158=( BOUNDED_CURVE ( )  B_SPLINE_CURVE ( 3, ( #20281, #33684, #14705, #27277 ),
 .UNSPECIFIED., .F., .T. ) 
 B_SPLINE_CURVE_WITH_KNOTS ( ( 4, 4 ),
 ( 1.381924640371169355, 1.574767692156078036 ),
 .UNSPECIFIED. ) 
 CURVE ( )  GEOMETRIC_REPRESENTATION_ITEM ( )  RATIONAL_B_SPLINE_CURVE ( ( 1.000000000000000000, 0.9969033633783032089, 0.9969033633783032089, 1.000000000000000000 ) ) 
 REPRESENTATION_ITEM ( '' )  );
#24161=CARTESIAN_POINT ( 'NONE',  ( 2.338742698598150316, -26.23039339646865287, 6.894806418505346812 ) ) ;
#24162=CARTESIAN_POINT ( 'NONE',  ( 4.885209878933623351, -28.37958095652696144, 7.730758795053806587 ) ) ;
#24171=AXIS2_PLACEMENT_3D ( 'NONE', #11277, #29633, #29829 ) ;
#24176=CARTESIAN_POINT ( 'NONE',  ( -0.9886485709270328437, -27.32959591667594523, 7.756742906098588186 ) ) ;
#24177=CARTESIAN_POINT ( 'NONE',  ( -0.8494288436016770305, -27.16237997642270585, 7.387053503561888057 ) ) ;
#24178=CARTESIAN_POINT ( 'NONE',  ( 3.055224846074477529, -26.45152950476128595, 6.929923840112066635 ) ) ;
#24180=FACE_OUTER_BOUND ( 'NONE', #39971, .T. ) ;
#24181=ORIENTED_EDGE ( 'NONE', *, *, #27944, .F. ) ;
#24199=CARTESIAN_POINT ( 'NONE',  ( 2.413333108735914223, -26.24550221827435337, 6.863904403958575706 ) ) ;
#24200=CARTESIAN_POINT ( 'NONE',  ( -1.750118104476454439, -30.09189987372638342, 7.780491323090171996 ) ) ;
#24201=CARTESIAN_POINT ( 'NONE',  ( 2.850561110411099275, -26.37038230420113649, 7.635761828346577573 ) ) ;
#24205=CARTESIAN_POINT ( 'NONE',  ( 3.977572546501451978, -32.22783162523180778, 7.697032948437509070 ) ) ;
#24206=ADVANCED_FACE ( 'NONE', ( #18596 ), #37136, .F. ) ;
#24209=ORIENTED_EDGE ( 'NONE', *, *, #16666, .T. ) ;
#24213=B_SPLINE_CURVE_WITH_KNOTS ( 'NONE', 3,
 ( #37087, #2536, #8877, #21662 ),
 .UNSPECIFIED., .F., .F.,
 ( 4, 4 ),
 ( 0.000000000000000000, 6.391136169899793690E-06 ),
 .UNSPECIFIED. ) ;
#24215=DIRECTION ( 'NONE',  ( 1.000000000000000000, -0.000000000000000000, -0.000000000000000000 ) ) ;
#24218=DIRECTION ( 'NONE',  ( 0.1736481776669273613, 0.9848077530122086864, -0.000000000000000000 ) ) ;
#24222=AXIS2_PLACEMENT_3D ( 'NONE', #30349, #2155, #14675 ) ;
#24227=CARTESIAN_POINT ( 'NONE',  ( 3.099557997805675313, -32.67648533487435714, 7.505001789837626447 ) ) ;
#24230=CARTESIAN_POINT ( 'NONE',  ( 4.740470269852407270, -27.86479572999185450, 7.785096263473211486 ) ) ;
#24233=CARTESIAN_POINT ( 'NONE',  ( 3.224716257031337019, -32.60908495567738896, 6.911401339314956260 ) ) ;
#24235=CARTESIAN_POINT ( 'NONE',  ( 4.955822899483663946, -30.85533363526925754, 6.863805608295730387 ) ) ;
#24237=CARTESIAN_POINT ( 'NONE',  ( -1.228840775939959551, -27.84377650683858718, 7.782167645815904145 ) ) ;
#24239=DIRECTION ( 'NONE',  ( 0.9396926207859082059, 0.3420201433256695456, -0.000000000000000000 ) ) ;
#24241=DIRECTION ( 'NONE',  ( 0.8660254037844449249, -0.4999999999999888423, -0.000000000000000000 ) ) ;
#24249=CARTESIAN_POINT ( 'NONE',  ( 4.546924931960046656, -31.42929550842064756, 7.013842709614101167 ) ) ;
#24252=CARTESIAN_POINT ( 'NONE',  ( 5.059341540990399011, -29.04314055594101163, 6.880147297696982633 ) ) ;
#24258=VERTEX_POINT ( 'NONE', #12434 ) ;
#24261=ADVANCED_FACE ( 'NONE', ( #12005 ), #24585, .F. ) ;
#24262=CARTESIAN_POINT ( 'NONE',  ( -1.215384403943503555, -27.82114229413565099, 6.887041543973311697 ) ) ;
#24264=VERTEX_POINT ( 'NONE', #18397 ) ;
#24265=ORIENTED_EDGE ( 'NONE', *, *, #14569, .F. ) ;
#24269=( BOUNDED_CURVE ( )  B_SPLINE_CURVE ( 3, ( #13189, #38293, #16474, #19373 ),
 .UNSPECIFIED., .F., .T. ) 
 B_SPLINE_CURVE_WITH_KNOTS ( ( 4, 4 ),
 ( 1.381924640371167579, 1.574767692156075594 ),
 .UNSPECIFIED. ) 
 CURVE ( )  GEOMETRIC_REPRESENTATION_ITEM ( )  RATIONAL_B_SPLINE_CURVE ( ( 1.000000000000000000, 0.9969033633783032089, 0.9969033633783032089, 1.000000000000000000 ) ) 
 REPRESENTATION_ITEM ( '' )  );
#24271=CARTESIAN_POINT ( 'NONE',  ( 1.751596854648554302, -26.17031492517298474, 6.892063359921933419 ) ) ;
#24276=ORIENTED_EDGE ( 'NONE', *, *, #11545, .F. ) ;
#24283=CARTESIAN_POINT ( 'NONE',  ( 4.349665778881001366, -27.43886483293057665, 7.784476445165072533 ) ) ;
#24287=CARTESIAN_POINT ( 'NONE',  ( 0.06174230887167742737, -26.59084733370359999, 7.784476445165073422 ) ) ;
#24289=CARTESIAN_POINT ( 'NONE',  ( -1.794332605514025181, -29.37780194793158373, 6.951256099901591767 ) ) ;
#24295=PLANE ( 'NONE',  #6567 ) ;
#24306=CARTESIAN_POINT ( 'NONE',  ( 5.197144683283896782, -29.57049166273291263, 7.767720160662275219 ) ) ;
#24307=DIRECTION ( 'NONE',  ( -0.5000000000000039968, 0.8660254037844362651, -0.000000000000000000 ) ) ;
#24308=CARTESIAN_POINT ( 'NONE',  ( 1.578585683582428345, -33.06757917596850405, 7.754798119455333705 ) ) ;
#24312=EDGE_CURVE ( 'NONE', #24578, #7785, #39019, .T. ) ;
#24320=FACE_OUTER_BOUND ( 'NONE', #35618, .T. ) ;
#24321=AXIS2_PLACEMENT_3D ( 'NONE', #34711, #19238, #22137 ) ;
#24327=CARTESIAN_POINT ( 'NONE',  ( 1.272790698195233938, -26.09614646471635524, 6.912143950357348743 ) ) ;
#24344=CARTESIAN_POINT ( 'NONE',  ( -0.8969834501566193996, -27.37591117031255195, 7.775108481317158926 ) ) ;
#24346=CARTESIAN_POINT ( 'NONE',  ( 3.503008481831729082, -26.68712402683863161, 7.757178535559534183 ) ) ;
#24347=DIRECTION ( 'NONE',  ( -0.4999999999999962808, 0.8660254037844408170, 0.000000000000000000 ) ) ;
#24351=CARTESIAN_POINT ( 'NONE',  ( 1.574665456181726375, -33.06768670341953253, 6.867199677474203234 ) ) ;
#24356=CARTESIAN_POINT ( 'NONE',  ( -0.5909859742846951258, -26.91526153312021563, 7.255881584735162093 ) ) ;
#24357=CARTESIAN_POINT ( 'NONE',  ( 5.172564876073734830, -29.12947328719863194, 7.013842709614101167 ) ) ;
#24361=CARTESIAN_POINT ( 'NONE',  ( 3.369155479471896530, -26.60763004909045293, 7.695279973900954751 ) ) ;
#24363=CARTESIAN_POINT ( 'NONE',  ( -0.07465813067054014041, -26.55344152887859011, 7.730015791551945625 ) ) ;
#24364=CARTESIAN_POINT ( 'NONE',  ( 6.019945922396399141, -27.01350538757900210, 7.695279973900954751 ) ) ;
#24367=CARTESIAN_POINT ( 'NONE',  ( 4.882868366733327470, -28.37333834040810032, 7.695279973900954751 ) ) ;
#24375=CARTESIAN_POINT ( 'NONE',  ( 2.270779804372443422, -33.02314641928401784, 6.887161170156907097 ) ) ;
#24378=CYLINDRICAL_SURFACE ( 'NONE', #7455, 0.09010775117052870209 ) ;
#24379=CARTESIAN_POINT ( 'NONE',  ( 3.043504320637459681, -26.44646349201601865, 6.903372536218459032 ) ) ;
#24381=CARTESIAN_POINT ( 'NONE',  ( -0.8732574325522374226, -27.19792959302312596, 6.887547729233686411 ) ) ;
#24382=CARTESIAN_POINT ( 'NONE',  ( 4.903710960591165069, -30.70956631902851086, 7.740055089680402567 ) ) ;
#24385=ORIENTED_EDGE ( 'NONE', *, *, #18840, .F. ) ;
#24391=B_SPLINE_CURVE_WITH_KNOTS ( 'NONE', 3,
 ( #2171, #32849, #5445, #20466, #36137, #23762, #14691, #21097, #39401, #4639, #23956, #20669, #33254, #27258, #17987, #5037, #17569, #11594, #33668, #2380, #36937, #15316, #18809, #28487, #34697, #12223, #28076, #19024, #37341, #34292, #9331 ),
 .UNSPECIFIED., .F., .F.,
 ( 4, 3, 3, 3, 3, 3, 3, 3, 3, 3, 4 ),
 ( 1.117570019170468176E-18, 2.999644130997731624E-05, 6.002588995694847643E-05, 8.960886084588059531E-05, 0.0001190604700446496486, 0.0001489538463052702297, 0.0001796139255493970418, 0.0002109707048517063196, 0.0002426195318110334050, 0.0002740640997890030940, 0.0002849778069099824138 ),
 .UNSPECIFIED. ) ;
#24397=PLANE ( 'NONE',  #1529 ) ;
#24408=CARTESIAN_POINT ( 'NONE',  ( 2.338742698598150316, -26.23039339646865287, 6.894806418505346812 ) ) ;
#24411=CARTESIAN_POINT ( 'NONE',  ( 3.288727556110957462, -26.44342115354165301, 7.139344958878409031 ) ) ;
#24412=CARTESIAN_POINT ( 'NONE',  ( -1.411741797515851271, -31.17137799540083876, 7.013842709614101167 ) ) ;
#24413=CARTESIAN_POINT ( 'NONE',  ( 5.052258071467315759, -28.99977615411923537, 7.779495906702013741 ) ) ;
#24416=CARTESIAN_POINT ( 'NONE',  ( -0.4475183596422435683, -26.93431084857535751, 6.894806418505348589 ) ) ;
#24422=CARTESIAN_POINT ( 'NONE',  ( 4.952473364809343082, -30.82556682577061835, 7.784725160561909441 ) ) ;
#24428=CARTESIAN_POINT ( 'NONE',  ( -1.605899657953074211, -28.77718300982459709, 6.929923840112066635 ) ) ;
#24430=ADVANCED_FACE ( 'NONE', ( #1313 ), #25405, .F. ) ;
#24434=CARTESIAN_POINT ( 'NONE',  ( -1.699609906766908596, -29.35555682840059433, 7.376738162537630039 ) ) ;
#24436=CARTESIAN_POINT ( 'NONE',  ( -1.799609906766908685, -29.56993018339339940, 7.620413589471895399 ) ) ;
#24439=CARTESIAN_POINT ( 'NONE',  ( 4.298799322723926508, -31.91476908534313850, 7.750000000000000888 ) ) ;
#24440=CARTESIAN_POINT ( 'NONE',  ( 4.918781769468254517, -30.94541378637557827, 6.941203072598468360 ) ) ;
#24442=FACE_OUTER_BOUND ( 'NONE', #14411, .T. ) ;
#24450=CARTESIAN_POINT ( 'NONE',  ( 2.875937710231030398, -32.76024173560432473, 7.635761828346577573 ) ) ;
#24455=VERTEX_POINT ( 'NONE', #14038 ) ;
#24458=CARTESIAN_POINT ( 'NONE',  ( 4.006432741929322638, -26.93700985481278920, 6.867280401193709416 ) ) ;
#24460=CARTESIAN_POINT ( 'NONE',  ( -0.1589752317941719728, -32.41646502212034875, 7.013842709614101167 ) ) ;
#24465=CARTESIAN_POINT ( 'NONE',  ( -1.219418532703906877, -27.82788610016705988, 6.894806418505346812 ) ) ;
#24466=VERTEX_POINT ( 'NONE', #11542 ) ;
#24467=ORIENTED_EDGE ( 'NONE', *, *, #25583, .T. ) ;
#24471=VECTOR ( 'NONE', #29247, 1000.000000000000114 ) ;
#24474=CARTESIAN_POINT ( 'NONE',  ( -1.740649852066194381, -30.20965207207213155, 7.670465701733752972 ) ) ;
#24475=ADVANCED_FACE ( 'NONE', ( #23906 ), #14441, .F. ) ;
#24477=B_SPLINE_CURVE_WITH_KNOTS ( 'NONE', 3,
 ( #33271, #5053, #31400, #22699, #25015, #31197, #18827, #8942, #9349, #3773, #673, #29068, #35266, #18610, #10316, #37554, #22894, #21929, #31002, #21527, #10111, #7236, #2607, #34504, #25778, #32176, #21725, #34307, #16493, #38515, #12448 ),
 .UNSPECIFIED., .F., .F.,
 ( 4, 3, 3, 3, 3, 3, 3, 3, 3, 3, 4 ),
 ( 8.673617379884035472E-19, 2.999644130997694354E-05, 6.002588995694842222E-05, 8.960886084587984992E-05, 0.0001190604700446502720, 0.0001489538463052734552, 0.0001796139255494000775, 0.0002109707048517115509, 0.0002426195318110373352, 0.0002740640997890081898, 0.0002849778069099824680 ),
 .UNSPECIFIED. ) ;
#24480=CARTESIAN_POINT ( 'NONE',  ( 0.02919540433882696420, -32.53086290775901546, 7.670860738520328681 ) ) ;
#24490=CARTESIAN_POINT ( 'NONE',  ( -0.8241947473075555974, -27.29254761058917822, 7.754798119455333705 ) ) ;
#24491=ORIENTED_EDGE ( 'NONE', *, *, #18644, .F. ) ;
#24492=CARTESIAN_POINT ( 'NONE',  ( 4.885173765863568107, -28.37948784604718000, 7.661510568013096822 ) ) ;
#24493=DIRECTION ( 'NONE',  ( 0.000000000000000000, 0.000000000000000000, 1.000000000000000000 ) ) ;
#24494=CARTESIAN_POINT ( 'NONE',  ( -1.795519090086910019, -29.40075872605237706, 7.013842709614101167 ) ) ;
#24498=ORIENTED_EDGE ( 'NONE', *, *, #8536, .F. ) ;
#24499=CARTESIAN_POINT ( 'NONE',  ( 0.5185917657260591396, -26.38192185697194603, 7.643333865083957512 ) ) ;
#24500=EDGE_CURVE ( 'NONE', #29219, #40258, #6688, .T. ) ;
#24504=FACE_OUTER_BOUND ( 'NONE', #4817, .T. ) ;
#24509=CARTESIAN_POINT ( 'NONE',  ( 2.715114166433969078, -32.91960704172863927, 6.951256099901589103 ) ) ;
#24516=CARTESIAN_POINT ( 'NONE',  ( 5.198039085808181525, -29.69173459304409946, 7.754798119455333705 ) ) ;
#24517=( BOUNDED_CURVE ( )  B_SPLINE_CURVE ( 3, ( #38839, #4486, #1399, #14124 ),
 .UNSPECIFIED., .F., .T. ) 
 B_SPLINE_CURVE_WITH_KNOTS ( ( 4, 4 ),
 ( 4.708531083176467291, 4.895802057644188743 ),
 .UNSPECIFIED. ) 
 CURVE ( )  GEOMETRIC_REPRESENTATION_ITEM ( )  RATIONAL_B_SPLINE_CURVE ( ( 1.000000000000000000, 0.9970795998553221295, 0.9970795998553221295, 1.000000000000000000 ) ) 
 REPRESENTATION_ITEM ( '' )  );
#24519=CARTESIAN_POINT ( 'NONE',  ( 4.331577083009899631, -31.85530975974228696, 7.785593909369612931 ) ) ;
#24526=DIRECTION ( 'NONE',  ( -0.7660444431189726844, -0.6427876096865458022, -0.000000000000000000 ) ) ;
#24528=CARTESIAN_POINT ( 'NONE',  ( -0.4574210171174863948, -32.19744825413003753, 7.703977250142846067 ) ) ;
#24532=FACE_OUTER_BOUND ( 'NONE', #21041, .T. ) ;
#24533=FACE_OUTER_BOUND ( 'NONE', #10332, .T. ) ;
#24538=CARTESIAN_POINT ( 'NONE',  ( -0.1538752734239677844, -32.41980122938345232, 6.887945620086118659 ) ) ;
#24541=CARTESIAN_POINT ( 'NONE',  ( 3.872357652763316782, -32.30533874404253680, 7.776484688137383472 ) ) ;
#24543=CARTESIAN_POINT ( 'NONE',  ( 0.5100408663666432529, -26.38511039769286981, 7.730758795053808363 ) ) ;
#24546=EDGE_LOOP ( 'NONE', ( #16091, #30221, #28892, #19779 ) ) ;
#24547=EDGE_CURVE ( 'NONE', #35491, #4130, #6201, .T. ) ;
#24548=EDGE_CURVE ( 'NONE', #27683, #14186, #6616, .T. ) ;
#24553=CARTESIAN_POINT ( 'NONE',  ( 4.261851404573053337, -31.95508217798681017, 6.998987538705435441 ) ) ;
#24554=CARTESIAN_POINT ( 'NONE',  ( -1.693090760297530029, -29.35948301055791632, 6.949473656533217358 ) ) ;
#24561=VECTOR ( 'NONE', #30895, 1000.000000000000114 ) ;
#24564=B_SPLINE_CURVE_WITH_KNOTS ( 'NONE', 3,
 ( #32564, #10703, #10908, #4361 ),
 .UNSPECIFIED., .F., .F.,
 ( 4, 4 ),
 ( 9.697399036122160616E-19, 6.391136169898363898E-06 ),
 .UNSPECIFIED. ) ;
#24566=CARTESIAN_POINT ( 'NONE',  ( -1.799471907747695942, -29.53885005966835919, 6.894806418505347700 ) ) ;
#24567=CARTESIAN_POINT ( 'NONE',  ( 2.124883528784431430, -33.04409396078893479, 6.989977667959444751 ) ) ;
#24571=CARTESIAN_POINT ( 'NONE',  ( 5.042819392577695403, -28.94688871985320588, 7.670860738520327793 ) ) ;
#24572=CARTESIAN_POINT ( 'NONE',  ( 0.4271750062121888458, -32.81914278374281935, 7.780491323090173772 ) ) ;
#24578=VERTEX_POINT ( 'NONE', #15261 ) ;
#24579=ORIENTED_EDGE ( 'NONE', *, *, #8866, .F. ) ;
#24583=EDGE_LOOP ( 'NONE', ( #30532, #25410, #19292, #33896 ) ) ;
#24585=CYLINDRICAL_SURFACE ( 'NONE', #16693, 0.09010775117052735594 ) ;
#24586=CARTESIAN_POINT ( 'NONE',  ( 2.908949165453299734, -26.39197723079101010, 6.894806418505348589 ) ) ;
#24589=ORIENTED_EDGE ( 'NONE', *, *, #10907, .F. ) ;
#24591=PLANE ( 'NONE',  #31421 ) ;
#24593=ORIENTED_EDGE ( 'NONE', *, *, #20624, .F. ) ;
#24606=CARTESIAN_POINT ( 'NONE',  ( -1.799464741694478898, -29.60207515963518077, 7.667456792664608223 ) ) ;
#24609=CARTESIAN_POINT ( 'NONE',  ( 1.719158177631397333, -32.96987838285291872, 7.748216051605118615 ) ) ;
#24616=CARTESIAN_POINT ( 'NONE',  ( 5.064524549198025305, -29.07729924941551047, 7.774064877406527962 ) ) ;
#24618=CARTESIAN_POINT ( 'NONE',  ( 3.908300141282813556, -32.15549264052357614, 7.661510568013099487 ) ) ;
#24626=CARTESIAN_POINT ( 'NONE',  ( 4.954542941690649016, -30.81756555562317601, 7.785593909369613819 ) ) ;
#24633=CARTESIAN_POINT ( 'NONE',  ( -0.6763298692248193023, -32.13921067023287037, 7.013842709614101167 ) ) ;
#24634=ORIENTED_EDGE ( 'NONE', *, *, #27478, .F. ) ;
#24636=EDGE_CURVE ( 'NONE', #3709, #37354, #18341, .T. ) ;
#24637=MECHANICAL_DESIGN_GEOMETRIC_PRESENTATION_REPRESENTATION('',(#30561),#37127);
#24640=ORIENTED_EDGE ( 'NONE', *, *, #36484, .T. ) ;
#24642=CARTESIAN_POINT ( 'NONE',  ( -1.560938997313471965, -28.29960244491221033, 6.866770815808350470 ) ) ;
#24644=CARTESIAN_POINT ( 'NONE',  ( -1.740904132959085304, -28.93157757802832819, 6.894806418505347700 ) ) ;
#24645=EDGE_LOOP ( 'NONE', ( #23851, #31801, #15543, #27296, #13199 ) ) ;
#24646=VECTOR ( 'NONE', #1459, 1000.000000000000114 ) ;
#24648=CARTESIAN_POINT ( 'NONE',  ( -0.01240450716718164911, -26.53256281584198817, 7.783750581861600182 ) ) ;
#24655=EDGE_LOOP ( 'NONE', ( #4302, #29620, #26732, #17364 ) ) ;
#24658=CARTESIAN_POINT ( 'NONE',  ( -0.04165398999324298329, -32.48973880933039737, 6.894806418505347700 ) ) ;
#24661=CARTESIAN_POINT ( 'NONE',  ( -1.479147532598991122, -25.61012871437631944, 7.013842709614101167 ) ) ;
#24663=CARTESIAN_POINT ( 'NONE',  ( 2.879233941065469260, -26.27442913159145021, 7.643192810543819604 ) ) ;
#24664=CARTESIAN_POINT ( 'NONE',  ( 4.619408797998243443, -31.31332657468931302, 7.785868773668302545 ) ) ;
#24665=ADVANCED_FACE ( 'NONE', ( #11952 ), #30932, .F. ) ;
#24672=CARTESIAN_POINT ( 'NONE',  ( 1.855597646007116186, -26.17346053900190839, 6.871394612369935651 ) ) ;
#24683=EDGE_CURVE ( 'NONE', #11306, #29197, #35838, .T. ) ;
#24685=CARTESIAN_POINT ( 'NONE',  ( 1.158056475448751454, -26.21346265829786049, 6.894806418505346812 ) ) ;
#24687=EDGE_CURVE ( 'NONE', #15530, #31847, #31737, .T. ) ;
#24688=CARTESIAN_POINT ( 'NONE',  ( -0.2791676774040683928, -26.67527632528762993, 7.501983001166817822 ) ) ;
#24689=ORIENTED_EDGE ( 'NONE', *, *, #21310, .T. ) ;
#24695=CARTESIAN_POINT ( 'NONE',  ( 4.377466420158320659, -27.47391912907700373, 7.761597726988851420 ) ) ;
#24703=CARTESIAN_POINT ( 'NONE',  ( 4.882879936320184910, -28.37336910974825344, 7.692469944509197077 ) ) ;
#24710=VECTOR ( 'NONE', #22377, 1000.000000000000227 ) ;
#24717=CARTESIAN_POINT ( 'NONE',  ( 2.724709505007048893, -32.91668746611431118, 6.912143950357347855 ) ) ;
#24719=CARTESIAN_POINT ( 'NONE',  ( 1.060668204554370719, -26.12889023809411171, 7.670465701733749420 ) ) ;
#24721=CARTESIAN_POINT ( 'NONE',  ( 3.024075050411040078, -32.70932073997259693, 7.139196562012272373 ) ) ;
#24722=CARTESIAN_POINT ( 'NONE',  ( -1.348441917761853182, -27.85102839191939950, 7.700536657684218689 ) ) ;
#24723=EDGE_CURVE ( 'NONE', #17087, #24059, #34293, .T. ) ;
#24726=CARTESIAN_POINT ( 'NONE',  ( 1.721493557208823466, -33.06986693911196795, 7.744938106820261403 ) ) ;
#24729=ORIENTED_EDGE ( 'NONE', *, *, #40, .T. ) ;
#24732=ORIENTED_EDGE ( 'NONE', *, *, #23184, .F. ) ;
#24734=CARTESIAN_POINT ( 'NONE',  ( 4.300627460203361174, -31.91262744306316179, 7.753200566781576875 ) ) ;
#24736=EDGE_CURVE ( 'NONE', #32517, #19029, #35600, .T. ) ;
#24741=VERTEX_POINT ( 'NONE', #241 ) ;
#24752=DIRECTION ( 'NONE',  ( 0.7660444431189770143, 0.6427876096865404731, -0.000000000000000000 ) ) ;
#24753=CARTESIAN_POINT ( 'NONE',  ( 1.826415646469069731, -26.07219983930859897, 7.750000000000000888 ) ) ;
#24754=CARTESIAN_POINT ( 'NONE',  ( 0.5944372483576262356, -26.35483013752983794, 7.785172627573962778 ) ) ;
#24758=CARTESIAN_POINT ( 'NONE',  ( 4.740217150655367639, -31.30470820734161563, 7.640616322432097540 ) ) ;
#24759=EDGE_LOOP ( 'NONE', ( #20335, #11183, #1767, #24385 ) ) ;
#24762=( BOUNDED_CURVE ( )  B_SPLINE_CURVE ( 3, ( #8843, #30278, #27181, #21429 ),
 .UNSPECIFIED., .F., .T. ) 
 B_SPLINE_CURVE_WITH_KNOTS ( ( 4, 4 ),
 ( 1.381924640371168467, 1.574767692156076926 ),
 .UNSPECIFIED. ) 
 CURVE ( )  GEOMETRIC_REPRESENTATION_ITEM ( )  RATIONAL_B_SPLINE_CURVE ( ( 1.000000000000000000, 0.9969033633783032089, 0.9969033633783032089, 1.000000000000000000 ) ) 
 REPRESENTATION_ITEM ( '' )  );
#24764=CYLINDRICAL_SURFACE ( 'NONE', #16337, 0.09010775117052907679 ) ;
#24766=VECTOR ( 'NONE', #6480, 1000.000000000000114 ) ;
#24767=CARTESIAN_POINT ( 'NONE',  ( -1.422348494510240480, -31.15059581268885580, 6.961115707816239784 ) ) ;
#24769=CARTESIAN_POINT ( 'NONE',  ( 1.537640963180244347, -33.06615115872732247, 6.887547729233690852 ) ) ;
#24771=AXIS2_PLACEMENT_3D ( 'NONE', #28572, #18111, #21432 ) ;
#24774=EDGE_CURVE ( 'NONE', #18417, #5658, #3551, .T. ) ;
#24780=FACE_OUTER_BOUND ( 'NONE', #16276, .T. ) ;
#24781=CARTESIAN_POINT ( 'NONE',  ( -89.20959394718985891, -30.20828278875847062, 6.894806418505347700 ) ) ;
#24782=CARTESIAN_POINT ( 'NONE',  ( 0.4016364682254440766, -32.81725445528589091, 7.766640943994648438 ) ) ;
#24783=B_SPLINE_CURVE_WITH_KNOTS ( 'NONE', 3,
 ( #15149, #14946, #3045, #40262, #9178, #31026, #12046, #15567, #28121, #27512, #24626, #24422, #8964, #37178, #5899, #21553, #11765, #7333, #30333 ),
 .UNSPECIFIED., .F., .F.,
 ( 4, 3, 3, 3, 3, 3, 4 ),
 ( 0.000000000000000000, 2.546128104244680068E-05, 5.711050680483513924E-05, 8.113074941675454152E-05, 0.0001053129305727007356, 0.0001360598016347043700, 0.0001612931755701971497 ),
 .UNSPECIFIED. ) ;
#24785=CARTESIAN_POINT ( 'NONE',  ( 5.098113783035356228, -29.69476113458859601, 6.863904403958576594 ) ) ;
#24787=CARTESIAN_POINT ( 'NONE',  ( 2.829942967996462944, -26.36304532024056968, 7.680992449362121555 ) ) ;
#24792=CARTESIAN_POINT ( 'NONE',  ( -2.485163400083383323, -30.43163963246801984, 7.754798119455333705 ) ) ;
#24795=EDGE_CURVE ( 'NONE', #25345, #23979, #15487, .T. ) ;
#24801=CARTESIAN_POINT ( 'NONE',  ( 4.851634552394991751, -30.84651091276440482, 7.754798119455333705 ) ) ;
#24804=CARTESIAN_POINT ( 'NONE',  ( 5.033830403340459725, -30.23945351880105648, 7.782034975670476307 ) ) ;
#24810=CARTESIAN_POINT ( 'NONE',  ( -1.676799063830336056, -29.96313308435724210, 6.997764925645183709 ) ) ;
#24815=CARTESIAN_POINT ( 'NONE',  ( 2.896981936218417708, -32.75240845689362601, 7.703977250142848732 ) ) ;
#24817=EDGE_LOOP ( 'NONE', ( #11503, #35215, #760, #2081 ) ) ;
#24821=CARTESIAN_POINT ( 'NONE',  ( 1.670112593087247577, -32.96979536792423460, 7.782167645815905033 ) ) ;
#24823=CARTESIAN_POINT ( 'NONE',  ( 3.720465652270369183, -32.30476016926337479, 6.949473656533220023 ) ) ;
#24825=FACE_OUTER_BOUND ( 'NONE', #28532, .T. ) ;
#24828=CARTESIAN_POINT ( 'NONE',  ( 5.047799653463134639, -28.97418023640373974, 7.763628509615286610 ) ) ;
#24830=CARTESIAN_POINT ( 'NONE',  ( 3.913265336722258514, -32.15124441476239525, 7.692469944509199742 ) ) ;
#24834=VERTEX_POINT ( 'NONE', #37187 ) ;
#24838=EDGE_CURVE ( 'NONE', #5805, #422, #11622, .T. ) ;
#24844=FACE_OUTER_BOUND ( 'NONE', #30338, .T. ) ;
#24849=VERTEX_POINT ( 'NONE', #33928 ) ;
#24859=VERTEX_POINT ( 'NONE', #8766 ) ;
#24862=LINE ( 'NONE', #37402, #38998 ) ;
#24868=CARTESIAN_POINT ( 'NONE',  ( 5.025435985552490159, -30.27990892530747047, 7.754798119455333705 ) ) ;
#24872=CARTESIAN_POINT ( 'NONE',  ( 5.008335689530277968, -30.35575962765878089, 6.911401339314956260 ) ) ;
#24879=DIRECTION ( 'NONE',  ( 0.6427876096865425826, -0.7660444431189752379, 0.000000000000000000 ) ) ;
#24880=ORIENTED_EDGE ( 'NONE', *, *, #3947, .F. ) ;
#24883=DIRECTION ( 'NONE',  ( -0.000000000000000000, -0.000000000000000000, -1.000000000000000000 ) ) ;
#24886=CARTESIAN_POINT ( 'NONE',  ( 1.881295483120765111, -26.17473677672775878, 6.887945620086118659 ) ) ;
#24887=ORIENTED_EDGE ( 'NONE', *, *, #23021, .T. ) ;
#24889=AXIS2_PLACEMENT_3D ( 'NONE', #35527, #10776, #4820 ) ;
#24896=CARTESIAN_POINT ( 'NONE',  ( -1.036828849638991690, -31.59861137850023738, 7.386948897581449458 ) ) ;
#24905=CARTESIAN_POINT ( 'NONE',  ( -1.506684114051581869, -28.44091511309124343, 7.693875151218752428 ) ) ;
#24911=CARTESIAN_POINT ( 'NONE',  ( 4.749222104228042696, -31.28883197486738510, 7.700536657684216024 ) ) ;
#24914=FACE_OUTER_BOUND ( 'NONE', #18127, .T. ) ;
#24915=CARTESIAN_POINT ( 'NONE',  ( 0.5949730329236684323, -26.25663028810755861, 7.776484688137383472 ) ) ;
#24917=EDGE_CURVE ( 'NONE', #28596, #16444, #12488, .T. ) ;
#24919=ORIENTED_EDGE ( 'NONE', *, *, #3127, .F. ) ;
#24923=ORIENTED_EDGE ( 'NONE', *, *, #23703, .T. ) ;
#24929=CARTESIAN_POINT ( 'NONE',  ( -0.9128197825508301833, -27.39481314169073300, 7.635761828346577573 ) ) ;
#24936=CARTESIAN_POINT ( 'NONE',  ( 5.099675413223700993, -29.64036099912623712, 7.784476445165074310 ) ) ;
#24937=CARTESIAN_POINT ( 'NONE',  ( 0.9716734364680117420, -32.99315042889409000, 7.753200566781576875 ) ) ;
#24941=ORIENTED_EDGE ( 'NONE', *, *, #33464, .F. ) ;
#24960=ORIENTED_EDGE ( 'NONE', *, *, #302, .T. ) ;
#24962=CARTESIAN_POINT ( 'NONE',  ( 2.350580150463965623, -26.13084565137115689, 6.883108633650832253 ) ) ;
#24970=FACE_OUTER_BOUND ( 'NONE', #30190, .T. ) ;
#24972=CARTESIAN_POINT ( 'NONE',  ( 4.254005347624293165, -31.96347340058011710, 6.951256099901589103 ) ) ;
#24973=CARTESIAN_POINT ( 'NONE',  ( -1.579832256282212244, -30.79065755753165234, 7.651421919295140484 ) ) ;
#24980=CIRCLE ( 'NONE', #30224, 0.04999999999999969746 ) ;
#24984=CARTESIAN_POINT ( 'NONE',  ( 0.5215462454007337989, -32.86543123519535925, 7.643192810543816940 ) ) ;
#25000=DIRECTION ( 'NONE',  ( -0.7660444431189813441, 0.6427876096865353661, -0.000000000000000000 ) ) ;
#25002=CARTESIAN_POINT ( 'NONE',  ( 4.877799951173103388, -30.77995818745698031, 7.785868773668302545 ) ) ;
#25009=( BOUNDED_CURVE ( )  B_SPLINE_CURVE ( 3, ( #38205, #18455, #31041, #12690 ),
 .UNSPECIFIED., .F., .T. ) 
 B_SPLINE_CURVE_WITH_KNOTS ( ( 4, 4 ),
 ( 1.347909859412854461, 1.534781240595299634 ),
 .UNSPECIFIED. ) 
 CURVE ( )  GEOMETRIC_REPRESENTATION_ITEM ( )  RATIONAL_B_SPLINE_CURVE ( ( 1.000000000000000000, 0.9970920404276226723, 0.9970920404276226723, 1.000000000000000000 ) ) 
 REPRESENTATION_ITEM ( '' )  );
#25011=CARTESIAN_POINT ( 'NONE',  ( -1.482288828291198790, -30.76598833619782170, 7.680992449362119778 ) ) ;
#25015=CARTESIAN_POINT ( 'NONE',  ( 4.433156500894046559, -27.54706021590136444, 6.979335674598000416 ) ) ;
#25016=EDGE_CURVE ( 'NONE', #18362, #6354, #5040, .T. ) ;
#25019=CARTESIAN_POINT ( 'NONE',  ( 4.667929121870860065, -31.42551012740447902, 7.753200566781599079 ) ) ;
#25022=ORIENTED_EDGE ( 'NONE', *, *, #1420, .T. ) ;
#25028=EDGE_CURVE ( 'NONE', #5967, #12173, #15862, .T. ) ;
#25030=CARTESIAN_POINT ( 'NONE',  ( 3.431207382034987763, -26.52784317818328219, 7.743886751744251562 ) ) ;
#25033=CARTESIAN_POINT ( 'NONE',  ( -1.799583860900191734, -29.58343279012807159, 7.635761828346577573 ) ) ;
#25035=CARTESIAN_POINT ( 'NONE',  ( 0.05382362115409088099, -33.98870358965611160, 7.695279973900954751 ) ) ;
#25036=CARTESIAN_POINT ( 'NONE',  ( 1.731470216958145070, -26.07006818241261215, 6.894806418505347700 ) ) ;
#25037=CARTESIAN_POINT ( 'NONE',  ( 3.481305170888918887, -32.58295880691792945, 7.700536657684214248 ) ) ;
#25039=CARTESIAN_POINT ( 'NONE',  ( 3.912857414353567709, -32.15159409943261437, 7.680992449362120666 ) ) ;
#25043=B_SPLINE_CURVE_WITH_KNOTS ( 'NONE', 3,
 ( #26865, #1175, #36143, #35942, #8108, #23373, #7723, #4456, #13499, #4841 ),
 .UNSPECIFIED., .F., .F.,
 ( 4, 3, 3, 4 ),
 ( 8.673617379884035472E-19, 3.025570593003193312E-05, 6.051145698343867694E-05, 6.468151674593740786E-05 ),
 .UNSPECIFIED. ) ;
#25045=ORIENTED_EDGE ( 'NONE', *, *, #19629, .T. ) ;
#25048=CARTESIAN_POINT ( 'NONE',  ( 3.963477911421234623, -32.23984282750152630, 7.750000000000001776 ) ) ;
#25058=VERTEX_POINT ( 'NONE', #2842 ) ;
#25060=CARTESIAN_POINT ( 'NONE',  ( -1.699145597547422781, -29.51370389567643571, 7.785387725071483800 ) ) ;
#25064=ORIENTED_EDGE ( 'NONE', *, *, #30841, .F. ) ;
#25066=CARTESIAN_POINT ( 'NONE',  ( -0.01981084510887724456, -26.53464568598458229, 7.781480525794718162 ) ) ;
#25068=DIRECTION ( 'NONE',  ( 0.000000000000000000, 0.7541618601367565677, -0.6566885781822819901 ) ) ;
#25070=CARTESIAN_POINT ( 'NONE',  ( -1.582528736513596490, -30.78337320113038444, 7.750000000000000000 ) ) ;
#25073=CARTESIAN_POINT ( 'NONE',  ( 3.427626883898521548, -33.95934199490189087, 7.754798119455333705 ) ) ;
#25085=CARTESIAN_POINT ( 'NONE',  ( -1.544665293549569052, -28.25920506871950622, 7.754798119455333705 ) ) ;
#25086=CARTESIAN_POINT ( 'NONE',  ( 4.582084150952498547, -31.37432464074042215, 7.754798119455333705 ) ) ;
#25087=CARTESIAN_POINT ( 'NONE',  ( 4.086607214483024997, -27.00946490984718196, 6.912143950357347855 ) ) ;
#25089=CARTESIAN_POINT ( 'NONE',  ( -1.526829923184012339, -28.21528965334980654, 7.013842709614101167 ) ) ;
#25091=EDGE_LOOP ( 'NONE', ( #38974, #23376, #25907, #18304, #9855 ) ) ;
#25093=B_SPLINE_CURVE_WITH_KNOTS ( 'NONE', 3,
 ( #30136, #4816, #33454, #39590, #20862, #1953, #17151, #14068, #14271, #26647, #27449, #40005, #23555, #17757, #39180, #17964, #17346, #30345, #29924, #2151, #27240, #26841, #14670, #39381, #39807, #36315, #8085, #33649, #20652, #11576, #24357 ),
 .UNSPECIFIED., .F., .F.,
 ( 4, 3, 3, 3, 3, 3, 3, 3, 3, 3, 4 ),
 ( 8.673617379884035472E-19, 3.077658087705791864E-05, 6.152638666998900326E-05, 9.267501192706637957E-05, 0.0001241882240135233184, 0.0001556618703051675047, 0.0001866161554452220868, 0.0002167966385861002884, 0.0002463805737537799290, 0.0002758761370306525443, 0.0002847094172290028265 ),
 .UNSPECIFIED. ) ;
#25103=CARTESIAN_POINT ( 'NONE',  ( 1.018372654493346685, -32.90083822981368655, 6.866852738645442322 ) ) ;
#25104=VECTOR ( 'NONE', #6592, 1000.000000000000114 ) ;
#25105=VERTEX_POINT ( 'NONE', #10793 ) ;
#25117=CARTESIAN_POINT ( 'NONE',  ( 0.5233279421899477146, -26.28305482120240910, 7.778495531946297170 ) ) ;
#25121=CARTESIAN_POINT ( 'NONE',  ( 5.144846875551112753, -28.94886861257825572, 7.635761828346576685 ) ) ;
#25123=DIRECTION ( 'NONE',  ( 0.000000000000000000, -0.6662082868431813409, -0.7457657263118716573 ) ) ;
#25125=ORIENTED_EDGE ( 'NONE', *, *, #16450, .F. ) ;
#25126=CARTESIAN_POINT ( 'NONE',  ( 1.057293288892434457, -26.12951937787816448, 7.698786668945013290 ) ) ;
#25129=ORIENTED_EDGE ( 'NONE', *, *, #22349, .F. ) ;
#25130=CARTESIAN_POINT ( 'NONE',  ( 0.5270406883574831891, -32.76106163285440687, 7.775108481317162479 ) ) ;
#25133=CARTESIAN_POINT ( 'NONE',  ( 5.098282653295018285, -29.68964042297140793, 7.757178535559534183 ) ) ;
#25134=CARTESIAN_POINT ( 'NONE',  ( 4.834836695125773076, -27.99731481096146624, 7.387053503561885393 ) ) ;
#25136=AXIS2_PLACEMENT_3D ( 'NONE', #4587, #23900, #14032 ) ;
#25137=CARTESIAN_POINT ( 'NONE',  ( -1.229343149638864485, -31.29523348278805983, 7.730758795053808363 ) ) ;
#25153=ADVANCED_FACE ( 'NONE', ( #7517 ), #10599, .F. ) ;
#25155=CARTESIAN_POINT ( 'NONE',  ( -1.750039336912785126, -28.98295539875205762, 7.744938106820263179 ) ) ;
#25164=ORIENTED_EDGE ( 'NONE', *, *, #9110, .F. ) ;
#25169=EDGE_CURVE ( 'NONE', #5237, #35661, #25783, .T. ) ;
#25171=CARTESIAN_POINT ( 'NONE',  ( 4.267027349875077924, -31.94950500413386862, 7.009310105710487626 ) ) ;
#25172=CARTESIAN_POINT ( 'NONE',  ( -1.583891440918162585, -30.77968007673214146, 7.635761828346579350 ) ) ;
#25174=( BOUNDED_CURVE ( )  B_SPLINE_CURVE ( 3, ( #19862, #32434, #36126, #29731 ),
 .UNSPECIFIED., .F., .T. ) 
 B_SPLINE_CURVE_WITH_KNOTS ( ( 4, 4 ),
 ( 4.748221474220561511, 4.941946782021394924 ),
 .UNSPECIFIED. ) 
 CURVE ( )  GEOMETRIC_REPRESENTATION_ITEM ( )  RATIONAL_B_SPLINE_CURVE ( ( 1.000000000000000000, 0.9968749865767494445, 0.9968749865767494445, 1.000000000000000000 ) ) 
 REPRESENTATION_ITEM ( '' )  );
#25175=CARTESIAN_POINT ( 'NONE',  ( -1.412656310956876826, -31.16960079952658091, 7.011627023500184741 ) ) ;
#25178=CARTESIAN_POINT ( 'NONE',  ( 4.692798180838874345, -31.35690285333599903, 7.785344483711592822 ) ) ;
#25182=CARTESIAN_POINT ( 'NONE',  ( 5.036005266467588726, -25.61570514420120048, 7.635761828346577573 ) ) ;
#25185=CARTESIAN_POINT ( 'NONE',  ( 1.727929540585121382, -33.06982342786876217, 7.655937882338900380 ) ) ;
#25190=DIRECTION ( 'NONE',  ( -0.9396926207858986579, 0.3420201433256953027, 0.000000000000000000 ) ) ;
#25191=ADVANCED_FACE ( 'NONE', ( #10198 ), #9998, .F. ) ;
#25193=CARTESIAN_POINT ( 'NONE',  ( -1.544331477769930183, -30.58574382593747742, 6.871394612369937427 ) ) ;
#25194=ORIENTED_EDGE ( 'NONE', *, *, #26873, .T. ) ;
#25195=B_SPLINE_CURVE_WITH_KNOTS ( 'NONE', 3,
 ( #28628, #25538, #22262, #3137, #10076, #16458, #34829, #834, #28200, #31, #25130, #22049, #38081, #636, #6605, #22659, #13176, #19564, #18950, #9883, #38475, #19151, #15857, #22458, #25940 ),
 .UNSPECIFIED., .F., .F.,
 ( 4, 3, 3, 3, 3, 3, 3, 3, 4 ),
 ( 6.468151674593708260E-05, 9.076621574722118632E-05, 0.0001210204262067982105, 0.0001512763324577447578, 0.0001815301820994211050, 0.0002117781465860732264, 0.0002420274594459720092, 0.0002722905548971162764, 0.0002816827545175584085 ),
 .UNSPECIFIED. ) ;
#25196=CARTESIAN_POINT ( 'NONE',  ( 4.503588519744932128, -31.67704982672819014, 7.139344958878411695 ) ) ;
#25199=ORIENTED_EDGE ( 'NONE', *, *, #28255, .T. ) ;
#25203=CARTESIAN_POINT ( 'NONE',  ( 5.047147375954016191, -28.54561077161946869, 6.912143950357347855 ) ) ;
#25205=EDGE_CURVE ( 'NONE', #26823, #35733, #13525, .T. ) ;
#25206=CARTESIAN_POINT ( 'NONE',  ( 3.522825846568940378, -26.58183247331710319, 6.865554069792297653 ) ) ;
#25207=CARTESIAN_POINT ( 'NONE',  ( 5.025873565333792925, -30.27785960640749963, 7.757178535559534183 ) ) ;
#25209=EDGE_CURVE ( 'NONE', #31513, #4122, #16432, .T. ) ;
#25211=DIRECTION ( 'NONE',  ( -0.6427876096865179356, -0.7660444431189958880, 0.000000000000000000 ) ) ;
#25212=VECTOR ( 'NONE', #5639, 1000.000000000000000 ) ;
#25214=CARTESIAN_POINT ( 'NONE',  ( 0.4702888575080005906, -26.29321669331516631, 7.710604733652626663 ) ) ;
#25215=ORIENTED_EDGE ( 'NONE', *, *, #33013, .F. ) ;
#25217=B_SPLINE_CURVE_WITH_KNOTS ( 'NONE', 3,
 ( #39384, #8498, #11176, #8908, #34068, #5022, #27452, #27650, #27048, #14275, #21081, #23747, #39810, #8702, #11989, #5843, #8088, #40008, #39594 ),
 .UNSPECIFIED., .F., .F.,
 ( 4, 3, 3, 3, 3, 3, 4 ),
 ( 4.336808689942017255E-19, 2.546128104244576053E-05, 5.711050680483990296E-05, 8.113074941675622203E-05, 0.0001053129305727039069, 0.0001360598016347098994, 0.0001612931755702010528 ),
 .UNSPECIFIED. ) ;
#25219=CARTESIAN_POINT ( 'NONE',  ( -0.9993095062657011418, -27.34246030201092381, 7.730015791551952731 ) ) ;
#25225=CARTESIAN_POINT ( 'NONE',  ( 2.748053412748273860, -32.80449376584813592, 7.754798119455333705 ) ) ;
#25228=EDGE_LOOP ( 'NONE', ( #21572, #3350, #12440, #9947 ) ) ;
#25231=VERTEX_POINT ( 'NONE', #27261 ) ;
#25232=DIRECTION ( 'NONE',  ( 0.1736481776669404897, -0.9848077530122062440, -0.000000000000000000 ) ) ;
#25237=FACE_OUTER_BOUND ( 'NONE', #835, .T. ) ;
#25243=CIRCLE ( 'NONE', #7475, 3.499999999999999556 ) ;
#25254=ADVANCED_FACE ( 'NONE', ( #24180 ), #1976, .F. ) ;
#25257=( BOUNDED_CURVE ( )  B_SPLINE_CURVE ( 3, ( #21898, #15712, #18180, #40615 ),
 .UNSPECIFIED., .F., .T. ) 
 B_SPLINE_CURVE_WITH_KNOTS ( ( 4, 4 ),
 ( 1.347909859412854683, 1.534781240595299190 ),
 .UNSPECIFIED. ) 
 CURVE ( )  GEOMETRIC_REPRESENTATION_ITEM ( )  RATIONAL_B_SPLINE_CURVE ( ( 1.000000000000000000, 0.9970920404276226723, 0.9970920404276226723, 1.000000000000000000 ) ) 
 REPRESENTATION_ITEM ( '' )  );
#25262=CARTESIAN_POINT ( 'NONE',  ( 0.03162470699431392529, -32.53223031769636009, 7.693875151218754205 ) ) ;
#25266=CARTESIAN_POINT ( 'NONE',  ( -1.697502466828836099, -29.45021994381539088, 7.757178535559534183 ) ) ;
#25268=CARTESIAN_POINT ( 'NONE',  ( -1.336162095501038483, -31.09943851454543662, 7.006423389747789443 ) ) ;
#25274=FACE_OUTER_BOUND ( 'NONE', #4048, .T. ) ;
#25275=CARTESIAN_POINT ( 'NONE',  ( 5.036005266467588726, -25.61570514420120048, 7.635761828346577573 ) ) ;
#25278=DIRECTION ( 'NONE',  ( 0.5000000000000101030, -0.8660254037844328234, -0.000000000000000000 ) ) ;
#25279=CIRCLE ( 'NONE', #40385, 3.499999999999999556 ) ;
#25280=CARTESIAN_POINT ( 'NONE',  ( -0.9697213352172494583, -31.67483301990728251, 6.864651958020303368 ) ) ;
#25281=CARTESIAN_POINT ( 'NONE',  ( -1.654012860102806792, -29.01496998062980381, 7.693875151218752428 ) ) ;
#25284=DIRECTION ( 'NONE',  ( -0.000000000000000000, -0.000000000000000000, -1.000000000000000000 ) ) ;
#25287=CARTESIAN_POINT ( 'NONE',  ( -0.03042719556877983289, -32.61201718860353083, 7.743886751744253338 ) ) ;
#25292=CARTESIAN_POINT ( 'NONE',  ( 4.088894828626523648, -27.01159991581719311, 6.989977667959445640 ) ) ;
#25295=PLANE ( 'NONE',  #12822 ) ;
#25298=VECTOR ( 'NONE', #2306, 1000.000000000000000 ) ;
#25301=ORIENTED_EDGE ( 'NONE', *, *, #17452, .T. ) ;
#25309=CARTESIAN_POINT ( 'NONE',  ( -1.651164297088600907, -28.99801832941991364, 7.748216051605116839 ) ) ;
#25311=ORIENTED_EDGE ( 'NONE', *, *, #24838, .F. ) ;
#25313=EDGE_CURVE ( 'NONE', #37415, #35661, #36140, .T. ) ;
#25320=ORIENTED_EDGE ( 'NONE', *, *, #2630, .F. ) ;
#25323=CARTESIAN_POINT ( 'NONE',  ( 4.886497164546935501, -28.38302832708262713, 7.652160403243383868 ) ) ;
#25325=DIRECTION ( 'NONE',  ( 1.000000000000000000, 0.000000000000000000, 0.000000000000000000 ) ) ;
#25330=AXIS2_PLACEMENT_3D ( 'NONE', #8602, #5527, #20549 ) ;
#25341=CARTESIAN_POINT ( 'NONE',  ( -1.659519015307392209, -30.57436305425760281, 7.387053503561888057 ) ) ;
#25342=CARTESIAN_POINT ( 'NONE',  ( -1.339380734913657500, -27.83505459351727396, 7.750000000000002665 ) ) ;
#25343=CARTESIAN_POINT ( 'NONE',  ( -1.292372527722988274, -31.18345358561926162, 7.774064877406527074 ) ) ;
#25345=VERTEX_POINT ( 'NONE', #11396 ) ;
#25347=CARTESIAN_POINT ( 'NONE',  ( 1.700390093233090871, -29.56993018339339940, 7.750000000000000888 ) ) ;
#25349=EDGE_CURVE ( 'NONE', #18928, #19595, #4838, .T. ) ;
#25355=EDGE_CURVE ( 'NONE', #38144, #33085, #39404, .T. ) ;
#25356=CARTESIAN_POINT ( 'NONE',  ( 4.935900671829004160, -28.52514296371000668, 6.863904403958575706 ) ) ;
#25357=ORIENTED_EDGE ( 'NONE', *, *, #12980, .F. ) ;
#25368=CARTESIAN_POINT ( 'NONE',  ( 3.907524105502494738, -32.26773122059653076, 7.785096263473212375 ) ) ;
#25384=LINE ( 'NONE', #13223, #39918 ) ;
#25386=CARTESIAN_POINT ( 'NONE',  ( -0.6412884647684967687, -32.03499445358951903, 6.969307238440504371 ) ) ;
#25387=AXIS2_PLACEMENT_3D ( 'NONE', #10744, #7671, #20223 ) ;
#25391=DIRECTION ( 'NONE',  ( 0.9396926207859135349, -0.3420201433256548351, 0.000000000000000000 ) ) ;
#25398=CARTESIAN_POINT ( 'NONE',  ( 0.4238093638620683556, -32.72117464255529029, 7.754798119455333705 ) ) ;
#25400=ORIENTED_EDGE ( 'NONE', *, *, #20262, .F. ) ;
#25403=ORIENTED_EDGE ( 'NONE', *, *, #23301, .F. ) ;
#25404=CYLINDRICAL_SURFACE ( 'NONE', #35133, 3.399999999999999911 ) ;
#25405=CYLINDRICAL_SURFACE ( 'NONE', #8787, 0.09010775117052882699 ) ;
#25406=EDGE_CURVE ( 'NONE', #18768, #651, #11864, .T. ) ;
#25408=CARTESIAN_POINT ( 'NONE',  ( 3.582330644718626722, -26.61893302209879408, 6.880828092187098122 ) ) ;
#25410=ORIENTED_EDGE ( 'NONE', *, *, #29699, .F. ) ;
#25411=FACE_OUTER_BOUND ( 'NONE', #18747, .T. ) ;
#25412=EDGE_LOOP ( 'NONE', ( #31627, #33976, #35049, #21550 ) ) ;
#25413=CARTESIAN_POINT ( 'NONE',  ( 0.4697380470346541603, -26.29342357708423350, 7.700536657684214248 ) ) ;
#25430=CARTESIAN_POINT ( 'NONE',  ( -0.06090154667645011205, -32.58437486080601531, 7.778495531946292729 ) ) ;
#25432=CARTESIAN_POINT ( 'NONE',  ( 3.419291884707112761, -26.52109817239846734, 7.700536657684210695 ) ) ;
#25434=CARTESIAN_POINT ( 'NONE',  ( -0.02684669743237798334, -25.18051837188491149, 7.754798119455333705 ) ) ;
#25436=CARTESIAN_POINT ( 'NONE',  ( 5.196021075228325792, -29.74475591867008362, 7.006908160621407866 ) ) ;
#25437=ADVANCED_FACE ( 'NONE', ( #12839 ), #31591, .F. ) ;
#25441=DIRECTION ( 'NONE',  ( 0.9848077530122077983, -0.1736481776669321353, 0.000000000000000000 ) ) ;
#25445=B_SPLINE_CURVE_WITH_KNOTS ( 'NONE', 3,
 ( #19429, #3807, #35298, #22534, #9545, #10144, #22735, #16326, #28900, #13243, #905, #19635, #19026, #38548, #25809, #6874, #102, #15925, #32209, #22334, #28490, #15730, #35098, #4009, #16526 ),
 .UNSPECIFIED., .F., .F.,
 ( 4, 3, 3, 3, 3, 3, 3, 3, 4 ),
 ( 6.468151674593381644E-05, 9.076621574722021054E-05, 0.0001210204262067969501, 0.0001512763324577428333, 0.0001815301820994210237, 0.0002117781465860714375, 0.0002420274594459746113, 0.0002722905548971154633, 0.0002816827545175555896 ),
 .UNSPECIFIED. ) ;
#25450=B_SPLINE_CURVE_WITH_KNOTS ( 'NONE', 3,
 ( #31964, #13206, #32172, #29064, #4162, #4558, #19793, #16679, #871, #14004, #19985, #17084, #1277, #10512, #669, #35657, #38511, #10312, #19599 ),
 .UNSPECIFIED., .F., .F.,
 ( 4, 3, 3, 3, 3, 3, 4 ),
 ( 0.000000000000000000, 2.546128104244556401E-05, 5.711050680484009269E-05, 8.113074941675658795E-05, 0.0001053129305727048420, 0.0001360598016347089507, 0.0001612931755713726417 ),
 .UNSPECIFIED. ) ;
#25454=ORIENTED_EDGE ( 'NONE', *, *, #24683, .F. ) ;
#25457=CARTESIAN_POINT ( 'NONE',  ( 1.161761687666269749, -26.12572513379734218, 7.784725160561909441 ) ) ;
#25465=CARTESIAN_POINT ( 'NONE',  ( 2.510480264938812045, -26.15794710555851310, 7.387053503561887169 ) ) ;
#25469=B_SPLINE_CURVE_WITH_KNOTS ( 'NONE', 3,
 ( #37839, #34794, #6572, #400 ),
 .UNSPECIFIED., .F., .F.,
 ( 4, 4 ),
 ( 8.673617379884035472E-19, 2.475319317933456399E-05 ),
 .UNSPECIFIED. ) ;
#25470=CARTESIAN_POINT ( 'NONE',  ( 0.9463359558106179126, -32.98775010660822460, 6.877402575842992860 ) ) ;
#25477=VERTEX_POINT ( 'NONE', #19228 ) ;
#25478=CARTESIAN_POINT ( 'NONE',  ( -1.346119371218626792, -31.29294500718514271, 6.894806418505347700 ) ) ;
#25484=CARTESIAN_POINT ( 'NONE',  ( -0.02105859379946962290, -32.61732735699371943, 7.720710062488898906 ) ) ;
#25485=ORIENTED_EDGE ( 'NONE', *, *, #16621, .F. ) ;
#25490=CARTESIAN_POINT ( 'NONE',  ( 1.694962496619858427, -26.16992440333174130, 7.763628509615287498 ) ) ;
#25491=CARTESIAN_POINT ( 'NONE',  ( -1.799609906766908685, -29.56993018339339940, 6.929570838012926615 ) ) ;
#25492=CARTESIAN_POINT ( 'NONE',  ( 4.674598849011252000, -27.92248298331306700, 7.785172627573962778 ) ) ;
#25500=CARTESIAN_POINT ( 'NONE',  ( -1.347083181716895339, -31.26079133133813315, 7.785593909369612931 ) ) ;
#25501=EDGE_LOOP ( 'NONE', ( #31852, #5057, #29384, #38855 ) ) ;
#25502=CARTESIAN_POINT ( 'NONE',  ( 2.912097039036203761, -32.85349084633266159, 7.638132480492516585 ) ) ;
#25505=ORIENTED_EDGE ( 'NONE', *, *, #9860, .F. ) ;
#25518=CARTESIAN_POINT ( 'NONE',  ( 4.695449071104084382, -27.96066553437519886, 6.864651958020304257 ) ) ;
#25522=CARTESIAN_POINT ( 'NONE',  ( 3.793404844923233377, -32.38367570474625978, 7.387053503561885393 ) ) ;
#25523=CARTESIAN_POINT ( 'NONE',  ( 5.181826490399478402, -29.15396049260679945, 7.398879060202674829 ) ) ;
#25527=EDGE_CURVE ( 'NONE', #9233, #34426, #5119, .T. ) ;
#25538=CARTESIAN_POINT ( 'NONE',  ( 0.5713750229309363382, -32.77700439067807281, 7.703977250142848732 ) ) ;
#25543=CARTESIAN_POINT ( 'NONE',  ( 5.100200997230469824, -29.53407189201577410, 7.691066658568944447 ) ) ;
#25544=CARTESIAN_POINT ( 'NONE',  ( 5.140791489254627145, -28.92678305073006584, 7.695279973900954751 ) ) ;
#25546=ORIENTED_EDGE ( 'NONE', *, *, #21640, .F. ) ;
#25547=FACE_OUTER_BOUND ( 'NONE', #40679, .T. ) ;
#25550=ORIENTED_EDGE ( 'NONE', *, *, #35860, .F. ) ;
#25553=CARTESIAN_POINT ( 'NONE',  ( 1.657039758437295340, -33.05528407258798040, 7.785096263473211486 ) ) ;
#25557=CARTESIAN_POINT ( 'NONE',  ( 3.011115207906999380, -26.32487479661073948, 7.754798119455333705 ) ) ;
#25558=CARTESIAN_POINT ( 'NONE',  ( 2.293941986480968254, -26.12062633890310437, 7.636816916992233750 ) ) ;
#25564=CARTESIAN_POINT ( 'NONE',  ( 2.858160284951835717, -26.37311349386845549, 7.763628509615289275 ) ) ;
#25575=VECTOR ( 'NONE', #39939, 1000.000000000000114 ) ;
#25578=CARTESIAN_POINT ( 'NONE',  ( -0.9707194483615372294, -31.83160614747662720, 7.638132480492516585 ) ) ;
#25581=CARTESIAN_POINT ( 'NONE',  ( -1.699482881577310422, -29.59931989509443895, 7.661510568013095934 ) ) ;
#25583=EDGE_CURVE ( 'NONE', #26604, #5603, #8015, .T. ) ;
#25584=CARTESIAN_POINT ( 'NONE',  ( 4.688455439100348343, -31.36368888288187406, 7.785593909369613819 ) ) ;
#25587=EDGE_CURVE ( 'NONE', #37354, #6054, #16336, .T. ) ;
#25588=FACE_OUTER_BOUND ( 'NONE', #11851, .T. ) ;
#25591=CARTESIAN_POINT ( 'NONE',  ( 1.736346942945644400, -33.06974547922812491, 7.695279973900954751 ) ) ;
#25592=CARTESIAN_POINT ( 'NONE',  ( 1.733559400163837250, -32.96977048603782379, 7.670860738520327793 ) ) ;
#25593=CARTESIAN_POINT ( 'NONE',  ( 2.099095770640518666, -32.94647852641658403, 7.006423389747791219 ) ) ;
#25596=VERTEX_POINT ( 'NONE', #4199 ) ;
#25599=CARTESIAN_POINT ( 'NONE',  ( 2.976261230439396499, -26.31076574427040526, 6.865554069792297653 ) ) ;
#25601=FACE_OUTER_BOUND ( 'NONE', #22436, .T. ) ;
#25605=CARTESIAN_POINT ( 'NONE',  ( -1.434533901437197168, -28.25375393532444335, 6.876076431790004939 ) ) ;
#25606=CARTESIAN_POINT ( 'NONE',  ( 3.558149082814241915, -26.60364649932381198, 6.867199677474203234 ) ) ;
#25607=DIRECTION ( 'NONE',  ( 0.8660254037844449249, -0.4999999999999888423, -0.000000000000000000 ) ) ;
#25611=EDGE_LOOP ( 'NONE', ( #36905, #39159, #20051, #32046 ) ) ;
#25612=CARTESIAN_POINT ( 'NONE',  ( -1.233825218002540414, -31.30161613693384481, 7.257242401810563237 ) ) ;
#25616=CARTESIAN_POINT ( 'NONE',  ( -1.657321944901828825, -30.10450465805885045, 6.887041543973312585 ) ) ;
#25621=CARTESIAN_POINT ( 'NONE',  ( 3.977772666037320715, -27.04534534285276592, 7.754798119455333705 ) ) ;
#25622=CARTESIAN_POINT ( 'NONE',  ( -1.601964535056334960, -30.69171433492233092, 7.782861076432731728 ) ) ;
#25625=CARTESIAN_POINT ( 'NONE',  ( 3.875507134935765041, -26.95672030760948346, 7.635761828346577573 ) ) ;
#25626=EDGE_LOOP ( 'NONE', ( #666, #3836, #35017, #2375, #22999 ) ) ;
#25630=CARTESIAN_POINT ( 'NONE',  ( -0.1425244880348677801, -32.54239410267695121, 7.766640943994648438 ) ) ;
#25637=CARTESIAN_POINT ( 'NONE',  ( 3.780365410620694977, -32.25950308696851465, 6.865312560952604670 ) ) ;
#25641=LINE ( 'NONE', #3245, #17721 ) ;
#25642=CARTESIAN_POINT ( 'NONE',  ( 1.746581778429556975, -26.07022345230773652, 6.880608371227950215 ) ) ;
#25645=DIRECTION ( 'NONE',  ( -0.3420201433256726542, 0.9396926207859070956, -0.000000000000000000 ) ) ;
#25649=CARTESIAN_POINT ( 'NONE',  ( 2.289108667884883985, -26.11979771739482459, 7.747520101777647383 ) ) ;
#25651=DIRECTION ( 'NONE',  ( 1.000000000000000000, 0.000000000000000000, 0.000000000000000000 ) ) ;
#25654=EDGE_CURVE ( 'NONE', #38807, #24578, #13333, .T. ) ;
#25668=EDGE_CURVE ( 'NONE', #16321, #22181, #7269, .T. ) ;
#25670=CARTESIAN_POINT ( 'NONE',  ( 0.9556399531351862375, -32.98977626601526936, 6.872971584836693459 ) ) ;
#25671=CARTESIAN_POINT ( 'NONE',  ( -1.793434212015915241, -29.46706035826072068, 7.771081512783700518 ) ) ;
#25677=CARTESIAN_POINT ( 'NONE',  ( -0.5222078730473904695, -32.14287757506037480, 6.894806418505348589 ) ) ;
#25681=CARTESIAN_POINT ( 'NONE',  ( -0.02499863111512088884, -26.64024867341794334, 7.661510568013094158 ) ) ;
#25686=CARTESIAN_POINT ( 'NONE',  ( 3.388683086819756163, -26.61871572696936994, 7.635761828346577573 ) ) ;
#25688=EDGE_LOOP ( 'NONE', ( #10902, #35207, #13672, #40469, #28919 ) ) ;
#25689=CARTESIAN_POINT ( 'NONE',  ( 1.720943750993247701, -26.16997840318206059, 7.779495906702013741 ) ) ;
#25690=AXIS2_PLACEMENT_3D ( 'NONE', #12768, #28421, #6810 ) ;
#25692=CARTESIAN_POINT ( 'NONE',  ( 4.484829609511931103, -25.15321385373581720, 6.954324564059724878 ) ) ;
#25697=CARTESIAN_POINT ( 'NONE',  ( 4.285375923250596131, -31.77851530935270929, 7.782167645815903256 ) ) ;
#25701=CARTESIAN_POINT ( 'NONE',  ( -0.4019653665099892637, -26.77169832722271181, 6.980586498568963627 ) ) ;
#25702=CARTESIAN_POINT ( 'NONE',  ( -1.363502849816506712, -31.24056455800023002, 7.780491323090173772 ) ) ;
#25703=DIRECTION ( 'NONE',  ( 0.2567910337120216657, 0.7055275666422177183, -0.6605219282605403475 ) ) ;
#25704=CARTESIAN_POINT ( 'NONE',  ( 3.991766160750894077, -32.22459883366656896, 7.255881584735161205 ) ) ;
#25714=EDGE_CURVE ( 'NONE', #19304, #30375, #9367, .T. ) ;
#25716=ORIENTED_EDGE ( 'NONE', *, *, #15845, .T. ) ;
#25717=EDGE_CURVE ( 'NONE', #2507, #30413, #12486, .T. ) ;
#25718=AXIS2_PLACEMENT_3D ( 'NONE', #39909, #23842, #24049 ) ;
#25720=B_SPLINE_CURVE_WITH_KNOTS ( 'NONE', 3,
 ( #13016, #3778, #29476, #32375, #677, #4173, #10116, #1088, #25578, #38123 ),
 .UNSPECIFIED., .F., .F.,
 ( 4, 3, 3, 4 ),
 ( 0.0002170292169044743470, 0.0002420761345915946555, 0.0002723302478206985223, 0.0002816811360866763132 ),
 .UNSPECIFIED. ) ;
#25728=VERTEX_POINT ( 'NONE', #30518 ) ;
#25732=DIRECTION ( 'NONE',  ( -0.000000000000000000, -0.000000000000000000, -1.000000000000000000 ) ) ;
#25737=DIRECTION ( 'NONE',  ( 1.000000000000000000, 0.000000000000000000, 0.000000000000000000 ) ) ;
#25741=CYLINDRICAL_SURFACE ( 'NONE', #7216, 0.09010775117052950700 ) ;
#25745=PRODUCT_DEFINITION_SHAPE ( 'NONE', 'NONE',  #38149 ) ;
#25747=CARTESIAN_POINT ( 'NONE',  ( 2.913833110970087681, -32.85284901314008010, 7.750000000000001776 ) ) ;
#25748=EDGE_CURVE ( 'NONE', #37415, #35810, #3275, .T. ) ;
#25749=CARTESIAN_POINT ( 'NONE',  ( -1.302126302899671906, -31.16520435485670859, 7.757178535559533294 ) ) ;
#25759=ORIENTED_EDGE ( 'NONE', *, *, #33305, .F. ) ;
#25764=ORIENTED_EDGE ( 'NONE', *, *, #14723, .T. ) ;
#25766=CARTESIAN_POINT ( 'NONE',  ( 3.801569219118249965, -32.36904792630235050, 6.931070083220557621 ) ) ;
#25767=VERTEX_POINT ( 'NONE', #36891 ) ;
#25768=EDGE_CURVE ( 'NONE', #14030, #18413, #694, .T. ) ;
#25770=CARTESIAN_POINT ( 'NONE',  ( 2.851183333853939850, -26.37060056268141039, 7.756377446753168314 ) ) ;
#25778=CARTESIAN_POINT ( 'NONE',  ( 4.357793904757863324, -27.44903297171773460, 6.870716933885666400 ) ) ;
#25779=CARTESIAN_POINT ( 'NONE',  ( 1.794853143836061315, -26.07837181994090159, 7.776484688137384360 ) ) ;
#25781=LINE ( 'NONE', #7840, #28232 ) ;
#25783=B_SPLINE_CURVE_WITH_KNOTS ( 'NONE', 3,
 ( #35349, #13900, #19684, #4246, #4056, #16572, #22981, #29352, #32654, #23371, #35741, #13287, #1172, #28951, #35149, #4453, #19483, #20076, #38602 ),
 .UNSPECIFIED., .F., .F.,
 ( 4, 3, 3, 3, 3, 3, 4 ),
 ( 4.336808689942017736E-19, 2.546128104244715982E-05, 5.711050680484228820E-05, 8.113074941675809228E-05, 0.0001053129305727074576, 0.0001360598016347136941, 0.0001612931755713733735 ),
 .UNSPECIFIED. ) ;
#25787=CARTESIAN_POINT ( 'NONE',  ( 2.378989766893257141, -26.23833859934407187, 7.778050822775631978 ) ) ;
#25795=CARTESIAN_POINT ( 'NONE',  ( 3.262282976461500894, -25.12033811116058502, 7.695279973900954751 ) ) ;
#25796=CARTESIAN_POINT ( 'NONE',  ( 3.416617830832153757, -32.50498765347735031, 7.748216051605118615 ) ) ;
#25799=CARTESIAN_POINT ( 'NONE',  ( -1.477019764706915872, -28.35990217932980073, 7.785868773668302545 ) ) ;
#25801=FACE_OUTER_BOUND ( 'NONE', #28615, .T. ) ;
#25807=CARTESIAN_POINT ( 'NONE',  ( 5.045002655040953243, -28.53863642728069649, 7.006908160621412307 ) ) ;
#25809=CARTESIAN_POINT ( 'NONE',  ( 1.159600155072761707, -26.21319852615044610, 7.785868773668302545 ) ) ;
#25813=ORIENTED_EDGE ( 'NONE', *, *, #21613, .T. ) ;
#25823=CARTESIAN_POINT ( 'NONE',  ( -1.710676486807355845, -28.78592482586367396, 6.908075350836297979 ) ) ;
#25832=ORIENTED_EDGE ( 'NONE', *, *, #23301, .T. ) ;
#25836=CARTESIAN_POINT ( 'NONE',  ( -0.1177018426203055718, -32.54868846376324143, 7.780491323090173772 ) ) ;
#25841=CARTESIAN_POINT ( 'NONE',  ( 3.358563326585730646, -32.65222908060306395, 6.863784140767622333 ) ) ;
#25843=CARTESIAN_POINT ( 'NONE',  ( 5.196273801610021614, -29.73962725910407201, 6.895394898881660239 ) ) ;
#25845=DIRECTION ( 'NONE',  ( 0.000000000000000000, -1.000000000000000000, 0.000000000000000000 ) ) ;
#25852=( BOUNDED_CURVE ( )  B_SPLINE_CURVE ( 3, ( #517, #16142, #9961, #22741 ),
 .UNSPECIFIED., .F., .F. ) 
 B_SPLINE_CURVE_WITH_KNOTS ( ( 4, 4 ),
 ( 4.708531083176465515, 4.895802057644187855 ),
 .UNSPECIFIED. ) 
 CURVE ( )  GEOMETRIC_REPRESENTATION_ITEM ( )  RATIONAL_B_SPLINE_CURVE ( ( 1.000000000000000000, 0.9970795998553221295, 0.9970795998553221295, 1.000000000000000000 ) ) 
 REPRESENTATION_ITEM ( '' )  );
#25859=CARTESIAN_POINT ( 'NONE',  ( 2.231244765351310999, -32.92823233136791572, 7.785172627573962778 ) ) ;
#25861=VERTEX_POINT ( 'NONE', #17726 ) ;
#25866=CARTESIAN_POINT ( 'NONE',  ( -1.722970638209900596, -28.84261588273779964, 7.754798119455333705 ) ) ;
#25869=CARTESIAN_POINT ( 'NONE',  ( 2.721684545581986470, -26.21510794498386332, 7.139344958878412584 ) ) ;
#25871=VERTEX_POINT ( 'NONE', #18548 ) ;
#25872=DIRECTION ( 'NONE',  ( -0.000000000000000000, -0.000000000000000000, -1.000000000000000000 ) ) ;
#25873=CARTESIAN_POINT ( 'NONE',  ( 0.9057233922578412644, -32.97852313274928804, 6.935328752148349096 ) ) ;
#25874=DIRECTION ( 'NONE',  ( -0.9848077530122069101, -0.1736481776669374644, -0.000000000000000000 ) ) ;
#25878=CARTESIAN_POINT ( 'NONE',  ( 5.200336455197794194, -29.55055330619316223, 7.643192810543819604 ) ) ;
#25879=CARTESIAN_POINT ( 'NONE',  ( -1.032376314427851050, -31.59280015088546278, 6.979335674598005745 ) ) ;
#25883=DIRECTION ( 'NONE',  ( -0.7055275666422188285, 0.2567910337120248299, 0.6605219282605380160 ) ) ;
#25888=CARTESIAN_POINT ( 'NONE',  ( -1.267760583032661037, -27.71561997405539302, 7.754798119455333705 ) ) ;
#25895=CARTESIAN_POINT ( 'NONE',  ( 3.913023411691590514, -33.78267210696904499, 6.894806418505347700 ) ) ;
#25896=CARTESIAN_POINT ( 'NONE',  ( -0.9894248136993964993, -27.33053388830764874, 7.635761828346571356 ) ) ;
#25900=EDGE_CURVE ( 'NONE', #29061, #34783, #35696, .T. ) ;
#25906=CARTESIAN_POINT ( 'NONE',  ( 4.358291535071522560, -27.29274773012506827, 7.686927408461905920 ) ) ;
#25907=ORIENTED_EDGE ( 'NONE', *, *, #38331, .T. ) ;
#25910=DIRECTION ( 'NONE',  ( 0.000000000000000000, 0.000000000000000000, -1.000000000000000000 ) ) ;
#25913=AXIS2_PLACEMENT_3D ( 'NONE', #15131, #40243, #12028 ) ;
#25920=VERTEX_POINT ( 'NONE', #15061 ) ;
#25923=CARTESIAN_POINT ( 'NONE',  ( 5.671973749040267521, -26.25500220387225170, 7.635761828346577573 ) ) ;
#25925=CARTESIAN_POINT ( 'NONE',  ( 4.607344540115766662, -31.33336738918632847, 6.874555630061443878 ) ) ;
#25930=ORIENTED_EDGE ( 'NONE', *, *, #25668, .T. ) ;
#25931=CARTESIAN_POINT ( 'NONE',  ( 5.149333021513059272, -30.16559723925941228, 7.756742906098589074 ) ) ;
#25936=CARTESIAN_POINT ( 'NONE',  ( 0.4870777624547221185, -32.74607263478868191, 6.889465824494258150 ) ) ;
#25940=CARTESIAN_POINT ( 'NONE',  ( 0.4238093638620683556, -32.72117464255529029, 7.754798119455333705 ) ) ;
#25942=FACE_OUTER_BOUND ( 'NONE', #11282, .T. ) ;
#25943=AXIS2_PLACEMENT_3D ( 'NONE', #1504, #13847, #26613 ) ;
#25947=CARTESIAN_POINT ( 'NONE',  ( 0.5502190760550982329, -32.76947806258566231, 7.635761828346577573 ) ) ;
#25948=DIRECTION ( 'NONE',  ( -0.6427876096865545730, 0.7660444431189653569, 0.000000000000000000 ) ) ;
#25952=ORIENTED_EDGE ( 'NONE', *, *, #29421, .T. ) ;
#25968=CARTESIAN_POINT ( 'NONE',  ( 3.816332953347056467, -32.35790253036758202, 7.011627023500185629 ) ) ;
#25974=LINE ( 'NONE', #29656, #10782 ) ;
#25983=VECTOR ( 'NONE', #13993, 1000.000000000000114 ) ;
#25984=CARTESIAN_POINT ( 'NONE',  ( 1.700951572572590331, -26.07317559334259371, 7.767720160662275219 ) ) ;
#25989=CARTESIAN_POINT ( 'NONE',  ( -1.699450209411329737, -29.60309949032410515, 7.670860738520326905 ) ) ;
#25991=ADVANCED_FACE ( 'NONE', ( #24533 ), #21250, .F. ) ;
#25993=CARTESIAN_POINT ( 'NONE',  ( -0.5341021525900384592, -32.13256682235309114, 6.880147297696980857 ) ) ;
#25994=CARTESIAN_POINT ( 'NONE',  ( 3.922483456672744673, -26.86580350659783178, 7.695279973900954751 ) ) ;
#25998=LINE ( 'NONE', #26802, #37104 ) ;
#26000=CARTESIAN_POINT ( 'NONE',  ( 2.198740986243329587, -32.93322359727931570, 6.866852738645442322 ) ) ;
#26004=CARTESIAN_POINT ( 'NONE',  ( -1.500935203769204973, -28.42471564332976541, 7.748216051605119503 ) ) ;
#26009=CARTESIAN_POINT ( 'NONE',  ( -1.347521135996686992, -31.09247807141954212, 7.386948897581450346 ) ) ;
#26014=PLANE ( 'NONE',  #9494 ) ;
#26017=CARTESIAN_POINT ( 'NONE',  ( 2.323431556773316586, -32.91235948273799750, 7.670860738520328681 ) ) ;
#26018=DIRECTION ( 'NONE',  ( 1.000000000000000000, 3.965082230804130614E-15, 0.000000000000000000 ) ) ;
#26019=CARTESIAN_POINT ( 'NONE',  ( 1.245175783478524867, -26.09964713766223099, 6.880828092187098122 ) ) ;
#26020=ORIENTED_EDGE ( 'NONE', *, *, #29916, .F. ) ;
#26023=CARTESIAN_POINT ( 'NONE',  ( 0.4724743091557946362, -26.29239483759356588, 7.720710062488890024 ) ) ;
#26024=ORIENTED_EDGE ( 'NONE', *, *, #31351, .T. ) ;
#26027=CARTESIAN_POINT ( 'NONE',  ( -1.740368116565756518, -28.92869283221914145, 6.891642963669610822 ) ) ;
#26032=FACE_OUTER_BOUND ( 'NONE', #32907, .T. ) ;
#26038=ORIENTED_EDGE ( 'NONE', *, *, #2297, .F. ) ;
#26041=EDGE_CURVE ( 'NONE', #32186, #12012, #24213, .T. ) ;
#26044=CARTESIAN_POINT ( 'NONE',  ( 1.736346942945568905, -25.86893018339335981, 7.695279973900954751 ) ) ;
#26045=EDGE_CURVE ( 'NONE', #35202, #5880, #37480, .T. ) ;
#26048=CYLINDRICAL_SURFACE ( 'NONE', #37763, 0.09010775117052929883 ) ;
#26050=CARTESIAN_POINT ( 'NONE',  ( -1.089794412209061480, -31.68295418363346272, 7.006908160621417636 ) ) ;
#26051=CARTESIAN_POINT ( 'NONE',  ( 5.195250593675200257, -29.75957179320715085, 6.931070083220548739 ) ) ;
#26054=EDGE_CURVE ( 'NONE', #422, #36032, #26375, .T. ) ;
#26058=EDGE_CURVE ( 'NONE', #37348, #109, #31952, .T. ) ;
#26069=CARTESIAN_POINT ( 'NONE',  ( 2.322457828100205290, -32.91253870567615536, 7.721096864323903297 ) ) ;
#26076=CARTESIAN_POINT ( 'NONE',  ( 5.166866161692755810, -29.08666662507720702, 7.750000000000000888 ) ) ;
#26078=CARTESIAN_POINT ( 'NONE',  ( -1.666958026621576883, -30.04000107135736641, 7.754798119455333705 ) ) ;
#26080=DIRECTION ( 'NONE',  ( 0.000000000000000000, 0.000000000000000000, 1.000000000000000000 ) ) ;
#26081=CYLINDRICAL_SURFACE ( 'NONE', #14987, 0.09010775117053118621 ) ;
#26083=CYLINDRICAL_SURFACE ( 'NONE', #23096, 0.09010775117052960415 ) ;
#26087=EDGE_LOOP ( 'NONE', ( #14842, #9675, #29855, #12274, #5547 ) ) ;
#26088=CARTESIAN_POINT ( 'NONE',  ( -1.020414035563122601, -31.60885757119451256, 7.013842709614101167 ) ) ;
#26097=CARTESIAN_POINT ( 'NONE',  ( -0.03448549664302677509, -32.60970101154014600, 7.750000000000000000 ) ) ;
#26098=CARTESIAN_POINT ( 'NONE',  ( -0.8809027425463855643, -31.78283038357269419, 7.695279973900954751 ) ) ;
#26099=CARTESIAN_POINT ( 'NONE',  ( 3.922523015185340522, -26.86583601202378802, 7.698786668945015066 ) ) ;
#26105=CARTESIAN_POINT ( 'NONE',  ( 1.062037487867982355, -25.86893018339336692, 6.894806418505347700 ) ) ;
#26106=CARTESIAN_POINT ( 'NONE',  ( -0.3962189974208576992, -26.89332219547525327, 6.864276522220859711 ) ) ;
#26111=CARTESIAN_POINT ( 'NONE',  ( 4.227867036651674404, -31.84410382479391188, 7.759451378593101190 ) ) ;
#26114=CARTESIAN_POINT ( 'NONE',  ( 4.819878230686599707, -30.92226195030272606, 6.920489980334474822 ) ) ;
#26115=CARTESIAN_POINT ( 'NONE',  ( -1.233832883691663662, -27.66196159070634408, 6.989977667959444751 ) ) ;
#26126=B_SPLINE_CURVE_WITH_KNOTS ( 'NONE', 3,
 ( #21533, #34315, #126, #5883, #2813, #3028, #40047, #3236, #6085, #34111 ),
 .UNSPECIFIED., .F., .F.,
 ( 4, 3, 3, 4 ),
 ( 0.0002170292169044765425, 0.0002420761345915954958, 0.0002723302478207011244, 0.0002816811360866737111 ),
 .UNSPECIFIED. ) ;
#26131=CARTESIAN_POINT ( 'NONE',  ( 4.602267184982021142, -31.34168336721522508, 6.870716933885666400 ) ) ;
#26133=CARTESIAN_POINT ( 'NONE',  ( -1.253435461249161831, -27.88620972153293565, 7.748216051605118615 ) ) ;
#26137=CARTESIAN_POINT ( 'NONE',  ( 5.121205169401321200, -30.24961392475126232, 7.782861076432731728 ) ) ;
#26145=FACE_OUTER_BOUND ( 'NONE', #16823, .T. ) ;
#26155=CARTESIAN_POINT ( 'NONE',  ( -1.765620486186735949, -30.05597079739024835, 7.753200566781599079 ) ) ;
#26157=CARTESIAN_POINT ( 'NONE',  ( 2.902716051567627797, -32.85547488104512581, 7.762796336881261361 ) ) ;
#26160=CARTESIAN_POINT ( 'NONE',  ( 3.422521930177921057, -32.50152978473241205, 7.652160403243384756 ) ) ;
#26165=CARTESIAN_POINT ( 'NONE',  ( -1.635341556108417027, -30.62959728375151514, 6.875780273367530171 ) ) ;
#26173=DIRECTION ( 'NONE',  ( -0.6427876096865430267, 0.7660444431189749048, -0.000000000000000000 ) ) ;
#26179=ORIENTED_EDGE ( 'NONE', *, *, #36764, .F. ) ;
#26181=CARTESIAN_POINT ( 'NONE',  ( -1.598573221982714454, -28.40080711106888600, 7.660770905198783787 ) ) ;
#26182=CARTESIAN_POINT ( 'NONE',  ( -1.003736583562490070, -27.34783681995376270, 7.695279973900954751 ) ) ;
#26191=CARTESIAN_POINT ( 'NONE',  ( 1.651482305834180986, -26.06346787019676370, 7.255881584735163869 ) ) ;
#26197=CARTESIAN_POINT ( 'NONE',  ( 3.570212250164635392, -26.73024761574886199, 6.911401339314953596 ) ) ;
#26198=FACE_OUTER_BOUND ( 'NONE', #7131, .T. ) ;
#26199=ORIENTED_EDGE ( 'NONE', *, *, #26873, .F. ) ;
#26200=CARTESIAN_POINT ( 'NONE',  ( 0.6845764506890200662, -26.32520861239037302, 6.871394612369935651 ) ) ;
#26202=DIRECTION ( 'NONE',  ( 0.5751513419797962268, -0.4826092789263561333, -0.6605219282605402364 ) ) ;
#26206=CARTESIAN_POINT ( 'NONE',  ( 4.976896699542257885, -28.33927813719497024, 7.700536657684219577 ) ) ;
#26208=CARTESIAN_POINT ( 'NONE',  ( 3.293813124479239018, -32.57342865076346783, 7.754798119455333705 ) ) ;
#26214=PLANE ( 'NONE',  #2135 ) ;
#26216=AXIS2_PLACEMENT_3D ( 'NONE', #34319, #15551, #30391 ) ;
#26217=EDGE_CURVE ( 'NONE', #40515, #13771, #12923, .T. ) ;
#26219=VERTEX_POINT ( 'NONE', #8016 ) ;
#26222=CARTESIAN_POINT ( 'NONE',  ( 0.4695943777967593880, -26.29347754267606874, 7.695279973900954751 ) ) ;
#26223=CARTESIAN_POINT ( 'NONE',  ( 0.3259002109880320686, -32.78874652230489062, 6.935328752148349096 ) ) ;
#26234=CARTESIAN_POINT ( 'NONE',  ( -1.738754558334627331, -28.92005600624478845, 6.883132039304661554 ) ) ;
#26236=ADVANCED_FACE ( 'NONE', ( #23630 ), #4896, .T. ) ;
#26239=ADVANCED_FACE ( 'NONE', ( #17639 ), #8169, .F. ) ;
#26243=B_SPLINE_CURVE_WITH_KNOTS ( 'NONE', 3,
 ( #7998, #35634, #7406, #32541, #16862, #29443, #1256, #13792, #26360, #37580, #18234, #40674, #34535, #33138, #2833, #21750, #36978, #2629, #27708, #18437, #9376, #37385, #2426, #21962, #34333 ),
 .UNSPECIFIED., .F., .F.,
 ( 4, 3, 3, 3, 3, 3, 3, 3, 4 ),
 ( 6.468151674593709615E-05, 9.076621574722030540E-05, 0.0001210204262067986035, 0.0001512763324577439175, 0.0001815301820994234361, 0.0002117781465860742022, 0.0002420274594459773760, 0.0002722905548971168727, 0.0002816827545175609564 ),
 .UNSPECIFIED. ) ;
#26251=CARTESIAN_POINT ( 'NONE',  ( -0.9934091780005464001, -31.78413689346535520, 7.783750581861599294 ) ) ;
#26255=CARTESIAN_POINT ( 'NONE',  ( -1.059861091245062559, -31.72193407659015207, 6.867199677474204123 ) ) ;
#26256=CARTESIAN_POINT ( 'NONE',  ( 5.200096824318753086, -29.61612186858987172, 6.880608371227953768 ) ) ;
#26259=CARTESIAN_POINT ( 'NONE',  ( 5.093940842300026084, -29.77924726035835334, 6.969307238440511476 ) ) ;
#26260=CARTESIAN_POINT ( 'NONE',  ( 1.882503106173801566, -26.07466918923286414, 6.912143950357346078 ) ) ;
#26267=ORIENTED_EDGE ( 'NONE', *, *, #18126, .T. ) ;
#26268=CARTESIAN_POINT ( 'NONE',  ( 2.870175459834257925, -26.27120282332167633, 7.730015791551948290 ) ) ;
#26270=CARTESIAN_POINT ( 'NONE',  ( 2.326171464738295835, -32.91184545387483951, 7.695279973900954751 ) ) ;
#26271=FACE_OUTER_BOUND ( 'NONE', #29996, .T. ) ;
#26275=EDGE_LOOP ( 'NONE', ( #6883, #11494, #32544, #11816 ) ) ;
#26284=CARTESIAN_POINT ( 'NONE',  ( 0.9089306018589854430, -32.97926988754144162, 6.984548363133216142 ) ) ;
#26287=CARTESIAN_POINT ( 'NONE',  ( 3.504784550580148483, -26.68823612567400971, 7.754798119455333705 ) ) ;
#26294=CARTESIAN_POINT ( 'NONE',  ( 5.140791489254627145, -28.92678305073006584, 7.695279973900954751 ) ) ;
#26298=CARTESIAN_POINT ( 'NONE',  ( 3.876017184916769942, -26.95713821644390862, 7.756377446753162097 ) ) ;
#26299=CARTESIAN_POINT ( 'NONE',  ( -1.582528736513596490, -30.78337320113038444, 7.750000000000000000 ) ) ;
#26300=CARTESIAN_POINT ( 'NONE',  ( -2.515717719208200531, -28.88150288888238393, 7.695279973900954751 ) ) ;
#26302=CARTESIAN_POINT ( 'NONE',  ( 4.472525015499347667, -27.43328141189353886, 6.875780273367532835 ) ) ;
#26304=CARTESIAN_POINT ( 'NONE',  ( 4.978554560952730412, -30.79615924950642025, 6.894806418505347700 ) ) ;
#26305=CARTESIAN_POINT ( 'NONE',  ( 1.700390093233090871, -29.56993018339339940, 7.750000000000000888 ) ) ;
#26309=CARTESIAN_POINT ( 'NONE',  ( 4.240191228329224238, -31.83034962878108942, 7.774064877406530627 ) ) ;
#26312=CARTESIAN_POINT ( 'NONE',  ( -0.4516137999636575251, -26.80967899891524553, 6.867199677474200570 ) ) ;
#26313=CARTESIAN_POINT ( 'NONE',  ( -1.250607068061524885, -27.68798963190787532, 6.880828092187095457 ) ) ;
#26314=CARTESIAN_POINT ( 'NONE',  ( 2.380073834590987758, -26.14911510722517463, 7.782861076432730840 ) ) ;
#26316=B_SPLINE_CURVE_WITH_KNOTS ( 'NONE', 3,
 ( #1934, #21261, #20630, #33217, #30122, #17735, #11355, #36497, #5614, #39988 ),
 .UNSPECIFIED., .F., .F.,
 ( 4, 3, 3, 4 ),
 ( 9.697399036122160616E-19, 3.025570593003156381E-05, 6.051145698344085212E-05, 6.468151674593620168E-05 ),
 .UNSPECIFIED. ) ;
#26317=DIRECTION ( 'NONE',  ( -0.9848077530122092416, 0.1736481776669241694, -0.000000000000000000 ) ) ;
#26320=DIRECTION ( 'NONE',  ( 0.5000000000000101030, -0.8660254037844328234, -0.000000000000000000 ) ) ;
#26326=ORIENTED_EDGE ( 'NONE', *, *, #22523, .T. ) ;
#26327=EDGE_CURVE ( 'NONE', #23918, #22737, #35546, .T. ) ;
#26329=CARTESIAN_POINT ( 'NONE',  ( -0.1040043641139408170, -32.45162424111279620, 7.754798119455333705 ) ) ;
#26341=CARTESIAN_POINT ( 'NONE',  ( 5.125265918664630327, -30.21784728057895109, 7.785096263473211486 ) ) ;
#26345=CARTESIAN_POINT ( 'NONE',  ( 0.4111392921005667112, -32.71602809928322131, 6.865312560952602894 ) ) ;
#26348=CARTESIAN_POINT ( 'NONE',  ( -1.406165058247869748, -30.96909808796597119, 7.505001789837627335 ) ) ;
#26350=ORIENTED_EDGE ( 'NONE', *, *, #12687, .F. ) ;
#26351=PLANE ( 'NONE',  #9300 ) ;
#26355=FACE_OUTER_BOUND ( 'NONE', #374, .T. ) ;
#26360=CARTESIAN_POINT ( 'NONE',  ( -1.647019466996949566, -30.16568013038308038, 7.763628509615286610 ) ) ;
#26361=CARTESIAN_POINT ( 'NONE',  ( 5.013689988518933660, -28.46451312308398229, 7.776484688137385248 ) ) ;
#26363=VERTEX_POINT ( 'NONE', #8377 ) ;
#26366=CARTESIAN_POINT ( 'NONE',  ( 3.217454984196751688, -26.40825593670985327, 7.501983001166817822 ) ) ;
#26370=CARTESIAN_POINT ( 'NONE',  ( 5.140791489254627145, -28.92678305073006939, 7.697032948437507294 ) ) ;
#26373=B_SPLINE_CURVE_WITH_KNOTS ( 'NONE', 3,
 ( #36646, #30270, #5153, #27170, #14807, #21003, #32960, #11711, #33384, #20789, #14003, #1674, #2086, #23678, #14205, #14598, #24287, #39727, #33581, #17896, #4950, #39317, #26574, #27375, #39114 ),
 .UNSPECIFIED., .F., .F.,
 ( 4, 3, 3, 3, 3, 3, 3, 3, 4 ),
 ( 6.468151674593734010E-05, 9.076621574721644293E-05, 0.0001210204262067928165, 0.0001512763324577402313, 0.0001815301820994173645, 0.0002117781465860688896, 0.0002420274594459692445, 0.0002722905548971095544, 0.0002816827545175569448 ),
 .UNSPECIFIED. ) ;
#26374=CARTESIAN_POINT ( 'NONE',  ( -2.512558355278247557, -30.27627512112215058, 7.695279973900954751 ) ) ;
#26375=LINE ( 'NONE', #10305, #12027 ) ;
#26380=EDGE_CURVE ( 'NONE', #5603, #35202, #31384, .T. ) ;
#26382=CARTESIAN_POINT ( 'NONE',  ( 2.483678319220730568, -26.15870172506354763, 6.906857269533146493 ) ) ;
#26390=CARTESIAN_POINT ( 'NONE',  ( -2.999244243438122126, -27.67182067344772278, 6.954324564059724878 ) ) ;
#26395=CARTESIAN_POINT ( 'NONE',  ( -0.1815504582524301025, -32.52092734468801183, 6.880828092187098122 ) ) ;
#26397=CARTESIAN_POINT ( 'NONE',  ( 2.388070188599133559, -26.24018815714575581, 7.774064877406527962 ) ) ;
#26400=LINE ( 'NONE', #38931, #35605 ) ;
#26405=CARTESIAN_POINT ( 'NONE',  ( 4.983308922979784228, -28.35648716565642857, 7.750000000000000000 ) ) ;
#26407=CARTESIAN_POINT ( 'NONE',  ( -1.568403543439855552, -28.35049121020558260, 7.781480525794717273 ) ) ;
#26414=CARTESIAN_POINT ( 'NONE',  ( 2.995714826359392902, -26.31843225177813395, 6.863784140767622333 ) ) ;
#26416=ORIENTED_EDGE ( 'NONE', *, *, #10605, .F. ) ;
#26418=CARTESIAN_POINT ( 'NONE',  ( 3.831455443695943153, -32.21920586904128214, 7.784476445165072533 ) ) ;
#26420=CARTESIAN_POINT ( 'NONE',  ( 0.9672887567242401952, -32.88995464571426197, 6.868387053540520704 ) ) ;
#26421=CARTESIAN_POINT ( 'NONE',  ( 3.614428224949046253, -26.63966429966296090, 6.961115707816239784 ) ) ;
#26425=CARTESIAN_POINT ( 'NONE',  ( -1.742531660465676202, -30.19946305178996226, 7.743886751744254227 ) ) ;
#26429=EDGE_CURVE ( 'NONE', #2006, #31681, #5309, .T. ) ;
#26433=CARTESIAN_POINT ( 'NONE',  ( -1.707806439853804648, -28.77356564420016838, 6.946906449495744873 ) ) ;
#26446=CARTESIAN_POINT ( 'NONE',  ( -1.799609906766908907, -29.51351222115033934, 7.139253571461081194 ) ) ;
#26452=CARTESIAN_POINT ( 'NONE',  ( 2.684728112252080301, -32.82432899398588688, 6.895222827070020877 ) ) ;
#26453=CARTESIAN_POINT ( 'NONE',  ( 2.670542827047279744, -32.83592445859822107, 7.386948897581449458 ) ) ;
#26455=ORIENTED_EDGE ( 'NONE', *, *, #2641, .T. ) ;
#26461=EDGE_CURVE ( 'NONE', #38041, #33085, #612, .T. ) ;
#26462=B_SPLINE_CURVE_WITH_KNOTS ( 'NONE', 3,
 ( #33670, #27473, #5448, #6214, #30575, #23573, #10992, #33046, #30367, #14904, #14291, #2382, #8309, #20672, #24381, #8722, #33474, #33877, #17780, #4836, #26862, #18759, #33256, #5042, #26665, #27069, #17571, #39611, #243, #31949, #7019 ),
 .UNSPECIFIED., .F., .F.,
 ( 4, 3, 3, 3, 3, 3, 3, 3, 3, 3, 4 ),
 ( 2.168404344971008868E-18, 3.077658087705444919E-05, 6.152638666998851537E-05, 9.267501192706007764E-05, 0.0001241882240135153495, 0.0001556618703051646587, 0.0001866161554452198913, 0.0002167966385860966021, 0.0002463805737537766221, 0.0002758761370306538454, 0.0002847094172290106869 ),
 .UNSPECIFIED. ) ;
#26468=LINE ( 'NONE', #29355, #28709 ) ;
#26479=CARTESIAN_POINT ( 'NONE',  ( 3.924847313950914351, -26.99858887786119510, 6.892063359921932530 ) ) ;
#26490=CARTESIAN_POINT ( 'NONE',  ( 5.142755578586930554, -28.93735303436349682, 7.651421919295142260 ) ) ;
#26493=CARTESIAN_POINT ( 'NONE',  ( -1.482088180267138622, -30.76652202637871625, 7.695279973900954751 ) ) ;
#26495=CARTESIAN_POINT ( 'NONE',  ( -2.395465747220443031, -30.94034030041199657, 6.894806418505347700 ) ) ;
#26496=CARTESIAN_POINT ( 'NONE',  ( -1.641525177248355893, -30.19571155489859393, 7.693875151218753317 ) ) ;
#26498=CARTESIAN_POINT ( 'NONE',  ( 4.416683729637440159, -27.36272632311469266, 6.875671892026060661 ) ) ;
#26500=CARTESIAN_POINT ( 'NONE',  ( -0.3201374542954114055, -26.83543417321557101, 6.959317978105164393 ) ) ;
#26501=CARTESIAN_POINT ( 'NONE',  ( 4.229935080175720508, -31.84180213379760715, 6.864276522220859711 ) ) ;
#26509=CARTESIAN_POINT ( 'NONE',  ( 4.823919574101139141, -30.91291510963706912, 7.006423389747790331 ) ) ;
#26510=CARTESIAN_POINT ( 'NONE',  ( 5.113812245512664667, -30.34358980514384285, 7.013842709614101167 ) ) ;
#26523=CARTESIAN_POINT ( 'NONE',  ( 5.002712648450646782, -28.73146642408099183, 7.505001789837627335 ) ) ;
#26526=PLANE ( 'NONE',  #7999 ) ;
#26528=CARTESIAN_POINT ( 'NONE',  ( 4.095104150702293389, -32.13180824307641359, 7.139344958878409919 ) ) ;
#26530=CARTESIAN_POINT ( 'NONE',  ( 5.123906412958439738, -30.28506088044589717, 7.766640943994651103 ) ) ;
#26532=ADVANCED_FACE ( 'NONE', ( #28274 ), #40624, .F. ) ;
#26539=CARTESIAN_POINT ( 'NONE',  ( -0.5125101069461969194, -26.98863734761392053, 7.695279973900954751 ) ) ;
#26540=ORIENTED_EDGE ( 'NONE', *, *, #30371, .F. ) ;
#26552=CARTESIAN_POINT ( 'NONE',  ( 3.412070287718869999, -32.50764203308273181, 7.635761828346577573 ) ) ;
#26554=EDGE_CURVE ( 'NONE', #12935, #6584, #14752, .T. ) ;
#26555=CARTESIAN_POINT ( 'NONE',  ( -1.135370486211617180, -27.69417381966504621, 6.929923840112066635 ) ) ;
#26556=ORIENTED_EDGE ( 'NONE', *, *, #17506, .F. ) ;
#26559=CARTESIAN_POINT ( 'NONE',  ( -1.645942781641917430, -30.59564475252808435, 6.998987538705431888 ) ) ;
#26566=( BOUNDED_CURVE ( )  B_SPLINE_CURVE ( 3, ( #23309, #36076, #10933, #7853 ),
 .UNSPECIFIED., .F., .T. ) 
 B_SPLINE_CURVE_WITH_KNOTS ( ( 4, 4 ),
 ( 1.570796326794896780, 1.574767692156076260 ),
 .UNSPECIFIED. ) 
 CURVE ( )  GEOMETRIC_REPRESENTATION_ITEM ( )  RATIONAL_B_SPLINE_CURVE ( ( 1.000000000000000000, 0.9999986856885290099, 0.9999986856885290099, 1.000000000000000000 ) ) 
 REPRESENTATION_ITEM ( '' )  );
#26569=VERTEX_POINT ( 'NONE', #2376 ) ;
#26572=CARTESIAN_POINT ( 'NONE',  ( -1.312560436656866392, -31.35097737660188244, 7.695279973900954751 ) ) ;
#26574=CARTESIAN_POINT ( 'NONE',  ( 0.1031518550754170205, -26.56845796774315716, 7.759451378593098525 ) ) ;
#26581=DIRECTION ( 'NONE',  ( -1.000000000000000000, 0.000000000000000000, 0.000000000000000000 ) ) ;
#26583=CARTESIAN_POINT ( 'NONE',  ( 0.1967285774411879351, -25.49757015976072694, 7.013842709614101167 ) ) ;
#26589=DIRECTION ( 'NONE',  ( 0.000000000000000000, 0.000000000000000000, 1.000000000000000000 ) ) ;
#26595=CARTESIAN_POINT ( 'NONE',  ( 0.1197244639376408848, -26.44719159565006095, 6.961115707816241560 ) ) ;
#26598=CARTESIAN_POINT ( 'NONE',  ( 4.980322978310361748, -28.34843557914865286, 7.737115613922532553 ) ) ;
#26602=EDGE_CURVE ( 'NONE', #32530, #17047, #15516, .T. ) ;
#26603=DIRECTION ( 'NONE',  ( -0.7126435865141277359, 0.000000000000000000, 0.7015262779114412872 ) ) ;
#26604=VERTEX_POINT ( 'NONE', #11790 ) ;
#26608=CARTESIAN_POINT ( 'NONE',  ( 4.721744115977328349, -27.80317613450962355, 7.643192810543820492 ) ) ;
#26613=DIRECTION ( 'NONE',  ( 0.9848077530122081313, 0.1736481776669300814, 0.000000000000000000 ) ) ;
#26614=CARTESIAN_POINT ( 'NONE',  ( 3.913290293412392096, -32.15122301917286762, 7.703977250142849620 ) ) ;
#26617=CARTESIAN_POINT ( 'NONE',  ( 3.596532054354828922, -26.62805159003958266, 7.011627023500182965 ) ) ;
#26618=CARTESIAN_POINT ( 'NONE',  ( 1.263793096374429492, -26.09726748785000083, 7.009310105710487626 ) ) ;
#26621=CARTESIAN_POINT ( 'NONE',  ( 1.664433243520589967, -33.27093018339341768, 7.695279973900954751 ) ) ;
#26624=CARTESIAN_POINT ( 'NONE',  ( 6.107923577950775673, -31.97397320985677993, 7.754798119455333705 ) ) ;
#26625=ORIENTED_EDGE ( 'NONE', *, *, #7037, .T. ) ;
#26628=CARTESIAN_POINT ( 'NONE',  ( -1.725425523115296622, -28.85306876528290942, 6.864293497989290671 ) ) ;
#26630=EDGE_CURVE ( 'NONE', #9389, #21810, #12219, .T. ) ;
#26633=CARTESIAN_POINT ( 'NONE',  ( -0.8583414810284668572, -27.33095856289763859, 7.784476445165075198 ) ) ;
#26637=B_SPLINE_CURVE_WITH_KNOTS ( 'NONE', 3,
 ( #40439, #9359, #31821, #37974, #21942, #34723, #24609, #6704, #6503, #19252, #37365, #326, #24821, #12030, #8949, #31615, #18620, #9160, #12866, #3438, #21735, #9778, #34316, #15133, #31209 ),
 .UNSPECIFIED., .F., .F.,
 ( 4, 3, 3, 3, 3, 3, 3, 3, 4 ),
 ( 6.468151674593626945E-05, 9.076621574721905857E-05, 0.0001210204262067960963, 0.0001512763324577423183, 0.0001815301820994208069, 0.0002117781465860700822, 0.0002420274594459736626, 0.0002722905548971149212, 0.0002816827545175583543 ),
 .UNSPECIFIED. ) ;
#26647=CARTESIAN_POINT ( 'NONE',  ( 5.165377781178596805, -29.07610802675595707, 6.865482280155369210 ) ) ;
#26650=CARTESIAN_POINT ( 'NONE',  ( 3.791157483716739218, -32.25110375459131973, 7.754798119455333705 ) ) ;
#26651=CARTESIAN_POINT ( 'NONE',  ( 5.117081926811264836, -30.32907536032250206, 6.880828092187096345 ) ) ;
#26652=DIRECTION ( 'NONE',  ( 1.000000000000000000, 0.000000000000000000, 0.000000000000000000 ) ) ;
#26653=CARTESIAN_POINT ( 'NONE',  ( 2.765119862722436928, -32.79893335921538977, 6.864651958020304257 ) ) ;
#26655=CARTESIAN_POINT ( 'NONE',  ( 1.892167102583406146, -26.07518817540235645, 6.941203072598474577 ) ) ;
#26657=EDGE_CURVE ( 'NONE', #2179, #19731, #7058, .T. ) ;
#26658=EDGE_LOOP ( 'NONE', ( #33673, #28843, #31223, #20367, #4796 ) ) ;
#26663=FACE_OUTER_BOUND ( 'NONE', #13340, .T. ) ;
#26665=CARTESIAN_POINT ( 'NONE',  ( -0.8559337256230342694, -27.17927995110327188, 6.980586498568965403 ) ) ;
#26667=DIRECTION ( 'NONE',  ( -1.000000000000000000, 0.000000000000000000, 0.000000000000000000 ) ) ;
#26668=CARTESIAN_POINT ( 'NONE',  ( 2.431875535358183793, -26.14722233025152676, 7.750000000000000888 ) ) ;
#26671=ORIENTED_EDGE ( 'NONE', *, *, #24636, .F. ) ;
#26672=VERTEX_POINT ( 'NONE', #16126 ) ;
#26677=PLANE ( 'NONE',  #26929 ) ;
#26681=EDGE_CURVE ( 'NONE', #12108, #28243, #30289, .T. ) ;
#26683=DIRECTION ( 'NONE',  ( -1.000000000000000000, 0.000000000000000000, 0.000000000000000000 ) ) ;
#26686=ADVANCED_FACE ( 'NONE', ( #32200 ), #19220, .F. ) ;
#26690=CARTESIAN_POINT ( 'NONE',  ( 0.1649012726517564975, -26.53640515764040231, 7.013842709614101167 ) ) ;
#26691=CARTESIAN_POINT ( 'NONE',  ( 2.372793067090987584, -26.23708241598081514, 6.870716933885664623 ) ) ;
#26700=CARTESIAN_POINT ( 'NONE',  ( 4.167347423248069838, -31.90961425007534658, 6.929923840112069300 ) ) ;
#26706=CARTESIAN_POINT ( 'NONE',  ( 1.158056475448751454, -26.21346265829786049, 6.894806418505346812 ) ) ;
#26709=DIRECTION ( 'NONE',  ( -0.9848077530122149037, 0.1736481776668921395, 0.000000000000000000 ) ) ;
#26710=CARTESIAN_POINT ( 'NONE',  ( 5.162074113069795800, -30.13065620592465876, 7.255881584735161205 ) ) ;
#26712=ORIENTED_EDGE ( 'NONE', *, *, #3155, .T. ) ;
#26714=CARTESIAN_POINT ( 'NONE',  ( 4.870584666682655772, -30.79873755356147669, 7.784476445165072533 ) ) ;
#26716=LINE ( 'NONE', #1222, #2483 ) ;
#26717=ORIENTED_EDGE ( 'NONE', *, *, #34724, .T. ) ;
#26722=CARTESIAN_POINT ( 'NONE',  ( -0.9894248136993964993, -27.33053388830764874, 7.635761828346571356 ) ) ;
#26725=CARTESIAN_POINT ( 'NONE',  ( -0.08465666289843364056, -32.46366374979973557, 7.774064877406527962 ) ) ;
#26729=EDGE_CURVE ( 'NONE', #28383, #27482, #13432, .T. ) ;
#26732=ORIENTED_EDGE ( 'NONE', *, *, #32002, .T. ) ;
#26733=CARTESIAN_POINT ( 'NONE',  ( 5.135438731485244546, -30.19400213985234060, 7.778495531946297170 ) ) ;
#26742=LINE ( 'NONE', #39281, #6900 ) ;
#26744=CARTESIAN_POINT ( 'NONE',  ( 0.5713750229309367823, -32.77700439067807281, 7.695279973900954751 ) ) ;
#26751=FACE_OUTER_BOUND ( 'NONE', #27390, .T. ) ;
#26755=AXIS2_PLACEMENT_3D ( 'NONE', #13172, #25732, #40541 ) ;
#26756=CARTESIAN_POINT ( 'NONE',  ( 5.007838232645942078, -28.45671592495904179, 7.780491323090172884 ) ) ;
#26760=CARTESIAN_POINT ( 'NONE',  ( -1.623020518067741502, -30.66767645291113453, 6.863784140767622333 ) ) ;
#26768=DIRECTION ( 'NONE',  ( -0.1736481776669340227, 0.9848077530122073542, -0.000000000000000000 ) ) ;
#26771=CARTESIAN_POINT ( 'NONE',  ( 4.819850852585312317, -27.98280284135210749, 6.989977667959443863 ) ) ;
#26773=ADVANCED_FACE ( 'NONE', ( #25801 ), #26214, .F. ) ;
#26776=ADVANCED_FACE ( 'NONE', ( #38142 ), #7258, .F. ) ;
#26777=CARTESIAN_POINT ( 'NONE',  ( -1.312638530291446948, -31.35084526104921920, 7.700536657684216024 ) ) ;
#26786=DIRECTION ( 'NONE',  ( 0.5000000000000072164, -0.8660254037844344888, 0.000000000000000000 ) ) ;
#26789=CARTESIAN_POINT ( 'NONE',  ( -1.256819626896593656, -27.89215637338188714, 7.652160403243381204 ) ) ;
#26795=CARTESIAN_POINT ( 'NONE',  ( 4.660834209608292866, -31.24198599401081111, 7.721096864323899744 ) ) ;
#26802=CARTESIAN_POINT ( 'NONE',  ( 6.349790915967283844, -30.58285303640981212, 6.894806418505347700 ) ) ;
#26809=CARTESIAN_POINT ( 'NONE',  ( 3.014835793218893389, -26.32611455060292727, 6.867199677474200570 ) ) ;
#26816=CARTESIAN_POINT ( 'NONE',  ( 5.011198270955363299, -30.34358980514384285, 7.013842709614101167 ) ) ;
#26817=CARTESIAN_POINT ( 'NONE',  ( 0.3366481700427572665, -32.79331784342181066, 6.906857269533146493 ) ) ;
#26823=VERTEX_POINT ( 'NONE', #6669 ) ;
#26829=EDGE_CURVE ( 'NONE', #35977, #2740, #20525, .T. ) ;
#26832=ADVANCED_FACE ( 'NONE', ( #7663 ), #29687, .F. ) ;
#26837=EDGE_LOOP ( 'NONE', ( #9298, #7795, #21841, #23176 ) ) ;
#26841=CARTESIAN_POINT ( 'NONE',  ( 5.175382819553307812, -29.15228733116008186, 6.951256099901594432 ) ) ;
#26846=CARTESIAN_POINT ( 'NONE',  ( -1.077356027815240758, -31.69929886267264862, 6.880828092187099010 ) ) ;
#26849=CARTESIAN_POINT ( 'NONE',  ( 5.093870946763709995, -29.78037735622890736, 6.949473656533221799 ) ) ;
#26851=CARTESIAN_POINT ( 'NONE',  ( 1.764561002481344731, -26.07050696156566971, 6.870737987065012931 ) ) ;
#26859=DIRECTION ( 'NONE',  ( 0.9396926207859126468, -0.3420201433256568890, -0.000000000000000000 ) ) ;
#26861=ORIENTED_EDGE ( 'NONE', *, *, #28244, .F. ) ;
#26862=CARTESIAN_POINT ( 'NONE',  ( -0.8534657166897973157, -27.17664360927492950, 6.941203072598472801 ) ) ;
#26865=CARTESIAN_POINT ( 'NONE',  ( 5.051054751933684805, -30.14703185982037681, 7.635761828346577573 ) ) ;
#26869=CARTESIAN_POINT ( 'NONE',  ( 0.5568522185922281098, -26.36799081952789692, 7.779495906702013741 ) ) ;
#26872=DIRECTION ( 'NONE',  ( -0.6662082868431843385, 0.000000000000000000, 0.7457657263118689928 ) ) ;
#26873=EDGE_CURVE ( 'NONE', #24258, #22465, #15318, .T. ) ;
#26874=CARTESIAN_POINT ( 'NONE',  ( 4.021359916180923477, -27.08534488404830043, 6.887945620086120435 ) ) ;
#26877=FACE_OUTER_BOUND ( 'NONE', #22543, .T. ) ;
#26883=AXIS2_PLACEMENT_3D ( 'NONE', #5767, #24493, #40333 ) ;
#26887=CARTESIAN_POINT ( 'NONE',  ( -1.482088180267139066, -30.76652202637871625, 7.703977250142849620 ) ) ;
#26889=CARTESIAN_POINT ( 'NONE',  ( -0.07765682019414094084, -26.55520811102057621, 7.670465701733746755 ) ) ;
#26892=CARTESIAN_POINT ( 'NONE',  ( 4.180804271322692500, -31.89534315857266122, 7.013842709614101167 ) ) ;
#26898=EDGE_LOOP ( 'NONE', ( #15529, #16516, #21648, #2302 ) ) ;
#26899=LINE ( 'NONE', #2632, #8914 ) ;
#26906=CARTESIAN_POINT ( 'NONE',  ( -0.6934048292311358885, -32.12330951052082639, 6.961115707816235343 ) ) ;
#26912=( BOUNDED_CURVE ( )  B_SPLINE_CURVE ( 3, ( #10917, #33589, #2289, #14816 ),
 .UNSPECIFIED., .F., .F. ) 
 B_SPLINE_CURVE_WITH_KNOTS ( ( 4, 4 ),
 ( 4.708531083176466403, 4.895802057644187855 ),
 .UNSPECIFIED. ) 
 CURVE ( )  GEOMETRIC_REPRESENTATION_ITEM ( )  RATIONAL_B_SPLINE_CURVE ( ( 1.000000000000000000, 0.9970795998553221295, 0.9970795998553221295, 1.000000000000000000 ) ) 
 REPRESENTATION_ITEM ( '' )  );
#26920=ADVANCED_FACE ( 'NONE', ( #13843 ), #7460, .F. ) ;
#26921=DIRECTION ( 'NONE',  ( 0.000000000000000000, 0.000000000000000000, -1.000000000000000000 ) ) ;
#26923=CARTESIAN_POINT ( 'NONE',  ( -1.208261940723883932, -27.80929264776421306, 7.784476445165072533 ) ) ;
#26925=CARTESIAN_POINT ( 'NONE',  ( 4.662690227536057996, -31.23869556963216354, 7.695279973900954751 ) ) ;
#26929=AXIS2_PLACEMENT_3D ( 'NONE', #7730, #20277, #23770 ) ;
#26935=VERTEX_POINT ( 'NONE', #5184 ) ;
#26936=CARTESIAN_POINT ( 'NONE',  ( -1.624655799086301533, -28.85995144147929992, 7.754798119455333705 ) ) ;
#26948=CARTESIAN_POINT ( 'NONE',  ( -1.142479071211579544, -27.70495301360842078, 7.006423389747789443 ) ) ;
#26952=DIRECTION ( 'NONE',  ( -0.6427876096865328126, -0.7660444431189835646, -0.000000000000000000 ) ) ;
#26953=ADVANCED_FACE ( 'NONE', ( #20412 ), #16917, .T. ) ;
#26960=ORIENTED_EDGE ( 'NONE', *, *, #14347, .F. ) ;
#26962=CARTESIAN_POINT ( 'NONE',  ( 4.912497208772558466, -28.45531190136118127, 6.892063359921931642 ) ) ;
#26967=CARTESIAN_POINT ( 'NONE',  ( 4.815108193535243331, -27.97351822038067226, 7.006908160621411419 ) ) ;
#26969=ORIENTED_EDGE ( 'NONE', *, *, #28721, .T. ) ;
#26974=ORIENTED_EDGE ( 'NONE', *, *, #36581, .T. ) ;
#26977=CARTESIAN_POINT ( 'NONE',  ( -1.794547911424669184, -29.38175913461375188, 6.980586498568969844 ) ) ;
#26982=CYLINDRICAL_SURFACE ( 'NONE', #20142, 0.09010775117052972905 ) ;
#26985=CARTESIAN_POINT ( 'NONE',  ( 1.822194502883781375, -26.17211269480022295, 7.754798119455333705 ) ) ;
#26992=CARTESIAN_POINT ( 'NONE',  ( 0.1104740917191936872, -26.45188886312317322, 6.912143950357348743 ) ) ;
#26994=DIRECTION ( 'NONE',  ( -0.6427876096865430267, 0.7660444431189749048, -0.000000000000000000 ) ) ;
#27002=ORIENTED_EDGE ( 'NONE', *, *, #27188, .F. ) ;
#27007=ADVANCED_FACE ( 'NONE', ( #6207 ), #18750, .F. ) ;
#27008=DIRECTION ( 'NONE',  ( 1.000000000000000000, -9.912705577010326536E-16, 0.000000000000000000 ) ) ;
#27010=CARTESIAN_POINT ( 'NONE',  ( -0.4574210171174859507, -32.19744825413003753, 7.695279973900954751 ) ) ;
#27014=CARTESIAN_POINT ( 'NONE',  ( 0.4108041967164411945, -32.82370865775250479, 6.863654226668487901 ) ) ;
#27015=CARTESIAN_POINT ( 'NONE',  ( -1.699601713409903292, -29.55877364174393307, 7.775108481317161591 ) ) ;
#27016=ORIENTED_EDGE ( 'NONE', *, *, #29566, .F. ) ;
#27021=CARTESIAN_POINT ( 'NONE',  ( 1.717829174068238984, -33.06988673718940674, 7.750000000000000888 ) ) ;
#27022=ORIENTED_EDGE ( 'NONE', *, *, #39351, .F. ) ;
#27028=CARTESIAN_POINT ( 'NONE',  ( -0.9542785570400912354, -31.86130625091119484, 7.255881584735162981 ) ) ;
#27034=CARTESIAN_POINT ( 'NONE',  ( 4.339855541068658340, -31.86847383987311133, 6.870737987065013819 ) ) ;
#27038=CARTESIAN_POINT ( 'NONE',  ( -1.772272602310306366, -30.00652718025207122, 7.009310105710486738 ) ) ;
#27043=CARTESIAN_POINT ( 'NONE',  ( 4.996814229376580485, -30.74619960369405547, 7.743886751744252450 ) ) ;
#27045=CARTESIAN_POINT ( 'NONE',  ( -1.699609906766908818, -29.56993018339339940, 7.222147233343546802 ) ) ;
#27048=CARTESIAN_POINT ( 'NONE',  ( 3.405524546634664418, -32.61001036001269426, 7.785096263473211486 ) ) ;
#27049=PLANE ( 'NONE',  #24222 ) ;
#27050=DIRECTION ( 'NONE',  ( 0.1736481776669273336, 0.9848077530122085754, -0.000000000000000000 ) ) ;
#27051=( BOUNDED_CURVE ( )  B_SPLINE_CURVE ( 3, ( #37116, #34679, #31367, #27648 ),
 .UNSPECIFIED., .F., .T. ) 
 B_SPLINE_CURVE_WITH_KNOTS ( ( 4, 4 ),
 ( 1.396263401595463360, 1.534781240595298968 ),
 .UNSPECIFIED. ) 
 CURVE ( )  GEOMETRIC_REPRESENTATION_ITEM ( )  RATIONAL_B_SPLINE_CURVE ( ( 1.000000000000000000, 0.9984017064007810749, 0.9984017064007810749, 1.000000000000000000 ) ) 
 REPRESENTATION_ITEM ( '' )  );
#27053=DIRECTION ( 'NONE',  ( 0.7660444431189857850, -0.6427876096865300370, -0.000000000000000000 ) ) ;
#27054=CARTESIAN_POINT ( 'NONE',  ( 5.097704832850760148, -29.70540078745077039, 6.865312560952604670 ) ) ;
#27055=CARTESIAN_POINT ( 'NONE',  ( 1.891502090683779613, -26.07515052243017806, 6.971170733404099984 ) ) ;
#27062=ORIENTED_EDGE ( 'NONE', *, *, #36209, .T. ) ;
#27067=CARTESIAN_POINT ( 'NONE',  ( 4.890732190868795293, -28.37407357224292070, 7.257242401810564125 ) ) ;
#27068=CARTESIAN_POINT ( 'NONE',  ( -1.420942960651109033, -28.22185930593809999, 6.997764925645181933 ) ) ;
#27069=CARTESIAN_POINT ( 'NONE',  ( -0.8579401743431254168, -27.18142544799997751, 6.989977667959442975 ) ) ;
#27071=DIRECTION ( 'NONE',  ( 0.000000000000000000, 0.6662082868431850047, -0.7457657263118682156 ) ) ;
#27081=CARTESIAN_POINT ( 'NONE',  ( 3.980030838668743520, -27.04736262030031213, 6.863904403958576594 ) ) ;
#27084=ORIENTED_EDGE ( 'NONE', *, *, #37553, .T. ) ;
#27088=DIRECTION ( 'NONE',  ( 0.9396926207859080948, 0.3420201433256694901, -0.000000000000000000 ) ) ;
#27089=CARTESIAN_POINT ( 'NONE',  ( 2.496365493979189498, -26.26441612936079295, 6.959317978105167057 ) ) ;
#27090=CARTESIAN_POINT ( 'NONE',  ( -1.533527784978453878, -30.61958705502705769, 7.757178535559535959 ) ) ;
#27091=CARTESIAN_POINT ( 'NONE',  ( 3.916367062334308535, -26.99125986761471907, 7.784838882742138644 ) ) ;
#27093=CARTESIAN_POINT ( 'NONE',  ( 0.6690963371203834109, -26.22531762158553903, 7.006908160621413195 ) ) ;
#27095=CARTESIAN_POINT ( 'NONE',  ( -0.4352988304694859756, -26.92438771328325586, 6.880147297696980857 ) ) ;
#27100=ORIENTED_EDGE ( 'NONE', *, *, #20331, .F. ) ;
#27108=CARTESIAN_POINT ( 'NONE',  ( -0.3282911018737336706, -26.83271124052131640, 7.386948897581451234 ) ) ;
#27135=CARTESIAN_POINT ( 'NONE',  ( 1.700390093233090871, -29.56993018339339940, 7.800000000000000711 ) ) ;
#27137=FACE_OUTER_BOUND ( 'NONE', #30614, .T. ) ;
#27138=CARTESIAN_POINT ( 'NONE',  ( 1.700390093233090871, -29.56993018339339940, 7.800000000000000711 ) ) ;
#27147=CARTESIAN_POINT ( 'NONE',  ( 4.986456615447258933, -28.37449729532158926, 7.767720160662274331 ) ) ;
#27152=( BOUNDED_CURVE ( )  B_SPLINE_CURVE ( 3, ( #3883, #12911, #13307, #25478 ),
 .UNSPECIFIED., .F., .F. ) 
 B_SPLINE_CURVE_WITH_KNOTS ( ( 4, 4 ),
 ( 4.708531083176467291, 4.895802057644188743 ),
 .UNSPECIFIED. ) 
 CURVE ( )  GEOMETRIC_REPRESENTATION_ITEM ( )  RATIONAL_B_SPLINE_CURVE ( ( 1.000000000000000000, 0.9970795998553221295, 0.9970795998553221295, 1.000000000000000000 ) ) 
 REPRESENTATION_ITEM ( '' )  );
#27153=CARTESIAN_POINT ( 'NONE',  ( 3.480418331975892343, -32.58348369386324350, 7.678495282201404315 ) ) ;
#27160=CYLINDRICAL_SURFACE ( 'NONE', #15442, 0.09010775117053118621 ) ;
#27163=EDGE_LOOP ( 'NONE', ( #11199, #16851, #3915, #18157, #8577 ) ) ;
#27164=CARTESIAN_POINT ( 'NONE',  ( 4.782688990442776955, -27.91175695004079316, 6.863784140767622333 ) ) ;
#27165=VERTEX_POINT ( 'NONE', #31528 ) ;
#27169=LINE ( 'NONE', #20787, #27867 ) ;
#27170=CARTESIAN_POINT ( 'NONE',  ( -0.02740181272327065973, -26.64166531666571558, 7.721096864323898856 ) ) ;
#27174=AXIS2_PLACEMENT_3D ( 'NONE', #5649, #18186, #31177 ) ;
#27179=CARTESIAN_POINT ( 'NONE',  ( 1.731470216958145070, -26.07006818241261215, 6.894806418505347700 ) ) ;
#27181=CARTESIAN_POINT ( 'NONE',  ( 3.729071288339932622, -32.30714912626547886, 7.386948897581449458 ) ) ;
#27187=CARTESIAN_POINT ( 'NONE',  ( -1.510909903798922427, -30.68686900403765705, 6.894806418505348589 ) ) ;
#27188=EDGE_CURVE ( 'NONE', #18928, #25767, #24269, .T. ) ;
#27189=CARTESIAN_POINT ( 'NONE',  ( -0.9229550489645098610, -27.40704778601062941, 7.661510568013089717 ) ) ;
#27192=DIRECTION ( 'NONE',  ( -0.1736481776669174526, -0.9848077530122102408, 0.000000000000000000 ) ) ;
#27195=DIRECTION ( 'NONE',  ( -0.9396926207859057634, -0.3420201433256757073, -0.000000000000000000 ) ) ;
#27201=ORIENTED_EDGE ( 'NONE', *, *, #38118, .T. ) ;
#27203=DIRECTION ( 'NONE',  ( -0.5000000000000036637, 0.8660254037844367092, 0.000000000000000000 ) ) ;
#27212=CARTESIAN_POINT ( 'NONE',  ( 1.271343038760671451, -26.09632215832020208, 6.998987538705438105 ) ) ;
#27213=ORIENTED_EDGE ( 'NONE', *, *, #27775, .T. ) ;
#27216=EDGE_CURVE ( 'NONE', #32660, #40343, #19270, .T. ) ;
#27218=CARTESIAN_POINT ( 'NONE',  ( -0.1786029313623582471, -32.40354722338927473, 6.949473656533215582 ) ) ;
#27227=ADVANCED_FACE ( 'NONE', ( #6411 ), #19776, .F. ) ;
#27229=CARTESIAN_POINT ( 'NONE',  ( 3.370276098127634068, -26.60826056296400210, 7.712764235869109974 ) ) ;
#27235=CARTESIAN_POINT ( 'NONE',  ( 1.605929549753502217, -33.06867024173331515, 6.863805608295730387 ) ) ;
#27237=EDGE_CURVE ( 'NONE', #35883, #19738, #15870, .T. ) ;
#27240=CARTESIAN_POINT ( 'NONE',  ( 5.175340845672220524, -29.15193808794737862, 6.941203072598479018 ) ) ;
#27241=CARTESIAN_POINT ( 'NONE',  ( 5.149847078580999771, -30.16259136557591702, 7.637894019485641728 ) ) ;
#27243=LINE ( 'NONE', #11579, #17378 ) ;
#27245=CARTESIAN_POINT ( 'NONE',  ( 4.995276389714080167, -30.75049260218879965, 7.640616322432101093 ) ) ;
#27247=CARTESIAN_POINT ( 'NONE',  ( 2.809903756998512137, -32.78380314757816905, 6.887041543973316138 ) ) ;
#27248=CARTESIAN_POINT ( 'NONE',  ( 5.096413826755827436, -29.73452413738529287, 6.876076431790007604 ) ) ;
#27258=CARTESIAN_POINT ( 'NONE',  ( 0.1658859576577136064, -26.53590150653912261, 6.895222827070022653 ) ) ;
#27259=CARTESIAN_POINT ( 'NONE',  ( 2.911245606938221098, -26.39285055561105153, 6.892063359921934307 ) ) ;
#27260=DIRECTION ( 'NONE',  ( 0.9396926207859126468, -0.3420201433256568335, -0.000000000000000000 ) ) ;
#27261=CARTESIAN_POINT ( 'NONE',  ( 2.427704393887406109, -26.14656945195773119, 7.754798119455333705 ) ) ;
#27262=ORIENTED_EDGE ( 'NONE', *, *, #9010, .T. ) ;
#27265=EDGE_CURVE ( 'NONE', #39495, #35525, #6743, .T. ) ;
#27271=EDGE_CURVE ( 'NONE', #15871, #23038, #32707, .T. ) ;
#27277=CARTESIAN_POINT ( 'NONE',  ( 2.277491769660097365, -26.21926552469281191, 7.635761828346577573 ) ) ;
#27286=CARTESIAN_POINT ( 'NONE',  ( 1.575559142037938454, -32.96765387319566543, 6.863904403958575706 ) ) ;
#27287=CARTESIAN_POINT ( 'NONE',  ( 2.443030458780631076, -26.25201205342539268, 6.871394612369935651 ) ) ;
#27288=CARTESIAN_POINT ( 'NONE',  ( -1.743365991543899485, -30.19486540288534826, 7.750000000000001776 ) ) ;
#27290=CARTESIAN_POINT ( 'NONE',  ( -0.8885437841551658833, -31.78482907790084511, 7.257242401810562349 ) ) ;
#27291=CARTESIAN_POINT ( 'NONE',  ( 0.6575462507011821112, -26.22889365144838791, 6.887547729233689076 ) ) ;
#27293=CARTESIAN_POINT ( 'NONE',  ( 4.851634552394991751, -30.84651091276440482, 7.754798119455333705 ) ) ;
#27296=ORIENTED_EDGE ( 'NONE', *, *, #24774, .F. ) ;
#27301=LINE ( 'NONE', #5695, #38474 ) ;
#27305=CARTESIAN_POINT ( 'NONE',  ( 4.835314087903390678, -30.88610643146232704, 6.876076431790003163 ) ) ;
#27306=CARTESIAN_POINT ( 'NONE',  ( -1.630517953187181401, -28.88791274465361525, 6.866852738645442322 ) ) ;
#27308=VECTOR ( 'NONE', #8351, 1000.000000000000000 ) ;
#27318=CARTESIAN_POINT ( 'NONE',  ( -0.7716361497966220950, -27.23559914909565904, 6.997764925645183709 ) ) ;
#27321=CARTESIAN_POINT ( 'NONE',  ( 3.218352612218526421, -32.61226313541482114, 6.929923840112066635 ) ) ;
#27323=CARTESIAN_POINT ( 'NONE',  ( -0.9606818258635283492, -27.29645349747919170, 6.894806418505347700 ) ) ;
#27326=CARTESIAN_POINT ( 'NONE',  ( -2.466074105205459333, -31.90971050668977327, 7.013842709614101167 ) ) ;
#27333=CIRCLE ( 'NONE', #17434, 3.499999999999999556 ) ;
#27334=EDGE_CURVE ( 'NONE', #32411, #24028, #28601, .T. ) ;
#27335=CARTESIAN_POINT ( 'NONE',  ( 3.273005465665050906, -32.70437678528606540, 7.387053503561888057 ) ) ;
#27336=CARTESIAN_POINT ( 'NONE',  ( 1.036786817713226450, -32.99129474682166574, 7.785593909369612931 ) ) ;
#27341=CARTESIAN_POINT ( 'NONE',  ( -0.01048567703486024197, -32.63106951773389852, 7.255881584735165646 ) ) ;
#27344=CARTESIAN_POINT ( 'NONE',  ( 5.057249517591178467, -29.03002200468333527, 6.892063359921931642 ) ) ;
#27349=EDGE_LOOP ( 'NONE', ( #40220, #24181, #37547, #11248 ) ) ;
#27350=CARTESIAN_POINT ( 'NONE',  ( 2.798682367290367345, -32.88823465369409860, 7.771081512783694301 ) ) ;
#27351=FACE_OUTER_BOUND ( 'NONE', #17421, .T. ) ;
#27360=ORIENTED_EDGE ( 'NONE', *, *, #3388, .F. ) ;
#27374=B_SPLINE_CURVE_WITH_KNOTS ( 'NONE', 3,
 ( #9501, #37906, #3372, #2750, #34862, #15686, #3171, #37098, #40377, #28237 ),
 .UNSPECIFIED., .F., .F.,
 ( 4, 3, 3, 4 ),
 ( 0.0002170292169044764612, 0.0002420761345915976642, 0.0002723302478207013412, 0.0002816811360866761506 ),
 .UNSPECIFIED. ) ;
#27375=CARTESIAN_POINT ( 'NONE',  ( 0.1051159217697939657, -26.56741378726063019, 7.757178535559535959 ) ) ;
#27377=CARTESIAN_POINT ( 'NONE',  ( -1.795830882100833747, -29.40718105334054044, 6.887547729233689964 ) ) ;
#27380=CARTESIAN_POINT ( 'NONE',  ( 4.595043951338862342, -27.59037241275625263, 7.501983001166816933 ) ) ;
#27383=EDGE_CURVE ( 'NONE', #33469, #6532, #13591, .T. ) ;
#27385=CARTESIAN_POINT ( 'NONE',  ( -1.650274565467498622, -28.99282850696639713, 7.635761828346577573 ) ) ;
#27389=CARTESIAN_POINT ( 'NONE',  ( 3.554700302571109916, -26.60177950712765593, 7.754798119455333705 ) ) ;
#27390=EDGE_LOOP ( 'NONE', ( #27817, #3366, #22617, #26038 ) ) ;
#27392=CARTESIAN_POINT ( 'NONE',  ( 1.057242960569752199, -26.12952878737186424, 7.695279973900954751 ) ) ;
#27394=CARTESIAN_POINT ( 'NONE',  ( 4.640282458258592868, -31.46914920237587410, 7.006908160621408754 ) ) ;
#27395=( BOUNDED_CURVE ( )  B_SPLINE_CURVE ( 3, ( #19435, #15931, #25612, #108 ),
 .UNSPECIFIED., .F., .F. ) 
 B_SPLINE_CURVE_WITH_KNOTS ( ( 4, 4 ),
 ( 4.748221474220560623, 4.941946782021394924 ),
 .UNSPECIFIED. ) 
 CURVE ( )  GEOMETRIC_REPRESENTATION_ITEM ( )  RATIONAL_B_SPLINE_CURVE ( ( 1.000000000000000000, 0.9968749865767494445, 0.9968749865767494445, 1.000000000000000000 ) ) 
 REPRESENTATION_ITEM ( '' )  );
#27400=CARTESIAN_POINT ( 'NONE',  ( 0.05821587971655942800, -26.47918129880799043, 7.753200566781599079 ) ) ;
#27401=CARTESIAN_POINT ( 'NONE',  ( 1.734342869981767121, -33.06976549508323160, 7.714178352335856026 ) ) ;
#27402=EDGE_LOOP ( 'NONE', ( #28771, #6380, #35598, #6703 ) ) ;
#27405=EDGE_CURVE ( 'NONE', #20092, #28513, #29117, .T. ) ;
#27422=AXIS2_PLACEMENT_3D ( 'NONE', #36577, #17616, #20929 ) ;
#27423=DIRECTION ( 'NONE',  ( -0.000000000000000000, -0.000000000000000000, -1.000000000000000000 ) ) ;
#27434=ORIENTED_EDGE ( 'NONE', *, *, #33054, .T. ) ;
#27436=CARTESIAN_POINT ( 'NONE',  ( -0.9023186554178064256, -27.38225855133887876, 7.769368695748482878 ) ) ;
#27439=CARTESIAN_POINT ( 'NONE',  ( 4.357018571862512069, -31.84860785277257733, 6.887161170156905321 ) ) ;
#27441=ORIENTED_EDGE ( 'NONE', *, *, #36581, .F. ) ;
#27443=CARTESIAN_POINT ( 'NONE',  ( -1.771850874358142480, -30.00986502286520974, 6.895394898881670009 ) ) ;
#27445=FACE_OUTER_BOUND ( 'NONE', #12772, .T. ) ;
#27448=CARTESIAN_POINT ( 'NONE',  ( 4.999117453304829262, -30.73971554999452493, 7.730015791551950066 ) ) ;
#27449=CARTESIAN_POINT ( 'NONE',  ( 5.166839686415635846, -29.08636573508110246, 6.867199677474203234 ) ) ;
#27450=CARTESIAN_POINT ( 'NONE',  ( -1.799609906766908685, -29.55956997194928704, 6.917973428066297004 ) ) ;
#27452=CARTESIAN_POINT ( 'NONE',  ( 3.420591031575084262, -32.60521468080220586, 7.781480525794718162 ) ) ;
#27455=CARTESIAN_POINT ( 'NONE',  ( 0.4447534508558593225, -32.82201345496964251, 7.784725160561910329 ) ) ;
#27467=ORIENTED_EDGE ( 'NONE', *, *, #15247, .T. ) ;
#27471=ADVANCED_FACE ( 'NONE', ( #23957 ), #35591, .F. ) ;
#27473=CARTESIAN_POINT ( 'NONE',  ( -0.9562383853963228875, -27.29125251401421082, 6.887161170156905321 ) ) ;
#27474=CARTESIAN_POINT ( 'NONE',  ( 4.854127076346722802, -30.84034076322234696, 7.761597726988851420 ) ) ;
#27478=EDGE_CURVE ( 'NONE', #4150, #23269, #28737, .T. ) ;
#27481=B_SPLINE_CURVE_WITH_KNOTS ( 'NONE', 3,
 ( #11509, #24073, #36644, #8423, #21001, #3517, #38064, #9867, #40529, #31700, #22642, #21820, #31907, #616, #22440, #31093, #3718, #31298, #19134, #204, #12744, #16040, #25518, #16243, #38261, #12337, #34811, #34402, #37642, #35008, #18508 ),
 .UNSPECIFIED., .F., .F.,
 ( 4, 3, 3, 3, 3, 3, 3, 3, 3, 3, 4 ),
 ( 0.000000000000000000, 2.999644130997738061E-05, 6.002588995695006208E-05, 8.960886084588186925E-05, 0.0001190604700446505160, 0.0001489538463052745123, 0.0001796139255494018936, 0.0002109707048517112527, 0.0002426195318110425665, 0.0002740640997890109003, 0.0002849778069099932016 ),
 .UNSPECIFIED. ) ;
#27482=VERTEX_POINT ( 'NONE', #39805 ) ;
#27485=AXIS2_PLACEMENT_3D ( 'NONE', #12075, #27937, #3073 ) ;
#27489=B_SPLINE_CURVE_WITH_KNOTS ( 'NONE', 3,
 ( #159, #25268, #6536, #19083, #31651, #5709, #21571, #18251, #34149, #5917, #31043, #2851, #15371, #27929, #40473, #9194, #29161, #38815, #4064, #28758, #10208, #35358, #7525, #22790, #7130, #3871, #16985, #22991, #35751, #4256, #969 ),
 .UNSPECIFIED., .F., .F.,
 ( 4, 3, 3, 3, 3, 3, 3, 3, 3, 3, 4 ),
 ( 8.940560153363745023E-19, 2.999644130997779397E-05, 6.002588995694919472E-05, 8.960886084588147622E-05, 0.0001190604700446495673, 0.0001489538463052725878, 0.0001796139255493967707, 0.0002109707048517091385, 0.0002426195318110357089, 0.0002740640997890029856, 0.0002849778069099823054 ),
 .UNSPECIFIED. ) ;
#27491=CARTESIAN_POINT ( 'NONE',  ( 0.9453370993353911178, -33.77429008742427641, 7.635761828346577573 ) ) ;
#27494=VERTEX_POINT ( 'NONE', #11575 ) ;
#27497=CARTESIAN_POINT ( 'NONE',  ( -0.1564234597993582332, -32.53678801801031284, 7.751599049952197618 ) ) ;
#27499=FACE_OUTER_BOUND ( 'NONE', #37236, .T. ) ;
#27500=CARTESIAN_POINT ( 'NONE',  ( 2.452196827863095674, -26.25408112137242611, 6.876076431790005827 ) ) ;
#27503=CARTESIAN_POINT ( 'NONE',  ( 2.884763386751913572, -26.27641232226080703, 7.635761828346579350 ) ) ;
#27512=CARTESIAN_POINT ( 'NONE',  ( 4.957641325759844619, -30.81012851192526014, 7.785344483711591934 ) ) ;
#27520=CARTESIAN_POINT ( 'NONE',  ( -1.607555503064097113, -28.78410073912801437, 6.911401339314956260 ) ) ;
#27521=CARTESIAN_POINT ( 'NONE',  ( -0.6817374880303864737, -32.13420688251338220, 6.903112506833889661 ) ) ;
#27522=EDGE_CURVE ( 'NONE', #35485, #4455, #24517, .T. ) ;
#27523=VECTOR ( 'NONE', #18580, 999.9999999999998863 ) ;
#27524=ORIENTED_EDGE ( 'NONE', *, *, #32997, .T. ) ;
#27530=CARTESIAN_POINT ( 'NONE',  ( 4.782632897257695248, -27.91715820809518789, 7.766640943994648438 ) ) ;
#27536=CARTESIAN_POINT ( 'NONE',  ( -1.193343473173243074, -27.78488342726187099, 7.774064877406527962 ) ) ;
#27539=CARTESIAN_POINT ( 'NONE',  ( 5.024341273715212886, -30.28507763625619020, 6.864216812889196717 ) ) ;
#27548=CARTESIAN_POINT ( 'NONE',  ( 3.444544078574621970, -26.65138038738905735, 6.892063359921931642 ) ) ;
#27556=CARTESIAN_POINT ( 'NONE',  ( 4.323672655924887920, -31.73289041085212148, 7.730758795053802146 ) ) ;
#27563=CARTESIAN_POINT ( 'NONE',  ( 3.465568536097964447, -32.59220555077066450, 7.640616322432101093 ) ) ;
#27565=ADVANCED_FACE ( 'NONE', ( #29389 ), #1799, .F. ) ;
#27567=CARTESIAN_POINT ( 'NONE',  ( -1.740011302788441627, -30.21307731605675073, 7.686927408461906808 ) ) ;
#27571=ORIENTED_EDGE ( 'NONE', *, *, #4755, .T. ) ;
#27572=DIRECTION ( 'NONE',  ( 0.3420201433256662704, 0.9396926207859093161, -0.000000000000000000 ) ) ;
#27580=VECTOR ( 'NONE', #28259, 1000.000000000000114 ) ;
#27583=B_SPLINE_CURVE_WITH_KNOTS ( 'NONE', 3,
 ( #31510, #12554, #35022, #15437, #26, #6394, #6601, #25126, #15850, #2917 ),
 .UNSPECIFIED., .F., .F.,
 ( 4, 3, 3, 4 ),
 ( 0.0001585009270395724978, 0.0001815657551981850074, 0.0002118214035944123428, 0.0002170292169044763799 ),
 .UNSPECIFIED. ) ;
#27586=CARTESIAN_POINT ( 'NONE',  ( -1.798596309351013334, -29.48570337927768392, 6.865554069792297653 ) ) ;
#27590=CARTESIAN_POINT ( 'NONE',  ( 0.5038905087661823545, -26.38741722279598534, 7.691066658568948888 ) ) ;
#27592=CARTESIAN_POINT ( 'NONE',  ( -2.527465627618633803, -28.94812858826901802, 7.754798119455333705 ) ) ;
#27593=ORIENTED_EDGE ( 'NONE', *, *, #2976, .F. ) ;
#27597=CARTESIAN_POINT ( 'NONE',  ( 2.721716728528035922, -32.91760109509163357, 6.989977667959444751 ) ) ;
#27599=CARTESIAN_POINT ( 'NONE',  ( 0.6456758497273269448, -26.33765886672673062, 6.864276522220859711 ) ) ;
#27602=CARTESIAN_POINT ( 'NONE',  ( 0.9904113513190105911, -32.89497607571279758, 7.754798119455333705 ) ) ;
#27603=CARTESIAN_POINT ( 'NONE',  ( 5.196076649799282521, -29.67970906813446064, 7.766640943994654656 ) ) ;
#27607=ORIENTED_EDGE ( 'NONE', *, *, #34525, .T. ) ;
#27611=FACE_OUTER_BOUND ( 'NONE', #11789, .T. ) ;
#27613=CYLINDRICAL_SURFACE ( 'NONE', #29233, 0.09010775117052866046 ) ;
#27617=EDGE_LOOP ( 'NONE', ( #13904, #15235, #20531, #23050 ) ) ;
#27619=DIRECTION ( 'NONE',  ( 0.000000000000000000, 0.000000000000000000, 1.000000000000000000 ) ) ;
#27620=VERTEX_POINT ( 'NONE', #13930 ) ;
#27637=( BOUNDED_CURVE ( )  B_SPLINE_CURVE ( 3, ( #17708, #37065, #39752, #23891 ),
 .UNSPECIFIED., .F., .T. ) 
 B_SPLINE_CURVE_WITH_KNOTS ( ( 4, 4 ),
 ( 4.748221474220557958, 4.941946782021392259 ),
 .UNSPECIFIED. ) 
 CURVE ( )  GEOMETRIC_REPRESENTATION_ITEM ( )  RATIONAL_B_SPLINE_CURVE ( ( 1.000000000000000000, 0.9968749865767494445, 0.9968749865767494445, 1.000000000000000000 ) ) 
 REPRESENTATION_ITEM ( '' )  );
#27641=EDGE_CURVE ( 'NONE', #36985, #33555, #10831, .T. ) ;
#27642=CARTESIAN_POINT ( 'NONE',  ( -1.760064674761432801, -30.09457558617890527, 6.865554069792297653 ) ) ;
#27647=CARTESIAN_POINT ( 'NONE',  ( 5.001192086984713292, -30.73384879920740431, 7.710604733652629328 ) ) ;
#27648=CARTESIAN_POINT ( 'NONE',  ( 5.166866161692755810, -29.08666662507720702, 7.750000000000000888 ) ) ;
#27650=CARTESIAN_POINT ( 'NONE',  ( 3.413184693633389610, -32.60729755094480709, 7.783750581861600182 ) ) ;
#27651=CYLINDRICAL_SURFACE ( 'NONE', #17620, 0.09010775117052910455 ) ;
#27654=LINE ( 'NONE', #21701, #1007 ) ;
#27656=CARTESIAN_POINT ( 'NONE',  ( 5.097277635046815192, -29.71537786563932215, 6.868387053540522480 ) ) ;
#27658=EDGE_CURVE ( 'NONE', #22592, #2595, #32943, .T. ) ;
#27661=ORIENTED_EDGE ( 'NONE', *, *, #13870, .T. ) ;
#27670=CARTESIAN_POINT ( 'NONE',  ( 2.989640894365640289, -26.42383226750358816, 6.865312560952603782 ) ) ;
#27672=CARTESIAN_POINT ( 'NONE',  ( 5.048237804244037008, -30.16315501756571393, 7.769368695748486431 ) ) ;
#27675=AXIS2_PLACEMENT_3D ( 'NONE', #15498, #31567, #3390 ) ;
#27676=ORIENTED_EDGE ( 'NONE', *, *, #15351, .T. ) ;
#27683=VERTEX_POINT ( 'NONE', #26985 ) ;
#27688=LINE ( 'NONE', #30599, #39232 ) ;
#27689=CARTESIAN_POINT ( 'NONE',  ( -1.799609906766908685, -29.56993018339339940, 6.929570838012926615 ) ) ;
#27694=DIRECTION ( 'NONE',  ( -1.000000000000000000, 0.000000000000000000, -0.000000000000000000 ) ) ;
#27697=ADVANCED_FACE ( 'NONE', ( #36063 ), #14215, .T. ) ;
#27698=CARTESIAN_POINT ( 'NONE',  ( 5.066811727378471630, -29.09326952720500969, 7.761597726988851420 ) ) ;
#27708=CARTESIAN_POINT ( 'NONE',  ( -1.662376691416499019, -30.07172650866636587, 7.778050822775631978 ) ) ;
#27714=CARTESIAN_POINT ( 'NONE',  ( -1.558538563793567588, -30.53915227141846955, 6.920489980334481928 ) ) ;
#27716=CARTESIAN_POINT ( 'NONE',  ( -1.604992392964304626, -28.77340840982227732, 6.949473656533219135 ) ) ;
#27722=CARTESIAN_POINT ( 'NONE',  ( -1.519718581689926351, -28.19846911342024143, 6.984548363133217030 ) ) ;
#27730=CARTESIAN_POINT ( 'NONE',  ( 4.918643498309219986, -30.94573722681042582, 6.951256099901581997 ) ) ;
#27732=CARTESIAN_POINT ( 'NONE',  ( 3.438683469850188690, -26.53211252316276259, 7.635761828346582014 ) ) ;
#27736=CARTESIAN_POINT ( 'NONE',  ( -1.303108374136985104, -31.16335321463953534, 7.754798119455333705 ) ) ;
#27741=CARTESIAN_POINT ( 'NONE',  ( 5.009673027830494618, -30.35011694869506371, 7.006423389747791219 ) ) ;
#27744=DIRECTION ( 'NONE',  ( 0.8660254037844380415, 0.5000000000000009992, -0.000000000000000000 ) ) ;
#27746=CARTESIAN_POINT ( 'NONE',  ( 2.869513165557623147, -26.27096686817759874, 7.660770905198779346 ) ) ;
#27753=CARTESIAN_POINT ( 'NONE',  ( -0.4014682958407423952, -26.89743201442601972, 7.768425012602594215 ) ) ;
#27756=DIRECTION ( 'NONE',  ( -0.000000000000000000, -0.000000000000000000, -1.000000000000000000 ) ) ;
#27762=VECTOR ( 'NONE', #37336, 1000.000000000000000 ) ;
#27764=ORIENTED_EDGE ( 'NONE', *, *, #34058, .F. ) ;
#27767=ORIENTED_EDGE ( 'NONE', *, *, #26630, .T. ) ;
#27769=DIRECTION ( 'NONE',  ( 0.4999999999999979461, 0.8660254037844397068, -0.000000000000000000 ) ) ;
#27775=EDGE_CURVE ( 'NONE', #28759, #28641, #14285, .T. ) ;
#27780=CARTESIAN_POINT ( 'NONE',  ( -1.799316637852572009, -29.52373849819694485, 6.880608371227948439 ) ) ;
#27784=ORIENTED_EDGE ( 'NONE', *, *, #31745, .F. ) ;
#27787=CARTESIAN_POINT ( 'NONE',  ( 3.543304674501073226, -26.59746626410985826, 7.766640943994650215 ) ) ;
#27793=ADVANCED_FACE ( 'NONE', ( #11119 ), #33174, .T. ) ;
#27795=CARTESIAN_POINT ( 'NONE',  ( 2.788398779348973733, -32.89652560498232248, 6.865482280155368322 ) ) ;
#27800=CARTESIAN_POINT ( 'NONE',  ( 5.100295740189424443, -29.54432006460276128, 7.652160403243382980 ) ) ;
#27801=CARTESIAN_POINT ( 'NONE',  ( 4.633009665528590837, -31.48036009422220616, 6.980586498568963627 ) ) ;
#27813=FACE_OUTER_BOUND ( 'NONE', #7924, .T. ) ;
#27816=CARTESIAN_POINT ( 'NONE',  ( -1.531573891984414848, -33.61112889622174293, 7.754798119455333705 ) ) ;
#27817=ORIENTED_EDGE ( 'NONE', *, *, #28369, .F. ) ;
#27821=CARTESIAN_POINT ( 'NONE',  ( -0.1730901457863348591, -32.40719633966231328, 6.920489980334476599 ) ) ;
#27825=CARTESIAN_POINT ( 'NONE',  ( -1.852189108926798777, -33.38420822586166281, 6.894806418505347700 ) ) ;
#27827=CARTESIAN_POINT ( 'NONE',  ( 0.5199030923387487624, -26.38144301222279964, 7.748216051605120391 ) ) ;
#27830=VERTEX_POINT ( 'NONE', #17094 ) ;
#27831=B_SPLINE_CURVE_WITH_KNOTS ( 'NONE', 3,
 ( #10060, #22645, #23237, #23042, #29016, #29418, #35211, #13765, #820, #35806 ),
 .UNSPECIFIED., .F., .F.,
 ( 4, 3, 3, 4 ),
 ( 0.0002170292169044783044, 0.0002420761345915947911, 0.0002723302478207000944, 0.0002816811360866801079 ),
 .UNSPECIFIED. ) ;
#27832=AXIS2_PLACEMENT_3D ( 'NONE', #38377, #13077, #4040 ) ;
#27837=DIRECTION ( 'NONE',  ( -1.000000000000000000, 0.000000000000000000, 0.000000000000000000 ) ) ;
#27838=CARTESIAN_POINT ( 'NONE',  ( -1.698824908307911219, -29.49622598863939871, 6.874555630061442102 ) ) ;
#27839=VERTEX_POINT ( 'NONE', #1479 ) ;
#27842=CARTESIAN_POINT ( 'NONE',  ( -1.601932461984457490, -30.40839394270583540, 7.505001789837628223 ) ) ;
#27843=CARTESIAN_POINT ( 'NONE',  ( 1.510748483419375621, -33.06479068383551123, 6.931070083220559397 ) ) ;
#27845=ADVANCED_FACE ( 'NONE', ( #24504 ), #5367, .F. ) ;
#27846=LINE ( 'NONE', #14876, #2481 ) ;
#27847=CARTESIAN_POINT ( 'NONE',  ( 1.664433243520564654, -26.07011488755866679, 7.695279973900954751 ) ) ;
#27848=CARTESIAN_POINT ( 'NONE',  ( 5.198120437317888864, -29.69595573662939358, 7.750000000000000888 ) ) ;
#27849=EDGE_CURVE ( 'NONE', #25767, #24264, #1051, .T. ) ;
#27852=CARTESIAN_POINT ( 'NONE',  ( 1.138951562800235795, -32.92325491812241012, 7.661510568013095934 ) ) ;
#27854=DIRECTION ( 'NONE',  ( -1.000000000000000000, 0.000000000000000000, 0.000000000000000000 ) ) ;
#27867=VECTOR ( 'NONE', #17687, 1000.000000000000000 ) ;
#27871=CARTESIAN_POINT ( 'NONE',  ( 1.192341134868766028, -26.20810236866151754, 6.870716933885665512 ) ) ;
#27873=CARTESIAN_POINT ( 'NONE',  ( 5.046791071466609324, -30.17131961341260649, 7.775108481317161591 ) ) ;
#27874=ORIENTED_EDGE ( 'NONE', *, *, #10918, .F. ) ;
#27876=VECTOR ( 'NONE', #27919, 1000.000000000000114 ) ;
#27879=( BOUNDED_CURVE ( )  B_SPLINE_CURVE ( 3, ( #11269, #36409, #8180, #20752 ),
 .UNSPECIFIED., .F., .T. ) 
 B_SPLINE_CURVE_WITH_KNOTS ( ( 4, 4 ),
 ( 1.347909859412854461, 1.534781240595299856 ),
 .UNSPECIFIED. ) 
 CURVE ( )  GEOMETRIC_REPRESENTATION_ITEM ( )  RATIONAL_B_SPLINE_CURVE ( ( 1.000000000000000000, 0.9970920404276226723, 0.9970920404276226723, 1.000000000000000000 ) ) 
 REPRESENTATION_ITEM ( '' )  );
#27880=CARTESIAN_POINT ( 'NONE',  ( -1.485716978080746209, -30.75683203970418944, 7.652160403243385645 ) ) ;
#27883=EDGE_CURVE ( 'NONE', #21217, #35449, #24762, .T. ) ;
#27885=CARTESIAN_POINT ( 'NONE',  ( 2.806342938108580043, -32.78503022925695376, 7.785172627573962778 ) ) ;
#27893=EDGE_CURVE ( 'NONE', #39394, #9668, #16001, .T. ) ;
#27897=CARTESIAN_POINT ( 'NONE',  ( -1.754526989783608437, -30.08320498581767666, 7.776484688137383472 ) ) ;
#27901=CARTESIAN_POINT ( 'NONE',  ( 5.050665697719591840, -28.99051485080055102, 7.775108481317161591 ) ) ;
#27907=ORIENTED_EDGE ( 'NONE', *, *, #35268, .F. ) ;
#27912=DIRECTION ( 'NONE',  ( -0.9848077530122015810, -0.1736481776669674404, 0.000000000000000000 ) ) ;
#27916=ORIENTED_EDGE ( 'NONE', *, *, #37780, .T. ) ;
#27919=DIRECTION ( 'NONE',  ( -0.7660444431189725734, -0.6427876096865456912, -0.000000000000000000 ) ) ;
#27920=ORIENTED_EDGE ( 'NONE', *, *, #7555, .F. ) ;
#27929=CARTESIAN_POINT ( 'NONE',  ( -1.333638583621181928, -31.10443431896878508, 6.895222827070020877 ) ) ;
#27933=ADVANCED_FACE ( 'NONE', ( #5569 ), #18108, .F. ) ;
#27934=DIRECTION ( 'NONE',  ( 0.7660444431189857850, -0.6427876096865300370, -0.000000000000000000 ) ) ;
#27937=DIRECTION ( 'NONE',  ( 1.047444401652940007E-14, -1.000000000000000000, -0.000000000000000000 ) ) ;
#27938=DIRECTION ( 'NONE',  ( -0.6427876096865328126, -0.7660444431189835646, -0.000000000000000000 ) ) ;
#27944=EDGE_CURVE ( 'NONE', #38484, #39394, #37139, .T. ) ;
#27945=CARTESIAN_POINT ( 'NONE',  ( 5.007316143351812521, -30.36002356176803829, 6.920489980334479263 ) ) ;
#27951=CARTESIAN_POINT ( 'NONE',  ( 4.639291099620161063, -31.27958793520167191, 7.775108481317161591 ) ) ;
#27953=CARTESIAN_POINT ( 'NONE',  ( 4.029674975067525367, -26.95754872143103498, 6.863784140767622333 ) ) ;
#27956=CARTESIAN_POINT ( 'NONE',  ( -2.585338981833881000, -32.18494463595775557, 7.754798119455333705 ) ) ;
#27957=CARTESIAN_POINT ( 'NONE',  ( 1.793640042356549946, -26.17119502933373809, 6.866852738645443210 ) ) ;
#27967=DIRECTION ( 'NONE',  ( 0.000000000000000000, 0.6834397476448840214, 0.7300069255418726311 ) ) ;
#27968=PLANE ( 'NONE',  #14523 ) ;
#27973=CARTESIAN_POINT ( 'NONE',  ( -1.506494769919744403, -28.44037730863004398, 7.680992449362117114 ) ) ;
#27975=ORIENTED_EDGE ( 'NONE', *, *, #35088, .T. ) ;
#27983=CARTESIAN_POINT ( 'NONE',  ( 4.740160921379847458, -31.30480577326951064, 7.750000000000000000 ) ) ;
#27987=CARTESIAN_POINT ( 'NONE',  ( 0.5871758347987294790, -26.26248204398054753, 7.780491323090171996 ) ) ;
#27991=ORIENTED_EDGE ( 'NONE', *, *, #11596, .T. ) ;
#27993=AXIS2_PLACEMENT_3D ( 'NONE', #14655, #39166, #39792 ) ;
#28002=B_SPLINE_CURVE_WITH_KNOTS ( 'NONE', 3,
 ( #3593, #16117, #28683, #13028, #25592, #38136, #3791, #9937, #22518, #6861 ),
 .UNSPECIFIED., .F., .F.,
 ( 4, 3, 3, 4 ),
 ( 2.168404344971008868E-19, 3.025570593003071339E-05, 6.051145698343921226E-05, 6.468151674593626945E-05 ),
 .UNSPECIFIED. ) ;
#28003=CARTESIAN_POINT ( 'NONE',  ( 2.730055066371769090, -32.91505153338314216, 6.903112506833889661 ) ) ;
#28017=EDGE_CURVE ( 'NONE', #20612, #309, #15764, .T. ) ;
#28019=VECTOR ( 'NONE', #38566, 1000.000000000000000 ) ;
#28020=ORIENTED_EDGE ( 'NONE', *, *, #21656, .T. ) ;
#28026=CARTESIAN_POINT ( 'NONE',  ( 1.700390093233090871, -29.56993018339339940, 7.800000000000000711 ) ) ;
#28028=VERTEX_POINT ( 'NONE', #32671 ) ;
#28030=EDGE_CURVE ( 'NONE', #33546, #10597, #32682, .T. ) ;
#28034=CARTESIAN_POINT ( 'NONE',  ( -0.1781345077003545219, -32.40385772722507340, 6.959317978105162616 ) ) ;
#28037=CARTESIAN_POINT ( 'NONE',  ( 2.338742698598151204, -26.12863595720122234, 6.894806418505347700 ) ) ;
#28046=CARTESIAN_POINT ( 'NONE',  ( 4.292159273299870570, -31.92212432182409287, 6.870724624169667116 ) ) ;
#28063=CARTESIAN_POINT ( 'NONE',  ( 1.754540994691119460, -33.27093018339341768, 7.695279973900954751 ) ) ;
#28064=CARTESIAN_POINT ( 'NONE',  ( 4.358291535071522560, -27.29274773012506827, 7.697032948437508182 ) ) ;
#28066=CARTESIAN_POINT ( 'NONE',  ( 2.111802210604301511, -32.94495686453777239, 6.887945620086121323 ) ) ;
#28069=CARTESIAN_POINT ( 'NONE',  ( -1.512578315116791750, -30.68206402898919904, 6.889465824494257262 ) ) ;
#28073=CIRCLE ( 'NONE', #26755, 3.449999999999999734 ) ;
#28075=CARTESIAN_POINT ( 'NONE',  ( -0.9624133124989321386, -27.31194369618440732, 7.778495531946297170 ) ) ;
#28076=CARTESIAN_POINT ( 'NONE',  ( 0.05654071202359058079, -26.59372095824146243, 6.880147297696980857 ) ) ;
#28079=CIRCLE ( 'NONE', #23472, 3.499999999999999556 ) ;
#28081=EDGE_CURVE ( 'NONE', #38902, #19590, #28526, .T. ) ;
#28085=ORIENTED_EDGE ( 'NONE', *, *, #21256, .T. ) ;
#28086=EDGE_CURVE ( 'NONE', #20612, #32452, #776, .T. ) ;
#28090=CARTESIAN_POINT ( 'NONE',  ( -1.678016691892348700, -29.95251036351044149, 6.959317978105168834 ) ) ;
#28096=DIRECTION ( 'NONE',  ( -0.000000000000000000, -0.000000000000000000, -1.000000000000000000 ) ) ;
#28103=CARTESIAN_POINT ( 'NONE',  ( 1.616945372681888538, -32.96890605541899077, 6.870716933885664623 ) ) ;
#28105=FACE_OUTER_BOUND ( 'NONE', #15781, .T. ) ;
#28108=CARTESIAN_POINT ( 'NONE',  ( 4.317861630214887114, -31.73992721779714898, 7.643333865083951295 ) ) ;
#28110=CARTESIAN_POINT ( 'NONE',  ( 0.7149948906900660539, -26.31585638355339185, 7.013842709614101167 ) ) ;
#28117=ORIENTED_EDGE ( 'NONE', *, *, #23641, .T. ) ;
#28121=CARTESIAN_POINT ( 'NONE',  ( 4.960724736016636882, -30.80272740983260604, 7.785096263473211486 ) ) ;
#28124=( BOUNDED_CURVE ( )  B_SPLINE_CURVE ( 3, ( #6966, #39039, #16424, #4494 ),
 .UNSPECIFIED., .F., .T. ) 
 B_SPLINE_CURVE_WITH_KNOTS ( ( 4, 4 ),
 ( 1.381924640371167579, 1.574767692156076260 ),
 .UNSPECIFIED. ) 
 CURVE ( )  GEOMETRIC_REPRESENTATION_ITEM ( )  RATIONAL_B_SPLINE_CURVE ( ( 1.000000000000000000, 0.9969033633783032089, 0.9969033633783032089, 1.000000000000000000 ) ) 
 REPRESENTATION_ITEM ( '' )  );
#28135=CARTESIAN_POINT ( 'NONE',  ( -1.697580213352021250, -29.45244296570870901, 7.759451378593097637 ) ) ;
#28140=CARTESIAN_POINT ( 'NONE',  ( 0.009528945288370773911, -26.52245690844340231, 7.785593909369613819 ) ) ;
#28150=CARTESIAN_POINT ( 'NONE',  ( 5.012588991809223238, -30.33765636181075109, 6.887945620086120435 ) ) ;
#28156=CARTESIAN_POINT ( 'NONE',  ( 4.584375091198674035, -31.37066225182081425, 7.759451378593099413 ) ) ;
#28158=CARTESIAN_POINT ( 'NONE',  ( 4.094185015697331842, -27.01655085626599018, 6.961115707816238896 ) ) ;
#28162=ORIENTED_EDGE ( 'NONE', *, *, #7495, .F. ) ;
#28170=CARTESIAN_POINT ( 'NONE',  ( 2.930077627932792250, -32.84679970447462694, 7.678495282201405203 ) ) ;
#28171=ORIENTED_EDGE ( 'NONE', *, *, #19193, .F. ) ;
#28173=ORIENTED_EDGE ( 'NONE', *, *, #345, .T. ) ;
#28185=CARTESIAN_POINT ( 'NONE',  ( 4.882868366733327470, -28.37333834040810032, 7.695279973900954751 ) ) ;
#28187=CARTESIAN_POINT ( 'NONE',  ( 5.913338541744446175, -28.86358524566460915, 7.695279973900954751 ) ) ;
#28194=CARTESIAN_POINT ( 'NONE',  ( 3.439741984728057478, -26.53271409599866715, 7.756742906098588186 ) ) ;
#28195=EDGE_LOOP ( 'NONE', ( #28404, #14465, #15213, #39292, #29126 ) ) ;
#28200=CARTESIAN_POINT ( 'NONE',  ( 0.5426199015143727822, -32.76674687291834687, 7.763628509615287498 ) ) ;
#28206=EDGE_CURVE ( 'NONE', #9863, #11496, #40438, .T. ) ;
#28207=EDGE_CURVE ( 'NONE', #24466, #13676, #31016, .T. ) ;
#28209=CARTESIAN_POINT ( 'NONE',  ( -1.225953191357326277, -31.30097466021442187, 7.695279973900954751 ) ) ;
#28210=ORIENTED_EDGE ( 'NONE', *, *, #8857, .F. ) ;
#28214=ORIENTED_EDGE ( 'NONE', *, *, #4793, .T. ) ;
#28224=ORIENTED_EDGE ( 'NONE', *, *, #30609, .T. ) ;
#28232=VECTOR ( 'NONE', #14011, 999.9999999999998863 ) ;
#28233=CARTESIAN_POINT ( 'NONE',  ( 2.963912204589347343, -26.41341833881434198, 7.768425012602590662 ) ) ;
#28234=ORIENTED_EDGE ( 'NONE', *, *, #3997, .T. ) ;
#28237=CARTESIAN_POINT ( 'NONE',  ( 2.321451664048270302, -33.01438696571141662, 7.635761828346576685 ) ) ;
#28238=CARTESIAN_POINT ( 'NONE',  ( 1.700390093233090871, -29.56993018339339940, 7.800000000000000711 ) ) ;
#28243=VERTEX_POINT ( 'NONE', #15132 ) ;
#28244=EDGE_CURVE ( 'NONE', #35733, #3023, #27688, .T. ) ;
#28245=FACE_OUTER_BOUND ( 'NONE', #38882, .T. ) ;
#28249=CARTESIAN_POINT ( 'NONE',  ( -1.699007393330835392, -29.50544089494019673, 6.880147297696982633 ) ) ;
#28251=CARTESIAN_POINT ( 'NONE',  ( 2.170460981197068762, -32.93727830324805694, 7.754798119455333705 ) ) ;
#28255=EDGE_CURVE ( 'NONE', #31660, #7424, #26126, .T. ) ;
#28257=CARTESIAN_POINT ( 'NONE',  ( 1.664433243520564654, -26.07011488755866679, 7.695279973900954751 ) ) ;
#28258=CARTESIAN_POINT ( 'NONE',  ( 1.664433243520564654, -26.07011488755866679, 7.701614758090453705 ) ) ;
#28259=DIRECTION ( 'NONE',  ( -0.1736481776669206722, -0.9848077530122096857, -0.000000000000000000 ) ) ;
#28261=FACE_OUTER_BOUND ( 'NONE', #26837, .T. ) ;
#28265=CARTESIAN_POINT ( 'NONE',  ( 0.4969225441612274974, -32.85060279565202990, 7.773839561854630098 ) ) ;
#28271=CARTESIAN_POINT ( 'NONE',  ( -1.513482870951689430, -30.67944384715880091, 6.887041543973314361 ) ) ;
#28274=FACE_OUTER_BOUND ( 'NONE', #9624, .T. ) ;
#28278=CARTESIAN_POINT ( 'NONE',  ( 2.966849565284320978, -26.30708134228679640, 6.867280401193709416 ) ) ;
#28280=DIRECTION ( 'NONE',  ( -1.000000000000000000, 0.000000000000000000, 0.000000000000000000 ) ) ;
#28282=CARTESIAN_POINT ( 'NONE',  ( 3.483130834601454229, -26.55797363598811245, 6.887161170156904433 ) ) ;
#28288=CARTESIAN_POINT ( 'NONE',  ( 4.666500650180242182, -31.42793668606411117, 7.750000000000000888 ) ) ;
#28299=CARTESIAN_POINT ( 'NONE',  ( 2.868360829923958022, -32.76303417817520369, 7.763628509615287498 ) ) ;
#28303=ORIENTED_EDGE ( 'NONE', *, *, #7385, .T. ) ;
#28306=VERTEX_POINT ( 'NONE', #21324 ) ;
#28312=CARTESIAN_POINT ( 'NONE',  ( 1.700390093233090871, -29.56993018339339940, -8.199999999999999289 ) ) ;
#28313=CARTESIAN_POINT ( 'NONE',  ( 3.733834482138272737, -32.29483457019856019, 6.903372536218459032 ) ) ;
#28318=EDGE_CURVE ( 'NONE', #28942, #20340, #36900, .T. ) ;
#28324=EDGE_CURVE ( 'NONE', #14526, #24466, #4966, .T. ) ;
#28329=CARTESIAN_POINT ( 'NONE',  ( 2.187796539937281182, -33.03559314236433408, 7.754798119455333705 ) ) ;
#28332=CARTESIAN_POINT ( 'NONE',  ( -1.796521113867400654, -29.56993018341788826, 7.767301406056523305 ) ) ;
#28337=DIRECTION ( 'NONE',  ( 0.7660444431189770143, 0.6427876096865404731, -0.000000000000000000 ) ) ;
#28338=ORIENTED_EDGE ( 'NONE', *, *, #5120, .F. ) ;
#28346=ORIENTED_EDGE ( 'NONE', *, *, #28318, .F. ) ;
#28349=B_SPLINE_CURVE_WITH_KNOTS ( 'NONE', 3,
 ( #22401, #34970, #19295, #31865, #3678, #16203, #27642, #8693, #7537, #30757, #1191, #17542, #32467, #21069, #14871, #27443, #29371, #8488, #40198, #10616, #21273, #18165, #33845, #33643, #20644, #36506, #4267, #5623, #27038, #5418, #2352 ),
 .UNSPECIFIED., .F., .F.,
 ( 4, 3, 3, 3, 3, 3, 3, 3, 3, 3, 4 ),
 ( 3.885015761172426832E-18, 3.077658087705615681E-05, 6.152638666998687552E-05, 9.267501192706369616E-05, 0.0001241882240135191984, 0.0001556618703051669626, 0.0001866161554452214634, 0.0002167966385860943524, 0.0002463805737537729358, 0.0002758761370306496170, 0.0002847094172290017965 ),
 .UNSPECIFIED. ) ;
#28350=FACE_OUTER_BOUND ( 'NONE', #24817, .T. ) ;
#28351=DIRECTION ( 'NONE',  ( -0.000000000000000000, -0.000000000000000000, -1.000000000000000000 ) ) ;
#28352=DIRECTION ( 'NONE',  ( 0.9848077530122081313, 0.1736481776669300814, 0.000000000000000000 ) ) ;
#28358=CARTESIAN_POINT ( 'NONE',  ( 5.686407058211319310, -26.27220315192986888, 7.695279973900954751 ) ) ;
#28359=CARTESIAN_POINT ( 'NONE',  ( -1.656077431862442717, -30.11226380117775037, 6.894806418505347700 ) ) ;
#28366=CARTESIAN_POINT ( 'NONE',  ( 2.863609035986292461, -26.26888160889163615, 7.686927408461905031 ) ) ;
#28369=EDGE_CURVE ( 'NONE', #20410, #38669, #728, .T. ) ;
#28370=CARTESIAN_POINT ( 'NONE',  ( 4.059384891591554911, -26.98436573025793095, 6.875780273367531059 ) ) ;
#28374=( BOUNDED_CURVE ( )  B_SPLINE_CURVE ( 3, ( #38792, #4824, #26453, #20660 ),
 .UNSPECIFIED., .F., .T. ) 
 B_SPLINE_CURVE_WITH_KNOTS ( ( 4, 4 ),
 ( 1.381924640371167801, 1.574767692156075372 ),
 .UNSPECIFIED. ) 
 CURVE ( )  GEOMETRIC_REPRESENTATION_ITEM ( )  RATIONAL_B_SPLINE_CURVE ( ( 1.000000000000000000, 0.9969033633783033199, 0.9969033633783033199, 1.000000000000000000 ) ) 
 REPRESENTATION_ITEM ( '' )  );
#28378=ORIENTED_EDGE ( 'NONE', *, *, #29293, .T. ) ;
#28383=VERTEX_POINT ( 'NONE', #35121 ) ;
#28385=EDGE_LOOP ( 'NONE', ( #11444, #6181, #17119, #40039, #18978 ) ) ;
#28388=ORIENTED_EDGE ( 'NONE', *, *, #1032, .T. ) ;
#28391=EDGE_CURVE ( 'NONE', #13762, #19523, #16763, .T. ) ;
#28393=CARTESIAN_POINT ( 'NONE',  ( 4.381563664431031846, -27.47916279290977570, 7.754798119455333705 ) ) ;
#28394=ORIENTED_EDGE ( 'NONE', *, *, #31958, .T. ) ;
#28404=ORIENTED_EDGE ( 'NONE', *, *, #24687, .T. ) ;
#28408=CARTESIAN_POINT ( 'NONE',  ( 2.123610019918336089, -26.08872931251818983, 7.139344958878410807 ) ) ;
#28411=B_SPLINE_CURVE_WITH_KNOTS ( 'NONE', 3,
 ( #25591, #38135, #9936, #15710, #25185, #37716, #22517, #9523, #35084, #6859 ),
 .UNSPECIFIED., .F., .F.,
 ( 4, 3, 3, 4 ),
 ( 0.000000000000000000, 3.025505781527818361E-05, 6.051003801291508300E-05, 6.468145402690557617E-05 ),
 .UNSPECIFIED. ) ;
#28418=CARTESIAN_POINT ( 'NONE',  ( -1.751698146652124866, -30.14706689514045479, 6.894806418505347700 ) ) ;
#28420=CARTESIAN_POINT ( 'NONE',  ( 4.404484264602725574, -31.79206310534561553, 7.698786668945011513 ) ) ;
#28421=DIRECTION ( 'NONE',  ( -0.000000000000000000, -0.000000000000000000, -1.000000000000000000 ) ) ;
#28422=VECTOR ( 'NONE', #16707, 1000.000000000000227 ) ;
#28423=CARTESIAN_POINT ( 'NONE',  ( -1.268944822877880352, -31.22617634019398380, 7.785868773668303433 ) ) ;
#28429=EDGE_LOOP ( 'NONE', ( #10104, #17356, #25930, #35759 ) ) ;
#28433=CARTESIAN_POINT ( 'NONE',  ( 4.715819433959782536, -31.34677736058242559, 6.894806418505347700 ) ) ;
#28434=CARTESIAN_POINT ( 'NONE',  ( 4.952701570995533764, -28.57870110776509875, 6.887945620086120435 ) ) ;
#28442=CARTESIAN_POINT ( 'NONE',  ( 5.198120437317888864, -29.69595573662939358, 7.750000000000000888 ) ) ;
#28444=CARTESIAN_POINT ( 'NONE',  ( -1.752498985642891860, -28.99760421947165057, 7.701614758090454593 ) ) ;
#28448=CYLINDRICAL_SURFACE ( 'NONE', #15789, 0.09010775117052816086 ) ;
#28450=EDGE_CURVE ( 'NONE', #14209, #40275, #7439, .T. ) ;
#28453=VECTOR ( 'NONE', #25607, 1000.000000000000114 ) ;
#28454=ORIENTED_EDGE ( 'NONE', *, *, #25349, .T. ) ;
#28459=FACE_OUTER_BOUND ( 'NONE', #23522, .T. ) ;
#28463=CARTESIAN_POINT ( 'NONE',  ( 4.890701645444022638, -28.39438256639548896, 7.635761828346577573 ) ) ;
#28465=CYLINDRICAL_SURFACE ( 'NONE', #35992, 3.399999999999999911 ) ;
#28466=CARTESIAN_POINT ( 'NONE',  ( -0.6250228819461873808, -32.05034436148299193, 7.013842709614101167 ) ) ;
#28472=CARTESIAN_POINT ( 'NONE',  ( -0.9488855924148063004, -31.70099553385623992, 7.784476445165072533 ) ) ;
#28474=CARTESIAN_POINT ( 'NONE',  ( 3.356636250033691482, -32.53926509950436952, 7.785868773668303433 ) ) ;
#28477=FACE_OUTER_BOUND ( 'NONE', #11239, .T. ) ;
#28478=CARTESIAN_POINT ( 'NONE',  ( -1.504465140167883019, -28.43462789667258406, 7.730758795053805699 ) ) ;
#28486=CARTESIAN_POINT ( 'NONE',  ( -0.9039228576583087094, -27.23290037300662902, 7.761113333117551250 ) ) ;
#28487=CARTESIAN_POINT ( 'NONE',  ( 0.08177934104577368191, -26.57991422468078824, 6.866852738645442322 ) ) ;
#28489=( BOUNDED_CURVE ( )  B_SPLINE_CURVE ( 3, ( #2340, #27028, #12186, #5206 ),
 .UNSPECIFIED., .F., .F. ) 
 B_SPLINE_CURVE_WITH_KNOTS ( ( 4, 4 ),
 ( 1.347909859412854017, 1.534781240595299190 ),
 .UNSPECIFIED. ) 
 CURVE ( )  GEOMETRIC_REPRESENTATION_ITEM ( )  RATIONAL_B_SPLINE_CURVE ( ( 1.000000000000000000, 0.9970920404276226723, 0.9970920404276226723, 1.000000000000000000 ) ) 
 REPRESENTATION_ITEM ( '' )  );
#28490=CARTESIAN_POINT ( 'NONE',  ( 1.216376417621422679, -26.20454968296333220, 7.768425012602591551 ) ) ;
#28491=CARTESIAN_POINT ( 'NONE',  ( 5.054174351635810858, -30.12861716918250465, 7.721096864323902409 ) ) ;
#28494=DIRECTION ( 'NONE',  ( -0.000000000000000000, -0.000000000000000000, -1.000000000000000000 ) ) ;
#28495=AXIS2_PLACEMENT_3D ( 'NONE', #3491, #31675, #19107 ) ;
#28496=CARTESIAN_POINT ( 'NONE',  ( 0.6527267737179240914, -26.33536660093865578, 7.754798119455333705 ) ) ;
#28505=VECTOR ( 'NONE', #31383, 1000.000000000000000 ) ;
#28506=CARTESIAN_POINT ( 'NONE',  ( -1.627984416835427162, -30.65173788820889200, 7.754798119455333705 ) ) ;
#28507=CARTESIAN_POINT ( 'NONE',  ( 2.890739320099559695, -32.75474996909392189, 7.730758795053806587 ) ) ;
#28513=VERTEX_POINT ( 'NONE', #22957 ) ;
#28515=ORIENTED_EDGE ( 'NONE', *, *, #20331, .T. ) ;
#28516=DIRECTION ( 'NONE',  ( -0.7508067542896647018, -7.864283315039239776E-15, 0.6605219282605377940 ) ) ;
#28517=CARTESIAN_POINT ( 'NONE',  ( 1.596524671759634195, -32.96835966857143774, 6.864651958020304257 ) ) ;
#28519=CARTESIAN_POINT ( 'NONE',  ( -1.560415995823573931, -30.53281333591209545, 6.949473656533220911 ) ) ;
#28521=CARTESIAN_POINT ( 'NONE',  ( 5.741588806061445283, -32.80189416861090024, 7.754798119455333705 ) ) ;
#28522=CARTESIAN_POINT ( 'NONE',  ( 5.199130151573005953, -29.66439072687301959, 6.863805608295730387 ) ) ;
#28524=DIRECTION ( 'NONE',  ( 0.4999999999999979461, 0.8660254037844397068, -0.000000000000000000 ) ) ;
#28526=B_SPLINE_CURVE_WITH_KNOTS ( 'NONE', 3,
 ( #38627, #23193, #16791, #31866, #7538, #4077, #16591, #34971, #28774, #983, #35170, #581, #10426, #19296, #35569, #29372, #13728, #19897, #13120 ),
 .UNSPECIFIED., .F., .F.,
 ( 4, 3, 3, 3, 3, 3, 4 ),
 ( 9.697399036122160616E-19, 2.546128104244903007E-05, 5.711050680484518844E-05, 8.113074941676767392E-05, 0.0001053129305727209560, 0.0001360598016347318545, 0.0001612931755713721809 ),
 .UNSPECIFIED. ) ;
#28531=ORIENTED_EDGE ( 'NONE', *, *, #4346, .T. ) ;
#28532=EDGE_LOOP ( 'NONE', ( #6168, #40176 ) ) ;
#28536=B_SPLINE_CURVE_WITH_KNOTS ( 'NONE', 3,
 ( #37815, #27741, #31262, #34774, #12084, #18470, #9620, #21583, #31462, #31055, #27945, #24872, #37411, #15598, #28150, #3285, #40091, #33946, #5722, #36399, #27539, #24029 ),
 .UNSPECIFIED., .F., .F.,
 ( 4, 3, 3, 3, 3, 3, 3, 4 ),
 ( 4.982613841084487634E-18, 2.999644130997582546E-05, 6.002588995694560330E-05, 8.960886084587831848E-05, 0.0001190604700446494589, 0.0001489538463052702839, 0.0001796139255493956323, 0.0002076538946377561555 ),
 .UNSPECIFIED. ) ;
#28546=ORIENTED_EDGE ( 'NONE', *, *, #25748, .F. ) ;
#28547=EDGE_CURVE ( 'NONE', #33357, #23776, #16354, .T. ) ;
#28550=CARTESIAN_POINT ( 'NONE',  ( -1.699110614488611226, -29.51162730196624651, 7.785315938117270740 ) ) ;
#28552=CARTESIAN_POINT ( 'NONE',  ( -0.8150251588124118873, -27.28240185911760918, 6.865312560952603782 ) ) ;
#28555=EDGE_CURVE ( 'NONE', #5955, #33555, #38695, .T. ) ;
#28556=AXIS2_PLACEMENT_3D ( 'NONE', #25923, #14152, #7375 ) ;
#28561=CARTESIAN_POINT ( 'NONE',  ( 3.422192536544015340, -26.52273535105849689, 7.670465701733744091 ) ) ;
#28568=CARTESIAN_POINT ( 'NONE',  ( -0.9891828103420344798, -31.64990550078098508, 6.865312560952604670 ) ) ;
#28569=CARTESIAN_POINT ( 'NONE',  ( 1.700390093233090871, -29.56993018339339940, 7.750000000000000888 ) ) ;
#28572=CARTESIAN_POINT ( 'NONE',  ( 2.406396206790859527, -33.27093018339341057, 6.954324564059724878 ) ) ;
#28576=ORIENTED_EDGE ( 'NONE', *, *, #37534, .T. ) ;
#28580=CARTESIAN_POINT ( 'NONE',  ( 1.681622008834811721, -26.16998198393388009, 7.748216051605119503 ) ) ;
#28583=CARTESIAN_POINT ( 'NONE',  ( -1.748756095191392523, -28.97546355617463121, 7.635761828346576685 ) ) ;
#28585=VECTOR ( 'NONE', #19616, 1000.000000000000000 ) ;
#28593=ORIENTED_EDGE ( 'NONE', *, *, #1781, .T. ) ;
#28594=CARTESIAN_POINT ( 'NONE',  ( -1.633050216874273541, -28.90040684798571746, 7.782034975670478083 ) ) ;
#28596=VERTEX_POINT ( 'NONE', #29921 ) ;
#28601=B_SPLINE_CURVE_WITH_KNOTS ( 'NONE', 3,
 ( #7813, #7613, #32751, #39096, #20364, #20560, #11285, #14189, #16867, #32944 ),
 .UNSPECIFIED., .F., .F.,
 ( 4, 3, 3, 4 ),
 ( 0.0002170292169044780875, 0.0002420761345915950621, 0.0002723302478206961370, 0.0002816811360866806500 ),
 .UNSPECIFIED. ) ;
#28605=EDGE_CURVE ( 'NONE', #15988, #32186, #33231, .T. ) ;
#28606=CARTESIAN_POINT ( 'NONE',  ( 4.745871275333505501, -31.29476187647891550, 7.730015791551949178 ) ) ;
#28608=CARTESIAN_POINT ( 'NONE',  ( 4.591583649630617714, -31.35909501955320167, 6.864651958020304257 ) ) ;
#28611=B_SPLINE_CURVE_WITH_KNOTS ( 'NONE', 3,
 ( #34055, #5828, #12606, #18369, #40598, #24973, #21883, #34460, #73, #25172 ),
 .UNSPECIFIED., .F., .F.,
 ( 4, 3, 3, 4 ),
 ( 0.0002170292169044690887, 0.0002420761345915941947, 0.0002723302478206990102, 0.0002816811360866637907 ),
 .UNSPECIFIED. ) ;
#28615=EDGE_LOOP ( 'NONE', ( #14561, #36442, #38667, #24276, #13341 ) ) ;
#28616=VECTOR ( 'NONE', #26994, 1000.000000000000000 ) ;
#28619=CARTESIAN_POINT ( 'NONE',  ( 3.480609529026132520, -26.57320034156991184, 7.785096263473211486 ) ) ;
#28627=CIRCLE ( 'NONE', #1681, 3.499999999999999556 ) ;
#28628=CARTESIAN_POINT ( 'NONE',  ( 0.5713750229309367823, -32.77700439067807281, 7.695279973900954751 ) ) ;
#28634=CARTESIAN_POINT ( 'NONE',  ( -1.301082122417146048, -31.16716842155108580, 7.759451378593094972 ) ) ;
#28636=VERTEX_POINT ( 'NONE', #23347 ) ;
#28637=ORIENTED_EDGE ( 'NONE', *, *, #33451, .F. ) ;
#28641=VERTEX_POINT ( 'NONE', #14668 ) ;
#28645=CARTESIAN_POINT ( 'NONE',  ( 4.942166287043163742, -28.54480233319798543, 6.868387053540520704 ) ) ;
#28654=CARTESIAN_POINT ( 'NONE',  ( 2.955826417700654130, -26.41018881579227795, 7.774064877406525298 ) ) ;
#28655=EDGE_CURVE ( 'NONE', #19268, #25058, #9236, .T. ) ;
#28659=CARTESIAN_POINT ( 'NONE',  ( 2.482793419929769207, -26.15850159197103508, 7.002103980607166989 ) ) ;
#28674=CARTESIAN_POINT ( 'NONE',  ( 3.875507134935765041, -26.95672030760948346, 7.635761828346577573 ) ) ;
#28675=CARTESIAN_POINT ( 'NONE',  ( 4.737606180627847330, -31.30928207488832626, 7.756742906098588186 ) ) ;
#28676=CARTESIAN_POINT ( 'NONE',  ( 1.668552422811426572, -26.07007435252865690, 7.724038915126860694 ) ) ;
#28681=CARTESIAN_POINT ( 'NONE',  ( 3.254454494278365306, -26.53796732577102802, 7.139196562012272373 ) ) ;
#28683=CARTESIAN_POINT ( 'NONE',  ( 1.726000212023766522, -32.96983583034973719, 7.652160403243383868 ) ) ;
#28684=CARTESIAN_POINT ( 'NONE',  ( 0.6959572223689035608, -26.21002107485291077, 7.387053503561886281 ) ) ;
#28687=CARTESIAN_POINT ( 'NONE',  ( -1.502930774124977997, -28.43029404775827373, 7.740055089680399902 ) ) ;
#28689=ORIENTED_EDGE ( 'NONE', *, *, #14723, .F. ) ;
#28693=ORIENTED_EDGE ( 'NONE', *, *, #10067, .T. ) ;
#28694=DIRECTION ( 'NONE',  ( 1.000000000000000000, -0.000000000000000000, -0.000000000000000000 ) ) ;
#28697=CARTESIAN_POINT ( 'NONE',  ( 5.004837170140412184, -28.41636597135046216, 6.880608371227948439 ) ) ;
#28698=DIRECTION ( 'NONE',  ( -0.000000000000000000, -0.000000000000000000, -1.000000000000000000 ) ) ;
#28699=CARTESIAN_POINT ( 'NONE',  ( 1.138162326717552908, -26.11537075939349606, 6.880608371227948439 ) ) ;
#28703=CARTESIAN_POINT ( 'NONE',  ( -1.411741797515851271, -31.17137799540083876, 7.013842709614101167 ) ) ;
#28708=CARTESIAN_POINT ( 'NONE',  ( 4.224974933773748553, -31.84731275619759927, 7.754798119455333705 ) ) ;
#28709=VECTOR ( 'NONE', #30159, 1000.000000000000114 ) ;
#28715=B_SPLINE_CURVE_WITH_KNOTS ( 'NONE', 3,
 ( #19263, #13080, #25642, #38793, #26851, #39391, #4827, #20457, #1750, #33035, #17162, #33244, #1356, #8095, #32841, #39189, #11182, #26260, #29540, #5029, #26655, #36324, #35728, #27055, #7908, #36127, #29338, #32643, #17354, #38984, #4439 ),
 .UNSPECIFIED., .F., .F.,
 ( 4, 3, 3, 3, 3, 3, 3, 3, 3, 3, 4 ),
 ( 4.336808689942017736E-19, 3.077658087705600095E-05, 6.152638666998949115E-05, 9.267501192706537668E-05, 0.0001241882240135188460, 0.0001556618703051674505, 0.0001866161554452211923, 0.0002167966385860986621, 0.0002463805737537775979, 0.0002758761370306543332, 0.0002847094172290070006 ),
 .UNSPECIFIED. ) ;
#28718=ORIENTED_EDGE ( 'NONE', *, *, #7495, .T. ) ;
#28721=EDGE_CURVE ( 'NONE', #32112, #34664, #38972, .T. ) ;
#28722=CARTESIAN_POINT ( 'NONE',  ( -0.08658257670950372797, -32.56233827099918443, 7.785344483711591934 ) ) ;
#28724=CARTESIAN_POINT ( 'NONE',  ( -1.042158050042817585, -31.73691429932165420, 7.771081512783705847 ) ) ;
#28736=ORIENTED_EDGE ( 'NONE', *, *, #16907, .F. ) ;
#28737=( BOUNDED_CURVE ( )  B_SPLINE_CURVE ( 3, ( #5838, #24356, #30344, #2150 ),
 .UNSPECIFIED., .F., .T. ) 
 B_SPLINE_CURVE_WITH_KNOTS ( ( 4, 4 ),
 ( 1.347909859412855127, 1.534781240595300744 ),
 .UNSPECIFIED. ) 
 CURVE ( )  GEOMETRIC_REPRESENTATION_ITEM ( )  RATIONAL_B_SPLINE_CURVE ( ( 1.000000000000000000, 0.9970920404276225613, 0.9970920404276225613, 1.000000000000000000 ) ) 
 REPRESENTATION_ITEM ( '' )  );
#28739=AXIS2_PLACEMENT_3D ( 'NONE', #34590, #25703, #27967 ) ;
#28743=CARTESIAN_POINT ( 'NONE',  ( 2.285759857818613572, -26.11922848102776484, 7.742274884880762542 ) ) ;
#28745=DIRECTION ( 'NONE',  ( 1.047444401652940007E-14, -1.000000000000000000, -0.000000000000000000 ) ) ;
#28750=CARTESIAN_POINT ( 'NONE',  ( 1.178420402900119512, -26.11942198568385010, 7.780491323090171996 ) ) ;
#28751=ORIENTED_EDGE ( 'NONE', *, *, #5617, .F. ) ;
#28756=CARTESIAN_POINT ( 'NONE',  ( 4.355058743506291741, -27.27855411587562884, 7.255881584735162093 ) ) ;
#28758=CARTESIAN_POINT ( 'NONE',  ( -1.309506077955794323, -31.15126656862256027, 6.865312560952602006 ) ) ;
#28759=VERTEX_POINT ( 'NONE', #28257 ) ;
#28762=CARTESIAN_POINT ( 'NONE',  ( -0.5217032702065450556, -32.27405686018898479, 7.697032948437508182 ) ) ;
#28763=CARTESIAN_POINT ( 'NONE',  ( -1.788336217227144198, -29.48479552071361809, 7.780491323090173772 ) ) ;
#28769=LINE ( 'NONE', #13117, #7097 ) ;
#28771=ORIENTED_EDGE ( 'NONE', *, *, #40102, .F. ) ;
#28772=EDGE_CURVE ( 'NONE', #38473, #7785, #27846, .T. ) ;
#28773=CARTESIAN_POINT ( 'NONE',  ( -0.9826570473272854267, -31.65831881584441021, 6.863904403958576594 ) ) ;
#28774=CARTESIAN_POINT ( 'NONE',  ( -0.5731604851916571874, -32.21200110443151488, 7.785096263473213263 ) ) ;
#28776=CARTESIAN_POINT ( 'NONE',  ( 1.700390093233090871, -29.56993018339339940, 7.800000000000000711 ) ) ;
#28781=CARTESIAN_POINT ( 'NONE',  ( -0.8809027425463861194, -31.78283038357269419, 7.693875151218755093 ) ) ;
#28782=CARTESIAN_POINT ( 'NONE',  ( 4.589539118170550935, -31.36237908435458976, 7.768425012602596880 ) ) ;
#28790=EDGE_CURVE ( 'NONE', #4723, #31392, #6374, .T. ) ;
#28793=CARTESIAN_POINT ( 'NONE',  ( 4.291692624794518629, -31.77112207655784815, 7.779495906702011965 ) ) ;
#28794=B_SPLINE_CURVE_WITH_KNOTS ( 'NONE', 3,
 ( #20635, #30330, #14865, #14261, #17141, #36500, #1523, #39576, #11560, #27436, #24344, #10964, #2137, #39371, #11162, #29713, #26633, #20846, #23545, #17950, #39992, #33439, #11763, #17537, #24137 ),
 .UNSPECIFIED., .F., .F.,
 ( 4, 3, 3, 3, 3, 3, 3, 3, 4 ),
 ( 6.468151674594376400E-05, 9.076621574722102369E-05, 0.0001210204262067959878, 0.0001512763324577431315, 0.0001815301820994218911, 0.0002117781465860683475, 0.0002420274594459756413, 0.0002722905548971167101, 0.0002816827545175690879 ),
 .UNSPECIFIED. ) ;
#28799=LINE ( 'NONE', #2888, #3108 ) ;
#28803=CARTESIAN_POINT ( 'NONE',  ( -1.640792392766696750, -28.94017299183985514, 7.784838882742138644 ) ) ;
#28804=ORIENTED_EDGE ( 'NONE', *, *, #9729, .F. ) ;
#28808=CARTESIAN_POINT ( 'NONE',  ( 5.153168895494497193, -30.14292259869292678, 7.707984471951054850 ) ) ;
#28811=ORIENTED_EDGE ( 'NONE', *, *, #18929, .T. ) ;
#28814=CARTESIAN_POINT ( 'NONE',  ( 4.538070851940716466, -31.44278039407777214, 6.988553391373220514 ) ) ;
#28834=CARTESIAN_POINT ( 'NONE',  ( 0.5687451785976556096, -32.77607959874935517, 7.670860738520328681 ) ) ;
#28843=ORIENTED_EDGE ( 'NONE', *, *, #29933, .T. ) ;
#28846=CARTESIAN_POINT ( 'NONE',  ( 1.649030408997186781, -33.05491794072131739, 7.785344483711591934 ) ) ;
#28848=CARTESIAN_POINT ( 'NONE',  ( -0.4524766833400662436, -26.81037104761097112, 7.751599049952197618 ) ) ;
#28849=ORIENTED_EDGE ( 'NONE', *, *, #22441, .F. ) ;
#28857=CARTESIAN_POINT ( 'NONE',  ( -1.751191296394976060, -28.98974609548212555, 7.733670252284493785 ) ) ;
#28858=EDGE_LOOP ( 'NONE', ( #10074, #6568, #33566, #35536 ) ) ;
#28870=CARTESIAN_POINT ( 'NONE',  ( -0.2075784994539575656, -32.50415316031815394, 6.989977667959447416 ) ) ;
#28872=B_SPLINE_CURVE_WITH_KNOTS ( 'NONE', 3,
 ( #14042, #39152, #1121, #4991, #16716, #36095, #29306, #14443, #27014, #23127, #4787, #1921, #4404, #8257, #7873, #13652, #17124, #26817, #39560, #11343, #26223, #4198, #20420, #35894, #23909, #38757, #39355, #1713, #14243, #20026, #11147 ),
 .UNSPECIFIED., .F., .F.,
 ( 4, 3, 3, 3, 3, 3, 3, 3, 3, 3, 4 ),
 ( 6.484403375995018940E-05, 8.983333709522135736E-05, 0.0001203539973219361814, 0.0001514144607149705657, 0.0001828916862241641026, 0.0002144221682127259491, 0.0002455195857862198022, 0.0002758614570916272644, 0.0003055381793602568452, 0.0003350143730643693964, 0.0003497271997307906436 ),
 .UNSPECIFIED. ) ;
#28874=CARTESIAN_POINT ( 'NONE',  ( 2.255350295996689347, -26.21552723005750352, 7.695279973900954751 ) ) ;
#28877=VERTEX_POINT ( 'NONE', #11573 ) ;
#28882=CARTESIAN_POINT ( 'NONE',  ( -0.9667203403901262204, -31.67862831489078701, 7.774064877406526186 ) ) ;
#28884=CARTESIAN_POINT ( 'NONE',  ( 2.083546779805665494, -32.94827274467561296, 6.939395833800443114 ) ) ;
#28885=B_SPLINE_CURVE_WITH_KNOTS ( 'NONE', 3,
 ( #10129, #16314, #6459, #9737, #691, #19011, #15913, #31775, #28064, #31986 ),
 .UNSPECIFIED., .F., .F.,
 ( 4, 3, 3, 4 ),
 ( 0.0001585009270395754794, 0.0001815657551981846279, 0.0002118214035944119905, 0.0002170292169044786025 ),
 .UNSPECIFIED. ) ;
#28892=ORIENTED_EDGE ( 'NONE', *, *, #9898, .T. ) ;
#28896=CARTESIAN_POINT ( 'NONE',  ( -0.9779184174635926485, -27.32182954066626834, 7.767720160662275219 ) ) ;
#28899=CARTESIAN_POINT ( 'NONE',  ( 5.048260384636090059, -28.54926152416005181, 6.921725064902950031 ) ) ;
#28900=CARTESIAN_POINT ( 'NONE',  ( 1.104640146243424548, -26.22252062316335852, 7.763628509615288387 ) ) ;
#28902=ORIENTED_EDGE ( 'NONE', *, *, #23184, .T. ) ;
#28907=ORIENTED_EDGE ( 'NONE', *, *, #12980, .T. ) ;
#28910=CARTESIAN_POINT ( 'NONE',  ( -1.740904132959085304, -28.93157757802832819, 6.894806418505347700 ) ) ;
#28919=ORIENTED_EDGE ( 'NONE', *, *, #17327, .F. ) ;
#28922=PLANE ( 'NONE',  #18693 ) ;
#28926=ADVANCED_FACE ( 'NONE', ( #5422 ), #30545, .T. ) ;
#28927=CARTESIAN_POINT ( 'NONE',  ( -0.03448549664302677509, -32.60970101154014600, 7.750000000000000000 ) ) ;
#28934=CARTESIAN_POINT ( 'NONE',  ( 1.011962798722023882, -33.78603799583471101, 7.695279973900954751 ) ) ;
#28942=VERTEX_POINT ( 'NONE', #21486 ) ;
#28946=B_SPLINE_CURVE_WITH_KNOTS ( 'NONE', 3,
 ( #13763, #818, #35410, #7579, #4698, #20132, #11052, #35998, #29014, #3924, #16438, #35803, #20326, #19740, #7778, #16831, #22840, #4309, #6981, #26725, #17232, #23235, #29805, #1617, #26329 ),
 .UNSPECIFIED., .F., .F.,
 ( 4, 3, 3, 3, 3, 3, 3, 3, 4 ),
 ( 6.468151674593822101E-05, 9.076621574722248736E-05, 0.0001210204262067999181, 0.0001512763324577458420, 0.0001815301820994231650, 0.0002117781465860723591, 0.0002420274594459760750, 0.0002722905548971156801, 0.0002816827545175590048 ),
 .UNSPECIFIED. ) ;
#28949=ORIENTED_EDGE ( 'NONE', *, *, #22649, .T. ) ;
#28951=CARTESIAN_POINT ( 'NONE',  ( 2.973605180254018432, -26.32071758304399012, 7.780491323090171996 ) ) ;
#28953=ADVANCED_FACE ( 'NONE', ( #15292 ), #34268, .F. ) ;
#28959=CARTESIAN_POINT ( 'NONE',  ( -1.720974470195171024, -28.90632690787352033, 7.785593909369613819 ) ) ;
#28963=CARTESIAN_POINT ( 'NONE',  ( 0.9231601816174473951, -32.98254913520433007, 6.898188844117810525 ) ) ;
#28964=CARTESIAN_POINT ( 'NONE',  ( -1.797258899342013549, -29.44812577374269580, 7.754798119455333705 ) ) ;
#28965=EDGE_CURVE ( 'NONE', #9636, #34839, #38594, .T. ) ;
#28966=EDGE_CURVE ( 'NONE', #7534, #5389, #39783, .T. ) ;
#28973=CARTESIAN_POINT ( 'NONE',  ( -0.9631319970678871023, -31.68316142368188082, 6.866852738645443210 ) ) ;
#28976=CARTESIAN_POINT ( 'NONE',  ( 3.198709474042557233, -25.09719924859204454, 7.754798119455333705 ) ) ;
#28977=CARTESIAN_POINT ( 'NONE',  ( -0.7036529332303063100, -33.97746366811107777, 7.754798119455333705 ) ) ;
#28982=CARTESIAN_POINT ( 'NONE',  ( -1.273915598905741353, -27.73393014892116071, 7.771081512783704071 ) ) ;
#28985=CARTESIAN_POINT ( 'NONE',  ( 1.664433243520564876, -26.17012032033359148, 7.695279973900954751 ) ) ;
#28986=CARTESIAN_POINT ( 'NONE',  ( -0.3287281863750422528, -26.84180003047303487, 6.997764925645181933 ) ) ;
#28987=CARTESIAN_POINT ( 'NONE',  ( 2.976970822604137368, -26.41868572423151207, 7.754798119455333705 ) ) ;
#28988=CARTESIAN_POINT ( 'NONE',  ( -1.711592984601793876, -28.75984001168768245, 7.387053503561888057 ) ) ;
#28989=EDGE_CURVE ( 'NONE', #6547, #33368, #25384, .T. ) ;
#28994=VERTEX_POINT ( 'NONE', #38129 ) ;
#28996=CARTESIAN_POINT ( 'NONE',  ( -0.4155527668808552955, -26.78195783641919903, 7.011627023500181188 ) ) ;
#29003=VERTEX_POINT ( 'NONE', #3983 ) ;
#29006=AXIS2_PLACEMENT_3D ( 'NONE', #32520, #35811, #19748 ) ;
#29013=AXIS2_PLACEMENT_3D ( 'NONE', #14469, #30547, #2565 ) ;
#29014=CARTESIAN_POINT ( 'NONE',  ( 0.005087639750836099595, -32.51713536024735163, 7.763628509615288387 ) ) ;
#29015=CARTESIAN_POINT ( 'NONE',  ( 4.534317637064775752, -31.44845478432683450, 6.959317978105160840 ) ) ;
#29016=CARTESIAN_POINT ( 'NONE',  ( 3.972814594200666960, -32.23190212178483449, 7.660770905198785563 ) ) ;
#29023=ORIENTED_EDGE ( 'NONE', *, *, #9203, .T. ) ;
#29027=CARTESIAN_POINT ( 'NONE',  ( 0.4306841250506159291, -32.72395091166418979, 6.864276522220859711 ) ) ;
#29030=VERTEX_POINT ( 'NONE', #29079 ) ;
#29034=CARTESIAN_POINT ( 'NONE',  ( 5.074422016658271417, -29.15051561556369819, 6.882085323592685988 ) ) ;
#29036=DIRECTION ( 'NONE',  ( -0.9396926207859104263, 0.3420201433256631063, -0.000000000000000000 ) ) ;
#29038=CARTESIAN_POINT ( 'NONE',  ( 4.400089692731897983, -31.79740006477585368, 7.730015791551948290 ) ) ;
#29040=CARTESIAN_POINT ( 'NONE',  ( 3.430943829990005245, -32.49656374204088394, 7.680992449362118002 ) ) ;
#29046=CARTESIAN_POINT ( 'NONE',  ( 4.911690090265110165, -28.45299136274915952, 6.894806418505345924 ) ) ;
#29048=ADVANCED_FACE ( 'NONE', ( #22512 ), #28465, .T. ) ;
#29050=CARTESIAN_POINT ( 'NONE',  ( 4.959102621865235427, -28.59998551706655334, 6.988553391373221402 ) ) ;
#29051=CARTESIAN_POINT ( 'NONE',  ( 2.281019115899110439, -26.11842600667238301, 7.655937882338900380 ) ) ;
#29052=EDGE_LOOP ( 'NONE', ( #6736, #12328, #8676, #14847 ) ) ;
#29054=CARTESIAN_POINT ( 'NONE',  ( 3.852393986429853090, -32.33018136787153907, 6.867199677474203234 ) ) ;
#29060=CARTESIAN_POINT ( 'NONE',  ( 2.976970822604137368, -26.41868572423151207, 7.754798119455333705 ) ) ;
#29061=VERTEX_POINT ( 'NONE', #35276 ) ;
#29064=CARTESIAN_POINT ( 'NONE',  ( 4.379420427854822329, -27.32268977692216438, 7.767720160662274331 ) ) ;
#29065=DIRECTION ( 'NONE',  ( -0.3754033771448275214, -0.6502177225477910882, -0.6605219282605403475 ) ) ;
#29067=ORIENTED_EDGE ( 'NONE', *, *, #36767, .T. ) ;
#29068=CARTESIAN_POINT ( 'NONE',  ( 4.428676815068841144, -27.54101827131068347, 6.911401339314951819 ) ) ;
#29069=EDGE_CURVE ( 'NONE', #9639, #19833, #34552, .T. ) ;
#29071=ADVANCED_FACE ( 'NONE', ( #26198 ), #30091, .F. ) ;
#29078=AXIS2_PLACEMENT_3D ( 'NONE', #31326, #37073, #34230 ) ;
#29079=CARTESIAN_POINT ( 'NONE',  ( 3.419158195859356653, -26.52102280379090971, 7.695279973900954751 ) ) ;
#29080=ORIENTED_EDGE ( 'NONE', *, *, #19715, .F. ) ;
#29081=CARTESIAN_POINT ( 'NONE',  ( 0.7215495951242570927, -26.31387869742729890, 6.903372536218458144 ) ) ;
#29082=CARTESIAN_POINT ( 'NONE',  ( 3.927318322983230470, -26.86978234060347503, 7.660770905198783787 ) ) ;
#29085=CARTESIAN_POINT ( 'NONE',  ( 1.128478239259624205, -32.92148457371509807, 7.748216051605118615 ) ) ;
#29086=CARTESIAN_POINT ( 'NONE',  ( -1.761293926603614501, -29.00920416086214360, 7.255881584735162981 ) ) ;
#29087=CARTESIAN_POINT ( 'NONE',  ( 3.330199591572231999, -32.55385491381601071, 7.782034975670475418 ) ) ;
#29090=CARTESIAN_POINT ( 'NONE',  ( -1.505427669403690327, -28.43735238352157424, 7.721096864323901521 ) ) ;
#29092=ORIENTED_EDGE ( 'NONE', *, *, #27405, .F. ) ;
#29096=CARTESIAN_POINT ( 'NONE',  ( 3.005221404606187807, -26.32225174351355790, 6.865482280155367434 ) ) ;
#29097=ORIENTED_EDGE ( 'NONE', *, *, #15351, .F. ) ;
#29098=PLANE ( 'NONE',  #19326 ) ;
#29101=CARTESIAN_POINT ( 'NONE',  ( 0.9256524183181416010, -32.88049123692185560, 6.895222827070021765 ) ) ;
#29102=CARTESIAN_POINT ( 'NONE',  ( 1.700390093233090871, -29.56993018339339940, 7.750000000000000888 ) ) ;
#29104=CARTESIAN_POINT ( 'NONE',  ( -3.033070997534465185, -27.73041033019772428, 7.013842709614101167 ) ) ;
#29105=ORIENTED_EDGE ( 'NONE', *, *, #3155, .F. ) ;
#29114=CARTESIAN_POINT ( 'NONE',  ( 5.152478333118308385, -28.99279347164636889, 6.894806418505347700 ) ) ;
#29117=B_SPLINE_CURVE_WITH_KNOTS ( 'NONE', 3,
 ( #17064, #10891, #11087, #29642, #4731, #7411, #35839, #14383, #26760, #33360, #17265, #1861, #26165, #20766, #29839, #1654, #23659, #36226, #4926, #33144, #13986, #1454, #23848, #38696, #30048, #8196, #26559, #35641, #19967, #32546, #23466 ),
 .UNSPECIFIED., .F., .F.,
 ( 4, 3, 3, 3, 3, 3, 3, 3, 3, 3, 4 ),
 ( 9.697399036122160616E-19, 3.077658087705748496E-05, 6.152638666999462756E-05, 9.267501192706795166E-05, 0.0001241882240135198760, 0.0001556618703051706218, 0.0001866161554452250683, 0.0002167966385861010473, 0.0002463805737537809589, 0.0002758761370306560680, 0.0002847094172290131806 ),
 .UNSPECIFIED. ) ;
#29121=ADVANCED_FACE ( 'NONE', ( #14019 ), #23303, .F. ) ;
#29126=ORIENTED_EDGE ( 'NONE', *, *, #14061, .F. ) ;
#29132=CARTESIAN_POINT ( 'NONE',  ( 6.074096823854431726, -32.03256286660679564, 7.695279973900954751 ) ) ;
#29133=CARTESIAN_POINT ( 'NONE',  ( 3.729302005315832336, -32.29821690522913258, 6.911401339314957148 ) ) ;
#29136=CARTESIAN_POINT ( 'NONE',  ( 6.160593259708746494, -32.30254410566374190, 7.013842709614101167 ) ) ;
#29142=DIRECTION ( 'NONE',  ( 0.7508067542896647018, 2.621427771679746855E-15, 0.6605219282605379050 ) ) ;
#29143=ORIENTED_EDGE ( 'NONE', *, *, #1308, .F. ) ;
#29146=ADVANCED_FACE ( 'NONE', ( #39131 ), #38730, .T. ) ;
#29152=DIRECTION ( 'NONE',  ( -0.2567910337120365427, 0.7055275666422146097, 0.6605219282605377940 ) ) ;
#29153=CARTESIAN_POINT ( 'NONE',  ( 1.075454873741154005, -26.12617409861640638, 7.750000000000000888 ) ) ;
#29155=EDGE_CURVE ( 'NONE', #4065, #32844, #20002, .T. ) ;
#29161=CARTESIAN_POINT ( 'NONE',  ( -1.322949708848405237, -31.12539950468849526, 6.876076431790004051 ) ) ;
#29162=EDGE_LOOP ( 'NONE', ( #26020, #37219, #28173, #32395 ) ) ;
#29165=CARTESIAN_POINT ( 'NONE',  ( 0.9303581240408361763, -32.98417252488322049, 6.890920332093119605 ) ) ;
#29166=CARTESIAN_POINT ( 'NONE',  ( 5.897691494960017877, -28.77484643370537754, 7.695279973900954751 ) ) ;
#29168=CARTESIAN_POINT ( 'NONE',  ( 3.378963426318634777, -26.61317069598981533, 7.740055089680407008 ) ) ;
#29169=ORIENTED_EDGE ( 'NONE', *, *, #25587, .F. ) ;
#29172=CARTESIAN_POINT ( 'NONE',  ( -0.9570137182916693686, -31.69082739506907842, 6.870716933885666400 ) ) ;
#29176=CARTESIAN_POINT ( 'NONE',  ( 4.713366678454989689, -27.78892706510198707, 7.698786668945011513 ) ) ;
#29181=CARTESIAN_POINT ( 'NONE',  ( 2.930491328958202857, -32.84664367347161829, 7.710604733652629328 ) ) ;
#29182=CARTESIAN_POINT ( 'NONE',  ( -2.227706725756020578, -32.93668375692303130, 7.695279973900954751 ) ) ;
#29185=CARTESIAN_POINT ( 'NONE',  ( -0.3196854658041705100, -26.83510019752340625, 6.949473656533217358 ) ) ;
#29186=DIRECTION ( 'NONE',  ( -0.000000000000000000, -0.000000000000000000, -1.000000000000000000 ) ) ;
#29191=CARTESIAN_POINT ( 'NONE',  ( 4.945445480008764605, -30.88065529806472043, 7.754798119455333705 ) ) ;
#29194=CARTESIAN_POINT ( 'NONE',  ( -0.3987955896700752234, -26.76931963055061559, 6.951256099901585550 ) ) ;
#29195=EDGE_CURVE ( 'NONE', #8844, #16031, #37060, .T. ) ;
#29196=CARTESIAN_POINT ( 'NONE',  ( -1.298113860838788547, -27.76464493488661134, 6.870737987065012931 ) ) ;
#29197=VERTEX_POINT ( 'NONE', #11726 ) ;
#29201=EDGE_CURVE ( 'NONE', #16761, #17469, #18843, .T. ) ;
#29202=VECTOR ( 'NONE', #16414, 1000.000000000000114 ) ;
#29211=ADVANCED_FACE ( 'NONE', ( #15239 ), #36866, .F. ) ;
#29213=( BOUNDED_CURVE ( )  B_SPLINE_CURVE ( 3, ( #1946, #11166, #39583, #30131 ),
 .UNSPECIFIED., .F., .T. ) 
 B_SPLINE_CURVE_WITH_KNOTS ( ( 4, 4 ),
 ( 4.748221474220557958, 4.941946782021392259 ),
 .UNSPECIFIED. ) 
 CURVE ( )  GEOMETRIC_REPRESENTATION_ITEM ( )  RATIONAL_B_SPLINE_CURVE ( ( 1.000000000000000000, 0.9968749865767494445, 0.9968749865767494445, 1.000000000000000000 ) ) 
 REPRESENTATION_ITEM ( '' )  );
#29214=CARTESIAN_POINT ( 'NONE',  ( 4.534007133228977970, -31.44892320798883745, 6.949473656533214694 ) ) ;
#29216=CARTESIAN_POINT ( 'NONE',  ( -1.258633014711773468, -27.89535841845185615, 7.730758795053805699 ) ) ;
#29219=VERTEX_POINT ( 'NONE', #2098 ) ;
#29220=CARTESIAN_POINT ( 'NONE',  ( 2.325325312725053717, -33.01368626817038887, 7.750000000000001776 ) ) ;
#29225=CARTESIAN_POINT ( 'NONE',  ( 0.4019100156039143723, -32.71221430294721699, 6.868387053540520704 ) ) ;
#29228=CARTESIAN_POINT ( 'NONE',  ( -1.784555172093402531, -29.51764096169078755, 7.785373291296188825 ) ) ;
#29229=ORIENTED_EDGE ( 'NONE', *, *, #26554, .T. ) ;
#29230=B_SPLINE_CURVE_WITH_KNOTS ( 'NONE', 3,
 ( #37471, #4535, #38891, #35435, #35631, #38485, #35831, #10288, #17258, #17058 ),
 .UNSPECIFIED., .F., .F.,
 ( 4, 3, 3, 4 ),
 ( 1.939479807224432123E-18, 3.025570593002944284E-05, 6.051145698343964594E-05, 6.468151674593845140E-05 ),
 .UNSPECIFIED. ) ;
#29233=AXIS2_PLACEMENT_3D ( 'NONE', #8459, #36479, #14843 ) ;
#29242=DIRECTION ( 'NONE',  ( -0.7660444431189725734, -0.6427876096865456912, -0.000000000000000000 ) ) ;
#29245=EDGE_LOOP ( 'NONE', ( #18775, #40071, #11694, #23585, #843, #6717 ) ) ;
#29247=DIRECTION ( 'NONE',  ( 0.6427876096865379196, 0.7660444431189792347, -0.000000000000000000 ) ) ;
#29248=EDGE_CURVE ( 'NONE', #908, #1323, #9499, .T. ) ;
#29249=EDGE_CURVE ( 'NONE', #33448, #11999, #33063, .T. ) ;
#29254=CARTESIAN_POINT ( 'NONE',  ( 4.926049798472932117, -28.49512058795590264, 6.866852738645443210 ) ) ;
#29257=ORIENTED_EDGE ( 'NONE', *, *, #30318, .T. ) ;
#29261=CARTESIAN_POINT ( 'NONE',  ( -1.314126787848640898, -31.34832920763589570, 7.720710062488891801 ) ) ;
#29262=VERTEX_POINT ( 'NONE', #18737 ) ;
#29265=CARTESIAN_POINT ( 'NONE',  ( 2.405371579693568407, -26.14164967438523135, 6.863654226668488789 ) ) ;
#29267=CARTESIAN_POINT ( 'NONE',  ( 4.273337484900067373, -31.79252814967387053, 6.894806418505345036 ) ) ;
#29272=CARTESIAN_POINT ( 'NONE',  ( 1.759798022315843147, -26.08531033596018389, 7.785593909369613819 ) ) ;
#29273=CARTESIAN_POINT ( 'NONE',  ( 1.433369704655312438, -26.07330752179259292, 7.501983001166817822 ) ) ;
#29276=CARTESIAN_POINT ( 'NONE',  ( -0.2125075820087856115, -32.50094215169137613, 6.971170733404105313 ) ) ;
#29278=CARTESIAN_POINT ( 'NONE',  ( 2.649739443830540608, -24.89739049809065818, 6.954324564059724878 ) ) ;
#29279=CARTESIAN_POINT ( 'NONE',  ( 3.576146456961454057, -26.73416960394870046, 6.929923840112063971 ) ) ;
#29281=CARTESIAN_POINT ( 'NONE',  ( 0.7014528802153003895, -26.31998796168418053, 6.882085323592685100 ) ) ;
#29282=CARTESIAN_POINT ( 'NONE',  ( 3.936673369916530607, -26.87752597194292647, 7.640616322432101981 ) ) ;
#29284=CARTESIAN_POINT ( 'NONE',  ( 1.030866757825423585, -32.90337049350075915, 7.782034975670476307 ) ) ;
#29285=CARTESIAN_POINT ( 'NONE',  ( 4.981688893911533356, -28.35210424544084518, 7.743886751744251562 ) ) ;
#29286=DIRECTION ( 'NONE',  ( -0.4826092789263555782, -0.5751513419797993354, 0.6605219282605380160 ) ) ;
#29287=CARTESIAN_POINT ( 'NONE',  ( 2.227179720685508180, -32.92888163115070199, 6.880147297696980857 ) ) ;
#29290=AXIS2_PLACEMENT_3D ( 'NONE', #18071, #30239, #14777 ) ;
#29293=EDGE_CURVE ( 'NONE', #14158, #9863, #25195, .T. ) ;
#29294=LINE ( 'NONE', #38742, #36050 ) ;
#29299=EDGE_CURVE ( 'NONE', #6054, #17262, #32742, .T. ) ;
#29303=CARTESIAN_POINT ( 'NONE',  ( -1.600641465967917121, -28.40666295028739796, 7.698786668945015066 ) ) ;
#29305=CARTESIAN_POINT ( 'NONE',  ( 0.9326639148157755965, -32.88212908196953776, 6.887945620086118659 ) ) ;
#29306=CARTESIAN_POINT ( 'NONE',  ( 0.4300623547519256684, -32.83125927393997046, 6.866770815808350470 ) ) ;
#29309=CARTESIAN_POINT ( 'NONE',  ( 4.945063611787737123, -30.88201195410851696, 7.753200566781576875 ) ) ;
#29325=ORIENTED_EDGE ( 'NONE', *, *, #19143, .T. ) ;
#29327=CARTESIAN_POINT ( 'NONE',  ( 0.06066625181903905623, -26.47779407321028700, 7.750000000000000888 ) ) ;
#29329=CARTESIAN_POINT ( 'NONE',  ( -0.07364990749213512489, -32.57193750258057463, 7.783750581861597517 ) ) ;
#29330=CYLINDRICAL_SURFACE ( 'NONE', #31532, 3.399999999999999911 ) ;
#29333=CARTESIAN_POINT ( 'NONE',  ( 3.287517435274415423, -32.68939094274560375, 6.989977667959440311 ) ) ;
#29334=CARTESIAN_POINT ( 'NONE',  ( -1.010232243575984068, -31.78411342390880634, 6.880608371227946662 ) ) ;
#29335=CARTESIAN_POINT ( 'NONE',  ( 5.196998877152752883, -29.72423992874466947, 6.880828092187092793 ) ) ;
#29336=CARTESIAN_POINT ( 'NONE',  ( -0.4475183596422435683, -26.93431084857535751, 6.894806418505348589 ) ) ;
#29337=FACE_OUTER_BOUND ( 'NONE', #30922, .T. ) ;
#29338=CARTESIAN_POINT ( 'NONE',  ( 1.881046931064791927, -26.07459083023339019, 6.998987538705434552 ) ) ;
#29341=ORIENTED_EDGE ( 'NONE', *, *, #11596, .F. ) ;
#29352=CARTESIAN_POINT ( 'NONE',  ( 2.926185339781475658, -26.30547128762431441, 7.783750581861601070 ) ) ;
#29353=CYLINDRICAL_SURFACE ( 'NONE', #16099, 0.09010775117052885475 ) ;
#29354=ORIENTED_EDGE ( 'NONE', *, *, #32103, .F. ) ;
#29355=CARTESIAN_POINT ( 'NONE',  ( 5.909439403370450705, -28.84147213309200808, 7.635761828346577573 ) ) ;
#29357=AXIS2_PLACEMENT_3D ( 'NONE', #4166, #35662, #20584 ) ;
#29362=CARTESIAN_POINT ( 'NONE',  ( 3.462070670749302970, -32.59424523688933562, 7.635761828346575797 ) ) ;
#29363=CARTESIAN_POINT ( 'NONE',  ( 1.050200036002242765, -33.00901471541564547, 6.883108633650832253 ) ) ;
#29364=CARTESIAN_POINT ( 'NONE',  ( -1.784512137809761700, -29.51577928193536593, 7.785387725071483800 ) ) ;
#29366=CARTESIAN_POINT ( 'NONE',  ( 3.395692546715378679, -26.62272500653946850, 7.763628509615292828 ) ) ;
#29371=CARTESIAN_POINT ( 'NONE',  ( -1.772710793196472290, -30.00307800544500125, 6.903112506833892326 ) ) ;
#29372=CARTESIAN_POINT ( 'NONE',  ( -0.6241997385101580864, -32.18023142865752817, 7.771081512783688972 ) ) ;
#29374=CARTESIAN_POINT ( 'NONE',  ( -0.01129010125266571157, -26.63221833370405633, 7.635761828346577573 ) ) ;
#29378=CARTESIAN_POINT ( 'NONE',  ( 3.931771986221714421, -27.00459690141179436, 7.785172627573962778 ) ) ;
#29382=VECTOR ( 'NONE', #31663, 1000.000000000000114 ) ;
#29384=ORIENTED_EDGE ( 'NONE', *, *, #29155, .T. ) ;
#29387=DIRECTION ( 'NONE',  ( 1.000000000000000000, 0.000000000000000000, 0.000000000000000000 ) ) ;
#29388=DIRECTION ( 'NONE',  ( 0.7660444431189800119, -0.6427876096865369204, 0.000000000000000000 ) ) ;
#29389=FACE_OUTER_BOUND ( 'NONE', #13781, .T. ) ;
#29396=CARTESIAN_POINT ( 'NONE',  ( -0.4678273493351438606, -26.82239709254809412, 6.863784140767622333 ) ) ;
#29398=CARTESIAN_POINT ( 'NONE',  ( 2.301917618511796437, -26.12340203079047285, 7.762796336881262249 ) ) ;
#29404=CIRCLE ( 'NONE', #11617, 3.499999999999999556 ) ;
#29406=B_SPLINE_CURVE_WITH_KNOTS ( 'NONE', 3,
 ( #19968, #4146, #1060, #16661 ),
 .UNSPECIFIED., .F., .F.,
 ( 4, 4 ),
 ( 0.000000000000000000, 6.391136169993149426E-06 ),
 .UNSPECIFIED. ) ;
#29418=CARTESIAN_POINT ( 'NONE',  ( 3.969400716823472841, -32.23481756830559419, 7.651421919295147589 ) ) ;
#29421=EDGE_CURVE ( 'NONE', #12828, #30228, #40027, .T. ) ;
#29423=ORIENTED_EDGE ( 'NONE', *, *, #23032, .T. ) ;
#29427=CARTESIAN_POINT ( 'NONE',  ( 4.041943119853272037, -26.96886997397920638, 7.754798119455333705 ) ) ;
#29432=FACE_OUTER_BOUND ( 'NONE', #10401, .T. ) ;
#29443=CARTESIAN_POINT ( 'NONE',  ( -1.643585222189360984, -30.18463677254168331, 7.740055089680399014 ) ) ;
#29446=EDGE_LOOP ( 'NONE', ( #23463, #12358, #22267, #40434 ) ) ;
#29450=CARTESIAN_POINT ( 'NONE',  ( 2.926619159346142141, -26.29176571567377607, 6.894806418505347700 ) ) ;
#29453=DIRECTION ( 'NONE',  ( -0.000000000000000000, -0.000000000000000000, -1.000000000000000000 ) ) ;
#29457=CARTESIAN_POINT ( 'NONE',  ( 3.892870342314429521, -32.29814067960646895, 6.867280401193707640 ) ) ;
#29461=EDGE_CURVE ( 'NONE', #5814, #26604, #15852, .T. ) ;
#29465=CARTESIAN_POINT ( 'NONE',  ( -1.597074440709042475, -28.39657532162993192, 7.651421919295147589 ) ) ;
#29471=FACE_OUTER_BOUND ( 'NONE', #34400, .T. ) ;
#29473=PLANE ( 'NONE',  #17698 ) ;
#29474=DIRECTION ( 'NONE',  ( -0.000000000000000000, -0.000000000000000000, -1.000000000000000000 ) ) ;
#29476=CARTESIAN_POINT ( 'NONE',  ( -0.9582821081414136799, -31.84621386888283823, 7.678495282201405203 ) ) ;
#29480=CARTESIAN_POINT ( 'NONE',  ( 2.360030607804072922, -26.23451782836966473, 7.784476445165072533 ) ) ;
#29482=EDGE_CURVE ( 'NONE', #13676, #38902, #20904, .T. ) ;
#29483=DIRECTION ( 'NONE',  ( 0.6427876096865481337, -0.7660444431189706860, -0.000000000000000000 ) ) ;
#29485=CARTESIAN_POINT ( 'NONE',  ( 0.7160520742141273098, -26.31553137280090127, 6.895222827070022653 ) ) ;
#29486=CARTESIAN_POINT ( 'NONE',  ( -1.360749241107399587, -27.85905441312543473, 7.255881584735163869 ) ) ;
#29488=CARTESIAN_POINT ( 'NONE',  ( 0.9969205846672903881, -32.89635929740111919, 7.761597726988852308 ) ) ;
#29489=B_SPLINE_CURVE_WITH_KNOTS ( 'NONE', 3,
 ( #19829, #7871, #4197, #4403, #35893, #1315, #38754, #16924, #16715, #33000, #4784, #16525, #29505, #29101, #29305, #7670, #13242, #1118, #26420, #17515, #20616, #11746, #15626, #25103, #11146, #17933, #30111, #1920, #17318, #14242, #39770 ),
 .UNSPECIFIED., .F., .F.,
 ( 4, 3, 3, 3, 3, 3, 3, 3, 3, 3, 4 ),
 ( 1.084202172485504434E-19, 2.999644130997740433E-05, 6.002588995694861873E-05, 8.960886084588098833E-05, 0.0001190604700446487542, 0.0001489538463052730486, 0.0001796139255493964726, 0.0002109707048517068617, 0.0002426195318110357631, 0.0002740640997890045577, 0.0002849778069099846906 ),
 .UNSPECIFIED. ) ;
#29490=CARTESIAN_POINT ( 'NONE',  ( 4.460814650971867579, -27.41817363093848314, 7.750000000000000888 ) ) ;
#29492=CARTESIAN_POINT ( 'NONE',  ( -1.799453152388704957, -29.60305503924953996, 7.717693117505774580 ) ) ;
#29493=CARTESIAN_POINT ( 'NONE',  ( 2.237702017751752592, -32.92720639772907987, 6.889465824494256374 ) ) ;
#29500=CARTESIAN_POINT ( 'NONE',  ( -0.9128197825508301833, -27.39481314169073300, 7.635761828346577573 ) ) ;
#29501=ORIENTED_EDGE ( 'NONE', *, *, #3054, .T. ) ;
#29502=DIRECTION ( 'NONE',  ( -0.6605219282605402364, 0.000000000000000000, 0.7508067542896625923 ) ) ;
#29504=DIRECTION ( 'NONE',  ( -0.9848077530122092416, 0.1736481776669241694, -0.000000000000000000 ) ) ;
#29505=CARTESIAN_POINT ( 'NONE',  ( 0.9200650878653321429, -32.87917373532453524, 6.903372536218457256 ) ) ;
#29508=ORIENTED_EDGE ( 'NONE', *, *, #4806, .F. ) ;
#29510=EDGE_CURVE ( 'NONE', #39459, #1323, #7436, .T. ) ;
#29512=AXIS2_PLACEMENT_3D ( 'NONE', #2982, #12614, #6245 ) ;
#29532=FACE_OUTER_BOUND ( 'NONE', #23327, .T. ) ;
#29535=DIRECTION ( 'NONE',  ( 0.9848077530122103518, -0.1736481776669172583, -0.000000000000000000 ) ) ;
#29537=CARTESIAN_POINT ( 'NONE',  ( -1.027820402979995995, -31.76241043247472717, 6.867280401193706751 ) ) ;
#29539=CARTESIAN_POINT ( 'NONE',  ( 5.077466957584408469, -30.51492847852392742, 7.501983001166816933 ) ) ;
#29540=CARTESIAN_POINT ( 'NONE',  ( 1.886314362785468601, -26.07487193409462378, 6.921725064902949143 ) ) ;
#29546=B_SPLINE_CURVE_WITH_KNOTS ( 'NONE', 3,
 ( #15540, #25019, #40239, #317 ),
 .UNSPECIFIED., .F., .F.,
 ( 4, 4 ),
 ( 0.000000000000000000, 6.391136169899991049E-06 ),
 .UNSPECIFIED. ) ;
#29551=CARTESIAN_POINT ( 'NONE',  ( 1.129730468697653256, -26.12992822677308169, 7.783750581861600182 ) ) ;
#29552=CARTESIAN_POINT ( 'NONE',  ( 5.067738213087761068, -29.09985929542945371, 7.754798119455333705 ) ) ;
#29555=CARTESIAN_POINT ( 'NONE',  ( 5.166671796352685142, -29.08527243180875743, 7.751599049952198506 ) ) ;
#29557=CARTESIAN_POINT ( 'NONE',  ( 1.587289166052635148, -33.88748355710808369, 6.894806418505347700 ) ) ;
#29559=AXIS2_PLACEMENT_3D ( 'NONE', #12136, #9878, #16050 ) ;
#29561=CARTESIAN_POINT ( 'NONE',  ( -1.796843176524750341, -29.45368158032236749, 7.761113333117551250 ) ) ;
#29566=EDGE_CURVE ( 'NONE', #40275, #16672, #37984, .T. ) ;
#29568=ADVANCED_FACE ( 'NONE', ( #26751 ), #35830, .F. ) ;
#29572=CARTESIAN_POINT ( 'NONE',  ( -0.03062609074085211741, -26.64357016194428951, 7.692469944509195301 ) ) ;
#29573=CYLINDRICAL_SURFACE ( 'NONE', #10268, 0.09010775117053060335 ) ;
#29575=CARTESIAN_POINT ( 'NONE',  ( -1.508037414099143714, -30.69513570029197425, 7.784838882742139532 ) ) ;
#29576=CARTESIAN_POINT ( 'NONE',  ( -2.759813073242583847, -26.83731626112308533, 7.013842709614101167 ) ) ;
#29577=CARTESIAN_POINT ( 'NONE',  ( -0.8809668920273273640, -31.78275555260969654, 7.691066658568952441 ) ) ;
#29578=FACE_OUTER_BOUND ( 'NONE', #40420, .T. ) ;
#29591=CARTESIAN_POINT ( 'NONE',  ( -0.3990770562238331598, -26.76953060260428430, 6.941203072598471024 ) ) ;
#29592=CARTESIAN_POINT ( 'NONE',  ( -1.376785424038392325, -31.22775445417016371, 7.771081512783700518 ) ) ;
#29593=CARTESIAN_POINT ( 'NONE',  ( -1.241488500120730754, -27.67378822227167134, 7.011627023500182077 ) ) ;
#29594=CARTESIAN_POINT ( 'NONE',  ( 4.944078209288079506, -30.88464969939810345, 7.750000000000000888 ) ) ;
#29595=ORIENTED_EDGE ( 'NONE', *, *, #8404, .F. ) ;
#29596=CARTESIAN_POINT ( 'NONE',  ( 4.993907954365692348, -30.75430347691218813, 7.635761828346578461 ) ) ;
#29604=ORIENTED_EDGE ( 'NONE', *, *, #40064, .T. ) ;
#29605=CARTESIAN_POINT ( 'NONE',  ( 4.934953675687837382, -28.52226686387824373, 7.754798119455333705 ) ) ;
#29608=CARTESIAN_POINT ( 'NONE',  ( -1.261910041069868260, -27.90116479715461750, 7.695279973900954751 ) ) ;
#29609=DIRECTION ( 'NONE',  ( -0.000000000000000000, -0.000000000000000000, -1.000000000000000000 ) ) ;
#29614=EDGE_CURVE ( 'NONE', #28877, #7270, #13882, .T. ) ;
#29620=ORIENTED_EDGE ( 'NONE', *, *, #39239, .F. ) ;
#29621=CARTESIAN_POINT ( 'NONE',  ( 0.4895345795279826828, -32.74700981117575793, 6.892063359921932530 ) ) ;
#29632=CYLINDRICAL_SURFACE ( 'NONE', #32540, 0.09010775117052602368 ) ;
#29633=DIRECTION ( 'NONE',  ( -0.000000000000000000, -0.000000000000000000, -1.000000000000000000 ) ) ;
#29634=VERTEX_POINT ( 'NONE', #20974 ) ;
#29638=CARTESIAN_POINT ( 'NONE',  ( 4.987105146749665430, -28.38306410523611945, 7.773839561854631874 ) ) ;
#29640=ORIENTED_EDGE ( 'NONE', *, *, #21939, .T. ) ;
#29642=CARTESIAN_POINT ( 'NONE',  ( -1.606999173425283756, -30.71499622462987489, 6.875671892026064214 ) ) ;
#29648=CARTESIAN_POINT ( 'NONE',  ( 4.913358501582978377, -28.45779633779761397, 6.889465824494254598 ) ) ;
#29652=DIRECTION ( 'NONE',  ( 1.000000000000000000, 9.912705577010326536E-16, 0.000000000000000000 ) ) ;
#29653=ORIENTED_EDGE ( 'NONE', *, *, #20123, .F. ) ;
#29656=CARTESIAN_POINT ( 'NONE',  ( 3.300479879060630228, -34.00561972003898603, 7.635761828346577573 ) ) ;
#29657=EDGE_LOOP ( 'NONE', ( #5131, #7383, #31939, #12372, #6792 ) ) ;
#29671=CARTESIAN_POINT ( 'NONE',  ( 2.350156857115043074, -26.23259544552930933, 7.785172627573962778 ) ) ;
#29673=DIRECTION ( 'NONE',  ( 0.3420201433256748746, -0.9396926207859060964, 0.000000000000000000 ) ) ;
#29676=CARTESIAN_POINT ( 'NONE',  ( 0.03282529437175818465, -26.49270213989298384, 6.863805608295728611 ) ) ;
#29680=CARTESIAN_POINT ( 'NONE',  ( 4.976860739914288345, -28.33918239773801417, 7.698786668945014178 ) ) ;
#29683=DIRECTION ( 'NONE',  ( -0.6502177225477896449, 0.3754033771448298529, -0.6605219282605402364 ) ) ;
#29686=( BOUNDED_CURVE ( )  B_SPLINE_CURVE ( 3, ( #27045, #5019, #36920, #8699 ),
 .UNSPECIFIED., .F., .T. ) 
 B_SPLINE_CURVE_WITH_KNOTS ( ( 4, 4 ),
 ( 4.886921905584129533, 4.941946782021394924 ),
 .UNSPECIFIED. ) 
 CURVE ( )  GEOMETRIC_REPRESENTATION_ITEM ( )  RATIONAL_B_SPLINE_CURVE ( ( 1.000000000000000000, 0.9997477044959499626, 0.9997477044959499626, 1.000000000000000000 ) ) 
 REPRESENTATION_ITEM ( '' )  );
#29687=CYLINDRICAL_SURFACE ( 'NONE', #10016, 0.09010775117052950700 ) ;
#29689=DIRECTION ( 'NONE',  ( 1.047444401652940007E-14, -1.000000000000000000, -0.000000000000000000 ) ) ;
#29692=CARTESIAN_POINT ( 'NONE',  ( 3.910420815644036097, -32.15368021116306352, 7.721096864323906850 ) ) ;
#29694=CARTESIAN_POINT ( 'NONE',  ( 0.4851296283628217521, -26.28768369622591194, 7.643192810543818716 ) ) ;
#29697=CARTESIAN_POINT ( 'NONE',  ( -1.699306555046655731, -29.52380873363099312, 7.785387725071483800 ) ) ;
#29699=EDGE_CURVE ( 'NONE', #6547, #14780, #3134, .T. ) ;
#29701=CARTESIAN_POINT ( 'NONE',  ( 4.944078209288079506, -30.88464969939810345, 7.750000000000000888 ) ) ;
#29705=CARTESIAN_POINT ( 'NONE',  ( 5.618319323718388603, -33.03553571191711313, 7.013842709614101167 ) ) ;
#29708=B_SPLINE_CURVE_WITH_KNOTS ( 'NONE', 3,
 ( #30986, #40026, #30785, #14902, #17570, #30153, #36533, #1973, #20885, #24178, #18398, #5039, #24379, #33473, #5240, #11192, #20670, #33669, #14492, #27670, #34087, #36938, #2792, #36735, #18193, #23763, #36333, #8517, #5447, #27259, #24586 ),
 .UNSPECIFIED., .F., .F.,
 ( 4, 3, 3, 3, 3, 3, 3, 3, 3, 3, 4 ),
 ( 0.000000000000000000, 2.999644130997572382E-05, 6.002588995694619961E-05, 8.960886084587850822E-05, 0.0001190604700446468297, 0.0001489538463052692810, 0.0001796139255493974483, 0.0002109707048517052354, 0.0002426195318110341910, 0.0002740640997890042866, 0.0002849778069099884853 ),
 .UNSPECIFIED. ) ;
#29713=CARTESIAN_POINT ( 'NONE',  ( -0.8649431887485288240, -27.33854829040479473, 7.785172627573962778 ) ) ;
#29719=ORIENTED_EDGE ( 'NONE', *, *, #21310, .F. ) ;
#29722=B_SPLINE_CURVE_WITH_KNOTS ( 'NONE', 3,
 ( #37018, #34374, #17861, #18687 ),
 .UNSPECIFIED., .F., .F.,
 ( 4, 4 ),
 ( 1.939479807224432123E-18, 6.391136169993889733E-06 ),
 .UNSPECIFIED. ) ;
#29723=LINE ( 'NONE', #10974, #626 ) ;
#29727=CARTESIAN_POINT ( 'NONE',  ( 3.296802056245847545, -32.68464828369553743, 7.006908160621408754 ) ) ;
#29728=CARTESIAN_POINT ( 'NONE',  ( 5.109556576806802752, -30.36213210669178153, 6.980586498568967180 ) ) ;
#29731=CARTESIAN_POINT ( 'NONE',  ( 2.105750943142600029, -32.94567937155306225, 7.013842709614101167 ) ) ;
#29732=CARTESIAN_POINT ( 'NONE',  ( 4.562230772466533857, -27.72120552588419784, 7.139196562012274150 ) ) ;
#29736=AXIS2_PLACEMENT_3D ( 'NONE', #25347, #37886, #235 ) ;
#29739=FACE_OUTER_BOUND ( 'NONE', #21708, .T. ) ;
#29742=CARTESIAN_POINT ( 'NONE',  ( 2.863609035986292461, -26.26888160889163615, 7.697032948437507294 ) ) ;
#29743=SHAPE_DEFINITION_REPRESENTATION ( #25745, #23772 ) ;
#29756=CARTESIAN_POINT ( 'NONE',  ( -0.5390062018526512455, -32.25974509032589310, 7.635761828346574021 ) ) ;
#29759=CYLINDRICAL_SURFACE ( 'NONE', #8153, 3.399999999999999911 ) ;
#29762=AXIS2_PLACEMENT_3D ( 'NONE', #35099, #22933, #35895 ) ;
#29765=CARTESIAN_POINT ( 'NONE',  ( 1.545182540459093978, -32.96639982778489752, 6.871394612369935651 ) ) ;
#29766=CARTESIAN_POINT ( 'NONE',  ( 2.392808652600788122, -26.24116651948626000, 6.864651958020304257 ) ) ;
#29779=AXIS2_PLACEMENT_3D ( 'NONE', #12697, #27934, #40475 ) ;
#29786=CARTESIAN_POINT ( 'NONE',  ( -0.4920901558482355109, -26.84171968718031209, 6.867280401193709416 ) ) ;
#29787=CARTESIAN_POINT ( 'NONE',  ( 4.362362031624546610, -27.29750568242585018, 7.660770905198782899 ) ) ;
#29789=CARTESIAN_POINT ( 'NONE',  ( 2.427704393887406109, -26.14656945195773119, 7.754798119455333705 ) ) ;
#29791=CARTESIAN_POINT ( 'NONE',  ( 0.8619263339206710839, -26.26760762817584549, 7.505001789837626447 ) ) ;
#29794=ORIENTED_EDGE ( 'NONE', *, *, #40215, .F. ) ;
#29803=VERTEX_POINT ( 'NONE', #31957 ) ;
#29805=CARTESIAN_POINT ( 'NONE',  ( -0.1003419751943278176, -32.45391518135897968, 7.759451378593096749 ) ) ;
#29813=FACE_OUTER_BOUND ( 'NONE', #6838, .T. ) ;
#29817=CARTESIAN_POINT ( 'NONE',  ( 0.3451799453360092085, -32.68817016762459104, 6.979335674598003969 ) ) ;
#29819=CARTESIAN_POINT ( 'NONE',  ( -0.5124851502560604510, -26.98861595202439290, 7.692469944509195301 ) ) ;
#29820=ORIENTED_EDGE ( 'NONE', *, *, #19158, .T. ) ;
#29829=DIRECTION ( 'NONE',  ( 1.000000000000000000, 6.938893903907229167E-15, 0.000000000000000000 ) ) ;
#29830=ORIENTED_EDGE ( 'NONE', *, *, #23204, .T. ) ;
#29831=FACE_OUTER_BOUND ( 'NONE', #20667, .T. ) ;
#29835=CARTESIAN_POINT ( 'NONE',  ( -1.168676970653521163, -27.74552502474002225, 6.868387053540521592 ) ) ;
#29836=VERTEX_POINT ( 'NONE', #28442 ) ;
#29839=CARTESIAN_POINT ( 'NONE',  ( -1.640646438711915733, -30.61277402592531871, 6.887547729233687299 ) ) ;
#29843=EDGE_CURVE ( 'NONE', #34207, #17544, #20376, .T. ) ;
#29844=AXIS2_PLACEMENT_3D ( 'NONE', #11144, #4782, #1710 ) ;
#29846=ADVANCED_FACE ( 'NONE', ( #7827 ), #38306, .F. ) ;
#29848=LINE ( 'NONE', #1659, #32574 ) ;
#29854=CARTESIAN_POINT ( 'NONE',  ( 4.289004371442884711, -27.36559100360608454, 7.740055089680401679 ) ) ;
#29855=ORIENTED_EDGE ( 'NONE', *, *, #17452, .F. ) ;
#29862=CARTESIAN_POINT ( 'NONE',  ( 5.401390093233090717, -29.51577928193538369, 7.695279973900954751 ) ) ;
#29865=DIRECTION ( 'NONE',  ( 0.7660444431189857850, -0.6427876096865299260, -0.000000000000000000 ) ) ;
#29869=CARTESIAN_POINT ( 'NONE',  ( 1.684177654150519787, -26.06996773262067890, 7.638991368224661294 ) ) ;
#29882=CYLINDRICAL_SURFACE ( 'NONE', #33838, 0.09010775117052746697 ) ;
#29883=CARTESIAN_POINT ( 'NONE',  ( -1.564068802536003444, -28.34413493684503749, 7.783750581861600182 ) ) ;
#29889=CARTESIAN_POINT ( 'NONE',  ( 3.065628457177692390, -26.34717386365430869, 6.998987538705432776 ) ) ;
#29891=EDGE_LOOP ( 'NONE', ( #28718, #29640, #19149, #27920, #3825 ) ) ;
#29893=FACE_OUTER_BOUND ( 'NONE', #27402, .T. ) ;
#29894=CARTESIAN_POINT ( 'NONE',  ( 5.889993154240193540, -27.29372336251594078, 6.954324564059724878 ) ) ;
#29898=CARTESIAN_POINT ( 'NONE',  ( 3.613287768474986450, -26.63891821509542623, 6.971170733404102648 ) ) ;
#29900=EDGE_LOOP ( 'NONE', ( #3999, #10383, #383, #28303, #33129 ) ) ;
#29916=EDGE_CURVE ( 'NONE', #39584, #10407, #20573, .T. ) ;
#29918=ORIENTED_EDGE ( 'NONE', *, *, #25313, .F. ) ;
#29921=CARTESIAN_POINT ( 'NONE',  ( -0.8954611659357714082, -31.76573441880953297, 7.635761828346577573 ) ) ;
#29924=CARTESIAN_POINT ( 'NONE',  ( 5.174635964963624879, -29.14611934969121521, 6.921725064902952695 ) ) ;
#29928=CARTESIAN_POINT ( 'NONE',  ( 3.295286368285633483, -32.68543217743695095, 6.903112506833884332 ) ) ;
#29932=CARTESIAN_POINT ( 'NONE',  ( 5.094318823446379874, -29.77302566397534278, 6.988553391373226731 ) ) ;
#29933=EDGE_CURVE ( 'NONE', #16079, #17495, #31092, .T. ) ;
#29935=CARTESIAN_POINT ( 'NONE',  ( 2.124200926935305045, -33.04417605512392697, 6.921725064902950031 ) ) ;
#29944=CARTESIAN_POINT ( 'NONE',  ( -1.425774885472621767, -28.23310838303483550, 7.013842709614101167 ) ) ;
#29947=CARTESIAN_POINT ( 'NONE',  ( 6.017943466947773601, -29.68303111057383248, 6.894806418505347700 ) ) ;
#29958=CARTESIAN_POINT ( 'NONE',  ( 0.5480081280804431909, -26.37116720998445984, 7.775108481317162479 ) ) ;
#29959=ORIENTED_EDGE ( 'NONE', *, *, #12055, .T. ) ;
#29961=EDGE_CURVE ( 'NONE', #35449, #29634, #39055, .T. ) ;
#29963=CARTESIAN_POINT ( 'NONE',  ( 4.034911153157309194, -27.09807998479585578, 6.911401339314957148 ) ) ;
#29967=ORIENTED_EDGE ( 'NONE', *, *, #25654, .F. ) ;
#29973=CARTESIAN_POINT ( 'NONE',  ( -1.492713901548710531, -30.73790092008425745, 7.763628509615288387 ) ) ;
#29974=CARTESIAN_POINT ( 'NONE',  ( 3.939361713728871006, -27.01119860913185633, 7.784476445165074310 ) ) ;
#29980=VECTOR ( 'NONE', #31417, 1000.000000000000227 ) ;
#29981=CARTESIAN_POINT ( 'NONE',  ( 4.447923184078407921, -27.40171274082518238, 6.863784140767622333 ) ) ;
#29983=CARTESIAN_POINT ( 'NONE',  ( 1.713892699967802136, -33.06990413752668445, 7.635761828346576685 ) ) ;
#29988=CARTESIAN_POINT ( 'NONE',  ( 2.307042206337215351, -33.01365871392055595, 7.767720160662275219 ) ) ;
#29992=CARTESIAN_POINT ( 'NONE',  ( -1.389564992689783951, -31.21326896663422090, 7.754798119455333705 ) ) ;
#29994=CARTESIAN_POINT ( 'NONE',  ( -1.638685409516953406, -28.92916437338612567, 6.892063359921932530 ) ) ;
#29996=EDGE_LOOP ( 'NONE', ( #8199, #9907, #15047, #35690, #40462 ) ) ;
#30000=ORIENTED_EDGE ( 'NONE', *, *, #25654, .T. ) ;
#30013=AXIS2_PLACEMENT_3D ( 'NONE', #37544, #6681, #21919 ) ;
#30015=CARTESIAN_POINT ( 'NONE',  ( 4.661322817598709811, -31.24112487228765289, 7.670860738520325128 ) ) ;
#30017=ORIENTED_EDGE ( 'NONE', *, *, #34344, .T. ) ;
#30022=EDGE_CURVE ( 'NONE', #27165, #38247, #28489, .T. ) ;
#30024=CARTESIAN_POINT ( 'NONE',  ( -0.9575113486053227208, -31.84711263666175540, 7.697032948437507294 ) ) ;
#30029=ORIENTED_EDGE ( 'NONE', *, *, #16858, .F. ) ;
#30032=ORIENTED_EDGE ( 'NONE', *, *, #30293, .T. ) ;
#30033=PLANE ( 'NONE',  #19713 ) ;
#30038=CARTESIAN_POINT ( 'NONE',  ( -0.4892492752782273691, -26.96886344085812937, 7.763628509615285722 ) ) ;
#30042=CARTESIAN_POINT ( 'NONE',  ( 4.985934790884831713, -28.36760422505889068, 7.762796336881261361 ) ) ;
#30043=ORIENTED_EDGE ( 'NONE', *, *, #26829, .T. ) ;
#30046=( BOUNDED_CURVE ( )  B_SPLINE_CURVE ( 3, ( #38927, #23103, #4573, #32581 ),
 .UNSPECIFIED., .F., .T. ) 
 B_SPLINE_CURVE_WITH_KNOTS ( ( 4, 4 ),
 ( 4.708531083176467291, 4.895802057644188743 ),
 .UNSPECIFIED. ) 
 CURVE ( )  GEOMETRIC_REPRESENTATION_ITEM ( )  RATIONAL_B_SPLINE_CURVE ( ( 1.000000000000000000, 0.9970795998553221295, 0.9970795998553221295, 1.000000000000000000 ) ) 
 REPRESENTATION_ITEM ( '' )  );
#30047=CARTESIAN_POINT ( 'NONE',  ( 2.118032945466439276, -33.04492290971361257, 6.951256099901589991 ) ) ;
#30048=CARTESIAN_POINT ( 'NONE',  ( -1.648135648921391416, -30.58844643467698887, 6.980586498568966292 ) ) ;
#30052=VECTOR ( 'NONE', #695, 1000.000000000000114 ) ;
#30055=ORIENTED_EDGE ( 'NONE', *, *, #33353, .T. ) ;
#30056=ORIENTED_EDGE ( 'NONE', *, *, #10684, .F. ) ;
#30057=CARTESIAN_POINT ( 'NONE',  ( 1.217126534916886937, -26.10345411493373291, 7.750000000000000888 ) ) ;
#30062=CARTESIAN_POINT ( 'NONE',  ( 4.343337730903781058, -27.43104547763413237, 7.785172627573962778 ) ) ;
#30063=VERTEX_POINT ( 'NONE', #2548 ) ;
#30068=B_SPLINE_CURVE_WITH_KNOTS ( 'NONE', 3,
 ( #29374, #23195, #35767, #25681, #16793, #7741, #6945, #29572, #39015, #20096 ),
 .UNSPECIFIED., .F., .F.,
 ( 4, 3, 3, 4 ),
 ( 1.905904691864261185E-18, 3.025570593002930732E-05, 6.051145698343765372E-05, 6.468151674593734010E-05 ),
 .UNSPECIFIED. ) ;
#30070=CARTESIAN_POINT ( 'NONE',  ( 1.077348629692890247, -26.22750088404879776, 7.670860738520330457 ) ) ;
#30071=CARTESIAN_POINT ( 'NONE',  ( 0.5325725529551263993, -26.27050565893173228, 6.894806418505347700 ) ) ;
#30080=DIRECTION ( 'NONE',  ( -1.000000000000000000, 0.000000000000000000, 0.000000000000000000 ) ) ;
#30084=CARTESIAN_POINT ( 'NONE',  ( -0.5596933955661176352, -26.89747389307597203, 7.635761828346574909 ) ) ;
#30085=VECTOR ( 'NONE', #23885, 1000.000000000000114 ) ;
#30086=CARTESIAN_POINT ( 'NONE',  ( 4.651281559046659630, -31.25879804726328004, 7.756377446753162097 ) ) ;
#30090=EDGE_CURVE ( 'NONE', #25861, #6597, #7958, .T. ) ;
#30091=CYLINDRICAL_SURFACE ( 'NONE', #32073, 0.09010775117052929883 ) ;
#30096=CARTESIAN_POINT ( 'NONE',  ( 4.636318400562632114, -31.47527517604001446, 6.912143950357340749 ) ) ;
#30097=DIRECTION ( 'NONE',  ( 0.6427876096865379196, 0.7660444431189792347, -0.000000000000000000 ) ) ;
#30100=LINE ( 'NONE', #33409, #12527 ) ;
#30101=ORIENTED_EDGE ( 'NONE', *, *, #38120, .T. ) ;
#30106=VECTOR ( 'NONE', #15996, 1000.000000000000227 ) ;
#30107=VERTEX_POINT ( 'NONE', #36376 ) ;
#30108=CARTESIAN_POINT ( 'NONE',  ( -0.4936289198477532558, -32.16730372678311767, 7.775108481317158926 ) ) ;
#30109=DIRECTION ( 'NONE',  ( -0.9396926207859058744, -0.3420201433256757628, -0.000000000000000000 ) ) ;
#30111=CARTESIAN_POINT ( 'NONE',  ( 1.046581363270776555, -32.90648473631282656, 6.880147297696980857 ) ) ;
#30113=CARTESIAN_POINT ( 'NONE',  ( 1.253554297217517766, -26.09856357079008760, 6.887547729233691740 ) ) ;
#30122=CARTESIAN_POINT ( 'NONE',  ( 2.258100775518462111, -26.21598130464280629, 7.670860738520328681 ) ) ;
#30127=CARTESIAN_POINT ( 'NONE',  ( 1.700390093233090871, -29.56993018339339940, 7.800000000000000711 ) ) ;
#30131=CARTESIAN_POINT ( 'NONE',  ( 4.180804271322692500, -31.89534315857266122, 7.013842709614101167 ) ) ;
#30136=CARTESIAN_POINT ( 'NONE',  ( 5.152478333118308385, -28.99279347164636889, 6.894806418505347700 ) ) ;
#30137=ADVANCED_FACE ( 'NONE', ( #24844 ), #30624, .F. ) ;
#30138=CARTESIAN_POINT ( 'NONE',  ( 5.152444924565728890, -30.14726668966421386, 7.665454363767880253 ) ) ;
#30142=CARTESIAN_POINT ( 'NONE',  ( 1.078588498108656424, -33.79778590424514562, 7.754798119455333705 ) ) ;
#30144=CARTESIAN_POINT ( 'NONE',  ( 2.663273245751797802, -32.83073627245006065, 6.949473656533215582 ) ) ;
#30147=DIRECTION ( 'NONE',  ( -0.1736481776669268062, 0.9848077530122086864, 0.000000000000000000 ) ) ;
#30153=CARTESIAN_POINT ( 'NONE',  ( 3.057746519440326605, -26.45262624289676978, 6.969307238440508812 ) ) ;
#30156=CARTESIAN_POINT ( 'NONE',  ( 2.193021027211013330, -32.93406463935832562, 7.774064877406527962 ) ) ;
#30158=LINE ( 'NONE', #4643, #21311 ) ;
#30159=DIRECTION ( 'NONE',  ( -0.9848077530122067991, -0.1736481776669374644, -0.000000000000000000 ) ) ;
#30164=CARTESIAN_POINT ( 'NONE',  ( -0.1589752317941719728, -32.41646502212034875, 7.013842709614101167 ) ) ;
#30165=EDGE_CURVE ( 'NONE', #21217, #22430, #15779, .T. ) ;
#30175=CARTESIAN_POINT ( 'NONE',  ( 1.500917888593657379, -32.96407850412315810, 6.911401339314955372 ) ) ;
#30176=CARTESIAN_POINT ( 'NONE',  ( 2.382407531972861037, -26.23902213697312291, 6.866852738645442322 ) ) ;
#30178=CARTESIAN_POINT ( 'NONE',  ( 3.539909946428774656, -24.83646909262585112, 7.013842709614101167 ) ) ;
#30181=CARTESIAN_POINT ( 'NONE',  ( 0.6853293712966370688, -26.22035530670912351, 6.941203072598474577 ) ) ;
#30182=CARTESIAN_POINT ( 'NONE',  ( 4.498621949403786680, -27.46757472365032982, 6.980586498568972509 ) ) ;
#30184=CARTESIAN_POINT ( 'NONE',  ( 5.172564876073734830, -29.12947328719863194, 7.013842709614101167 ) ) ;
#30185=ORIENTED_EDGE ( 'NONE', *, *, #25169, .T. ) ;
#30189=EDGE_CURVE ( 'NONE', #6925, #19965, #13453, .T. ) ;
#30190=EDGE_LOOP ( 'NONE', ( #12521, #13972, #19729, #34678, #30739 ) ) ;
#30191=CARTESIAN_POINT ( 'NONE',  ( 2.325325312725053717, -33.01368626817038887, 7.750000000000001776 ) ) ;
#30195=CARTESIAN_POINT ( 'NONE',  ( -1.617528036734913188, -28.82728981784584477, 6.871394612369936539 ) ) ;
#30204=EDGE_CURVE ( 'NONE', #38080, #18928, #20212, .T. ) ;
#30205=PLANE ( 'NONE',  #23375 ) ;
#30209=CARTESIAN_POINT ( 'NONE',  ( -0.7646816970285992277, -27.22825800806822016, 6.939395833800444002 ) ) ;
#30211=ADVANCED_FACE ( 'NONE', ( #27813 ), #34645, .F. ) ;
#30217=CARTESIAN_POINT ( 'NONE',  ( -1.233777691191984216, -27.85215430352675980, 7.779495906702012853 ) ) ;
#30221=ORIENTED_EDGE ( 'NONE', *, *, #38521, .F. ) ;
#30223=ORIENTED_EDGE ( 'NONE', *, *, #17431, .T. ) ;
#30224=AXIS2_PLACEMENT_3D ( 'NONE', #39081, #13974, #33548 ) ;
#30226=CARTESIAN_POINT ( 'NONE',  ( -0.9579939928752762013, -31.84654925493761368, 7.710604733652627552 ) ) ;
#30228=VERTEX_POINT ( 'NONE', #22481 ) ;
#30229=CARTESIAN_POINT ( 'NONE',  ( 1.109803157764845061, -33.01974279738480789, 7.750000000000000888 ) ) ;
#30234=DIRECTION ( 'NONE',  ( -0.4999999999999918954, -0.8660254037844432595, -0.000000000000000000 ) ) ;
#30235=CARTESIAN_POINT ( 'NONE',  ( 5.066705152069533646, -29.09251744304078002, 6.864276522220859711 ) ) ;
#30239=DIRECTION ( 'NONE',  ( 0.7394003126383927871, -0.1303762246624153853, -0.6605219282605403475 ) ) ;
#30261=CARTESIAN_POINT ( 'NONE',  ( 4.750267137322237154, -27.85286966892973126, 6.887161170156907097 ) ) ;
#30264=EDGE_CURVE ( 'NONE', #21904, #34419, #39385, .T. ) ;
#30266=DIRECTION ( 'NONE',  ( 0.1736481776669404897, -0.9848077530122062440, -0.000000000000000000 ) ) ;
#30268=DIRECTION ( 'NONE',  ( 0.6427876096865481337, -0.7660444431189707970, -0.000000000000000000 ) ) ;
#30270=CARTESIAN_POINT ( 'NONE',  ( -0.03065438358791858567, -26.64358689880297248, 7.703977250142846955 ) ) ;
#30271=LINE ( 'NONE', #11511, #25575 ) ;
#30277=CARTESIAN_POINT ( 'NONE',  ( -1.254132200242210837, -27.88741944239102466, 7.643333865083953071 ) ) ;
#30278=CARTESIAN_POINT ( 'NONE',  ( 3.549114750742319746, -32.43177086262681996, 7.139196562012271485 ) ) ;
#30283=CARTESIAN_POINT ( 'NONE',  ( 2.827544659576278985, -32.88348186366498282, 6.867280401193707640 ) ) ;
#30289=( BOUNDED_CURVE ( )  B_SPLINE_CURVE ( 3, ( #19625, #3798, #19822, #500 ),
 .UNSPECIFIED., .F., .T. ) 
 B_SPLINE_CURVE_WITH_KNOTS ( ( 4, 4 ),
 ( 4.748221474220558846, 4.941946782021393147 ),
 .UNSPECIFIED. ) 
 CURVE ( )  GEOMETRIC_REPRESENTATION_ITEM ( )  RATIONAL_B_SPLINE_CURVE ( ( 1.000000000000000000, 0.9968749865767494445, 0.9968749865767494445, 1.000000000000000000 ) ) 
 REPRESENTATION_ITEM ( '' )  );
#30292=CARTESIAN_POINT ( 'NONE',  ( 0.06066625181903905623, -26.47779407321028700, 7.750000000000000888 ) ) ;
#30293=EDGE_CURVE ( 'NONE', #14785, #7585, #30068, .T. ) ;
#30300=ADVANCED_FACE ( 'NONE', ( #1194 ), #3681, .F. ) ;
#30306=CARTESIAN_POINT ( 'NONE',  ( 3.809088224730495131, -32.23704061701660351, 7.774064877406527074 ) ) ;
#30311=ORIENTED_EDGE ( 'NONE', *, *, #15484, .T. ) ;
#30314=ADVANCED_FACE ( 'NONE', ( #16205 ), #3887, .T. ) ;
#30318=EDGE_CURVE ( 'NONE', #2808, #4035, #29404, .T. ) ;
#30322=CIRCLE ( 'NONE', #37538, 3.499999999999999556 ) ;
#30330=CARTESIAN_POINT ( 'NONE',  ( -0.9271279775035500270, -27.41211907304282036, 7.703977250142846067 ) ) ;
#30331=AXIS2_PLACEMENT_3D ( 'NONE', #38477, #10676, #35429 ) ;
#30333=CARTESIAN_POINT ( 'NONE',  ( 4.945445480008764605, -30.88065529806472043, 7.754798119455333705 ) ) ;
#30337=CARTESIAN_POINT ( 'NONE',  ( -1.267760583032661037, -27.71561997405539302, 7.754798119455333705 ) ) ;
#30338=EDGE_LOOP ( 'NONE', ( #19046, #16710, #30101, #8728 ) ) ;
#30339=CARTESIAN_POINT ( 'NONE',  ( 1.645206451479275911, -33.06949512287985016, 6.875671892026061549 ) ) ;
#30341=DIRECTION ( 'NONE',  ( 0.9396926207859082059, 0.3420201433256695456, -0.000000000000000000 ) ) ;
#30343=LINE ( 'NONE', #2149, #38195 ) ;
#30344=CARTESIAN_POINT ( 'NONE',  ( -0.7517451142625637406, -27.06299922110170542, 7.501983001166816933 ) ) ;
#30345=CARTESIAN_POINT ( 'NONE',  ( 5.174173811910133480, -29.14233078835555091, 6.912143950357348743 ) ) ;
#30348=CARTESIAN_POINT ( 'NONE',  ( 3.369184120440228636, -26.60764618298541251, 7.692469944509203295 ) ) ;
#30349=CARTESIAN_POINT ( 'NONE',  ( 1.700390093233090871, -29.56993018339339940, 6.800000000000000711 ) ) ;
#30350=CARTESIAN_POINT ( 'NONE',  ( 5.166866161692755810, -29.08666662507720702, 7.750000000000000888 ) ) ;
#30351=CARTESIAN_POINT ( 'NONE',  ( 4.999353408448902414, -30.73905325571789149, 7.660770905198780234 ) ) ;
#30354=CARTESIAN_POINT ( 'NONE',  ( 4.921995751488993598, -28.48303424522928040, 7.782034975670475418 ) ) ;
#30355=CARTESIAN_POINT ( 'NONE',  ( 2.835597840154314042, -26.36504276394633806, 7.661510568013100375 ) ) ;
#30364=DIRECTION ( 'NONE',  ( 0.3420201433256578882, 0.9396926207859123137, 0.000000000000000000 ) ) ;
#30366=CARTESIAN_POINT ( 'NONE',  ( -1.416913847263542081, -28.21257375718617055, 6.969307238440506147 ) ) ;
#30367=CARTESIAN_POINT ( 'NONE',  ( -0.9119913687292857674, -27.24064530155898112, 6.863784140767622333 ) ) ;
#30368=CARTESIAN_POINT ( 'NONE',  ( -1.798306572096198153, -29.57636892467929712, 7.762460296495606649 ) ) ;
#30370=CARTESIAN_POINT ( 'NONE',  ( 1.700390093233090871, -29.56993018339339940, 7.750000000000000888 ) ) ;
#30371=EDGE_CURVE ( 'NONE', #16587, #17641, #17280, .T. ) ;
#30374=ADVANCED_FACE ( 'NONE', ( #32472 ), #32082, .F. ) ;
#30375=VERTEX_POINT ( 'NONE', #10223 ) ;
#30380=CARTESIAN_POINT ( 'NONE',  ( 0.3856705772283747780, -32.81361829944838604, 7.750000000000000888 ) ) ;
#30381=B_SPLINE_CURVE_WITH_KNOTS ( 'NONE', 3,
 ( #2518, #15042, #21230, #24306, #5580, #30916, #40157, #39542, #15245, #11731, #39959, #33186, #33405, #33800, #2104, #5178, #27603, #40352, #24516 ),
 .UNSPECIFIED., .F., .F.,
 ( 4, 3, 3, 3, 3, 3, 4 ),
 ( 2.475319317933456060E-05, 2.546128104244956540E-05, 5.711050680483690107E-05, 8.113074941674912051E-05, 0.0001053129305726947589, 0.0001360598016346936364, 0.0001612931755702001855 ),
 .UNSPECIFIED. ) ;
#30382=CARTESIAN_POINT ( 'NONE',  ( 4.030693118979438161, -27.09410047637255303, 7.006423389747789443 ) ) ;
#30385=ORIENTED_EDGE ( 'NONE', *, *, #29961, .F. ) ;
#30389=CARTESIAN_POINT ( 'NONE',  ( 1.506564090326510508, -32.96440090511088528, 6.903372536218457256 ) ) ;
#30391=DIRECTION ( 'NONE',  ( -1.000000000000000000, 0.000000000000000000, 0.000000000000000000 ) ) ;
#30393=CARTESIAN_POINT ( 'NONE',  ( -0.5769924795711234289, -32.09451502393404354, 7.754798119455333705 ) ) ;
#30404=CARTESIAN_POINT ( 'NONE',  ( 1.011962798722023882, -33.78603799583471101, 7.695279973900954751 ) ) ;
#30405=CARTESIAN_POINT ( 'NONE',  ( -1.636164459686335615, -28.91612145343104245, 6.880147297696979969 ) ) ;
#30408=ORIENTED_EDGE ( 'NONE', *, *, #1279, .F. ) ;
#30410=UNCERTAINTY_MEASURE_WITH_UNIT (LENGTH_MEASURE( 1.000000000000000082E-05 ), #21229, 'distance_accuracy_value', 'NONE');
#30413=VERTEX_POINT ( 'NONE', #33072 ) ;
#30415=CARTESIAN_POINT ( 'NONE',  ( -1.526829923184012339, -28.21528965334980654, 7.013842709614101167 ) ) ;
#30419=CARTESIAN_POINT ( 'NONE',  ( 4.722721840544713778, -27.80484921947353527, 7.750000000000000888 ) ) ;
#30420=ORIENTED_EDGE ( 'NONE', *, *, #30318, .F. ) ;
#30423=B_SPLINE_CURVE_WITH_KNOTS ( 'NONE', 3,
 ( #10848, #11240, #39451, #23805 ),
 .UNSPECIFIED., .F., .F.,
 ( 4, 4 ),
 ( 0.000000000000000000, 6.391136169901225176E-06 ),
 .UNSPECIFIED. ) ;
#30425=PLANE ( 'NONE',  #7174 ) ;
#30427=CARTESIAN_POINT ( 'NONE',  ( -1.597957901506573020, -30.69845554356182049, 7.784725160561909441 ) ) ;
#30429=ORIENTED_EDGE ( 'NONE', *, *, #10415, .T. ) ;
#30437=ORIENTED_EDGE ( 'NONE', *, *, #10963, .F. ) ;
#30444=B_SPLINE_CURVE_WITH_KNOTS ( 'NONE', 3,
 ( #38033, #32678, #35177, #13527, #19904, #6755, #29577, #32477, #28781, #26098 ),
 .UNSPECIFIED., .F., .F.,
 ( 4, 3, 3, 4 ),
 ( 9.697399036122160616E-19, 3.025570593003526365E-05, 6.051145698344814338E-05, 6.468151674593860048E-05 ),
 .UNSPECIFIED. ) ;
#30446=CARTESIAN_POINT ( 'NONE',  ( 1.906962465809825202, -26.17621130067962554, 6.929923840112063083 ) ) ;
#30450=ADVANCED_FACE ( 'NONE', ( #27499 ), #33496, .F. ) ;
#30452=ORIENTED_EDGE ( 'NONE', *, *, #10120, .F. ) ;
#30457=CARTESIAN_POINT ( 'NONE',  ( 3.478437006660350050, -32.58465225576620838, 7.670465701733749420 ) ) ;
#30460=CARTESIAN_POINT ( 'NONE',  ( 0.3457495631895174948, -32.79715019981050972, 7.013842709614101167 ) ) ;
#30461=ORIENTED_EDGE ( 'NONE', *, *, #27775, .F. ) ;
#30463=VERTEX_POINT ( 'NONE', #1785 ) ;
#30465=EDGE_CURVE ( 'NONE', #7270, #30107, #21644, .T. ) ;
#30468=ORIENTED_EDGE ( 'NONE', *, *, #29843, .T. ) ;
#30470=CARTESIAN_POINT ( 'NONE',  ( 4.292837626212670621, -27.37010842044347925, 7.748216051605120391 ) ) ;
#30471=ORIENTED_EDGE ( 'NONE', *, *, #28086, .F. ) ;
#30476=ORIENTED_EDGE ( 'NONE', *, *, #2249, .T. ) ;
#30485=CARTESIAN_POINT ( 'NONE',  ( 1.512676170941966269, -26.06812520694141355, 7.139344958878410807 ) ) ;
#30486=EDGE_LOOP ( 'NONE', ( #24941, #577, #3864, #3845 ) ) ;
#30491=CARTESIAN_POINT ( 'NONE',  ( 2.743233935765024611, -32.91096671533840379, 6.887547729233689076 ) ) ;
#30498=CARTESIAN_POINT ( 'NONE',  ( 4.661238701438277232, -31.43633321245790313, 6.870724624169667116 ) ) ;
#30502=EDGE_CURVE ( 'NONE', #35504, #16824, #8990, .T. ) ;
#30505=CARTESIAN_POINT ( 'NONE',  ( 3.679947863870264957, -32.46458404149915111, 7.501983001166817822 ) ) ;
#30512=CARTESIAN_POINT ( 'NONE',  ( -0.5769924795711234289, -32.09451502393404354, 7.754798119455333705 ) ) ;
#30513=CARTESIAN_POINT ( 'NONE',  ( 3.870091955771714165, -32.18765598803872052, 7.779495906702013741 ) ) ;
#30518=CARTESIAN_POINT ( 'NONE',  ( -1.713032059046489142, -28.79627056164295595, 7.013842709614101167 ) ) ;
#30519=VERTEX_POINT ( 'NONE', #14111 ) ;
#30532=ORIENTED_EDGE ( 'NONE', *, *, #22528, .F. ) ;
#30537=( BOUNDED_CURVE ( )  B_SPLINE_CURVE ( 3, ( #18325, #25341, #12362, #28418 ),
 .UNSPECIFIED., .F., .T. ) 
 B_SPLINE_CURVE_WITH_KNOTS ( ( 4, 4 ),
 ( 4.708531083176466403, 4.895802057644187855 ),
 .UNSPECIFIED. ) 
 CURVE ( )  GEOMETRIC_REPRESENTATION_ITEM ( )  RATIONAL_B_SPLINE_CURVE ( ( 1.000000000000000000, 0.9970795998553221295, 0.9970795998553221295, 1.000000000000000000 ) ) 
 REPRESENTATION_ITEM ( '' )  );
#30543=CARTESIAN_POINT ( 'NONE',  ( 1.585021184048799547, -33.06802824016562425, 6.865482280155369210 ) ) ;
#30545=CYLINDRICAL_SURFACE ( 'NONE', #18885, 2.500000000000000444 ) ;
#30547=DIRECTION ( 'NONE',  ( 0.7660444431189857850, -0.6427876096865300370, -0.000000000000000000 ) ) ;
#30548=CARTESIAN_POINT ( 'NONE',  ( 0.5371711504799124848, -32.87097875789517332, 7.686927408461904143 ) ) ;
#30549=EDGE_CURVE ( 'NONE', #17688, #39584, #31537, .T. ) ;
#30551=CARTESIAN_POINT ( 'NONE',  ( 2.129437147705529387, -33.04353820846659318, 6.998987538705434552 ) ) ;
#30556=CARTESIAN_POINT ( 'NONE',  ( 1.578585683582352850, -25.86893018339335981, 7.754798119455333705 ) ) ;
#30557=CARTESIAN_POINT ( 'NONE',  ( 2.664368798089519874, -32.83041366969101205, 6.939395833800439561 ) ) ;
#30558=CARTESIAN_POINT ( 'NONE',  ( 5.099964974645724070, -29.62376613088546762, 6.889465824494256374 ) ) ;
#30561=STYLED_ITEM('',(#40766),#12876);
#30568=AXIS2_PLACEMENT_3D ( 'NONE', #11700, #36433, #6527 ) ;
#30569=CARTESIAN_POINT ( 'NONE',  ( 2.277526804980155362, -33.02201842327861669, 6.894806418505347700 ) ) ;
#30573=CARTESIAN_POINT ( 'NONE',  ( -2.253834945959114489, -26.23431501015891243, 7.635761828346577573 ) ) ;
#30575=CARTESIAN_POINT ( 'NONE',  ( -0.9390753546024662723, -27.27138652691368037, 6.870737987065013819 ) ) ;
#30576=CARTESIAN_POINT ( 'NONE',  ( 1.222977352880459723, -26.20361512455695774, 6.864276522220859711 ) ) ;
#30586=B_SPLINE_CURVE_WITH_KNOTS ( 'NONE', 3,
 ( #17646, #11875, #40094, #39681, #37006, #30226, #8788, #2042, #30024, #2662 ),
 .UNSPECIFIED., .F., .F.,
 ( 4, 3, 3, 4 ),
 ( 0.0001585009270395752084, 0.0001815657551981840858, 0.0002118214035944140504, 0.0002170292169044743470 ),
 .UNSPECIFIED. ) ;
#30597=CARTESIAN_POINT ( 'NONE',  ( 2.778259044425222868, -32.89982485500929954, 7.750000000000000888 ) ) ;
#30599=CARTESIAN_POINT ( 'NONE',  ( 0.8386806441584250260, -25.38437669007690900, 7.754798119455333705 ) ) ;
#30602=CARTESIAN_POINT ( 'NONE',  ( 2.493534863053076922, -26.26373349863179740, 6.979335674598005745 ) ) ;
#30603=CARTESIAN_POINT ( 'NONE',  ( -1.741606627443540223, -30.11652268061110860, 7.785593909369613819 ) ) ;
#30607=CARTESIAN_POINT ( 'NONE',  ( 4.668948836787977896, -27.91232378075620701, 6.894806418505348589 ) ) ;
#30609=EDGE_CURVE ( 'NONE', #20740, #29030, #38879, .T. ) ;
#30611=CARTESIAN_POINT ( 'NONE',  ( -0.4414210011093676611, -26.92935349710845827, 6.887041543973313473 ) ) ;
#30614=EDGE_LOOP ( 'NONE', ( #31638, #33141, #9506, #37489 ) ) ;
#30617=LINE ( 'NONE', #34130, #1410 ) ;
#30623=CARTESIAN_POINT ( 'NONE',  ( 4.872722190795648167, -30.79319270744810311, 6.880147297696983522 ) ) ;
#30624=CYLINDRICAL_SURFACE ( 'NONE', #27422, 0.09010775117052947925 ) ;
#30626=CARTESIAN_POINT ( 'NONE',  ( -1.605257465718879395, -28.77450919976473998, 6.969307238440508812 ) ) ;
#30637=VERTEX_POINT ( 'NONE', #21536 ) ;
#30639=CARTESIAN_POINT ( 'NONE',  ( 3.353554235774506953, -32.54096636651022578, 6.889465824494256374 ) ) ;
#30645=CARTESIAN_POINT ( 'NONE',  ( -1.797340250851707344, -29.44390463015740522, 7.750000000000000888 ) ) ;
#30649=CARTESIAN_POINT ( 'NONE',  ( 1.001059401594865061, -32.99204059322197935, 7.776484688137380807 ) ) ;
#30653=ORIENTED_EDGE ( 'NONE', *, *, #507, .F. ) ;
#30663=ORIENTED_EDGE ( 'NONE', *, *, #37780, .F. ) ;
#30678=CARTESIAN_POINT ( 'NONE',  ( 5.654615132425274027, -32.90554535662791835, 7.635761828346577573 ) ) ;
#30683=EDGE_CURVE ( 'NONE', #16841, #6774, #28073, .T. ) ;
#30692=CARTESIAN_POINT ( 'NONE',  ( -1.794949259926919227, -29.38927334556171544, 6.998987538705436329 ) ) ;
#30696=CARTESIAN_POINT ( 'NONE',  ( 0.5043319404286802365, -26.38725126186910686, 7.680992449362120666 ) ) ;
#30701=CARTESIAN_POINT ( 'NONE',  ( 0.1384972100046504007, -34.01952225562621379, 7.695279973900954751 ) ) ;
#30702=ORIENTED_EDGE ( 'NONE', *, *, #36035, .F. ) ;
#30705=CARTESIAN_POINT ( 'NONE',  ( 5.141684319425215755, -30.20828278875847062, 6.894806418505347700 ) ) ;
#30706=CARTESIAN_POINT ( 'NONE',  ( 2.845456134469579457, -32.87731945005177181, 6.875671892026061549 ) ) ;
#30710=EDGE_CURVE ( 'NONE', #28641, #29003, #37382, .T. ) ;
#30712=( NAMED_UNIT ( * ) SI_UNIT ( $, .STERADIAN. ) SOLID_ANGLE_UNIT ( ) );
#30713=CARTESIAN_POINT ( 'NONE',  ( 4.646831710089861289, -31.45898555212992775, 6.887547729233681970 ) ) ;
#30717=CARTESIAN_POINT ( 'NONE',  ( 1.575771303524207134, -33.06771121410476155, 7.751599049952198506 ) ) ;
#30723=DIRECTION ( 'NONE',  ( 0.000000000000000000, -0.6605219282605377940, -0.7508067542896645907 ) ) ;
#30724=EDGE_CURVE ( 'NONE', #19287, #16154, #27583, .T. ) ;
#30727=CARTESIAN_POINT ( 'NONE',  ( -0.5665229445002866182, -32.10393105754645404, 7.768425012602599544 ) ) ;
#30737=VECTOR ( 'NONE', #40704, 1000.000000000000000 ) ;
#30738=CARTESIAN_POINT ( 'NONE',  ( 1.700390093233090871, -29.56993018339339940, 7.750000000000000888 ) ) ;
#30739=ORIENTED_EDGE ( 'NONE', *, *, #6443, .T. ) ;
#30744=AXIS2_PLACEMENT_3D ( 'NONE', #35448, #9485, #3553 ) ;
#30745=EDGE_CURVE ( 'NONE', #6204, #18417, #13217, .T. ) ;
#30749=VERTEX_POINT ( 'NONE', #18730 ) ;
#30752=DIRECTION ( 'NONE',  ( -0.000000000000000000, -0.000000000000000000, -1.000000000000000000 ) ) ;
#30755=CARTESIAN_POINT ( 'NONE',  ( -1.697684928147993766, -29.45553547605979006, 6.864276522220859711 ) ) ;
#30757=CARTESIAN_POINT ( 'NONE',  ( -1.764597594712412176, -30.06375234003086305, 6.865482280155368322 ) ) ;
#30759=CARTESIAN_POINT ( 'NONE',  ( 1.669309969508061764, -33.06979218437418666, 6.894806418505347700 ) ) ;
#30760=DIRECTION ( 'NONE',  ( -0.9396926207859104263, 0.3420201433256631063, -0.000000000000000000 ) ) ;
#30768=CARTESIAN_POINT ( 'NONE',  ( 5.200252094213874798, -29.60101030711846448, 6.894806418505347700 ) ) ;
#30769=CARTESIAN_POINT ( 'NONE',  ( -0.06872588940044967176, -26.54995493937659390, 7.743886751744251562 ) ) ;
#30770=CYLINDRICAL_SURFACE ( 'NONE', #31148, 3.399999999999999911 ) ;
#30772=CARTESIAN_POINT ( 'NONE',  ( 4.634748283818988845, -27.85249419169753438, 7.643333865083956624 ) ) ;
#30773=DIRECTION ( 'NONE',  ( 0.3420201433256662704, 0.9396926207859093161, -0.000000000000000000 ) ) ;
#30780=B_SPLINE_CURVE_WITH_KNOTS ( 'NONE', 3,
 ( #12592, #2751, #34863, #24753 ),
 .UNSPECIFIED., .F., .F.,
 ( 4, 4 ),
 ( 0.000000000000000000, 6.391136169993470452E-06 ),
 .UNSPECIFIED. ) ;
#30785=CARTESIAN_POINT ( 'NONE',  ( 3.048460970688392280, -26.44859712950919928, 6.997764925645182821 ) ) ;
#30786=CARTESIAN_POINT ( 'NONE',  ( 1.307187192269261722, -26.19274102632997270, 6.997764925645181044 ) ) ;
#30792=EDGE_LOOP ( 'NONE', ( #15594, #33466, #39504, #30461 ) ) ;
#30794=( BOUNDED_CURVE ( )  B_SPLINE_CURVE ( 3, ( #15658, #24721, #12563, #12764 ),
 .UNSPECIFIED., .F., .T. ) 
 B_SPLINE_CURVE_WITH_KNOTS ( ( 4, 4 ),
 ( 1.381924640371166912, 1.574767692156075372 ),
 .UNSPECIFIED. ) 
 CURVE ( )  GEOMETRIC_REPRESENTATION_ITEM ( )  RATIONAL_B_SPLINE_CURVE ( ( 1.000000000000000000, 0.9969033633783032089, 0.9969033633783032089, 1.000000000000000000 ) ) 
 REPRESENTATION_ITEM ( '' )  );
#30801=CARTESIAN_POINT ( 'NONE',  ( 2.843927967873976392, -32.77186954725888768, 7.779495906702012853 ) ) ;
#30805=B_SPLINE_CURVE_WITH_KNOTS ( 'NONE', 3,
 ( #27010, #24528, #14635, #33815, #23712, #34029, #5597, #5803, #20822, #15056, #30108, #39350, #8054, #21042, #2532, #14239, #33419, #33615, #33199, #11142, #30727, #11742, #1917, #36676, #30512 ),
 .UNSPECIFIED., .F., .F.,
 ( 4, 3, 3, 3, 3, 3, 3, 3, 4 ),
 ( 6.468151674594082310E-05, 9.076621574721611767E-05, 0.0001210204262067929927, 0.0001512763324577386321, 0.0001815301820994170122, 0.0002117781465860660436, 0.0002420274594459704371, 0.0002722905548971097170, 0.0002816827545175626369 ),
 .UNSPECIFIED. ) ;
#30806=CARTESIAN_POINT ( 'NONE',  ( -1.799497888696266479, -29.59793221807746022, 7.658262384781102661 ) ) ;
#30807=CIRCLE ( 'NONE', #37362, 2.500000000000000000 ) ;
#30812=CARTESIAN_POINT ( 'NONE',  ( -1.763898702996634871, -30.06273584198100579, 7.761113333116788304 ) ) ;
#30816=CARTESIAN_POINT ( 'NONE',  ( 5.042305363714541855, -28.94414881188822619, 7.703977250142848732 ) ) ;
#30823=DIRECTION ( 'NONE',  ( -0.000000000000000000, -0.000000000000000000, -1.000000000000000000 ) ) ;
#30825=CARTESIAN_POINT ( 'NONE',  ( 2.313921169258307931, -33.01434178613541093, 7.762796336881262249 ) ) ;
#30828=CARTESIAN_POINT ( 'NONE',  ( 4.876532544628377153, -30.78324251417176072, 6.889465824494259039 ) ) ;
#30829=VERTEX_POINT ( 'NONE', #15650 ) ;
#30837=CARTESIAN_POINT ( 'NONE',  ( -1.517625692061476794, -28.19356706969799831, 6.955226052476383813 ) ) ;
#30839=CARTESIAN_POINT ( 'NONE',  ( -0.8432521732669862047, -27.31383173241063389, 6.866852738645442322 ) ) ;
#30841=EDGE_CURVE ( 'NONE', #34839, #16031, #9942, .T. ) ;
#30846=CARTESIAN_POINT ( 'NONE',  ( 4.925414808968284319, -30.92978884623197899, 7.006908160621406978 ) ) ;
#30847=DIRECTION ( 'NONE',  ( -1.000000000000000000, 0.000000000000000000, 0.000000000000000000 ) ) ;
#30849=B_SPLINE_CURVE_WITH_KNOTS ( 'NONE', 3,
 ( #10356, #28282, #31590, #22932, #12634, #22126, #25206, #509, #299, #37736, #25606, #34699, #12838, #25408, #34901, #6678, #19226, #31792, #16136, #10550, #33001, #32405, #26421, #29898, #32606, #35695, #23716, #17319, #38950, #26617, #16927 ),
 .UNSPECIFIED., .F., .F.,
 ( 4, 3, 3, 3, 3, 3, 3, 3, 3, 3, 4 ),
 ( 3.679904200040097469E-18, 3.077658087705444919E-05, 6.152638666998797327E-05, 9.267501192706533602E-05, 0.0001241882240135170300, 0.0001556618703051661765, 0.0001866161554452200268, 0.0002167966385860962497, 0.0002463805737537759716, 0.0002758761370306515685, 0.0002847094172290023386 ),
 .UNSPECIFIED. ) ;
#30850=CARTESIAN_POINT ( 'NONE',  ( 0.3767051360551654238, -26.43053962681419122, 7.139196562012272373 ) ) ;
#30855=CARTESIAN_POINT ( 'NONE',  ( 0.1463256921878338668, -32.60189304101577790, 7.139196562012272373 ) ) ;
#30856=CARTESIAN_POINT ( 'NONE',  ( 0.9923868681965268834, -32.99281228919391395, 7.771081512783695189 ) ) ;
#30861=CARTESIAN_POINT ( 'NONE',  ( 2.864725917214215212, -26.26927458485223355, 7.678495282201403427 ) ) ;
#30862=CARTESIAN_POINT ( 'NONE',  ( 4.634557877658172842, -31.28770606326002124, 7.779495906702013741 ) ) ;
#30869=CARTESIAN_POINT ( 'NONE',  ( 1.909707170198035708, -26.17637943432646708, 6.969307238440505259 ) ) ;
#30871=CARTESIAN_POINT ( 'NONE',  ( 4.327908163969746980, -31.72774129374395713, 7.695279973900954751 ) ) ;
#30881=CARTESIAN_POINT ( 'NONE',  ( -1.765272865745179498, -30.05733663009887024, 7.754798119455333705 ) ) ;
#30882=ORIENTED_EDGE ( 'NONE', *, *, #38947, .F. ) ;
#30886=ORIENTED_EDGE ( 'NONE', *, *, #591, .T. ) ;
#30889=EDGE_LOOP ( 'NONE', ( #8096, #34309, #15177, #13607, #40003 ) ) ;
#30891=EDGE_CURVE ( 'NONE', #19982, #19304, #16279, .T. ) ;
#30892=FACE_OUTER_BOUND ( 'NONE', #25611, .T. ) ;
#30894=ORIENTED_EDGE ( 'NONE', *, *, #24074, .T. ) ;
#30895=DIRECTION ( 'NONE',  ( -0.5000000000000039968, 0.8660254037844363761, -0.000000000000000000 ) ) ;
#30897=CARTESIAN_POINT ( 'NONE',  ( -1.794313667778303589, -29.37745747938051366, 6.961115707816239784 ) ) ;
#30899=ORIENTED_EDGE ( 'NONE', *, *, #20769, .T. ) ;
#30903=TOROIDAL_SURFACE ( 'NONE', #7200, 3.449999999999999289, 0.05000000000000000278 ) ;
#30910=CARTESIAN_POINT ( 'NONE',  ( -0.9271279775035500270, -27.41211907304282036, 7.693875151218750652 ) ) ;
#30916=CARTESIAN_POINT ( 'NONE',  ( 5.191621582129971380, -29.58803114832194936, 7.778495531946296282 ) ) ;
#30920=AXIS2_PLACEMENT_3D ( 'NONE', #9394, #21979, #15166 ) ;
#30922=EDGE_LOOP ( 'NONE', ( #815, #6502, #31176, #7816, #6545 ) ) ;
#30926=B_SPLINE_CURVE_WITH_KNOTS ( 'NONE', 3,
 ( #34372, #15815, #6143, #18477, #34173, #24458, #37419, #12512, #27953, #21795, #11885, #12718, #28370, #18685, #5938, #34580, #18273, #25087, #15396, #31270, #3089, #15606, #28158, #18902, #181, #25292, #37016, #8599, #21177, #33745, #5524 ),
 .UNSPECIFIED., .F., .F.,
 ( 4, 3, 3, 3, 3, 3, 3, 3, 3, 3, 4 ),
 ( 5.057544569639794935E-18, 3.077658087705700384E-05, 6.152638666998954536E-05, 9.267501192706765350E-05, 0.0001241882240135207434, 0.0001556618703051702694, 0.0001866161554452256104, 0.0002167966385861005865, 0.0002463805737537815010, 0.0002758761370306578569, 0.0002847094172290074343 ),
 .UNSPECIFIED. ) ;
#30929=ORIENTED_EDGE ( 'NONE', *, *, #7037, .F. ) ;
#30930=DIRECTION ( 'NONE',  ( -1.000000000000000000, 0.000000000000000000, 0.000000000000000000 ) ) ;
#30931=CIRCLE ( 'NONE', #19077, 0.04999999999999969746 ) ;
#30932=CYLINDRICAL_SURFACE ( 'NONE', #35142, 0.09010775117052974292 ) ;
#30941=LINE ( 'NONE', #40181, #12734 ) ;
#30942=EDGE_CURVE ( 'NONE', #25058, #18362, #13325, .T. ) ;
#30945=LINE ( 'NONE', #27825, #14725 ) ;
#30952=CARTESIAN_POINT ( 'NONE',  ( 4.749297472835599443, -31.28869828601962766, 7.686927408461905920 ) ) ;
#30953=ORIENTED_EDGE ( 'NONE', *, *, #29201, .F. ) ;
#30956=CARTESIAN_POINT ( 'NONE',  ( -1.696079551158403254, -29.41472263061939074, 6.871394612369935651 ) ) ;
#30963=CARTESIAN_POINT ( 'NONE',  ( 5.000416883752518693, -30.73605123097268788, 7.720710062488893577 ) ) ;
#30964=DIRECTION ( 'NONE',  ( -0.8660254037844344888, -0.5000000000000069944, -0.000000000000000000 ) ) ;
#30970=CARTESIAN_POINT ( 'NONE',  ( 0.3950279145847279683, -32.81649511626806515, 7.761113333117553026 ) ) ;
#30972=CARTESIAN_POINT ( 'NONE',  ( 2.123740571999295224, -26.18929573040587400, 7.139196562012271485 ) ) ;
#30977=ORIENTED_EDGE ( 'NONE', *, *, #39984, .F. ) ;
#30986=CARTESIAN_POINT ( 'NONE',  ( 3.037211893591657219, -26.44376520468768632, 7.013842709614101167 ) ) ;
#30988=CARTESIAN_POINT ( 'NONE',  ( 4.897206782758049215, -30.72770037511210717, 7.763628509615289275 ) ) ;
#30990=CARTESIAN_POINT ( 'NONE',  ( 4.104433119696450305, -25.16239669867571749, 7.754798119455333705 ) ) ;
#31001=ORIENTED_EDGE ( 'NONE', *, *, #21253, .T. ) ;
#31002=CARTESIAN_POINT ( 'NONE',  ( 4.396048886544873469, -27.49787234876598063, 6.868387053540518927 ) ) ;
#31003=CARTESIAN_POINT ( 'NONE',  ( 2.834760927471382530, -32.77511392390336908, 7.782167645815904145 ) ) ;
#31012=CYLINDRICAL_SURFACE ( 'NONE', #26216, 3.399999999999999911 ) ;
#31014=CARTESIAN_POINT ( 'NONE',  ( -0.06309262675075595628, -26.54666488804996405, 7.638132480492513920 ) ) ;
#31015=CARTESIAN_POINT ( 'NONE',  ( 4.313599969017027469, -31.74504722509605159, 7.635761828346577573 ) ) ;
#31016=B_SPLINE_CURVE_WITH_KNOTS ( 'NONE', 3,
 ( #22151, #18619, #27497, #2407 ),
 .UNSPECIFIED., .F., .F.,
 ( 4, 4 ),
 ( 1.134857258918348999E-18, 6.391136169993800794E-06 ),
 .UNSPECIFIED. ) ;
#31019=AXIS2_PLACEMENT_3D ( 'NONE', #14224, #39955, #11526 ) ;
#31022=ORIENTED_EDGE ( 'NONE', *, *, #10605, .T. ) ;
#31026=CARTESIAN_POINT ( 'NONE',  ( 4.974883666185707654, -30.78101102078142048, 7.778495531946297170 ) ) ;
#31027=EDGE_CURVE ( 'NONE', #17900, #38669, #20638, .T. ) ;
#31028=FACE_OUTER_BOUND ( 'NONE', #25501, .T. ) ;
#31032=( BOUNDED_CURVE ( )  B_SPLINE_CURVE ( 3, ( #4170, #26191, #29273, #1085 ),
 .UNSPECIFIED., .F., .T. ) 
 B_SPLINE_CURVE_WITH_KNOTS ( ( 4, 4 ),
 ( 1.347909859412853351, 1.534781240595298302 ),
 .UNSPECIFIED. ) 
 CURVE ( )  GEOMETRIC_REPRESENTATION_ITEM ( )  RATIONAL_B_SPLINE_CURVE ( ( 1.000000000000000000, 0.9970920404276226723, 0.9970920404276226723, 1.000000000000000000 ) ) 
 REPRESENTATION_ITEM ( '' )  );
#31037=VERTEX_POINT ( 'NONE', #2461 ) ;
#31041=CARTESIAN_POINT ( 'NONE',  ( 4.894814254439905810, -28.12309771077098830, 7.501983001166816933 ) ) ;
#31043=CARTESIAN_POINT ( 'NONE',  ( -1.340724465380329633, -31.09033463251039464, 6.920489980334475710 ) ) ;
#31045=CIRCLE ( 'NONE', #18528, 3.499999999999999556 ) ;
#31046=CARTESIAN_POINT ( 'NONE',  ( 0.02220050038877733126, -26.51254151590686092, 7.782861076432731728 ) ) ;
#31047=CARTESIAN_POINT ( 'NONE',  ( 4.926102704777563623, -30.92815744066947303, 7.009310105710482297 ) ) ;
#31052=CARTESIAN_POINT ( 'NONE',  ( 5.196299276553091318, -29.73910164073445017, 7.013842709614101167 ) ) ;
#31055=CARTESIAN_POINT ( 'NONE',  ( 5.006679844419255510, -30.36267735696220171, 6.929923840112066635 ) ) ;
#31061=CARTESIAN_POINT ( 'NONE',  ( 3.455938198587527044, -26.65821024669467931, 6.880147297696981745 ) ) ;
#31068=CARTESIAN_POINT ( 'NONE',  ( 1.814784800566712653, -26.17185516201231366, 6.864276522220859711 ) ) ;
#31070=EDGE_CURVE ( 'NONE', #34839, #39722, #15780, .T. ) ;
#31071=CARTESIAN_POINT ( 'NONE',  ( 4.265723375214720114, -31.80131207638199697, 7.785172627573962778 ) ) ;
#31073=CARTESIAN_POINT ( 'NONE',  ( 4.934953675687837382, -28.52226686387824373, 7.754798119455333705 ) ) ;
#31080=ORIENTED_EDGE ( 'NONE', *, *, #22623, .F. ) ;
#31082=ORIENTED_EDGE ( 'NONE', *, *, #4793, .F. ) ;
#31083=VERTEX_POINT ( 'NONE', #33123 ) ;
#31089=CARTESIAN_POINT ( 'NONE',  ( 4.361733393105681422, -27.45397842585655113, 7.778050822775631978 ) ) ;
#31092=LINE ( 'NONE', #18714, #23529 ) ;
#31093=CARTESIAN_POINT ( 'NONE',  ( 4.727494763369829656, -28.02182252691845576, 6.882085323592684212 ) ) ;
#31099=ORIENTED_EDGE ( 'NONE', *, *, #36136, .T. ) ;
#31102=DIRECTION ( 'NONE',  ( -0.000000000000000000, -0.000000000000000000, 1.000000000000000000 ) ) ;
#31108=ORIENTED_EDGE ( 'NONE', *, *, #35976, .T. ) ;
#31110=CARTESIAN_POINT ( 'NONE',  ( 2.778550765842568104, -32.89974653295162454, 6.867199677474202346 ) ) ;
#31114=CARTESIAN_POINT ( 'NONE',  ( 5.141351571375373020, -29.01534782536966617, 7.785344483711592822 ) ) ;
#31115=CARTESIAN_POINT ( 'NONE',  ( 4.926808446430161581, -28.19584895585300544, 7.139344958878410807 ) ) ;
#31122=ORIENTED_EDGE ( 'NONE', *, *, #19112, .F. ) ;
#31132=CARTESIAN_POINT ( 'NONE',  ( 3.914573333748507356, -32.28055252020246968, 6.880608371227946662 ) ) ;
#31137=DIRECTION ( 'NONE',  ( 1.000000000000000000, 1.090397613471135978E-14, 0.000000000000000000 ) ) ;
#31140=( BOUNDED_CURVE ( )  B_SPLINE_CURVE ( 3, ( #39408, #20272, #38997, #26668 ),
 .UNSPECIFIED., .F., .F. ) 
 B_SPLINE_CURVE_WITH_KNOTS ( ( 4, 4 ),
 ( 1.347909859412855127, 1.534781240595300078 ),
 .UNSPECIFIED. ) 
 CURVE ( )  GEOMETRIC_REPRESENTATION_ITEM ( )  RATIONAL_B_SPLINE_CURVE ( ( 1.000000000000000000, 0.9970920404276226723, 0.9970920404276226723, 1.000000000000000000 ) ) 
 REPRESENTATION_ITEM ( '' )  );
#31141=CARTESIAN_POINT ( 'NONE',  ( 0.03672680498656953618, -25.15737950931636036, 7.695279973900954751 ) ) ;
#31142=CARTESIAN_POINT ( 'NONE',  ( -0.03790328338398483987, -32.60774784362404688, 7.635761828346575797 ) ) ;
#31146=EDGE_LOOP ( 'NONE', ( #30663, #15977, #37589, #3111 ) ) ;
#31148=AXIS2_PLACEMENT_3D ( 'NONE', #37525, #21495, #27854 ) ;
#31149=CARTESIAN_POINT ( 'NONE',  ( 4.744007798040242641, -31.29805785553299557, 7.651421919295144036 ) ) ;
#31154=CARTESIAN_POINT ( 'NONE',  ( -1.693770939237457585, -29.37071670600890272, 6.997764925645181933 ) ) ;
#31157=CARTESIAN_POINT ( 'NONE',  ( -1.796364496817714818, -29.56936870405388618, 7.767720160662275219 ) ) ;
#31160=CARTESIAN_POINT ( 'NONE',  ( 1.358827467012312384, -32.95986981511961034, 7.505001789837626447 ) ) ;
#31162=CARTESIAN_POINT ( 'NONE',  ( 1.682951012397970292, -26.06997362959739206, 7.750000000000000888 ) ) ;
#31165=CARTESIAN_POINT ( 'NONE',  ( 2.140846989427893643, -33.04210496623404225, 7.013842709614101167 ) ) ;
#31170=FACE_OUTER_BOUND ( 'NONE', #12909, .T. ) ;
#31172=CARTESIAN_POINT ( 'NONE',  ( 1.674779974442441643, -26.17002453643706517, 7.652160403243383868 ) ) ;
#31174=CARTESIAN_POINT ( 'NONE',  ( 2.832035007868547893, -26.36378076803745429, 7.670860738520332234 ) ) ;
#31176=ORIENTED_EDGE ( 'NONE', *, *, #32503, .F. ) ;
#31177=DIRECTION ( 'NONE',  ( -0.3420201433256578882, -0.9396926207859123137, 0.000000000000000000 ) ) ;
#31183=CARTESIAN_POINT ( 'NONE',  ( 5.033334561780324456, -28.50148930192538543, 6.870724624169668004 ) ) ;
#31189=VECTOR ( 'NONE', #15673, 1000.000000000000114 ) ;
#31193=CARTESIAN_POINT ( 'NONE',  ( -1.484393579397379259, -30.76037252073963657, 7.661510568013098599 ) ) ;
#31197=CARTESIAN_POINT ( 'NONE',  ( 4.434547210566933018, -27.54894399270960292, 6.969307238440501706 ) ) ;
#31202=DIRECTION ( 'NONE',  ( -0.6834397476448861308, 0.000000000000000000, 0.7300069255418706327 ) ) ;
#31206=EDGE_CURVE ( 'NONE', #6285, #35485, #21787, .T. ) ;
#31209=CARTESIAN_POINT ( 'NONE',  ( 1.578585683582427235, -32.96774767198657941, 7.754798119455333705 ) ) ;
#31214=DIRECTION ( 'NONE',  ( 0.3420201433256662704, 0.9396926207859093161, -0.000000000000000000 ) ) ;
#31215=CARTESIAN_POINT ( 'NONE',  ( -0.02262473055865150268, -26.52342071894167574, 6.894806418505347700 ) ) ;
#31216=CARTESIAN_POINT ( 'NONE',  ( 5.044365408655546723, -28.95522359424513326, 7.740055089680399902 ) ) ;
#31222=EDGE_CURVE ( 'NONE', #31466, #5967, #34165, .T. ) ;
#31223=ORIENTED_EDGE ( 'NONE', *, *, #22001, .F. ) ;
#31226=FACE_OUTER_BOUND ( 'NONE', #29162, .T. ) ;
#31234=EDGE_CURVE ( 'NONE', #1652, #20764, #15807, .T. ) ;
#31250=CARTESIAN_POINT ( 'NONE',  ( 4.919044599153583164, -30.94480175767570884, 6.971170733404092879 ) ) ;
#31251=CARTESIAN_POINT ( 'NONE',  ( -0.7996099067669091287, -29.56993018339339940, -8.199999999999999289 ) ) ;
#31252=FACE_OUTER_BOUND ( 'NONE', #34158, .T. ) ;
#31255=CARTESIAN_POINT ( 'NONE',  ( -1.748756095191392523, -28.97546355617463121, 7.635761828346576685 ) ) ;
#31259=ADVANCED_FACE ( 'NONE', ( #12299 ), #38026, .T. ) ;
#31262=CARTESIAN_POINT ( 'NONE',  ( 5.008393135667492224, -30.35550703842281806, 6.997764925645181933 ) ) ;
#31266=EDGE_LOOP ( 'NONE', ( #6730, #9202, #4637, #29595 ) ) ;
#31270=CARTESIAN_POINT ( 'NONE',  ( 4.092117021882133443, -27.01461099462299131, 6.931070083220558509 ) ) ;
#31273=( BOUNDED_CURVE ( )  B_SPLINE_CURVE ( 3, ( #24436, #2649, #36995, #24644 ),
 .UNSPECIFIED., .F., .T. ) 
 B_SPLINE_CURVE_WITH_KNOTS ( ( 4, 4 ),
 ( 4.712388980384689674, 4.895802057644187855 ),
 .UNSPECIFIED. ) 
 CURVE ( )  GEOMETRIC_REPRESENTATION_ITEM ( )  RATIONAL_B_SPLINE_CURVE ( ( 1.000000000000000000, 0.9971986010846199955, 0.9971986010846199955, 1.000000000000000000 ) ) 
 REPRESENTATION_ITEM ( '' )  );
#31276=CARTESIAN_POINT ( 'NONE',  ( 1.128064129311358244, -33.02281926226938680, 7.695279973900954751 ) ) ;
#31280=CARTESIAN_POINT ( 'NONE',  ( 2.913938899263716742, -32.85281041678479141, 7.640616322432100205 ) ) ;
#31281=CARTESIAN_POINT ( 'NONE',  ( -2.512351830342552717, -31.78256350185187884, 6.894806418505347700 ) ) ;
#31284=EDGE_CURVE ( 'NONE', #9806, #14269, #18744, .T. ) ;
#31289=CARTESIAN_POINT ( 'NONE',  ( -1.506673198718692985, -28.44088410562211067, 7.692469944509197077 ) ) ;
#31294=EDGE_CURVE ( 'NONE', #38704, #12271, #28536, .T. ) ;
#31296=AXIS2_PLACEMENT_3D ( 'NONE', #12171, #5806, #14848 ) ;
#31298=CARTESIAN_POINT ( 'NONE',  ( 4.719422864845836507, -28.00610904475917806, 6.871394612369934762 ) ) ;
#31302=CARTESIAN_POINT ( 'NONE',  ( 0.5049572051612778445, -26.28386366117923245, 7.767720160662275219 ) ) ;
#31306=EDGE_CURVE ( 'NONE', #16841, #34783, #16954, .T. ) ;
#31313=ORIENTED_EDGE ( 'NONE', *, *, #17606, .T. ) ;
#31315=ORIENTED_EDGE ( 'NONE', *, *, #32486, .T. ) ;
#31317=EDGE_CURVE ( 'NONE', #36530, #26219, #17634, .T. ) ;
#31319=CARTESIAN_POINT ( 'NONE',  ( 5.143269691484856132, -28.97182734739054411, 7.773839561854633651 ) ) ;
#31321=VERTEX_POINT ( 'NONE', #27736 ) ;
#31326=CARTESIAN_POINT ( 'NONE',  ( 0.9943839796752991234, -25.86893018339336692, 6.954324564059724878 ) ) ;
#31341=CARTESIAN_POINT ( 'NONE',  ( 2.830618245060743554, -26.36328231767235764, 7.712764235869106422 ) ) ;
#31351=EDGE_CURVE ( 'NONE', #24034, #33766, #18678, .T. ) ;
#31354=CARTESIAN_POINT ( 'NONE',  ( 0.5370264050447969284, -32.87092774913090665, 7.700536657684211583 ) ) ;
#31356=CARTESIAN_POINT ( 'NONE',  ( 4.268313344242012697, -31.94811734417107019, 7.011627023500183853 ) ) ;
#31357=CARTESIAN_POINT ( 'NONE',  ( -1.699184788179541439, -29.51609423590135606, 6.889465824494257262 ) ) ;
#31361=AXIS2_PLACEMENT_3D ( 'NONE', #4674, #1208, #17209 ) ;
#31363=CARTESIAN_POINT ( 'NONE',  ( 1.512219044453454675, -33.06486818805116457, 6.980586498568970732 ) ) ;
#31364=AXIS2_PLACEMENT_3D ( 'NONE', #32281, #32083, #4081 ) ;
#31366=CARTESIAN_POINT ( 'NONE',  ( -0.6392939734488634063, -32.03688751340837371, 6.929923840112063083 ) ) ;
#31367=CARTESIAN_POINT ( 'NONE',  ( 5.189197560432777578, -29.24685097578066006, 7.566278858797852003 ) ) ;
#31370=CARTESIAN_POINT ( 'NONE',  ( -0.9766862336921242616, -31.66594123770981284, 7.761597726988848756 ) ) ;
#31375=CARTESIAN_POINT ( 'NONE',  ( -1.531881223433573025, -30.62464442689916666, 6.864276522220859711 ) ) ;
#31376=ORIENTED_EDGE ( 'NONE', *, *, #4554, .F. ) ;
#31379=CARTESIAN_POINT ( 'NONE',  ( 2.940766276717598160, -26.29708008006877407, 6.880608371227951103 ) ) ;
#31381=ORIENTED_EDGE ( 'NONE', *, *, #30293, .F. ) ;
#31382=CARTESIAN_POINT ( 'NONE',  ( -0.9416808278050282643, -27.29637960496864935, 7.785096263473211486 ) ) ;
#31383=DIRECTION ( 'NONE',  ( -3.491481338843133750E-15, 1.000000000000000000, -0.000000000000000000 ) ) ;
#31384=( BOUNDED_CURVE ( )  B_SPLINE_CURVE ( 3, ( #10661, #13961, #26528, #39062 ),
 .UNSPECIFIED., .F., .T. ) 
 B_SPLINE_CURVE_WITH_KNOTS ( ( 4, 4 ),
 ( 4.708531083176469068, 4.895802057644189631 ),
 .UNSPECIFIED. ) 
 CURVE ( )  GEOMETRIC_REPRESENTATION_ITEM ( )  RATIONAL_B_SPLINE_CURVE ( ( 1.000000000000000000, 0.9970795998553221295, 0.9970795998553221295, 1.000000000000000000 ) ) 
 REPRESENTATION_ITEM ( '' )  );
#31386=CARTESIAN_POINT ( 'NONE',  ( 4.891521542694104774, -30.74327958826899732, 7.775108481317163367 ) ) ;
#31387=DIRECTION ( 'NONE',  ( 0.7126435865141239612, 0.000000000000000000, 0.7015262779114451730 ) ) ;
#31392=VERTEX_POINT ( 'NONE', #8172 ) ;
#31395=CARTESIAN_POINT ( 'NONE',  ( -1.482122867364318530, -30.76642976786031980, 7.691066658568948000 ) ) ;
#31399=EDGE_CURVE ( 'NONE', #7610, #35491, #17393, .T. ) ;
#31400=CARTESIAN_POINT ( 'NONE',  ( 4.428520246153464512, -27.54081190378528277, 6.997764925645178380 ) ) ;
#31401=EDGE_CURVE ( 'NONE', #30749, #19738, #21881, .T. ) ;
#31403=CARTESIAN_POINT ( 'NONE',  ( 2.796830827761068949, -32.78830227222591986, 7.784476445165072533 ) ) ;
#31409=DIRECTION ( 'NONE',  ( -0.3420201433256601087, -0.9396926207859114255, -0.000000000000000000 ) ) ;
#31413=CARTESIAN_POINT ( 'NONE',  ( -1.560256750498681289, -30.53335229257609384, 6.959317978105168834 ) ) ;
#31414=CARTESIAN_POINT ( 'NONE',  ( 3.750629725403504366, -32.28222025834440245, 6.882085323592688653 ) ) ;
#31417=DIRECTION ( 'NONE',  ( 0.7660444431189857850, -0.6427876096865299260, -0.000000000000000000 ) ) ;
#31420=VECTOR ( 'NONE', #30266, 1000.000000000000000 ) ;
#31421=AXIS2_PLACEMENT_3D ( 'NONE', #34092, #33675, #36947 ) ;
#31422=CARTESIAN_POINT ( 'NONE',  ( 3.911174477942264804, -32.15303813520912257, 7.670860738520331346 ) ) ;
#31430=EDGE_CURVE ( 'NONE', #25231, #2110, #598, .T. ) ;
#31435=ORIENTED_EDGE ( 'NONE', *, *, #7592, .F. ) ;
#31441=EDGE_CURVE ( 'NONE', #5140, #6584, #8786, .T. ) ;
#31442=VECTOR ( 'NONE', #11168, 1000.000000000000000 ) ;
#31445=CARTESIAN_POINT ( 'NONE',  ( -1.727331447465891401, -28.92962485930595662, 7.783750581861600182 ) ) ;
#31449=ORIENTED_EDGE ( 'NONE', *, *, #31317, .T. ) ;
#31450=CARTESIAN_POINT ( 'NONE',  ( 0.05244770176878708196, -26.48311302728685490, 7.761113333116790081 ) ) ;
#31453=CARTESIAN_POINT ( 'NONE',  ( 5.654615132425274027, -32.90554535662791835, 7.635761828346577573 ) ) ;
#31456=ORIENTED_EDGE ( 'NONE', *, *, #30022, .F. ) ;
#31459=CARTESIAN_POINT ( 'NONE',  ( 4.954463893073100422, -28.58453498085037836, 7.013842709614101167 ) ) ;
#31462=CARTESIAN_POINT ( 'NONE',  ( 5.006040973414683570, -30.36534187942935148, 6.939395833800443114 ) ) ;
#31466=VERTEX_POINT ( 'NONE', #17848 ) ;
#31468=LINE ( 'NONE', #180, #5801 ) ;
#31469=ORIENTED_EDGE ( 'NONE', *, *, #6540, .F. ) ;
#31472=CARTESIAN_POINT ( 'NONE',  ( -1.624655799086301533, -28.85995144147929992, 7.754798119455333705 ) ) ;
#31473=CARTESIAN_POINT ( 'NONE',  ( 4.703888560603170177, -27.97650715214728123, 7.754798119455333705 ) ) ;
#31484=ORIENTED_EDGE ( 'NONE', *, *, #31399, .T. ) ;
#31485=EDGE_CURVE ( 'NONE', #18407, #33448, #28769, .T. ) ;
#31502=CARTESIAN_POINT ( 'NONE',  ( 0.5410499997217619317, -26.28128359000521641, 7.783750581861600182 ) ) ;
#31510=CARTESIAN_POINT ( 'NONE',  ( 1.075454873741154005, -26.12617409861640638, 7.750000000000000888 ) ) ;
#31513=VERTEX_POINT ( 'NONE', #34968 ) ;
#31514=DIRECTION ( 'NONE',  ( -0.000000000000000000, -0.000000000000000000, -1.000000000000000000 ) ) ;
#31520=ORIENTED_EDGE ( 'NONE', *, *, #4070, .T. ) ;
#31521=CYLINDRICAL_SURFACE ( 'NONE', #25690, 3.399999999999999911 ) ;
#31522=CARTESIAN_POINT ( 'NONE',  ( -1.278692756456701662, -31.20857796775482029, 7.784476445165072533 ) ) ;
#31523=EDGE_CURVE ( 'NONE', #32517, #13762, #22598, .T. ) ;
#31526=ORIENTED_EDGE ( 'NONE', *, *, #31222, .T. ) ;
#31528=CARTESIAN_POINT ( 'NONE',  ( -1.086373026989221113, -31.68746443619045650, 7.013842709614101167 ) ) ;
#31532=AXIS2_PLACEMENT_3D ( 'NONE', #13470, #934, #19457 ) ;
#31536=CARTESIAN_POINT ( 'NONE',  ( 4.959318750259752662, -28.60070809536833636, 6.920489980334478375 ) ) ;
#31537=B_SPLINE_CURVE_WITH_KNOTS ( 'NONE', 3,
 ( #14931, #36964, #20490, #5264, #32872, #36555, #4662, #17198, #36360, #39225, #20698, #30175, #30389, #5062, #8334, #23595, #17595, #29765, #1996, #2194, #27286, #39851, #28517, #40658, #28103, #37565, #21943, #12659, #15549, #21736, #9360 ),
 .UNSPECIFIED., .F., .F.,
 ( 4, 3, 3, 3, 3, 3, 3, 3, 3, 3, 4 ),
 ( 9.697399036122160616E-19, 2.999644130997777025E-05, 6.002588995694800887E-05, 8.960886084588142201E-05, 0.0001190604700446492420, 0.0001489538463052727504, 0.0001796139255493989120, 0.0002109707048517087591, 0.0002426195318110369015, 0.0002740640997890066719, 0.0002849778069099832270 ),
 .UNSPECIFIED. ) ;
#31549=CARTESIAN_POINT ( 'NONE',  ( 3.959546255067319276, -32.24317540230298107, 7.756742906098588186 ) ) ;
#31550=DIRECTION ( 'NONE',  ( -0.000000000000000000, -0.000000000000000000, -1.000000000000000000 ) ) ;
#31554=ORIENTED_EDGE ( 'NONE', *, *, #32842, .F. ) ;
#31562=CARTESIAN_POINT ( 'NONE',  ( -1.408800653676522074, -31.17709578999077280, 6.887547729233688187 ) ) ;
#31564=CARTESIAN_POINT ( 'NONE',  ( 1.523859786807980177, -33.06548219330246496, 6.903112506833891437 ) ) ;
#31566=CARTESIAN_POINT ( 'NONE',  ( 4.685027897762059190, -31.37120921750302571, 7.784725160561907664 ) ) ;
#31567=DIRECTION ( 'NONE',  ( 0.4999999999999980016, 0.8660254037844398178, -0.000000000000000000 ) ) ;
#31571=CARTESIAN_POINT ( 'NONE',  ( 4.862064339916653211, -31.08699507435702358, 7.501983001166817822 ) ) ;
#31572=CARTESIAN_POINT ( 'NONE',  ( -0.8833599345365857891, -31.77996090580433020, 7.721096864323906850 ) ) ;
#31574=CARTESIAN_POINT ( 'NONE',  ( 3.430328219694326108, -32.49692869527085293, 7.712764235869103757 ) ) ;
#31575=CARTESIAN_POINT ( 'NONE',  ( 2.167464131630131519, -32.93771148289538786, 6.863904403958576594 ) ) ;
#31576=ADVANCED_FACE ( 'NONE', ( #22201 ), #18669, .F. ) ;
#31578=CARTESIAN_POINT ( 'NONE',  ( -1.462749531912453271, -28.32311515628067511, 7.778050822775632867 ) ) ;
#31582=CARTESIAN_POINT ( 'NONE',  ( 6.107923577950775673, -31.97397320985677993, 7.754798119455333705 ) ) ;
#31585=EDGE_LOOP ( 'NONE', ( #3354, #3281, #5047, #16772, #702 ) ) ;
#31587=EDGE_CURVE ( 'NONE', #34426, #32530, #34532, .T. ) ;
#31590=CARTESIAN_POINT ( 'NONE',  ( 3.490246631599678739, -26.56219109107605547, 6.880608371227948439 ) ) ;
#31591=PLANE ( 'NONE',  #36994 ) ;
#31596=ORIENTED_EDGE ( 'NONE', *, *, #12055, .F. ) ;
#31601=CARTESIAN_POINT ( 'NONE',  ( -1.676158249790094645, -29.96863586080081632, 7.006423389747792108 ) ) ;
#31606=CARTESIAN_POINT ( 'NONE',  ( 2.825595610131681035, -32.77835769072562044, 7.784838882742139532 ) ) ;
#31607=ORIENTED_EDGE ( 'NONE', *, *, #39255, .F. ) ;
#31615=CARTESIAN_POINT ( 'NONE',  ( 1.640016842007158804, -32.96939412209556508, 7.785172627573962778 ) ) ;
#31618=DIRECTION ( 'NONE',  ( -1.000000000000000000, 0.000000000000000000, 0.000000000000000000 ) ) ;
#31620=CARTESIAN_POINT ( 'NONE',  ( 4.327887301732942227, -31.72776669797016424, 7.692469944509193525 ) ) ;
#31626=DIRECTION ( 'NONE',  ( 0.7660444431189840087, -0.6427876096865322575, 0.000000000000000000 ) ) ;
#31627=ORIENTED_EDGE ( 'NONE', *, *, #7347, .F. ) ;
#31632=CARTESIAN_POINT ( 'NONE',  ( 5.149536281657578485, -30.16439681061213918, 7.635761828346576685 ) ) ;
#31637=B_SPLINE_CURVE_WITH_KNOTS ( 'NONE', 3,
 ( #16689, #4374, #10522, #9925, #1289, #22901, #10324, #3577, #6843, #35469, #13218, #19401, #7241, #26395, #38519, #19804, #35071, #16497, #23296, #16896, #7039, #16105, #38925, #29276, #10717, #28870, #7437, #22507, #31761, #476, #880 ),
 .UNSPECIFIED., .F., .F.,
 ( 4, 3, 3, 3, 3, 3, 3, 3, 3, 3, 4 ),
 ( 2.032879073410320814E-19, 3.077658087706071046E-05, 6.152638666999271666E-05, 9.267501192707260018E-05, 0.0001241882240135244839, 0.0001556618703051763680, 0.0001866161554452290799, 0.0002167966385861025652, 0.0002463805737537836694, 0.0002758761370306578569, 0.0002847094172290117169 ),
 .UNSPECIFIED. ) ;
#31638=ORIENTED_EDGE ( 'NONE', *, *, #38903, .F. ) ;
#31641=DIRECTION ( 'NONE',  ( 0.9848077530122080203, 0.1736481776669307198, -0.000000000000000000 ) ) ;
#31642=ORIENTED_EDGE ( 'NONE', *, *, #24312, .T. ) ;
#31645=ORIENTED_EDGE ( 'NONE', *, *, #27265, .T. ) ;
#31646=CARTESIAN_POINT ( 'NONE',  ( 1.749140210850987920, -26.17027969752984973, 6.894806418505346812 ) ) ;
#31651=CARTESIAN_POINT ( 'NONE',  ( -1.342127135714882957, -31.08752830403540557, 6.979335674598002193 ) ) ;
#31652=ORIENTED_EDGE ( 'NONE', *, *, #11092, .F. ) ;
#31655=CYLINDRICAL_SURFACE ( 'NONE', #29779, 0.09010775117052882699 ) ;
#31657=CARTESIAN_POINT ( 'NONE',  ( 3.420189869592383580, -26.52160375395355629, 7.678495282201400762 ) ) ;
#31660=VERTEX_POINT ( 'NONE', #7738 ) ;
#31662=CARTESIAN_POINT ( 'NONE',  ( -1.024514293572082568, -31.60337457229856639, 6.903372536218459921 ) ) ;
#31663=DIRECTION ( 'NONE',  ( -0.9396926207859057634, -0.3420201433256757073, -0.000000000000000000 ) ) ;
#31666=CYLINDRICAL_SURFACE ( 'NONE', #24771, 0.09010775117052798044 ) ;
#31672=DIRECTION ( 'NONE',  ( 0.7660444431189770143, 0.6427876096865404731, -0.000000000000000000 ) ) ;
#31673=ORIENTED_EDGE ( 'NONE', *, *, #32503, .T. ) ;
#31674=CARTESIAN_POINT ( 'NONE',  ( 1.817877310917768607, -26.17195987680828750, 7.759451378593095860 ) ) ;
#31675=DIRECTION ( 'NONE',  ( 0.6502177225477844269, 0.3754033771448388457, -0.6605219282605403475 ) ) ;
#31676=CARTESIAN_POINT ( 'NONE',  ( 4.638438299886373350, -27.85881714212312588, 7.756377446753168314 ) ) ;
#31681=VERTEX_POINT ( 'NONE', #979 ) ;
#31686=DIRECTION ( 'NONE',  ( 0.000000000000000000, -0.6662082868431817850, 0.7457657263118712132 ) ) ;
#31691=VECTOR ( 'NONE', #33993, 1000.000000000000114 ) ;
#31692=ORIENTED_EDGE ( 'NONE', *, *, #336, .T. ) ;
#31700=CARTESIAN_POINT ( 'NONE',  ( 4.742723045254528813, -28.05196766440798939, 6.929923840112063971 ) ) ;
#31710=B_SPLINE_CURVE_WITH_KNOTS ( 'NONE', 3,
 ( #9840, #37618, #6562, #6957, #3694, #19108, #22216, #31676, #6760, #13319, #3296, #38235, #10032, #38431, #3900, #25492, #19717, #19311, #32292, #16217, #183, #4090, #22614, #22006, #31473 ),
 .UNSPECIFIED., .F., .F.,
 ( 4, 3, 3, 3, 3, 3, 3, 3, 4 ),
 ( 6.468151674593523946E-05, 9.076621574722267710E-05, 0.0001210204262067974651, 0.0001512763324577462215, 0.0001815301820994238426, 0.0002117781465860725217, 0.0002420274594459753432, 0.0002722905548971158969, 0.0002816827545175557522 ),
 .UNSPECIFIED. ) ;
#31716=B_SPLINE_CURVE_WITH_KNOTS ( 'NONE', 3,
 ( #8859, #18535, #24726, #2310, #2521, #9070, #27401, #8656, #40161, #36467 ),
 .UNSPECIFIED., .F., .F.,
 ( 4, 3, 3, 4 ),
 ( 0.0005050348086185288150, 0.0005143352185143272798, 0.0005445898203825178321, 0.0005634294782181692223 ),
 .UNSPECIFIED. ) ;
#31720=ADVANCED_FACE ( 'NONE', ( #32670 ), #1188, .F. ) ;
#31722=CARTESIAN_POINT ( 'NONE',  ( 5.100336825931343299, -29.54976608050401410, 7.643333865083955736 ) ) ;
#31724=CARTESIAN_POINT ( 'NONE',  ( 4.398201893633324033, -31.79968808245589429, 7.737115613922529889 ) ) ;
#31737=LINE ( 'NONE', #38098, #952 ) ;
#31738=CARTESIAN_POINT ( 'NONE',  ( 4.961196182289759449, -28.60704703087472112, 6.949473656533217358 ) ) ;
#31739=EDGE_LOOP ( 'NONE', ( #814, #35789, #19530, #25546 ) ) ;
#31745=EDGE_CURVE ( 'NONE', #36954, #5967, #5978, .T. ) ;
#31749=ORIENTED_EDGE ( 'NONE', *, *, #40163, .F. ) ;
#31756=AXIS2_PLACEMENT_3D ( 'NONE', #36944, #33049, #27071 ) ;
#31761=CARTESIAN_POINT ( 'NONE',  ( -0.1973417567568397646, -32.51078328414810414, 7.009310105710488514 ) ) ;
#31762=CARTESIAN_POINT ( 'NONE',  ( 2.737092283054774811, -32.91287029198328185, 7.013842709614101167 ) ) ;
#31766=CARTESIAN_POINT ( 'NONE',  ( -1.413520448806379726, -31.16791775245024354, 7.009310105710485850 ) ) ;
#31769=CARTESIAN_POINT ( 'NONE',  ( 4.740160921379847458, -31.30480577326951064, 7.750000000000000000 ) ) ;
#31775=CARTESIAN_POINT ( 'NONE',  ( 4.358324848093442228, -27.29278661098419079, 7.698786668945015066 ) ) ;
#31776=B_SPLINE_CURVE_WITH_KNOTS ( 'NONE', 3,
 ( #15021, #37856, #15637, #37047 ),
 .UNSPECIFIED., .F., .F.,
 ( 4, 4 ),
 ( 4.336808689942017736E-19, 6.391136169992664923E-06 ),
 .UNSPECIFIED. ) ;
#31777=CARTESIAN_POINT ( 'NONE',  ( 1.700390093233090871, -29.56993018339339940, 7.750000000000000888 ) ) ;
#31784=CARTESIAN_POINT ( 'NONE',  ( -2.772340841568255776, -28.07161080258395103, 7.754798119455333705 ) ) ;
#31789=CARTESIAN_POINT ( 'NONE',  ( -1.597345864091041623, -28.39734911814382201, 7.737115613922534330 ) ) ;
#31792=CARTESIAN_POINT ( 'NONE',  ( 3.605735085879740343, -26.63400187606387703, 6.912143950357348743 ) ) ;
#31793=CARTESIAN_POINT ( 'NONE',  ( 5.051944483554787091, -30.14184203736685674, 7.748216051605119503 ) ) ;
#31794=ORIENTED_EDGE ( 'NONE', *, *, #5627, .F. ) ;
#31798=AXIS2_PLACEMENT_3D ( 'NONE', #40303, #24883, #18686 ) ;
#31799=ORIENTED_EDGE ( 'NONE', *, *, #16501, .F. ) ;
#31801=ORIENTED_EDGE ( 'NONE', *, *, #28450, .T. ) ;
#31804=CARTESIAN_POINT ( 'NONE',  ( -1.661437721498786990, -30.07797914175773002, 6.870716933885664623 ) ) ;
#31810=CARTESIAN_POINT ( 'NONE',  ( -1.589597924990603817, -30.72125543040018769, 7.785096263473211486 ) ) ;
#31821=CARTESIAN_POINT ( 'NONE',  ( 1.735061201785046414, -32.96975431474913876, 7.712764235869103757 ) ) ;
#31826=DIRECTION ( 'NONE',  ( 1.000000000000000000, -0.000000000000000000, -0.000000000000000000 ) ) ;
#31828=DIRECTION ( 'NONE',  ( 0.000000000000000000, 0.000000000000000000, -1.000000000000000000 ) ) ;
#31829=VECTOR ( 'NONE', #15726, 1000.000000000000114 ) ;
#31832=CYLINDRICAL_SURFACE ( 'NONE', #23586, 0.09010775117053029803 ) ;
#31833=ORIENTED_EDGE ( 'NONE', *, *, #6530, .T. ) ;
#31842=CARTESIAN_POINT ( 'NONE',  ( 1.123288416806107026, -32.92059484209399045, 7.635761828346577573 ) ) ;
#31843=CARTESIAN_POINT ( 'NONE',  ( -1.766085975226569404, -30.05319374170961666, 7.750000000000000888 ) ) ;
#31845=CARTESIAN_POINT ( 'NONE',  ( 3.944592287501505368, -26.88591301102037434, 7.762796336881261361 ) ) ;
#31846=ORIENTED_EDGE ( 'NONE', *, *, #10083, .T. ) ;
#31847=VERTEX_POINT ( 'NONE', #2146 ) ;
#31849=CARTESIAN_POINT ( 'NONE',  ( -1.734658545019058140, -28.94585822693442978, 7.778495531946296282 ) ) ;
#31852=ORIENTED_EDGE ( 'NONE', *, *, #22474, .F. ) ;
#31854=CARTESIAN_POINT ( 'NONE',  ( -0.05419868157304204986, -26.54308200390424588, 7.762796336881261361 ) ) ;
#31856=DIRECTION ( 'NONE',  ( 0.1736481776669361321, -0.9848077530122070211, 0.000000000000000000 ) ) ;
#31861=EDGE_CURVE ( 'NONE', #11926, #29061, #5625, .T. ) ;
#31862=ORIENTED_EDGE ( 'NONE', *, *, #8343, .F. ) ;
#31863=EDGE_CURVE ( 'NONE', #12351, #39112, #13681, .T. ) ;
#31865=CARTESIAN_POINT ( 'NONE',  ( -1.755591130170437664, -30.12327797952368513, 6.875671892026062437 ) ) ;
#31866=CARTESIAN_POINT ( 'NONE',  ( -0.5477105494940386343, -32.24823869409008381, 7.767720160662275219 ) ) ;
#31868=ADVANCED_FACE ( 'NONE', ( #23739 ), #36709, .F. ) ;
#31870=CARTESIAN_POINT ( 'NONE',  ( 3.691161820386744008, -26.80493765813324103, 7.505001789837627335 ) ) ;
#31871=CARTESIAN_POINT ( 'NONE',  ( 5.133587308272485217, -30.25056153508439394, 6.867280401193709416 ) ) ;
#31874=( BOUNDED_CURVE ( )  B_SPLINE_CURVE ( 3, ( #28583, #28988, #38640, #1206 ),
 .UNSPECIFIED., .F., .T. ) 
 B_SPLINE_CURVE_WITH_KNOTS ( ( 4, 4 ),
 ( 4.708531083176467291, 4.895802057644188743 ),
 .UNSPECIFIED. ) 
 CURVE ( )  GEOMETRIC_REPRESENTATION_ITEM ( )  RATIONAL_B_SPLINE_CURVE ( ( 1.000000000000000000, 0.9970795998553221295, 0.9970795998553221295, 1.000000000000000000 ) ) 
 REPRESENTATION_ITEM ( '' )  );
#31876=ORIENTED_EDGE ( 'NONE', *, *, #27265, .F. ) ;
#31879=B_SPLINE_CURVE_WITH_KNOTS ( 'NONE', 3,
 ( #7832, #24078, #4951, #17478, #30070, #1882, #33582, #5359, #17897, #8633 ),
 .UNSPECIFIED., .F., .F.,
 ( 4, 3, 3, 4 ),
 ( 9.697399036122160616E-19, 3.025570593003099799E-05, 6.051145698343934779E-05, 6.468151674593381644E-05 ),
 .UNSPECIFIED. ) ;
#31880=CARTESIAN_POINT ( 'NONE',  ( 1.820100332811088739, -26.17203762333147310, 7.757178535559534183 ) ) ;
#31884=EDGE_LOOP ( 'NONE', ( #7321, #17476, #31846, #38912 ) ) ;
#31888=VECTOR ( 'NONE', #27744, 1000.000000000000000 ) ;
#31893=CARTESIAN_POINT ( 'NONE',  ( 2.931185808669444448, -32.84638282411071941, 7.695279973900954751 ) ) ;
#31896=CARTESIAN_POINT ( 'NONE',  ( -1.652919361092105577, -29.00839296038465065, 7.730758795053803034 ) ) ;
#31899=DIRECTION ( 'NONE',  ( 1.000000000000000000, -0.000000000000000000, -0.000000000000000000 ) ) ;
#31907=CARTESIAN_POINT ( 'NONE',  ( 4.737000972096239160, -28.04055306496577771, 6.903372536218456368 ) ) ;
#31916=AXIS2_PLACEMENT_3D ( 'NONE', #21029, #11940, #33185 ) ;
#31918=AXIS2_PLACEMENT_3D ( 'NONE', #21452, #5800, #27008 ) ;
#31920=EDGE_CURVE ( 'NONE', #31037, #35202, #20445, .T. ) ;
#31921=CARTESIAN_POINT ( 'NONE',  ( 1.905688531271448882, -26.06911211313256160, 7.387053503561885393 ) ) ;
#31923=AXIS2_PLACEMENT_3D ( 'NONE', #7705, #8502, #10981 ) ;
#31926=CARTESIAN_POINT ( 'NONE',  ( 2.737092283054774811, -32.91287029198328185, 7.013842709614101167 ) ) ;
#31932=CARTESIAN_POINT ( 'NONE',  ( 5.164678889462458677, -29.07712452480497589, 7.761113333117546809 ) ) ;
#31935=EDGE_LOOP ( 'NONE', ( #17081, #23591, #20249, #17101 ) ) ;
#31936=CARTESIAN_POINT ( 'NONE',  ( -1.237658113420181394, -31.28104322466368359, 7.756377446753165650 ) ) ;
#31939=ORIENTED_EDGE ( 'NONE', *, *, #8866, .T. ) ;
#31941=CARTESIAN_POINT ( 'NONE',  ( 1.590611208492059170, -33.06561673995959438, 7.766640943994648438 ) ) ;
#31942=ADVANCED_FACE ( 'NONE', ( #27445 ), #11370, .F. ) ;
#31946=B_SPLINE_CURVE_WITH_KNOTS ( 'NONE', 3,
 ( #23587, #39214, #11001, #30380 ),
 .UNSPECIFIED., .F., .F.,
 ( 4, 4 ),
 ( 0.000000000000000000, 6.391136169992754709E-06 ),
 .UNSPECIFIED. ) ;
#31949=CARTESIAN_POINT ( 'NONE',  ( -0.8675331577758178536, -27.19174302261571086, 7.011627023500183853 ) ) ;
#31950=ORIENTED_EDGE ( 'NONE', *, *, #30683, .T. ) ;
#31952=LINE ( 'NONE', #7224, #36378 ) ;
#31957=CARTESIAN_POINT ( 'NONE',  ( -0.7996099067669091287, -29.56993018339339940, 6.800000000000000711 ) ) ;
#31958=EDGE_CURVE ( 'NONE', #10407, #33823, #11808, .T. ) ;
#31960=ORIENTED_EDGE ( 'NONE', *, *, #26217, .T. ) ;
#31963=CARTESIAN_POINT ( 'NONE',  ( 2.492297145206303632, -26.16069239315658379, 6.925313231306332362 ) ) ;
#31964=CARTESIAN_POINT ( 'NONE',  ( 4.370302737341240196, -27.30684236520528785, 7.750000000000000000 ) ) ;
#31976=CARTESIAN_POINT ( 'NONE',  ( -1.699525402281838682, -29.59462277852799161, 7.740055089680398126 ) ) ;
#31977=CARTESIAN_POINT ( 'NONE',  ( 3.578431782309205111, -26.73568126667343847, 6.939395833800440450 ) ) ;
#31982=DIRECTION ( 'NONE',  ( -0.3420201433256601087, -0.9396926207859114255, -0.000000000000000000 ) ) ;
#31986=CARTESIAN_POINT ( 'NONE',  ( 4.358291535071521672, -27.29274773012506827, 7.695279973900954751 ) ) ;
#31987=FACE_OUTER_BOUND ( 'NONE', #8683, .T. ) ;
#31992=CARTESIAN_POINT ( 'NONE',  ( -1.487489740686422257, -28.38776406769778760, 7.779495906702012853 ) ) ;
#31994=DIRECTION ( 'NONE',  ( 0.000000000000000000, -0.6834397476448816899, -0.7300069255418748515 ) ) ;
#31996=ORIENTED_EDGE ( 'NONE', *, *, #15623, .T. ) ;
#31997=CARTESIAN_POINT ( 'NONE',  ( -0.9307968965437027897, -27.28455060704449053, 7.785593909369613819 ) ) ;
#32000=CARTESIAN_POINT ( 'NONE',  ( 5.013941773504689614, -28.44277561705024127, 6.867280401193707640 ) ) ;
#32002=EDGE_CURVE ( 'NONE', #30063, #35253, #4176, .T. ) ;
#32004=CARTESIAN_POINT ( 'NONE',  ( 1.185865733544545941, -26.10794094692920098, 6.863805608295730387 ) ) ;
#32010=CARTESIAN_POINT ( 'NONE',  ( -1.311841453708477045, -31.36551672632207399, 7.255881584735163869 ) ) ;
#32014=CARTESIAN_POINT ( 'NONE',  ( -1.712551861494080008, -28.79415494940930742, 7.011348038664006133 ) ) ;
#32022=DIRECTION ( 'NONE',  ( 0.1736481776669404897, -0.9848077530122062440, -0.000000000000000000 ) ) ;
#32025=ORIENTED_EDGE ( 'NONE', *, *, #17454, .T. ) ;
#32027=CARTESIAN_POINT ( 'NONE',  ( 4.401417849205680355, -27.34407100962124559, 6.894806418505347700 ) ) ;
#32037=CARTESIAN_POINT ( 'NONE',  ( -0.5627839327029573457, -26.90008998972287202, 7.640616322432102869 ) ) ;
#32043=CARTESIAN_POINT ( 'NONE',  ( 4.984179672459081445, -25.57221830738312107, 7.695279973900954751 ) ) ;
#32046=ORIENTED_EDGE ( 'NONE', *, *, #31401, .F. ) ;
#32056=CARTESIAN_POINT ( 'NONE',  ( 2.260952969954654446, -32.92340140904028800, 7.782167645815905033 ) ) ;
#32057=EDGE_CURVE ( 'NONE', #28636, #11806, #18998, .T. ) ;
#32059=VERTEX_POINT ( 'NONE', #28674 ) ;
#32064=CARTESIAN_POINT ( 'NONE',  ( -1.723525986837113777, -28.84815947364171151, 7.761113333116789192 ) ) ;
#32069=CARTESIAN_POINT ( 'NONE',  ( -0.5218218403989531851, -32.27395942177513888, 7.700536657684219577 ) ) ;
#32073=AXIS2_PLACEMENT_3D ( 'NONE', #38930, #4968, #29673 ) ;
#32075=ORIENTED_EDGE ( 'NONE', *, *, #7749, .F. ) ;
#32076=CARTESIAN_POINT ( 'NONE',  ( 5.200237804508150319, -29.53704989087483668, 7.720710062488890912 ) ) ;
#32078=ORIENTED_EDGE ( 'NONE', *, *, #35521, .F. ) ;
#32079=CARTESIAN_POINT ( 'NONE',  ( 2.325325312725053717, -33.01368626817038887, 7.750000000000001776 ) ) ;
#32082=PLANE ( 'NONE',  #34694 ) ;
#32083=DIRECTION ( 'NONE',  ( 0.9848077530122080203, 0.1736481776669307198, -0.000000000000000000 ) ) ;
#32087=CARTESIAN_POINT ( 'NONE',  ( -1.301617225954079693, -27.79589018266816680, 7.783750581861600182 ) ) ;
#32091=B_SPLINE_CURVE_WITH_KNOTS ( 'NONE', 3,
 ( #32490, #38847, #17215, #16817, #13939, #29786, #1601, #4290, #29396, #1214, #26312, #17014, #19919, #35395, #32299, #38244, #10840, #13749, #35782, #23416, #29591, #29194, #10641, #3911, #25701, #7761, #10045, #19727, #35980, #28996, #22626 ),
 .UNSPECIFIED., .F., .F.,
 ( 4, 3, 3, 3, 3, 3, 3, 3, 3, 3, 4 ),
 ( 2.453269466693398698E-18, 3.077658087705499807E-05, 6.152638666998692973E-05, 9.267501192706385880E-05, 0.0001241882240135157561, 0.0001556618703051645773, 0.0001866161554452180210, 0.0002167966385860964666, 0.0002463805737537765679, 0.0002758761370306512975, 0.0002847094172290078680 ),
 .UNSPECIFIED. ) ;
#32092=ORIENTED_EDGE ( 'NONE', *, *, #2506, .F. ) ;
#32095=CARTESIAN_POINT ( 'NONE',  ( -0.3330542956720734526, -26.84502579658822086, 6.903372536218457256 ) ) ;
#32100=AXIS2_PLACEMENT_3D ( 'NONE', #36116, #17545, #5420 ) ;
#32103=EDGE_CURVE ( 'NONE', #35810, #17652, #2050, .T. ) ;
#32106=CARTESIAN_POINT ( 'NONE',  ( 0.4869470754961160996, -26.28701135364670805, 7.750000000000001776 ) ) ;
#32109=ADVANCED_FACE ( 'NONE', ( #4967 ), #20594, .F. ) ;
#32112=VERTEX_POINT ( 'NONE', #39128 ) ;
#32117=CARTESIAN_POINT ( 'NONE',  ( 5.151971482861160467, -30.15011427130464483, 7.733670252284492008 ) ) ;
#32119=EDGE_LOOP ( 'NONE', ( #25164, #4812, #31022, #15820 ) ) ;
#32122=( BOUNDED_CURVE ( )  B_SPLINE_CURVE ( 3, ( #26650, #35925, #39386, #32836 ),
 .UNSPECIFIED., .F., .T. ) 
 B_SPLINE_CURVE_WITH_KNOTS ( ( 4, 4 ),
 ( 4.748221474220560623, 4.941946782021394924 ),
 .UNSPECIFIED. ) 
 CURVE ( )  GEOMETRIC_REPRESENTATION_ITEM ( )  RATIONAL_B_SPLINE_CURVE ( ( 1.000000000000000000, 0.9968749865767494445, 0.9968749865767494445, 1.000000000000000000 ) ) 
 REPRESENTATION_ITEM ( '' )  );
#32129=ORIENTED_EDGE ( 'NONE', *, *, #26681, .F. ) ;
#32133=ORIENTED_EDGE ( 'NONE', *, *, #18114, .T. ) ;
#32136=CARTESIAN_POINT ( 'NONE',  ( 1.128064129311358244, -33.02281926226938680, 7.695279973900954751 ) ) ;
#32140=CARTESIAN_POINT ( 'NONE',  ( 2.731683849345822424, -32.91454274520125267, 7.006908160621413195 ) ) ;
#32141=AXIS2_PLACEMENT_3D ( 'NONE', #4038, #18844, #6904 ) ;
#32148=ORIENTED_EDGE ( 'NONE', *, *, #22949, .F. ) ;
#32154=ORIENTED_EDGE ( 'NONE', *, *, #28790, .T. ) ;
#32156=DIRECTION ( 'NONE',  ( -0.4999999999999927836, -0.8660254037844429265, 0.000000000000000000 ) ) ;
#32161=EDGE_CURVE ( 'NONE', #6354, #2342, #36069, .T. ) ;
#32162=DIRECTION ( 'NONE',  ( 0.6427876096865379196, 0.7660444431189792347, -0.000000000000000000 ) ) ;
#32165=CARTESIAN_POINT ( 'NONE',  ( 3.817505324021141622, -32.35701164965254861, 6.895394898881671786 ) ) ;
#32166=ORIENTED_EDGE ( 'NONE', *, *, #18840, .T. ) ;
#32168=CARTESIAN_POINT ( 'NONE',  ( 2.938587699976823675, -26.40339382889528608, 7.782034975670474530 ) ) ;
#32171=CARTESIAN_POINT ( 'NONE',  ( -1.689549538493119174, -29.22836755717258228, 7.505001789837627335 ) ) ;
#32172=CARTESIAN_POINT ( 'NONE',  ( 4.376572504284961695, -27.31639088417337646, 7.762796336881261361 ) ) ;
#32173=FACE_OUTER_BOUND ( 'NONE', #32224, .T. ) ;
#32175=ORIENTED_EDGE ( 'NONE', *, *, #7526, .F. ) ;
#32176=CARTESIAN_POINT ( 'NONE',  ( 4.351715999300050264, -27.44141758656811092, 6.874555630061444766 ) ) ;
#32177=CARTESIAN_POINT ( 'NONE',  ( 1.735750141597346863, -26.08309558226786962, 7.783750581861601070 ) ) ;
#32179=CARTESIAN_POINT ( 'NONE',  ( -0.9146243593313261311, -25.28420110832643886, 7.754798119455333705 ) ) ;
#32181=CARTESIAN_POINT ( 'NONE',  ( 4.224974933773748553, -31.84731275619759927, 7.754798119455333705 ) ) ;
#32183=DIRECTION ( 'NONE',  ( 0.9396926207859112035, -0.3420201433256609413, 0.000000000000000000 ) ) ;
#32186=VERTEX_POINT ( 'NONE', #15395 ) ;
#32187=CARTESIAN_POINT ( 'NONE',  ( 0.7364210922827194583, -26.30944492956864877, 6.969307238440507035 ) ) ;
#32191=DIRECTION ( 'NONE',  ( -0.9848077530122091305, 0.1736481776669241417, -0.000000000000000000 ) ) ;
#32192=CARTESIAN_POINT ( 'NONE',  ( 3.421732255662511601, -32.50199707566237350, 7.740055089680399902 ) ) ;
#32193=CARTESIAN_POINT ( 'NONE',  ( 2.208439051597432812, -32.93175799812527771, 6.870716933885664623 ) ) ;
#32195=AXIS2_PLACEMENT_3D ( 'NONE', #17706, #2100, #27192 ) ;
#32196=EDGE_CURVE ( 'NONE', #22737, #2057, #11776, .T. ) ;
#32197=CARTESIAN_POINT ( 'NONE',  ( -1.456121751345974547, -28.30640807203716491, 7.768425012602593327 ) ) ;
#32198=ORIENTED_EDGE ( 'NONE', *, *, #27334, .T. ) ;
#32199=ORIENTED_EDGE ( 'NONE', *, *, #22001, .T. ) ;
#32200=FACE_OUTER_BOUND ( 'NONE', #5742, .T. ) ;
#32202=CARTESIAN_POINT ( 'NONE',  ( -1.339380734913657500, -27.83505459351727396, 7.750000000000002665 ) ) ;
#32203=ORIENTED_EDGE ( 'NONE', *, *, #29299, .T. ) ;
#32209=CARTESIAN_POINT ( 'NONE',  ( 1.198593767960137946, -26.20716339874380907, 7.778050822775631090 ) ) ;
#32210=CARTESIAN_POINT ( 'NONE',  ( 1.216825644920784377, -26.10348059021085376, 6.867199677474203234 ) ) ;
#32217=CARTESIAN_POINT ( 'NONE',  ( -1.709192382262307852, -28.77952057895107885, 6.985875436432904095 ) ) ;
#32220=ORIENTED_EDGE ( 'NONE', *, *, #15940, .T. ) ;
#32224=EDGE_LOOP ( 'NONE', ( #11682, #10378, #8638, #6028 ) ) ;
#32232=B_SPLINE_CURVE_WITH_KNOTS ( 'NONE', 3,
 ( #22090, #30952, #18563, #21474, #3179, #31149, #34257, #24758, #34456, #22299 ),
 .UNSPECIFIED., .F., .F.,
 ( 4, 3, 3, 4 ),
 ( 0.0002170292169044720702, 0.0002420761345915905356, 0.0002723302478206952697, 0.0002816811360866739822 ),
 .UNSPECIFIED. ) ;
#32238=DIRECTION ( 'NONE',  ( -0.7055275666422137215, -0.2567910337120389297, 0.6605219282605379050 ) ) ;
#32243=CARTESIAN_POINT ( 'NONE',  ( 3.472881818119431863, -32.58792320592009162, 7.737115613922532553 ) ) ;
#32244=B_SPLINE_CURVE_WITH_KNOTS ( 'NONE', 3,
 ( #3013, #2801, #40425, #25219, #12645, #9345, #15325, #38159, #40641, #6487 ),
 .UNSPECIFIED., .F., .F.,
 ( 4, 3, 3, 4 ),
 ( 0.0001585009270395785694, 0.0001815657551981846821, 0.0002118214035944131018, 0.0002170292169044822075 ),
 .UNSPECIFIED. ) ;
#32251=ORIENTED_EDGE ( 'NONE', *, *, #15845, .F. ) ;
#32260=CARTESIAN_POINT ( 'NONE',  ( 3.968771540420744870, -26.92158891409267696, 7.783750581861600182 ) ) ;
#32271=CARTESIAN_POINT ( 'NONE',  ( 3.757339589042690164, -26.85389010558039757, 7.139196562012272373 ) ) ;
#32275=CARTESIAN_POINT ( 'NONE',  ( 5.200346647029098435, -29.55249110255828882, 7.749999999999999112 ) ) ;
#32276=ORIENTED_EDGE ( 'NONE', *, *, #21391, .T. ) ;
#32281=CARTESIAN_POINT ( 'NONE',  ( -2.383717838810009759, -31.00696599979863066, 6.954324564059724878 ) ) ;
#32285=CARTESIAN_POINT ( 'NONE',  ( -1.321461783636408649, -27.81506318992830984, 7.773839561854630986 ) ) ;
#32286=CARTESIAN_POINT ( 'NONE',  ( 3.933165243051754523, -26.87461258339965298, 7.743886751744253338 ) ) ;
#32287=EDGE_CURVE ( 'NONE', #774, #12399, #31468, .T. ) ;
#32291=CARTESIAN_POINT ( 'NONE',  ( -0.3716677413943337838, -26.87427139008162058, 6.868387053540520704 ) ) ;
#32292=CARTESIAN_POINT ( 'NONE',  ( 4.688732775102122829, -27.94826190174027047, 7.778050822775631090 ) ) ;
#32293=FACE_OUTER_BOUND ( 'NONE', #4, .T. ) ;
#32299=CARTESIAN_POINT ( 'NONE',  ( -0.4222643637383041715, -26.78705640903759644, 6.887547729233686411 ) ) ;
#32300=EDGE_CURVE ( 'NONE', #21657, #1177, #18207, .T. ) ;
#32301=DIRECTION ( 'NONE',  ( 0.4826092789263541349, 0.5751513419797977811, -0.6605219282605403475 ) ) ;
#32302=CARTESIAN_POINT ( 'NONE',  ( 4.371499634827735292, -27.30825421931019648, 7.638132480492517473 ) ) ;
#32312=ORIENTED_EDGE ( 'NONE', *, *, #3716, .T. ) ;
#32316=CARTESIAN_POINT ( 'NONE',  ( 5.036944646152517358, -30.22373891335575635, 6.880147297696979969 ) ) ;
#32317=CARTESIAN_POINT ( 'NONE',  ( 4.559135941322734809, -31.41048459562103545, 6.876076431790004939 ) ) ;
#32319=CARTESIAN_POINT ( 'NONE',  ( 1.700390093233090871, -29.56993018339339940, 7.750000000000000888 ) ) ;
#32321=B_SPLINE_CURVE_WITH_KNOTS ( 'NONE', 3,
 ( #13026, #40613, #16116, #31572, #3397, #87, #12817, #38328, #34885, #22716, #18581, #9319, #2987, #6248, #37524, #12618, #28472, #15505, #12418, #28882, #3592, #31370, #19211, #22316, #6659 ),
 .UNSPECIFIED., .F., .F.,
 ( 4, 3, 3, 3, 3, 3, 3, 3, 4 ),
 ( 6.468151674593860048E-05, 9.076621574722655312E-05, 0.0001210204262068023304, 0.0001512763324577563588, 0.0001815301820994311068, 0.0002117781465860803008, 0.0002420274594459839897, 0.0002722905548971226190, 0.0002816827545175647511 ),
 .UNSPECIFIED. ) ;
#32325=ADVANCED_FACE ( 'NONE', ( #29578 ), #7151, .F. ) ;
#32326=ORIENTED_EDGE ( 'NONE', *, *, #20262, .T. ) ;
#32331=CARTESIAN_POINT ( 'NONE',  ( 0.4918310210129015481, -32.74788313599579936, 6.894806418505344148 ) ) ;
#32334=CARTESIAN_POINT ( 'NONE',  ( -1.796469343894664394, -29.56974349003418112, 7.767441775592068609 ) ) ;
#32336=EDGE_CURVE ( 'NONE', #36841, #18445, #36883, .T. ) ;
#32342=CARTESIAN_POINT ( 'NONE',  ( 5.166053052204034657, -29.08252373668924307, 7.754798119455333705 ) ) ;
#32349=VERTEX_POINT ( 'NONE', #16600 ) ;
#32351=CARTESIAN_POINT ( 'NONE',  ( 4.748301322462879170, -28.04738229536728156, 7.386948897581448570 ) ) ;
#32358=VERTEX_POINT ( 'NONE', #23010 ) ;
#32362=CARTESIAN_POINT ( 'NONE',  ( 4.460814650971867579, -27.41817363093848314, 7.750000000000000888 ) ) ;
#32365=CARTESIAN_POINT ( 'NONE',  ( -1.595110958568865422, -28.39108633556104522, 7.643192810543823157 ) ) ;
#32367=CARTESIAN_POINT ( 'NONE',  ( 2.881058359821971226, -26.27508231979332010, 7.750000000000000000 ) ) ;
#32371=CARTESIAN_POINT ( 'NONE',  ( 5.196299276553091318, -29.73910164073445017, 7.013842709614101167 ) ) ;
#32375=CARTESIAN_POINT ( 'NONE',  ( -0.9597769704937348934, -31.84446556299579001, 7.670465701733750308 ) ) ;
#32377=CARTESIAN_POINT ( 'NONE',  ( -1.699609906766908596, -29.56993018339339940, 7.767301406074262893 ) ) ;
#32378=CARTESIAN_POINT ( 'NONE',  ( 3.540944505460754232, -26.71118433530377345, 6.876076431790004939 ) ) ;
#32380=ADVANCED_FACE ( 'NONE', ( #35966 ), #19905, .F. ) ;
#32381=ADVANCED_FACE ( 'NONE', ( #1200 ), #38832, .F. ) ;
#32382=CARTESIAN_POINT ( 'NONE',  ( 4.733332635154806844, -31.31396321282658235, 7.762796336881264025 ) ) ;
#32384=CARTESIAN_POINT ( 'NONE',  ( 0.7375069407144074773, -26.30912409433673105, 6.949473656533218247 ) ) ;
#32388=CARTESIAN_POINT ( 'NONE',  ( 1.813491020413509069, -25.25237680967872578, 6.894806418505347700 ) ) ;
#32390=CARTESIAN_POINT ( 'NONE',  ( 3.299688604277355886, -32.57030420550657368, 7.761597726988850532 ) ) ;
#32393=CARTESIAN_POINT ( 'NONE',  ( -0.4574971862840269687, -32.19738569945798901, 7.691066658568940895 ) ) ;
#32394=DIRECTION ( 'NONE',  ( -0.9396926207859104263, 0.3420201433256631063, -0.000000000000000000 ) ) ;
#32395=ORIENTED_EDGE ( 'NONE', *, *, #31958, .F. ) ;
#32397=CARTESIAN_POINT ( 'NONE',  ( -2.340808619595282636, -26.33796619817592699, 7.754798119455333705 ) ) ;
#32399=CARTESIAN_POINT ( 'NONE',  ( 3.056873540704305725, -26.34348374009132243, 7.011627023500182965 ) ) ;
#32400=ORIENTED_EDGE ( 'NONE', *, *, #10235, .T. ) ;
#32401=DIRECTION ( 'NONE',  ( 1.000000000000000000, 0.000000000000000000, 0.000000000000000000 ) ) ;
#32402=DIRECTION ( 'NONE',  ( -0.7660444431189800119, -0.6427876096865369204, 0.000000000000000000 ) ) ;
#32404=CARTESIAN_POINT ( 'NONE',  ( 0.4707025585334126960, -26.29306066231216477, 7.678495282201402539 ) ) ;
#32405=CARTESIAN_POINT ( 'NONE',  ( 3.614139375300875923, -26.63947566482720219, 6.951256099901591767 ) ) ;
#32406=CARTESIAN_POINT ( 'NONE',  ( -1.744308430292528911, -30.22698574235089808, 7.255881584735163869 ) ) ;
#32411=VERTEX_POINT ( 'NONE', #19035 ) ;
#32414=CARTESIAN_POINT ( 'NONE',  ( -1.715256444303578709, -28.80609991944411163, 6.884455691889194817 ) ) ;
#32431=CARTESIAN_POINT ( 'NONE',  ( -1.094195156875065189, -31.67713398147757431, 6.912143950357348743 ) ) ;
#32432=CARTESIAN_POINT ( 'NONE',  ( 5.195729446393100304, -29.75058702122511889, 6.998987538705429223 ) ) ;
#32433=CARTESIAN_POINT ( 'NONE',  ( -0.8980191362577285563, -27.22509128144364610, 7.750000000000000888 ) ) ;
#32434=CARTESIAN_POINT ( 'NONE',  ( 2.538853852545528866, -32.87225273861094621, 7.505001789837629111 ) ) ;
#32436=FACE_OUTER_BOUND ( 'NONE', #424, .T. ) ;
#32438=VERTEX_POINT ( 'NONE', #6270 ) ;
#32449=CARTESIAN_POINT ( 'NONE',  ( 1.145807735209343869, -26.12896870525112192, 7.785344483711591934 ) ) ;
#32450=VERTEX_POINT ( 'NONE', #28288 ) ;
#32451=ORIENTED_EDGE ( 'NONE', *, *, #34523, .T. ) ;
#32452=VERTEX_POINT ( 'NONE', #34911 ) ;
#32456=CARTESIAN_POINT ( 'NONE',  ( 2.926619159346142141, -26.29176571567377607, 6.894806418505347700 ) ) ;
#32457=ORIENTED_EDGE ( 'NONE', *, *, #37374, .T. ) ;
#32461=CARTESIAN_POINT ( 'NONE',  ( 0.9044129672056784308, -32.97821799810775190, 6.965379264086542399 ) ) ;
#32462=CARTESIAN_POINT ( 'NONE',  ( 3.388683086819756163, -26.61871572696936994, 7.635761828346577573 ) ) ;
#32464=CARTESIAN_POINT ( 'NONE',  ( 3.402870446324275822, -26.62687723664940620, 7.769368695748491760 ) ) ;
#32467=CARTESIAN_POINT ( 'NONE',  ( -1.768673557917413319, -30.03425483734397972, 6.875780273367531059 ) ) ;
#32472=FACE_OUTER_BOUND ( 'NONE', #22483, .T. ) ;
#32477=CARTESIAN_POINT ( 'NONE',  ( -0.8809241381359119716, -31.78280542688255395, 7.692469944509201518 ) ) ;
#32482=CARTESIAN_POINT ( 'NONE',  ( 4.899153066642030652, -28.41754821824075705, 7.775108481317161591 ) ) ;
#32486=EDGE_CURVE ( 'NONE', #2342, #13356, #25852, .T. ) ;
#32490=CARTESIAN_POINT ( 'NONE',  ( -0.5254690805390769270, -26.86890242742082080, 6.894806418505347700 ) ) ;
#32492=CARTESIAN_POINT ( 'NONE',  ( -1.311566454172203189, -27.78718944202504915, 6.887161170156906209 ) ) ;
#32494=ORIENTED_EDGE ( 'NONE', *, *, #1832, .F. ) ;
#32495=CARTESIAN_POINT ( 'NONE',  ( 4.906207855869877399, -30.70250798326520680, 7.721096864323906850 ) ) ;
#32503=EDGE_CURVE ( 'NONE', #18803, #35245, #23199, .T. ) ;
#32505=EDGE_CURVE ( 'NONE', #24741, #20380, #27395, .T. ) ;
#32513=CARTESIAN_POINT ( 'NONE',  ( 6.041439283768642809, -29.54977971180056784, 7.013842709614101167 ) ) ;
#32514=CARTESIAN_POINT ( 'NONE',  ( 4.392721987511531978, -31.80629977964779442, 7.749999999999998224 ) ) ;
#32517=VERTEX_POINT ( 'NONE', #28496 ) ;
#32519=ORIENTED_EDGE ( 'NONE', *, *, #19424, .T. ) ;
#32520=CARTESIAN_POINT ( 'NONE',  ( 1.700390093233090871, -29.56993018339339940, 7.750000000000000888 ) ) ;
#32524=CARTESIAN_POINT ( 'NONE',  ( 1.115020328647592152, -33.02063188575903752, 7.742274884880761654 ) ) ;
#32527=CARTESIAN_POINT ( 'NONE',  ( -1.784512137809761700, -29.51577928193536593, 7.785387725071483800 ) ) ;
#32530=VERTEX_POINT ( 'NONE', #19641 ) ;
#32534=CARTESIAN_POINT ( 'NONE',  ( 5.077579250296520463, -29.17672728242957803, 6.997764925645182821 ) ) ;
#32537=CARTESIAN_POINT ( 'NONE',  ( 0.5564878831059402176, -32.77173156853538671, 7.643333865083955736 ) ) ;
#32539=CARTESIAN_POINT ( 'NONE',  ( -0.5115343435586707788, -26.98779995897780637, 7.712764235869101981 ) ) ;
#32540=AXIS2_PLACEMENT_3D ( 'NONE', #17056, #4533, #25948 ) ;
#32541=CARTESIAN_POINT ( 'NONE',  ( -1.642218429049665529, -30.19199791826050117, 7.721096864323902409 ) ) ;
#32542=CARTESIAN_POINT ( 'NONE',  ( 4.989036686621270533, -28.41059008988207424, 7.783750581861599294 ) ) ;
#32544=ORIENTED_EDGE ( 'NONE', *, *, #19112, .T. ) ;
#32546=CARTESIAN_POINT ( 'NONE',  ( -1.643142028458829396, -30.60472337334698878, 7.011627023500186517 ) ) ;
#32548=ADVANCED_FACE ( 'NONE', ( #6482 ), #16333, .T. ) ;
#32551=EDGE_CURVE ( 'NONE', #6774, #16841, #19297, .T. ) ;
#32552=CARTESIAN_POINT ( 'NONE',  ( 5.141357650781797517, -28.92980723922511288, 7.720710062488889136 ) ) ;
#32557=ORIENTED_EDGE ( 'NONE', *, *, #34344, .F. ) ;
#32559=EDGE_CURVE ( 'NONE', #4035, #23856, #1036, .T. ) ;
#32561=VECTOR ( 'NONE', #690, 1000.000000000000114 ) ;
#32562=VECTOR ( 'NONE', #23786, 1000.000000000000000 ) ;
#32563=EDGE_CURVE ( 'NONE', #30107, #26569, #34706, .T. ) ;
#32564=CARTESIAN_POINT ( 'NONE',  ( 3.855327937537480487, -32.32757912347058493, 7.754798119455333705 ) ) ;
#32567=VECTOR ( 'NONE', #35877, 1000.000000000000000 ) ;
#32568=CARTESIAN_POINT ( 'NONE',  ( 2.488040083129651414, -26.15970915046665723, 6.916197352289366052 ) ) ;
#32570=CYLINDRICAL_SURFACE ( 'NONE', #32981, 0.09010775117052928496 ) ;
#32574=VECTOR ( 'NONE', #26768, 1000.000000000000114 ) ;
#32575=DIRECTION ( 'NONE',  ( 0.8660254037844450359, -0.4999999999999888978, -0.000000000000000000 ) ) ;
#32579=CARTESIAN_POINT ( 'NONE',  ( 4.077682286559045188, -32.01059352804590219, 7.505001789837624671 ) ) ;
#32581=CARTESIAN_POINT ( 'NONE',  ( 4.746899557684813864, -27.84691535960167030, 6.894806418505347700 ) ) ;
#32583=CARTESIAN_POINT ( 'NONE',  ( 4.670958646267747483, -31.41922106168711082, 7.761113333116791857 ) ) ;
#32584=CARTESIAN_POINT ( 'NONE',  ( 0.7369679840504070878, -26.30928333966162569, 6.959317978105165281 ) ) ;
#32587=CARTESIAN_POINT ( 'NONE',  ( 1.021790419572949915, -32.90152176744273049, 7.778050822775632867 ) ) ;
#32588=CARTESIAN_POINT ( 'NONE',  ( 4.703510412144804143, -31.36750308876875337, 6.875671892026064214 ) ) ;
#32589=CARTESIAN_POINT ( 'NONE',  ( 5.153279172109078488, -30.14225614731512337, 7.695279973900954751 ) ) ;
#32590=CARTESIAN_POINT ( 'NONE',  ( -1.556861139293656660, -28.32973185486151735, 7.785344483711591934 ) ) ;
#32597=( BOUNDED_CURVE ( )  B_SPLINE_CURVE ( 3, ( #11850, #33514, #11641, #14132 ),
 .UNSPECIFIED., .F., .T. ) 
 B_SPLINE_CURVE_WITH_KNOTS ( ( 4, 4 ),
 ( 4.708531083176467291, 4.895802057644188743 ),
 .UNSPECIFIED. ) 
 CURVE ( )  GEOMETRIC_REPRESENTATION_ITEM ( )  RATIONAL_B_SPLINE_CURVE ( ( 1.000000000000000000, 0.9970795998553221295, 0.9970795998553221295, 1.000000000000000000 ) ) 
 REPRESENTATION_ITEM ( '' )  );
#32601=ORIENTED_EDGE ( 'NONE', *, *, #40, .F. ) ;
#32602=CARTESIAN_POINT ( 'NONE',  ( 4.978554560952730412, -30.79615924950642025, 6.894806418505347700 ) ) ;
#32605=CARTESIAN_POINT ( 'NONE',  ( 2.325611040346713398, -32.91195037927720790, 7.680992449362118002 ) ) ;
#32606=CARTESIAN_POINT ( 'NONE',  ( 3.610820004061922717, -26.63731061109791654, 6.980586498568969844 ) ) ;
#32614=EDGE_CURVE ( 'NONE', #27830, #2431, #6924, .T. ) ;
#32615=CARTESIAN_POINT ( 'NONE',  ( -0.02141235007780225783, -32.61712501572831968, 7.670465701733753860 ) ) ;
#32619=CARTESIAN_POINT ( 'NONE',  ( -1.711148526671566250, -28.78798112472082238, 7.003794266797748413 ) ) ;
#32628=ORIENTED_EDGE ( 'NONE', *, *, #35988, .T. ) ;
#32634=CARTESIAN_POINT ( 'NONE',  ( 0.9904113513190105911, -32.89497607571279758, 7.754798119455333705 ) ) ;
#32638=DIRECTION ( 'NONE',  ( 0.9396926207859126468, -0.3420201433256568335, -0.000000000000000000 ) ) ;
#32639=CARTESIAN_POINT ( 'NONE',  ( 5.108657383620684556, -30.36599178733747095, 6.951256099901588215 ) ) ;
#32642=CARTESIAN_POINT ( 'NONE',  ( 5.094538413962854229, -29.76940238803287286, 6.911401339314959813 ) ) ;
#32643=CARTESIAN_POINT ( 'NONE',  ( 1.875215828509756655, -26.07429920139816559, 7.006908160621413195 ) ) ;
#32644=ORIENTED_EDGE ( 'NONE', *, *, #26327, .T. ) ;
#32649=CARTESIAN_POINT ( 'NONE',  ( -1.506684114051581647, -28.44091511309124343, 7.695279973900954751 ) ) ;
#32654=CARTESIAN_POINT ( 'NONE',  ( 2.933187319672341253, -26.30959554060986605, 7.785096263473211486 ) ) ;
#32659=EDGE_CURVE ( 'NONE', #3202, #3667, #1928, .T. ) ;
#32660=VERTEX_POINT ( 'NONE', #27021 ) ;
#32664=CARTESIAN_POINT ( 'NONE',  ( 2.748053412748273860, -32.80449376584813592, 7.754798119455333705 ) ) ;
#32666=CARTESIAN_POINT ( 'NONE',  ( 3.972262043637318385, -27.04038519645078864, 6.864276522220859711 ) ) ;
#32670=FACE_OUTER_BOUND ( 'NONE', #37055, .T. ) ;
#32671=CARTESIAN_POINT ( 'NONE',  ( 5.046365345827218185, -28.96623356337001809, 7.635761828346577573 ) ) ;
#32673=CARTESIAN_POINT ( 'NONE',  ( 4.713340623123058570, -27.78888299018493058, 7.697032948437506406 ) ) ;
#32674=DIRECTION ( 'NONE',  ( -1.000000000000000000, 0.000000000000000000, 0.000000000000000000 ) ) ;
#32677=CARTESIAN_POINT ( 'NONE',  ( 3.888061725287626391, -26.96722143474251610, 7.769368695748485543 ) ) ;
#32678=CARTESIAN_POINT ( 'NONE',  ( -0.8911589727531790128, -31.77082041573498472, 7.643333865083956624 ) ) ;
#32679=CARTESIAN_POINT ( 'NONE',  ( 3.922483456672745561, -26.86580350659783178, 7.697032948437509070 ) ) ;
#32682=CIRCLE ( 'NONE', #37276, 3.499999999999999556 ) ;
#32683=VECTOR ( 'NONE', #13132, 1000.000000000000227 ) ;
#32684=CARTESIAN_POINT ( 'NONE',  ( 3.970022674624412051, -32.23428315255819854, 7.737115613922534330 ) ) ;
#32687=DIRECTION ( 'NONE',  ( 1.000000000000000000, -8.921435019309294079E-15, 0.000000000000000000 ) ) ;
#32695=CARTESIAN_POINT ( 'NONE',  ( -1.242285469042155643, -27.67502635069157435, 6.895394898881668233 ) ) ;
#32697=ORIENTED_EDGE ( 'NONE', *, *, #26380, .F. ) ;
#32707=( BOUNDED_CURVE ( )  B_SPLINE_CURVE ( 3, ( #29046, #12776, #32351, #9695 ),
 .UNSPECIFIED., .F., .T. ) 
 B_SPLINE_CURVE_WITH_KNOTS ( ( 4, 4 ),
 ( 1.381924640371167579, 1.574767692156077148 ),
 .UNSPECIFIED. ) 
 CURVE ( )  GEOMETRIC_REPRESENTATION_ITEM ( )  RATIONAL_B_SPLINE_CURVE ( ( 1.000000000000000000, 0.9969033633783032089, 0.9969033633783032089, 1.000000000000000000 ) ) 
 REPRESENTATION_ITEM ( '' )  );
#32712=EDGE_LOOP ( 'NONE', ( #22189, #18330, #25064, #1872, #28162 ) ) ;
#32714=CARTESIAN_POINT ( 'NONE',  ( 5.031298139653363144, -30.25194762213318356, 6.866852738645442322 ) ) ;
#32722=VERTEX_POINT ( 'NONE', #15067 ) ;
#32726=CARTESIAN_POINT ( 'NONE',  ( 1.126087027002167451, -33.02249097042057713, 7.714178352335856026 ) ) ;
#32729=CARTESIAN_POINT ( 'NONE',  ( -0.5046456199209383708, -26.98191322245490298, 7.652160403243381204 ) ) ;
#32741=CARTESIAN_POINT ( 'NONE',  ( -0.5125101069461969194, -26.98863734761392053, 7.695279973900954751 ) ) ;
#32742=CIRCLE ( 'NONE', #15654, 3.499999999999999556 ) ;
#32747=CARTESIAN_POINT ( 'NONE',  ( -1.139292474411453204, -27.70010802646186576, 6.911401339314956260 ) ) ;
#32751=CARTESIAN_POINT ( 'NONE',  ( -0.5226183895603513374, -32.27330558770101021, 7.678495282201406980 ) ) ;
#32754=ORIENTED_EDGE ( 'NONE', *, *, #40384, .T. ) ;
#32755=LINE ( 'NONE', #4352, #4299 ) ;
#32756=EDGE_CURVE ( 'NONE', #37348, #40076, #1533, .T. ) ;
#32757=AXIS2_PLACEMENT_3D ( 'NONE', #16785, #19498, #4467 ) ;
#32761=CARTESIAN_POINT ( 'NONE',  ( 4.301456835768374454, -27.38029081488210181, 7.763628509615287498 ) ) ;
#32766=DIRECTION ( 'NONE',  ( -0.3420201433256725987, 0.9396926207859068736, -0.000000000000000000 ) ) ;
#32767=ORIENTED_EDGE ( 'NONE', *, *, #5175, .T. ) ;
#32773=LINE ( 'NONE', #14412, #36575 ) ;
#32774=EDGE_CURVE ( 'NONE', #22827, #31513, #25243, .T. ) ;
#32777=CARTESIAN_POINT ( 'NONE',  ( -1.261861663380802412, -27.90107892266405898, 7.691066658568947112 ) ) ;
#32783=CARTESIAN_POINT ( 'NONE',  ( 3.489554929392924887, -26.67873662699589588, 6.864651958020304257 ) ) ;
#32786=CARTESIAN_POINT ( 'NONE',  ( -0.5260552471568549215, -32.13955055026278274, 6.889465824494256374 ) ) ;
#32787=CARTESIAN_POINT ( 'NONE',  ( 0.1138761091961189020, -26.45015881701811011, 6.921725064902953584 ) ) ;
#32790=CARTESIAN_POINT ( 'NONE',  ( -1.645585159361036220, -30.17362680341680203, 7.635761828346577573 ) ) ;
#32792=EDGE_CURVE ( 'NONE', #2057, #19833, #30941, .T. ) ;
#32794=CARTESIAN_POINT ( 'NONE',  ( 4.320748559849963755, -31.73643811260259184, 7.740055089680397238 ) ) ;
#32797=DIRECTION ( 'NONE',  ( -0.7541618601367592323, 0.000000000000000000, 0.6566885781822789925 ) ) ;
#32799=AXIS2_PLACEMENT_3D ( 'NONE', #11975, #37107, #27837 ) ;
#32800=CARTESIAN_POINT ( 'NONE',  ( 3.060248756071702214, -26.34490546765821861, 7.006908160621411419 ) ) ;
#32803=DIRECTION ( 'NONE',  ( 0.3420201433256748746, -0.9396926207859060964, 0.000000000000000000 ) ) ;
#32805=CARTESIAN_POINT ( 'NONE',  ( 2.326139153815881322, -32.91185150465383202, 7.692469944509197965 ) ) ;
#32806=CARTESIAN_POINT ( 'NONE',  ( -1.471942004329455544, -28.34666765933866728, 6.880147297696980857 ) ) ;
#32808=CARTESIAN_POINT ( 'NONE',  ( -1.699608699875451379, -29.56706542154453388, 7.769368695748485543 ) ) ;
#32809=ORIENTED_EDGE ( 'NONE', *, *, #15044, .F. ) ;
#32811=CARTESIAN_POINT ( 'NONE',  ( -1.741284284048380426, -30.20623001897737581, 7.730015791551952731 ) ) ;
#32813=B_SPLINE_CURVE_WITH_KNOTS ( 'NONE', 3,
 ( #23298, #16499, #17098, #25581, #25989, #38126, #9928, #22510, #35074, #19404, #38523, #31976, #35471, #19806, #22903, #32377 ),
 .UNSPECIFIED., .F., .F.,
 ( 4, 3, 3, 3, 3, 4 ),
 ( 0.000000000000000000, 3.025570593002918873E-05, 6.051145698343720649E-05, 9.076621574721710701E-05, 0.0001210204262067937652, 0.0001477827378591783816 ),
 .UNSPECIFIED. ) ;
#32821=DIRECTION ( 'NONE',  ( -1.000000000000000000, -0.000000000000000000, -0.000000000000000000 ) ) ;
#32830=AXIS2_PLACEMENT_3D ( 'NONE', #19267, #29142, #13084 ) ;
#32831=DIRECTION ( 'NONE',  ( 0.9396926207859126468, -0.3420201433256568335, -0.000000000000000000 ) ) ;
#32832=CARTESIAN_POINT ( 'NONE',  ( -1.323924960262854666, -31.33161076090960151, 7.635761828346577573 ) ) ;
#32836=CARTESIAN_POINT ( 'NONE',  ( 3.235878913814441038, -32.60345520914638939, 7.013842709614101167 ) ) ;
#32837=CARTESIAN_POINT ( 'NONE',  ( 5.111256656961197464, -30.35480174692847655, 6.998987538705433664 ) ) ;
#32839=CARTESIAN_POINT ( 'NONE',  ( 2.699327306250907110, -32.81987240510260762, 6.882085323592685100 ) ) ;
#32841=CARTESIAN_POINT ( 'NONE',  ( 1.863139223285963597, -26.07370920805947279, 6.887547729233689076 ) ) ;
#32842=EDGE_CURVE ( 'NONE', #28994, #37415, #3526, .T. ) ;
#32844=VERTEX_POINT ( 'NONE', #19593 ) ;
#32848=ORIENTED_EDGE ( 'NONE', *, *, #33013, .T. ) ;
#32849=CARTESIAN_POINT ( 'NONE',  ( 0.1708817620810553495, -26.53337799465926494, 7.006423389747790331 ) ) ;
#32850=CARTESIAN_POINT ( 'NONE',  ( -1.250824363190944588, -27.88163718980674233, 7.635761828346577573 ) ) ;
#32853=CARTESIAN_POINT ( 'NONE',  ( 2.303438722708047059, -32.91602753032043438, 7.756377446753163873 ) ) ;
#32864=AXIS2_PLACEMENT_3D ( 'NONE', #70, #35665, #7433 ) ;
#32872=CARTESIAN_POINT ( 'NONE',  ( 1.493410003970609523, -32.96362645543517544, 6.979335674598003969 ) ) ;
#32873=DIRECTION ( 'NONE',  ( -0.5000000000000039968, 0.8660254037844362651, -0.000000000000000000 ) ) ;
#32876=CARTESIAN_POINT ( 'NONE',  ( 3.908975219192432515, -26.98494435337591923, 7.782167645815903256 ) ) ;
#32877=CARTESIAN_POINT ( 'NONE',  ( -1.391086531092725398, -31.21089766107228414, 7.751599049952174525 ) ) ;
#32879=CARTESIAN_POINT ( 'NONE',  ( 0.5828135686266351367, -26.25315121703935972, 6.865554069792297653 ) ) ;
#32882=CARTESIAN_POINT ( 'NONE',  ( 4.489505707918894473, -27.45549474512610644, 7.009310105710486738 ) ) ;
#32885=CARTESIAN_POINT ( 'NONE',  ( 5.112373171067981836, -30.38002035509909149, 7.387053503561887169 ) ) ;
#32886=CARTESIAN_POINT ( 'NONE',  ( 4.268193593992276824, -31.79846898303070191, 6.887041543973309032 ) ) ;
#32895=CARTESIAN_POINT ( 'NONE',  ( -1.307348999084261276, -27.78007364502682464, 6.880608371227948439 ) ) ;
#32896=CARTESIAN_POINT ( 'NONE',  ( 2.296057149099136829, -26.12098725511343389, 7.756742906098588186 ) ) ;
#32900=ORIENTED_EDGE ( 'NONE', *, *, #5381, .F. ) ;
#32906=CARTESIAN_POINT ( 'NONE',  ( -0.7753363873652329152, -27.23952712957111544, 6.903372536218459032 ) ) ;
#32907=EDGE_LOOP ( 'NONE', ( #13515, #33343, #36120, #17622 ) ) ;
#32919=ORIENTED_EDGE ( 'NONE', *, *, #11321, .T. ) ;
#32920=CARTESIAN_POINT ( 'NONE',  ( 0.3430336670258780640, -32.68723412389003613, 6.969307238440504371 ) ) ;
#32923=DIRECTION ( 'NONE',  ( -1.000000000000000000, 0.000000000000000000, 0.000000000000000000 ) ) ;
#32927=CARTESIAN_POINT ( 'NONE',  ( -1.237321756456247979, -31.28161037787917209, 7.635761828346577573 ) ) ;
#32930=EDGE_CURVE ( 'NONE', #32438, #39701, #4457, .T. ) ;
#32934=CARTESIAN_POINT ( 'NONE',  ( 3.916835083226508640, -26.85238689360580011, 7.255881584735162093 ) ) ;
#32938=CARTESIAN_POINT ( 'NONE',  ( 3.431434570054125111, -32.49627346798381211, 7.693875151218753317 ) ) ;
#32943=( BOUNDED_CURVE ( )  B_SPLINE_CURVE ( 3, ( #11227, #23995, #2422, #11840 ),
 .UNSPECIFIED., .F., .T. ) 
 B_SPLINE_CURVE_WITH_KNOTS ( ( 4, 4 ),
 ( 4.748221474220561511, 4.941946782021395812 ),
 .UNSPECIFIED. ) 
 CURVE ( )  GEOMETRIC_REPRESENTATION_ITEM ( )  RATIONAL_B_SPLINE_CURVE ( ( 1.000000000000000000, 0.9968749865767494445, 0.9968749865767494445, 1.000000000000000000 ) ) 
 REPRESENTATION_ITEM ( '' )  );
#32944=CARTESIAN_POINT ( 'NONE',  ( -0.5390062018526512455, -32.25974509032589310, 7.635761828346574021 ) ) ;
#32950=CARTESIAN_POINT ( 'NONE',  ( 5.140800898748325132, -28.92683337905274854, 7.698786668945011513 ) ) ;
#32954=CARTESIAN_POINT ( 'NONE',  ( 4.797166834205789598, -27.93896158646020211, 6.870724624169667116 ) ) ;
#32958=CARTESIAN_POINT ( 'NONE',  ( -1.321941654078521378, -31.33501114731328130, 7.749999999999999112 ) ) ;
#32960=CARTESIAN_POINT ( 'NONE',  ( -0.01583764436594936598, -26.63487271330943784, 7.748216051605115950 ) ) ;
#32969=FACE_OUTER_BOUND ( 'NONE', #20860, .T. ) ;
#32977=CARTESIAN_POINT ( 'NONE',  ( 3.516368447621620597, -26.69550461626186078, 6.865312560952602894 ) ) ;
#32979=CARTESIAN_POINT ( 'NONE',  ( -0.5281487064042170720, -32.13773368415257892, 6.887041543973312585 ) ) ;
#32980=CARTESIAN_POINT ( 'NONE',  ( 0.1039781302203472563, -26.45521208309125427, 7.006908160621415860 ) ) ;
#32981=AXIS2_PLACEMENT_3D ( 'NONE', #29862, #1079, #14207 ) ;
#32993=EDGE_CURVE ( 'NONE', #12399, #21663, #16665, .T. ) ;
#32994=CARTESIAN_POINT ( 'NONE',  ( 3.024292301338818323, -26.32996603374844824, 6.870724624169665340 ) ) ;
#32997=EDGE_CURVE ( 'NONE', #25861, #31660, #9313, .T. ) ;
#32998=CARTESIAN_POINT ( 'NONE',  ( 3.791157483716739218, -32.25110375459131973, 7.754798119455333705 ) ) ;
#33000=CARTESIAN_POINT ( 'NONE',  ( 0.9076429196643266417, -32.87621993457957359, 6.929923840112063971 ) ) ;
#33001=CARTESIAN_POINT ( 'NONE',  ( 3.613844859187792746, -26.63928332947567057, 6.941203072598477242 ) ) ;
#33002=CARTESIAN_POINT ( 'NONE',  ( -1.699609515697033890, -29.56803366691413970, 7.768698451128750904 ) ) ;
#33003=EDGE_LOOP ( 'NONE', ( #38447, #21362, #9756, #11934 ) ) ;
#33008=ORIENTED_EDGE ( 'NONE', *, *, #40270, .F. ) ;
#33013=EDGE_CURVE ( 'NONE', #13756, #39610, #24564, .T. ) ;
#33017=EDGE_CURVE ( 'NONE', #35820, #38408, #25974, .T. ) ;
#33022=CARTESIAN_POINT ( 'NONE',  ( -1.323924960262854666, -31.33161076090960151, 7.635761828346577573 ) ) ;
#33030=FACE_OUTER_BOUND ( 'NONE', #33003, .T. ) ;
#33034=CARTESIAN_POINT ( 'NONE',  ( 2.187796539937281182, -33.03559314236433408, 7.754798119455333705 ) ) ;
#33035=CARTESIAN_POINT ( 'NONE',  ( 1.815759002417408396, -26.07183212662117455, 6.865482280155368322 ) ) ;
#33037=CARTESIAN_POINT ( 'NONE',  ( 2.155604402987680857, -33.04021322912456782, 6.880828092187096345 ) ) ;
#33038=ORIENTED_EDGE ( 'NONE', *, *, #6530, .F. ) ;
#33042=ORIENTED_EDGE ( 'NONE', *, *, #13156, .T. ) ;
#33044=CARTESIAN_POINT ( 'NONE',  ( -0.6943239642360979902, -27.00805212371037456, 7.139344958878412584 ) ) ;
#33046=CARTESIAN_POINT ( 'NONE',  ( -0.9190822194230292563, -27.24862244995199845, 6.863805608295730387 ) ) ;
#33049=DIRECTION ( 'NONE',  ( 0.1303762246624279586, -0.7394003126383905666, -0.6605219282605403475 ) ) ;
#33054=EDGE_CURVE ( 'NONE', #2740, #1123, #20104, .T. ) ;
#33060=CARTESIAN_POINT ( 'NONE',  ( 0.6310675123731709357, -26.34244895293124600, 7.774064877406527962 ) ) ;
#33063=B_SPLINE_CURVE_WITH_KNOTS ( 'NONE', 3,
 ( #17704, #8439, #2922, #30706, #33598, #30283, #5371, #5575, #5782, #27795, #31110, #34218, #17911, #18320, #30491, #40347, #28003, #24717, #2301, #5987, #18115, #24509, #40545, #2513, #15036, #27597, #6801, #32140, #19354, #10279, #31926 ),
 .UNSPECIFIED., .F., .F.,
 ( 4, 3, 3, 3, 3, 3, 3, 3, 3, 3, 4 ),
 ( 9.697399036122160616E-19, 3.077658087705627201E-05, 6.152638666999302836E-05, 9.267501192706609496E-05, 0.0001241882240135191171, 0.0001556618703051675860, 0.0001866161554452220326, 0.0002167966385860974152, 0.0002463805737537785195, 0.0002758761370306537369, 0.0002847094172290068922 ),
 .UNSPECIFIED. ) ;
#33069=VECTOR ( 'NONE', #33475, 1000.000000000000000 ) ;
#33072=CARTESIAN_POINT ( 'NONE',  ( 1.259933197038312302, -26.09775540055275656, 7.013842709614101167 ) ) ;
#33075=DIRECTION ( 'NONE',  ( -0.4999999999999918954, -0.8660254037844432595, -0.000000000000000000 ) ) ;
#33080=CARTESIAN_POINT ( 'NONE',  ( 1.119761070567095285, -33.02143436011441935, 7.655937882338900380 ) ) ;
#33084=B_SPLINE_CURVE_WITH_KNOTS ( 'NONE', 3,
 ( #31162, #3785, #6854, #15908, #12612, #28676, #9312, #3585, #28258, #27847 ),
 .UNSPECIFIED., .F., .F.,
 ( 4, 3, 3, 4 ),
 ( 0.0005050348086185285981, 0.0005143352185143270630, 0.0005445898203825176153, 0.0005634294782181690055 ),
 .UNSPECIFIED. ) ;
#33085=VERTEX_POINT ( 'NONE', #1274 ) ;
#33091=CARTESIAN_POINT ( 'NONE',  ( -1.619634369087763481, -28.83682884688450798, 6.868387053540521592 ) ) ;
#33096=ORIENTED_EDGE ( 'NONE', *, *, #34724, .F. ) ;
#33097=DIRECTION ( 'NONE',  ( 0.6427876096865425826, -0.7660444431189752379, 0.000000000000000000 ) ) ;
#33098=EDGE_LOOP ( 'NONE', ( #2145, #3327, #15828, #29794 ) ) ;
#33101=CARTESIAN_POINT ( 'NONE',  ( -1.531156124662372608, -28.22562180236089802, 6.883550009118464708 ) ) ;
#33104=CARTESIAN_POINT ( 'NONE',  ( 4.787207249339009429, -27.92198779192843716, 7.761113333117551250 ) ) ;
#33118=CARTESIAN_POINT ( 'NONE',  ( 2.343486897573773486, -33.01034098890863078, 7.698786668945011513 ) ) ;
#33122=CARTESIAN_POINT ( 'NONE',  ( 2.896448246037522267, -32.75260910491768840, 7.680992449362118002 ) ) ;
#33123=CARTESIAN_POINT ( 'NONE',  ( 5.100040579096636328, -29.61868030101130245, 6.894806418505348589 ) ) ;
#33126=CARTESIAN_POINT ( 'NONE',  ( 2.779598305578060646, -32.89939134339510929, 7.751599049952173637 ) ) ;
#33128=CYLINDRICAL_SURFACE ( 'NONE', #20742, 3.399999999999999911 ) ;
#33129=ORIENTED_EDGE ( 'NONE', *, *, #10557, .F. ) ;
#33137=CARTESIAN_POINT ( 'NONE',  ( 2.813604351667470027, -32.87737832280624417, 7.780491323090170219 ) ) ;
#33138=CARTESIAN_POINT ( 'NONE',  ( -1.654684078475540998, -30.12090371034253167, 7.784838882742139532 ) ) ;
#33141=ORIENTED_EDGE ( 'NONE', *, *, #4450, .F. ) ;
#33144=CARTESIAN_POINT ( 'NONE',  ( -1.648565780277510218, -30.58703805132190467, 6.931070083220555844 ) ) ;
#33147=CARTESIAN_POINT ( 'NONE',  ( -1.743696608120477221, -30.19304425262081182, 7.638132480492517473 ) ) ;
#33149=ORIENTED_EDGE ( 'NONE', *, *, #12233, .T. ) ;
#33151=LINE ( 'NONE', #17466, #24646 ) ;
#33165=DIRECTION ( 'NONE',  ( 0.3420201433256662704, 0.9396926207859093161, -0.000000000000000000 ) ) ;
#33173=CARTESIAN_POINT ( 'NONE',  ( 4.017981887854990219, -32.06726540440380546, 7.139196562012273262 ) ) ;
#33174=CYLINDRICAL_SURFACE ( 'NONE', #39890, 3.399999999999999911 ) ;
#33178=CARTESIAN_POINT ( 'NONE',  ( 5.401390093233090717, -28.93157757802832819, 6.894806418505347700 ) ) ;
#33185=DIRECTION ( 'NONE',  ( 0.3420201433256748746, -0.9396926207859060964, 0.000000000000000000 ) ) ;
#33186=CARTESIAN_POINT ( 'NONE',  ( 5.185801770105404884, -29.63756468397217958, 7.784725160561911217 ) ) ;
#33190=CARTESIAN_POINT ( 'NONE',  ( 4.371603794565618095, -31.82287587566080944, 7.773839561854630986 ) ) ;
#33192=ORIENTED_EDGE ( 'NONE', *, *, #7014, .T. ) ;
#33195=LINE ( 'NONE', #23903, #14805 ) ;
#33198=ORIENTED_EDGE ( 'NONE', *, *, #14885, .F. ) ;
#33199=CARTESIAN_POINT ( 'NONE',  ( -0.5530902551810904511, -32.11587329338448882, 7.778050822775636419 ) ) ;
#33200=CARTESIAN_POINT ( 'NONE',  ( 2.474049714983522108, -26.25912200567108457, 7.013842709614101167 ) ) ;
#33203=CARTESIAN_POINT ( 'NONE',  ( -1.474761067717296203, -28.35402923960093347, 6.887041543973313473 ) ) ;
#33205=FACE_OUTER_BOUND ( 'NONE', #25228, .T. ) ;
#33213=ADVANCED_FACE ( 'NONE', ( #30892 ), #11709, .F. ) ;
#33217=CARTESIAN_POINT ( 'NONE',  ( 2.261828623665968596, -26.21660544866439224, 7.661510568013097711 ) ) ;
#33228=DIRECTION ( 'NONE',  ( -0.7660444431189818992, 0.6427876096865345890, 0.000000000000000000 ) ) ;
#33231=LINE ( 'NONE', #1342, #22865 ) ;
#33233=CARTESIAN_POINT ( 'NONE',  ( 1.078588498108656424, -33.79778590424514562, 7.754798119455333705 ) ) ;
#33235=CARTESIAN_POINT ( 'NONE',  ( 5.151894269954111039, -30.15055920605938766, 7.655937882338901268 ) ) ;
#33238=CARTESIAN_POINT ( 'NONE',  ( 3.331358690166323910, -32.66670692436608192, 6.870724624169665340 ) ) ;
#33241=CARTESIAN_POINT ( 'NONE',  ( 2.815008375265338536, -32.78203729893284901, 6.892063359921933419 ) ) ;
#33242=LINE ( 'NONE', #4437, #19106 ) ;
#33244=CARTESIAN_POINT ( 'NONE',  ( 1.836318226000623666, -26.07255855739565575, 6.870724624169667116 ) ) ;
#33249=EDGE_CURVE ( 'NONE', #40258, #13756, #21618, .T. ) ;
#33252=VERTEX_POINT ( 'NONE', #24490 ) ;
#33254=CARTESIAN_POINT ( 'NONE',  ( 0.1710129748054547427, -26.53331930453025933, 6.903372536218457256 ) ) ;
#33256=CARTESIAN_POINT ( 'NONE',  ( -0.8529892338943324548, -27.17613526092917198, 6.961115707816235343 ) ) ;
#33268=DIRECTION ( 'NONE',  ( 0.1736481776669273336, 0.9848077530122085754, -0.000000000000000000 ) ) ;
#33271=CARTESIAN_POINT ( 'NONE',  ( 4.421194222029321885, -27.53100279559231112, 7.013842709614101167 ) ) ;
#33272=CARTESIAN_POINT ( 'NONE',  ( 3.987918417508891089, -27.05451493134790653, 6.865312560952604670 ) ) ;
#33282=CARTESIAN_POINT ( 'NONE',  ( 2.480715098600875468, -26.26068663146227067, 6.903372536218457256 ) ) ;
#33284=CARTESIAN_POINT ( 'NONE',  ( -1.532116777668663499, -30.62392227519150723, 7.761597726988851420 ) ) ;
#33287=CARTESIAN_POINT ( 'NONE',  ( 0.6859961916748535948, -26.22015330552546075, 6.961115707816238007 ) ) ;
#33289=AXIS2_PLACEMENT_3D ( 'NONE', #40663, #33907, #37170 ) ;
#33290=CARTESIAN_POINT ( 'NONE',  ( 4.460641277711257402, -27.41792629019667160, 6.867199677474203234 ) ) ;
#33291=ADVANCED_FACE ( 'NONE', ( #11300 ), #23865, .T. ) ;
#33292=CARTESIAN_POINT ( 'NONE',  ( 1.105923466014343548, -33.01907637181788147, 7.635761828346575797 ) ) ;
#33298=EDGE_CURVE ( 'NONE', #21194, #26672, #27169, .T. ) ;
#33300=DIRECTION ( 'NONE',  ( -0.3420201433256726542, 0.9396926207859070956, -0.000000000000000000 ) ) ;
#33304=CARTESIAN_POINT ( 'NONE',  ( -1.608853458698036976, -28.78960517802560304, 6.903372536218457256 ) ) ;
#33305=EDGE_CURVE ( 'NONE', #16334, #2658, #27481, .T. ) ;
#33306=CARTESIAN_POINT ( 'NONE',  ( 2.340695417320536986, -26.14220864269441691, 7.783750581861600182 ) ) ;
#33307=CARTESIAN_POINT ( 'NONE',  ( -0.4954141421830357550, -26.97407892422453202, 7.635761828346577573 ) ) ;
#33308=ORIENTED_EDGE ( 'NONE', *, *, #34584, .T. ) ;
#33316=CARTESIAN_POINT ( 'NONE',  ( -0.8082847640681127821, -27.27503357126796857, 6.868387053540521592 ) ) ;
#33317=ORIENTED_EDGE ( 'NONE', *, *, #37374, .F. ) ;
#33322=CARTESIAN_POINT ( 'NONE',  ( 5.200364047366366371, -29.55642757665872722, 7.635761828346577573 ) ) ;
#33329=CARTESIAN_POINT ( 'NONE',  ( 2.261116115764334022, -26.10824616355668937, 7.255881584735162981 ) ) ;
#33330=AXIS2_PLACEMENT_3D ( 'NONE', #33389, #23494, #26581 ) ;
#33334=CARTESIAN_POINT ( 'NONE',  ( 2.896981936218417708, -32.75240845689362601, 7.693875151218753317 ) ) ;
#33339=CYLINDRICAL_SURFACE ( 'NONE', #14772, 3.399999999999999911 ) ;
#33340=ORIENTED_EDGE ( 'NONE', *, *, #5052, .T. ) ;
#33343=ORIENTED_EDGE ( 'NONE', *, *, #12433, .F. ) ;
#33344=CYLINDRICAL_SURFACE ( 'NONE', #37445, 3.399999999999999911 ) ;
#33353=EDGE_CURVE ( 'NONE', #9639, #5985, #11260, .T. ) ;
#33356=CARTESIAN_POINT ( 'NONE',  ( -1.149480952756954055, -27.71566481673633220, 6.887945620086120435 ) ) ;
#33357=VERTEX_POINT ( 'NONE', #15635 ) ;
#33358=ORIENTED_EDGE ( 'NONE', *, *, #10132, .T. ) ;
#33360=CARTESIAN_POINT ( 'NONE',  ( -1.626205328355836199, -30.65793886950926961, 6.865482280155368322 ) ) ;
#33363=VECTOR ( 'NONE', #34925, 999.9999999999998863 ) ;
#33368=VERTEX_POINT ( 'NONE', #12542 ) ;
#33370=ORIENTED_EDGE ( 'NONE', *, *, #40675, .T. ) ;
#33371=CARTESIAN_POINT ( 'NONE',  ( 5.123750824668761972, -30.29724448404768111, 7.754798119455333705 ) ) ;
#33373=ORIENTED_EDGE ( 'NONE', *, *, #17981, .T. ) ;
#33376=CARTESIAN_POINT ( 'NONE',  ( 4.812762731218999335, -27.96895030771830548, 6.895394898881667345 ) ) ;
#33383=VERTEX_POINT ( 'NONE', #22030 ) ;
#33384=CARTESIAN_POINT ( 'NONE',  ( -0.004313233346292664333, -26.62815260315269228, 7.763628509615283946 ) ) ;
#33386=LINE ( 'NONE', #18307, #31691 ) ;
#33389=CARTESIAN_POINT ( 'NONE',  ( 1.700390093233090871, -29.56993018339339940, 7.800000000000000711 ) ) ;
#33391=CARTESIAN_POINT ( 'NONE',  ( 4.173564143869515242, -31.91328782742822767, 7.386948897581451234 ) ) ;
#33392=CARTESIAN_POINT ( 'NONE',  ( 6.136079629878683050, -27.96984039756584295, 7.635761828346577573 ) ) ;
#33396=PRODUCT_DEFINITION_FORMATION_WITH_SPECIFIED_SOURCE ( 'ANY', '', #22464, .NOT_KNOWN. ) ;
#33405=CARTESIAN_POINT ( 'NONE',  ( 5.187261144941242463, -29.64526969736682815, 7.782861076432734393 ) ) ;
#33409=CARTESIAN_POINT ( 'NONE',  ( 0.1214003938371286395, -25.12656084334626172, 7.695279973900954751 ) ) ;
#33415=B_SPLINE_CURVE_WITH_KNOTS ( 'NONE', 3,
 ( #13926, #14522, #36366, #26498, #1395, #17603, #11223, #20298, #29981, #10826, #33290, #7750, #26302, #23991, #4670, #8135, #38834, #36562, #1589, #1795, #8342, #5074, #35774, #10629, #30182, #39028, #39433, #20918, #32882, #23206, #7548 ),
 .UNSPECIFIED., .F., .F.,
 ( 4, 3, 3, 3, 3, 3, 3, 3, 3, 3, 4 ),
 ( 0.000000000000000000, 3.077658087705820324E-05, 6.152638666999296060E-05, 9.267501192706854797E-05, 0.0001241882240135193068, 0.0001556618703051694563, 0.0001866161554452238757, 0.0002167966385860975508, 0.0002463805737537784653, 0.0002758761370306542790, 0.0002847094172289964297 ),
 .UNSPECIFIED. ) ;
#33416=PLANE ( 'NONE',  #6278 ) ;
#33419=CARTESIAN_POINT ( 'NONE',  ( -0.5385815272626705008, -32.12866175765496024, 7.784476445165074310 ) ) ;
#33420=CARTESIAN_POINT ( 'NONE',  ( 3.895694199539312841, -32.16621117463044044, 7.756377446753167426 ) ) ;
#33425=CARTESIAN_POINT ( 'NONE',  ( -1.699609906766908596, -29.56993018339339940, 7.767301406074262893 ) ) ;
#33438=ORIENTED_EDGE ( 'NONE', *, *, #20574, .F. ) ;
#33439=CARTESIAN_POINT ( 'NONE',  ( -0.8286472691028512472, -27.29749316118379454, 7.761597726988854973 ) ) ;
#33441=( BOUNDED_CURVE ( )  B_SPLINE_CURVE ( 3, ( #3765, #32171, #13004, #38112 ),
 .UNSPECIFIED., .F., .T. ) 
 B_SPLINE_CURVE_WITH_KNOTS ( ( 4, 4 ),
 ( 4.748221474220559735, 4.941946782021394036 ),
 .UNSPECIFIED. ) 
 CURVE ( )  GEOMETRIC_REPRESENTATION_ITEM ( )  RATIONAL_B_SPLINE_CURVE ( ( 1.000000000000000000, 0.9968749865767494445, 0.9968749865767494445, 1.000000000000000000 ) ) 
 REPRESENTATION_ITEM ( '' )  );
#33442=CARTESIAN_POINT ( 'NONE',  ( 4.345741007283959512, -31.86168028790528695, 6.875671892026063325 ) ) ;
#33448=VERTEX_POINT ( 'NONE', #22244 ) ;
#33451=EDGE_CURVE ( 'NONE', #15988, #2006, #3509, .T. ) ;
#33453=CARTESIAN_POINT ( 'NONE',  ( -1.699609906766908818, -29.56993018339339940, 7.620413589471895399 ) ) ;
#33454=CARTESIAN_POINT ( 'NONE',  ( 5.154949517232994438, -29.00770241687787276, 6.880608371227950215 ) ) ;
#33457=CARTESIAN_POINT ( 'NONE',  ( 3.369652234211440334, -26.60790990542409773, 7.680992449362126884 ) ) ;
#33458=CARTESIAN_POINT ( 'NONE',  ( 1.145429890469515932, -32.92433313672930240, 7.695279973900954751 ) ) ;
#33461=FACE_OUTER_BOUND ( 'NONE', #35406, .T. ) ;
#33464=EDGE_CURVE ( 'NONE', #12271, #28306, #39273, .T. ) ;
#33466=ORIENTED_EDGE ( 'NONE', *, *, #3117, .F. ) ;
#33469=VERTEX_POINT ( 'NONE', #17030 ) ;
#33473=CARTESIAN_POINT ( 'NONE',  ( 3.038230656040339372, -26.44419577647722264, 6.895222827070024429 ) ) ;
#33474=CARTESIAN_POINT ( 'NONE',  ( -0.8638866058868895914, -27.18780260212992061, 6.903112506833886997 ) ) ;
#33475=DIRECTION ( 'NONE',  ( 0.3420201433256662704, 0.9396926207859093161, -0.000000000000000000 ) ) ;
#33482=EDGE_CURVE ( 'NONE', #18814, #22060, #28946, .T. ) ;
#33484=CYLINDRICAL_SURFACE ( 'NONE', #10699, 0.09010775117052870209 ) ;
#33485=CARTESIAN_POINT ( 'NONE',  ( 0.9179867665364390694, -32.98135877481576728, 7.002103980607166989 ) ) ;
#33488=ADVANCED_FACE ( 'NONE', ( #19546 ), #19933, .F. ) ;
#33496=CYLINDRICAL_SURFACE ( 'NONE', #20160, 0.09010775117052914618 ) ;
#33498=CARTESIAN_POINT ( 'NONE',  ( 4.907274956385933251, -30.69948305815673351, 7.680992449362120666 ) ) ;
#33499=CARTESIAN_POINT ( 'NONE',  ( 3.960809538620813974, -27.03012904829729024, 7.774064877406531515 ) ) ;
#33504=CARTESIAN_POINT ( 'NONE',  ( 4.263026732192791712, -31.80442242921652252, 6.880147297696977304 ) ) ;
#33510=ORIENTED_EDGE ( 'NONE', *, *, #32614, .T. ) ;
#33511=CARTESIAN_POINT ( 'NONE',  ( 0.5248424762351729944, -26.37961863118246697, 7.635761828346577573 ) ) ;
#33513=CARTESIAN_POINT ( 'NONE',  ( -0.2903816339205422259, -32.33492270865357199, 7.505001789837626447 ) ) ;
#33514=CARTESIAN_POINT ( 'NONE',  ( 2.106121278015897325, -33.05321266051473117, 7.387053503561885393 ) ) ;
#33517=CARTESIAN_POINT ( 'NONE',  ( 0.04278369059588756074, -26.60137143983851615, 6.894806418505345924 ) ) ;
#33524=CARTESIAN_POINT ( 'NONE',  ( -1.545690014252844247, -28.26108608583131954, 6.865706122441729065 ) ) ;
#33527=CARTESIAN_POINT ( 'NONE',  ( 4.728949138686682652, -27.82203914373970832, 7.767720160662275219 ) ) ;
#33530=CARTESIAN_POINT ( 'NONE',  ( 3.309654742251315618, -32.56498916126437138, 6.864651958020304257 ) ) ;
#33532=CARTESIAN_POINT ( 'NONE',  ( -1.102808333278741504, -27.46281054005859446, 7.139344958878411695 ) ) ;
#33535=EDGE_CURVE ( 'NONE', #6329, #21217, #34880, .T. ) ;
#33546=VERTEX_POINT ( 'NONE', #24439 ) ;
#33548=DIRECTION ( 'NONE',  ( 0.000000000000000000, 0.000000000000000000, -1.000000000000000000 ) ) ;
#33554=CARTESIAN_POINT ( 'NONE',  ( 1.909697446979260471, -26.17637777632732821, 6.939395833800439561 ) ) ;
#33555=VERTEX_POINT ( 'NONE', #21364 ) ;
#33559=ORIENTED_EDGE ( 'NONE', *, *, #9339, .T. ) ;
#33564=ORIENTED_EDGE ( 'NONE', *, *, #15201, .T. ) ;
#33566=ORIENTED_EDGE ( 'NONE', *, *, #40605, .T. ) ;
#33571=ORIENTED_EDGE ( 'NONE', *, *, #13773, .T. ) ;
#33581=CARTESIAN_POINT ( 'NONE',  ( 0.07872181157995387923, -26.58158750152437477, 7.778050822775634643 ) ) ;
#33582=CARTESIAN_POINT ( 'NONE',  ( 1.074705601983324099, -26.22799677331331125, 7.691066658568948000 ) ) ;
#33583=CARTESIAN_POINT ( 'NONE',  ( -1.795493615143840982, -29.40023310768274456, 6.895394898881668233 ) ) ;
#33589=CARTESIAN_POINT ( 'NONE',  ( -0.3926246584570329823, -26.75618466204053192, 7.387053503561885393 ) ) ;
#33591=ORIENTED_EDGE ( 'NONE', *, *, #39262, .T. ) ;
#33598=CARTESIAN_POINT ( 'NONE',  ( 2.836962395230103073, -32.88026010553018352, 6.870737987065012042 ) ) ;
#33599=FACE_OUTER_BOUND ( 'NONE', #27617, .T. ) ;
#33600=CARTESIAN_POINT ( 'NONE',  ( 0.02383944398482668731, -26.49760566920138061, 6.865554069792296765 ) ) ;
#33602=CARTESIAN_POINT ( 'NONE',  ( 5.514668135701366936, -33.12250938555327906, 6.894806418505347700 ) ) ;
#33603=CARTESIAN_POINT ( 'NONE',  ( 4.643350526641022213, -31.46439155470594073, 7.013842709614101167 ) ) ;
#33607=CARTESIAN_POINT ( 'NONE',  ( 3.301837905240542881, -32.68206207414233688, 7.013842709614101167 ) ) ;
#33608=VECTOR ( 'NONE', #39589, 1000.000000000000000 ) ;
#33609=EDGE_LOOP ( 'NONE', ( #14067, #28171, #30899, #37032 ) ) ;
#33615=CARTESIAN_POINT ( 'NONE',  ( -0.5461542787101242302, -32.12201250624161730, 7.782034975670479859 ) ) ;
#33621=CARTESIAN_POINT ( 'NONE',  ( 1.259933197038312302, -26.09775540055275656, 7.013842709614101167 ) ) ;
#33635=EDGE_CURVE ( 'NONE', #13175, #9154, #40231, .T. ) ;
#33640=DIRECTION ( 'NONE',  ( 0.8660254037844452579, -0.4999999999999886202, 0.000000000000000000 ) ) ;
#33643=CARTESIAN_POINT ( 'NONE',  ( -1.774482262040463665, -29.98858372608404110, 6.971170733404101760 ) ) ;
#33645=DIRECTION ( 'NONE',  ( 0.7660444431189857850, -0.6427876096865299260, -0.000000000000000000 ) ) ;
#33648=FACE_OUTER_BOUND ( 'NONE', #18919, .T. ) ;
#33649=CARTESIAN_POINT ( 'NONE',  ( 5.173272756311751763, -29.13508997310039206, 7.006908160621414972 ) ) ;
#33655=CYLINDRICAL_SURFACE ( 'NONE', #18631, 0.09010775117052972905 ) ;
#33656=CYLINDRICAL_SURFACE ( 'NONE', #12139, 0.09010775117052798044 ) ;
#33658=CARTESIAN_POINT ( 'NONE',  ( 4.908817600565330785, -28.44472466649483877, 7.784838882742139532 ) ) ;
#33667=VECTOR ( 'NONE', #33165, 1000.000000000000000 ) ;
#33668=CARTESIAN_POINT ( 'NONE',  ( 0.1279077100727408489, -26.55541543726089060, 6.868387053540520704 ) ) ;
#33669=CARTESIAN_POINT ( 'NONE',  ( 3.007898519841142981, -26.43137683128037452, 6.871394612369935651 ) ) ;
#33670=CARTESIAN_POINT ( 'NONE',  ( -0.9606818258635283492, -27.29645349747919170, 6.894806418505347700 ) ) ;
#33671=CARTESIAN_POINT ( 'NONE',  ( 4.894364063540053600, -30.73549025348913588, 7.769368695748489095 ) ) ;
#33673=ORIENTED_EDGE ( 'NONE', *, *, #5841, .F. ) ;
#33675=DIRECTION ( 'NONE',  ( 0.4826092789263594640, 0.5751513419797960047, 0.6605219282605379050 ) ) ;
#33678=( BOUNDED_CURVE ( )  B_SPLINE_CURVE ( 3, ( #18008, #8740, #5673, #30597 ),
 .UNSPECIFIED., .F., .T. ) 
 B_SPLINE_CURVE_WITH_KNOTS ( ( 4, 4 ),
 ( 1.347909859412852907, 1.534781240595297414 ),
 .UNSPECIFIED. ) 
 CURVE ( )  GEOMETRIC_REPRESENTATION_ITEM ( )  RATIONAL_B_SPLINE_CURVE ( ( 1.000000000000000000, 0.9970920404276226723, 0.9970920404276226723, 1.000000000000000000 ) ) 
 REPRESENTATION_ITEM ( '' )  );
#33682=CARTESIAN_POINT ( 'NONE',  ( -2.749201978999709084, -28.00803730016500737, 7.695279973900954751 ) ) ;
#33684=CARTESIAN_POINT ( 'NONE',  ( 2.704349939082798304, -26.31416920314327612, 7.139196562012273262 ) ) ;
#33687=VERTEX_POINT ( 'NONE', #18662 ) ;
#33693=CARTESIAN_POINT ( 'NONE',  ( -1.765272865745179498, -30.05733663009887024, 7.754798119455333705 ) ) ;
#33697=CARTESIAN_POINT ( 'NONE',  ( 5.049232725593039817, -28.98234782857963410, 7.769368695748486431 ) ) ;
#33698=VECTOR ( 'NONE', #16518, 1000.000000000000114 ) ;
#33712=CARTESIAN_POINT ( 'NONE',  ( -0.6777970675445941229, -32.13785343440231657, 7.011627023500182965 ) ) ;
#33713=ORIENTED_EDGE ( 'NONE', *, *, #12792, .T. ) ;
#33715=ADVANCED_FACE ( 'NONE', ( #28350 ), #31655, .F. ) ;
#33718=CARTESIAN_POINT ( 'NONE',  ( -1.557283979289156184, -28.29021886912457617, 6.864368109219936009 ) ) ;
#33725=CARTESIAN_POINT ( 'NONE',  ( 3.291145163220645209, -32.57486068939992663, 6.863904403958576594 ) ) ;
#33727=CARTESIAN_POINT ( 'NONE',  ( 4.936849669449925315, -30.90234506304400952, 6.875780273367530171 ) ) ;
#33733=CARTESIAN_POINT ( 'NONE',  ( -1.797364064287140906, -29.44672032744571055, 7.753200566781576875 ) ) ;
#33736=CARTESIAN_POINT ( 'NONE',  ( 1.076318136774142564, -33.00497882164555108, 7.778495531946297170 ) ) ;
#33740=ORIENTED_EDGE ( 'NONE', *, *, #27271, .T. ) ;
#33743=VERTEX_POINT ( 'NONE', #29362 ) ;
#33745=CARTESIAN_POINT ( 'NONE',  ( 4.078577254010792075, -27.00200693238450000, 7.011627023500183853 ) ) ;
#33749=CARTESIAN_POINT ( 'NONE',  ( 1.904238495577618151, -26.17604549525697522, 6.920489980334476599 ) ) ;
#33751=CYLINDRICAL_SURFACE ( 'NONE', #25718, 0.09010775117052914618 ) ;
#33754=PLANE ( 'NONE',  #10876 ) ;
#33755=B_SPLINE_CURVE_WITH_KNOTS ( 'NONE', 3,
 ( #30569, #24375, #38590, #10396, #35535, #7309, #19866, #8508, #17977, #10984, #1964, #2162, #13891, #33037, #5030, #7708, #20458, #14481, #29935, #34121, #39095, #30047, #751, #12679, #346, #24567, #30551, #37118, #34274, #6043, #31165 ),
 .UNSPECIFIED., .F., .F.,
 ( 4, 3, 3, 3, 3, 3, 3, 3, 3, 3, 4 ),
 ( 4.336808689942017736E-19, 3.077658087705710549E-05, 6.152638666999027720E-05, 9.267501192706690811E-05, 0.0001241882240135190087, 0.0001556618703051683178, 0.0001866161554452223036, 0.0002167966385860985808, 0.0002463805737537785737, 0.0002758761370306538996, 0.0002847094172290079222 ),
 .UNSPECIFIED. ) ;
#33762=ADVANCED_FACE ( 'NONE', ( #35559 ), #4652, .T. ) ;
#33766=VERTEX_POINT ( 'NONE', #13298 ) ;
#33772=DIRECTION ( 'NONE',  ( -0.9848077530122069101, -0.1736481776669374644, -0.000000000000000000 ) ) ;
#33775=EDGE_LOOP ( 'NONE', ( #9643, #29143, #17022, #5248 ) ) ;
#33783=CARTESIAN_POINT ( 'NONE',  ( -1.799033128594637931, -29.50575927414515576, 6.870737987065012042 ) ) ;
#33793=LINE ( 'NONE', #1899, #9596 ) ;
#33800=CARTESIAN_POINT ( 'NONE',  ( 5.189116403693322610, -29.65506484607316651, 7.780491323090178213 ) ) ;
#33803=CARTESIAN_POINT ( 'NONE',  ( 4.389428757393228686, -31.81026445011082870, 7.756742906098587298 ) ) ;
#33808=VERTEX_POINT ( 'NONE', #7529 ) ;
#33811=PLANE ( 'NONE',  #37546 ) ;
#33813=DIRECTION ( 'NONE',  ( 0.8660254037844449249, -0.4999999999999888423, -0.000000000000000000 ) ) ;
#33815=CARTESIAN_POINT ( 'NONE',  ( -0.4603391584254019064, -32.19504905708794951, 7.721096864323896192 ) ) ;
#33820=ORIENTED_EDGE ( 'NONE', *, *, #16501, .T. ) ;
#33823=VERTEX_POINT ( 'NONE', #767 ) ;
#33837=ORIENTED_EDGE ( 'NONE', *, *, #21102, .F. ) ;
#33838=AXIS2_PLACEMENT_3D ( 'NONE', #19617, #32191, #38934 ) ;
#33843=CARTESIAN_POINT ( 'NONE',  ( -1.694407884520888752, -29.38183540858682363, 6.895222827070020877 ) ) ;
#33845=CARTESIAN_POINT ( 'NONE',  ( -1.774643799394317156, -29.98723051182367882, 6.961115707816238896 ) ) ;
#33846=CARTESIAN_POINT ( 'NONE',  ( -1.267148935398236143, -27.71435023938598619, 7.753200566781576875 ) ) ;
#33847=CARTESIAN_POINT ( 'NONE',  ( 1.546080347881852335, -33.06653896731305764, 6.880828092187097234 ) ) ;
#33851=CARTESIAN_POINT ( 'NONE',  ( 2.474049714983546089, -33.27093018339341057, 7.013842709614101167 ) ) ;
#33853=CARTESIAN_POINT ( 'NONE',  ( 5.153279172109080264, -30.14225614731511982, 7.685194954629195330 ) ) ;
#33856=CARTESIAN_POINT ( 'NONE',  ( 5.200390093233090205, -29.56993018339339940, 6.929570838012950595 ) ) ;
#33859=DIRECTION ( 'NONE',  ( 0.000000000000000000, 0.000000000000000000, -1.000000000000000000 ) ) ;
#33860=B_SPLINE_CURVE_WITH_KNOTS ( 'NONE', 3,
 ( #5638, #30769, #21494, #24363, #8293, #37122, #8910, #2571, #18178, #40208 ),
 .UNSPECIFIED., .F., .F.,
 ( 4, 3, 3, 4 ),
 ( 0.0001585009270395693266, 0.0001815657551981851700, 0.0002118214035944126139, 0.0002170292169044741302 ),
 .UNSPECIFIED. ) ;
#33866=ORIENTED_EDGE ( 'NONE', *, *, #24110, .F. ) ;
#33869=ADVANCED_FACE ( 'NONE', ( #11207 ), #24397, .F. ) ;
#33877=CARTESIAN_POINT ( 'NONE',  ( -0.8600751803131411188, -27.18371306214347527, 6.912143950357343414 ) ) ;
#33878=CARTESIAN_POINT ( 'NONE',  ( 1.243865080918407529, -26.20070406487326764, 6.865312560952602894 ) ) ;
#33880=CARTESIAN_POINT ( 'NONE',  ( -1.799566460562916470, -29.58736926422850999, 7.749999999999998224 ) ) ;
#33881=EDGE_LOOP ( 'NONE', ( #34090, #8314, #37428, #9853 ) ) ;
#33884=EDGE_LOOP ( 'NONE', ( #30032, #16057, #21968, #34227, #19577 ) ) ;
#33889=CIRCLE ( 'NONE', #6923, 2.500000000000000444 ) ;
#33892=B_SPLINE_CURVE_WITH_KNOTS ( 'NONE', 3,
 ( #18682, #23009, #7150, #22811, #13127, #29181, #1199, #16599, #990, #588 ),
 .UNSPECIFIED., .F., .F.,
 ( 4, 3, 3, 4 ),
 ( 0.0001585009270395721455, 0.0001815657551981848447, 0.0002118214035944132373, 0.0002170292169044773015 ),
 .UNSPECIFIED. ) ;
#33894=ORIENTED_EDGE ( 'NONE', *, *, #40384, .F. ) ;
#33896=ORIENTED_EDGE ( 'NONE', *, *, #9542, .F. ) ;
#33898=FACE_OUTER_BOUND ( 'NONE', #8392, .T. ) ;
#33900=CARTESIAN_POINT ( 'NONE',  ( -1.426118936618665067, -27.98159272051555035, 7.139344958878413472 ) ) ;
#33906=CARTESIAN_POINT ( 'NONE',  ( 2.304086713256504382, -32.91590543598751850, 7.635761828346577573 ) ) ;
#33907=DIRECTION ( 'NONE',  ( -0.6502177225477870914, -0.3754033771448342938, -0.6605219282605403475 ) ) ;
#33911=ORIENTED_EDGE ( 'NONE', *, *, #39641, .T. ) ;
#33914=CYLINDRICAL_SURFACE ( 'NONE', #36894, 3.399999999999999911 ) ;
#33915=EDGE_CURVE ( 'NONE', #11496, #1708, #31946, .T. ) ;
#33916=AXIS2_PLACEMENT_3D ( 'NONE', #3487, #40709, #12510 ) ;
#33922=CARTESIAN_POINT ( 'NONE',  ( 4.838943445346131966, -30.87743861000141621, 6.871394612369933874 ) ) ;
#33928=CARTESIAN_POINT ( 'NONE',  ( 5.150202707224498688, -30.16051711886163744, 7.750000000000001776 ) ) ;
#33931=ORIENTED_EDGE ( 'NONE', *, *, #31284, .F. ) ;
#33933=CARTESIAN_POINT ( 'NONE',  ( -1.743365991543899485, -30.19486540288534826, 7.750000000000001776 ) ) ;
#33939=CARTESIAN_POINT ( 'NONE',  ( 4.918507887475499274, -30.94605444427887520, 6.961115707816230902 ) ) ;
#33946=CARTESIAN_POINT ( 'NONE',  ( 5.018308223201096041, -30.31257054894095049, 6.871394612369936539 ) ) ;
#33947=VECTOR ( 'NONE', #1584, 1000.000000000000000 ) ;
#33950=CARTESIAN_POINT ( 'NONE',  ( 2.887291949543890457, -32.75603725470723759, 7.652160403243384756 ) ) ;
#33951=CARTESIAN_POINT ( 'NONE',  ( 0.9852593961805760081, -32.99344650311874716, 7.766640943994643109 ) ) ;
#33955=ORIENTED_EDGE ( 'NONE', *, *, #27641, .T. ) ;
#33957=CARTESIAN_POINT ( 'NONE',  ( 3.463827299026049911, -26.66297573651074160, 6.874555630061442990 ) ) ;
#33965=CARTESIAN_POINT ( 'NONE',  ( 2.822174244762026607, -32.87228481168282457, 7.782861076432729952 ) ) ;
#33972=CARTESIAN_POINT ( 'NONE',  ( -1.321941654078521378, -31.33501114731328130, 7.749999999999999112 ) ) ;
#33976=ORIENTED_EDGE ( 'NONE', *, *, #19629, .F. ) ;
#33977=CARTESIAN_POINT ( 'NONE',  ( -1.741975392120745258, -30.20250733242332331, 7.651421919295148477 ) ) ;
#33978=ORIENTED_EDGE ( 'NONE', *, *, #2237, .F. ) ;
#33980=LINE ( 'NONE', #30678, #35832 ) ;
#33984=ORIENTED_EDGE ( 'NONE', *, *, #12366, .T. ) ;
#33988=AXIS2_PLACEMENT_3D ( 'NONE', #1084, #19604, #34868 ) ;
#33992=LINE ( 'NONE', #18305, #24561 ) ;
#33993=DIRECTION ( 'NONE',  ( -0.9848077530122067991, -0.1736481776669374644, -0.000000000000000000 ) ) ;
#33998=CARTESIAN_POINT ( 'NONE',  ( 2.896981936218417264, -32.75240845689362601, 7.695279973900954751 ) ) ;
#34003=ORIENTED_EDGE ( 'NONE', *, *, #19158, .F. ) ;
#34008=ADVANCED_FACE ( 'NONE', ( #2398 ), #33484, .F. ) ;
#34009=CARTESIAN_POINT ( 'NONE',  ( 3.558396595903837056, -26.60381962644626697, 7.750000000000000888 ) ) ;
#34013=CARTESIAN_POINT ( 'NONE',  ( 5.100210461593464473, -29.53486150151830358, 7.711434774245209844 ) ) ;
#34014=CARTESIAN_POINT ( 'NONE',  ( 4.643065655508351597, -31.46483401609519959, 6.895394898881657575 ) ) ;
#34016=ORIENTED_EDGE ( 'NONE', *, *, #24736, .F. ) ;
#34019=CARTESIAN_POINT ( 'NONE',  ( 4.314359296880712513, -31.88662353291251605, 7.776484688137386136 ) ) ;
#34020=LINE ( 'NONE', #40358, #2028 ) ;
#34024=B_SPLINE_CURVE_WITH_KNOTS ( 'NONE', 3,
 ( #24450, #14981, #33950, #11262, #14361, #33122, #36403, #8383, #33334, #21371 ),
 .UNSPECIFIED., .F., .F.,
 ( 4, 3, 3, 4 ),
 ( 0.000000000000000000, 3.025570593003025599E-05, 6.051145698343885989E-05, 6.468151674593503617E-05 ),
 .UNSPECIFIED. ) ;
#34027=CARTESIAN_POINT ( 'NONE',  ( -1.339436964189177459, -27.83515215944516896, 7.640616322432101981 ) ) ;
#34028=ORIENTED_EDGE ( 'NONE', *, *, #34393, .T. ) ;
#34029=CARTESIAN_POINT ( 'NONE',  ( -0.4661178359761078416, -32.19028865001026674, 7.740055089680395461 ) ) ;
#34034=DIRECTION ( 'NONE',  ( 1.000000000000000000, 0.000000000000000000, 0.000000000000000000 ) ) ;
#34045=DIRECTION ( 'NONE',  ( 0.5751513419797913418, 0.4826092789263654037, 0.6605219282605377940 ) ) ;
#34054=CARTESIAN_POINT ( 'NONE',  ( 4.279759429550099803, -31.93571510856349605, 6.880828092187097234 ) ) ;
#34055=CARTESIAN_POINT ( 'NONE',  ( -1.576062547484235354, -30.80072589882973944, 7.695279973900954751 ) ) ;
#34056=ORIENTED_EDGE ( 'NONE', *, *, #37467, .F. ) ;
#34058=EDGE_CURVE ( 'NONE', #36741, #35883, #24477, .T. ) ;
#34062=ADVANCED_FACE ( 'NONE', ( #7033 ), #6279, .F. ) ;
#34068=CARTESIAN_POINT ( 'NONE',  ( 3.439957088343224889, -32.60061551843173078, 7.773839561854630986 ) ) ;
#34076=FACE_OUTER_BOUND ( 'NONE', #9607, .T. ) ;
#34081=CARTESIAN_POINT ( 'NONE',  ( 4.629538257087431496, -31.49813288122227917, 7.387053503561886281 ) ) ;
#34084=ORIENTED_EDGE ( 'NONE', *, *, #18112, .T. ) ;
#34086=DIRECTION ( 'NONE',  ( 0.8660254037844380415, 0.5000000000000011102, 0.000000000000000000 ) ) ;
#34087=CARTESIAN_POINT ( 'NONE',  ( 2.979782760284078513, -26.41980900443600078, 6.863904403958576594 ) ) ;
#34088=CARTESIAN_POINT ( 'NONE',  ( 1.182707065140680358, -26.20955829661496850, 6.874555630061442990 ) ) ;
#34089=CARTESIAN_POINT ( 'NONE',  ( 5.054583831487962975, -30.12615907168387608, 7.712764235869103757 ) ) ;
#34090=ORIENTED_EDGE ( 'NONE', *, *, #31234, .F. ) ;
#34092=CARTESIAN_POINT ( 'NONE',  ( 5.741588806061445283, -32.80189416861090024, 7.754798119455333705 ) ) ;
#34096=AXIS2_PLACEMENT_3D ( 'NONE', #4260, #10611, #13511 ) ;
#34102=CARTESIAN_POINT ( 'NONE',  ( 6.117106422890660866, -32.35436969967226162, 6.954324564059724878 ) ) ;
#34104=CARTESIAN_POINT ( 'NONE',  ( 2.886433127740331894, -32.75636032089741434, 7.740055089680400791 ) ) ;
#34111=CARTESIAN_POINT ( 'NONE',  ( -1.323924960262854666, -31.33161076090960151, 7.635761828346577573 ) ) ;
#34112=EDGE_CURVE ( 'NONE', #19965, #11431, #37154, .T. ) ;
#34114=CARTESIAN_POINT ( 'NONE',  ( 3.425221786318646267, -26.52444900129300720, 7.730015791551944737 ) ) ;
#34116=CARTESIAN_POINT ( 'NONE',  ( -1.740187722448509389, -30.14826187258440626, 7.781480525794718162 ) ) ;
#34121=CARTESIAN_POINT ( 'NONE',  ( 2.120505722696732764, -33.04462681987888573, 6.931070083220556732 ) ) ;
#34123=CARTESIAN_POINT ( 'NONE',  ( 1.062037487868057184, -33.01122440958558002, 6.894806418505347700 ) ) ;
#34130=CARTESIAN_POINT ( 'NONE',  ( 0.9267304714826125611, -25.86893018339336692, 7.013842709614101167 ) ) ;
#34135=CARTESIAN_POINT ( 'NONE',  ( -1.549552128476125112, -30.56886739641119632, 6.882085323592688653 ) ) ;
#34149=CARTESIAN_POINT ( 'NONE',  ( -1.343166177233030556, -31.08544090138337168, 6.939395833800438673 ) ) ;
#34154=DIRECTION ( 'NONE',  ( -0.000000000000000000, -0.000000000000000000, -1.000000000000000000 ) ) ;
#34158=EDGE_LOOP ( 'NONE', ( #37454, #11541, #7609, #15372, #26861 ) ) ;
#34159=DIRECTION ( 'NONE',  ( -1.000000000000000000, 0.000000000000000000, 0.000000000000000000 ) ) ;
#34161=EDGE_CURVE ( 'NONE', #35515, #10191, #17483, .T. ) ;
#34165=LINE ( 'NONE', #21994, #503 ) ;
#34171=CARTESIAN_POINT ( 'NONE',  ( 4.603808887335269162, -31.33918005375042171, 7.782034975670476307 ) ) ;
#34173=CARTESIAN_POINT ( 'NONE',  ( 3.998933749712821673, -26.93046473555785170, 6.870737987065013819 ) ) ;
#34176=CARTESIAN_POINT ( 'NONE',  ( -0.4083080382643015649, -26.90281974977018109, 7.774064877406530627 ) ) ;
#34178=CARTESIAN_POINT ( 'NONE',  ( 4.272324738573828107, -31.79372274477328020, 7.785868773668302545 ) ) ;
#34185=FACE_OUTER_BOUND ( 'NONE', #2217, .T. ) ;
#34187=CARTESIAN_POINT ( 'NONE',  ( -1.650167670790918750, -28.99217783630842860, 7.756377446753162097 ) ) ;
#34188=CARTESIAN_POINT ( 'NONE',  ( -0.4585365243479023190, -26.81617090910717494, 7.761113333117548585 ) ) ;
#34190=ORIENTED_EDGE ( 'NONE', *, *, #20828, .F. ) ;
#34201=CARTESIAN_POINT ( 'NONE',  ( -1.499157785959173594, -28.41975916621540321, 7.635761828346577573 ) ) ;
#34207=VERTEX_POINT ( 'NONE', #23095 ) ;
#34211=ORIENTED_EDGE ( 'NONE', *, *, #21442, .T. ) ;
#34217=B_SPLINE_CURVE_WITH_KNOTS ( 'NONE', 3,
 ( #19439, #34304, #27880, #31193, #21721, #25011, #31395, #37958, #312, #18606 ),
 .UNSPECIFIED., .F., .F.,
 ( 4, 3, 3, 4 ),
 ( 1.748223473168675632E-18, 3.025570593003025938E-05, 6.051145698343942910E-05, 6.468151674593380289E-05 ),
 .UNSPECIFIED. ) ;
#34218=CARTESIAN_POINT ( 'NONE',  ( 2.768830974701133485, -32.90287465194062833, 6.870724624169667116 ) ) ;
#34222=CARTESIAN_POINT ( 'NONE',  ( 5.100381899876085257, -29.58108672504286574, 7.775108481317161591 ) ) ;
#34224=CARTESIAN_POINT ( 'NONE',  ( -0.9575113486053222767, -31.84711263666175540, 7.695279973900954751 ) ) ;
#34226=CARTESIAN_POINT ( 'NONE',  ( 2.170460981197068762, -32.93727830324805694, 7.754798119455333705 ) ) ;
#34227=ORIENTED_EDGE ( 'NONE', *, *, #4584, .T. ) ;
#34230=DIRECTION ( 'NONE',  ( 1.000000000000000000, 0.000000000000000000, 0.000000000000000000 ) ) ;
#34232=EDGE_CURVE ( 'NONE', #2601, #26604, #32773, .T. ) ;
#34233=CARTESIAN_POINT ( 'NONE',  ( -0.5003730563773006734, -26.86726130889041286, 7.785344483711591934 ) ) ;
#34234=ORIENTED_EDGE ( 'NONE', *, *, #14880, .F. ) ;
#34240=CARTESIAN_POINT ( 'NONE',  ( 3.920970191082350453, -32.27530831286587443, 6.887161170156903545 ) ) ;
#34246=CARTESIAN_POINT ( 'NONE',  ( -0.04376389210842144412, -32.48847997939775212, 6.892063359921934307 ) ) ;
#34247=ORIENTED_EDGE ( 'NONE', *, *, #12160, .T. ) ;
#34249=FACE_OUTER_BOUND ( 'NONE', #40474, .T. ) ;
#34251=CARTESIAN_POINT ( 'NONE',  ( -1.699609906766908818, -29.56993018339339940, 6.949309202340325342 ) ) ;
#34254=ORIENTED_EDGE ( 'NONE', *, *, #9339, .F. ) ;
#34257=CARTESIAN_POINT ( 'NONE',  ( 4.741120993177593945, -31.30312249647428757, 7.643192810543818716 ) ) ;
#34262=CARTESIAN_POINT ( 'NONE',  ( -0.8725572984338751947, -27.34733221711291051, 6.894806418505345036 ) ) ;
#34264=CARTESIAN_POINT ( 'NONE',  ( -1.353540684280711393, -31.27978037611249462, 6.880608371227950215 ) ) ;
#34268=CYLINDRICAL_SURFACE ( 'NONE', #20878, 0.09010775117053000660 ) ;
#34272=VECTOR ( 'NONE', #30097, 1000.000000000000114 ) ;
#34274=CARTESIAN_POINT ( 'NONE',  ( 2.136987090091772235, -33.04259287893679442, 7.009310105710486738 ) ) ;
#34279=B_SPLINE_CURVE_WITH_KNOTS ( 'NONE', 3,
 ( #15009, #39714, #352, #15976, #24480, #21198, #9598, #5347, #25262, #36837 ),
 .UNSPECIFIED., .F., .F.,
 ( 4, 3, 3, 4 ),
 ( 1.887418258779916733E-18, 3.025570593003297328E-05, 6.051145698344366427E-05, 6.468151674593822101E-05 ),
 .UNSPECIFIED. ) ;
#34281=CARTESIAN_POINT ( 'NONE',  ( 4.045228995182856835, -26.97152095390259063, 7.750000000000000888 ) ) ;
#34283=ADVANCED_FACE ( 'NONE', ( #29471 ), #36250, .T. ) ;
#34285=CARTESIAN_POINT ( 'NONE',  ( -1.525269612006747488, -30.64473977883090328, 6.866852738645441434 ) ) ;
#34291=CYLINDRICAL_SURFACE ( 'NONE', #17983, 0.09010775117052841066 ) ;
#34292=CARTESIAN_POINT ( 'NONE',  ( 0.04492882035419289849, -26.60017362597359636, 6.892063359921931642 ) ) ;
#34293=( BOUNDED_CURVE ( )  B_SPLINE_CURVE ( 3, ( #29596, #15876, #1411, #28433 ),
 .UNSPECIFIED., .F., .T. ) 
 B_SPLINE_CURVE_WITH_KNOTS ( ( 4, 4 ),
 ( 4.708531083176466403, 4.895802057644187855 ),
 .UNSPECIFIED. ) 
 CURVE ( )  GEOMETRIC_REPRESENTATION_ITEM ( )  RATIONAL_B_SPLINE_CURVE ( ( 1.000000000000000000, 0.9970795998553221295, 0.9970795998553221295, 1.000000000000000000 ) ) 
 REPRESENTATION_ITEM ( '' )  );
#34296=CARTESIAN_POINT ( 'NONE',  ( 1.202039200222869475, -26.20663676950747600, 6.866852738645443210 ) ) ;
#34304=CARTESIAN_POINT ( 'NONE',  ( -1.487618233188356065, -30.75172851090044190, 7.643333865083958401 ) ) ;
#34307=CARTESIAN_POINT ( 'NONE',  ( 4.340966779518038443, -27.42811908905094853, 6.887041543973317026 ) ) ;
#34308=CARTESIAN_POINT ( 'NONE',  ( 2.787286031397239405, -32.79153584164929214, 7.782034975670476307 ) ) ;
#34309=ORIENTED_EDGE ( 'NONE', *, *, #20621, .T. ) ;
#34314=CARTESIAN_POINT ( 'NONE',  ( -1.799527215904450417, -29.59426670074542898, 7.650127521910076389 ) ) ;
#34315=CARTESIAN_POINT ( 'NONE',  ( -1.312560436656867724, -31.35097737660188244, 7.686927408461905920 ) ) ;
#34316=CARTESIAN_POINT ( 'NONE',  ( 1.582902875548440669, -32.96790048997851130, 7.759451378593096749 ) ) ;
#34319=CARTESIAN_POINT ( 'NONE',  ( 1.700390093233090871, -29.56993018339339940, 7.800000000000000711 ) ) ;
#34322=CARTESIAN_POINT ( 'NONE',  ( -0.8402781915718714467, -33.89858303842947151, 7.695279973900954751 ) ) ;
#34333=CARTESIAN_POINT ( 'NONE',  ( -1.666958026621576883, -30.04000107135736641, 7.754798119455333705 ) ) ;
#34334=EDGE_CURVE ( 'NONE', #12118, #17239, #7836, .T. ) ;
#34339=B_SPLINE_CURVE_WITH_KNOTS ( 'NONE', 3,
 ( #16863, #14575, #30042, #27147, #29638, #8191, #23268, #32542, #1257, #1650, #36420, #7407, #17060, #26756, #26361, #4340, #1857, #17455, #39700 ),
 .UNSPECIFIED., .F., .F.,
 ( 4, 3, 3, 3, 3, 3, 4 ),
 ( 0.000000000000000000, 2.546128104244612306E-05, 5.711050680483668423E-05, 8.113074941675757728E-05, 0.0001053129305727077829, 0.0001360598016347089236, 0.0001612931755713787674 ),
 .UNSPECIFIED. ) ;
#34344=EDGE_CURVE ( 'NONE', #13771, #21663, #6126, .T. ) ;
#34348=ORIENTED_EDGE ( 'NONE', *, *, #35348, .F. ) ;
#34353=ORIENTED_EDGE ( 'NONE', *, *, #36080, .F. ) ;
#34355=CARTESIAN_POINT ( 'NONE',  ( 4.922574738379127623, -30.93651010398624379, 6.912143950357338085 ) ) ;
#34368=DIRECTION ( 'NONE',  ( 0.5000000000000101030, -0.8660254037844328234, -0.000000000000000000 ) ) ;
#34372=CARTESIAN_POINT ( 'NONE',  ( 3.973866779147308570, -26.90885826429679284, 6.894806418505347700 ) ) ;
#34374=CARTESIAN_POINT ( 'NONE',  ( 4.791138977812089195, -27.92775596988059306, 7.753200566781576875 ) ) ;
#34378=CARTESIAN_POINT ( 'NONE',  ( 4.297763636622812911, -31.76394919647423265, 7.775108481317161591 ) ) ;
#34380=ORIENTED_EDGE ( 'NONE', *, *, #9558, .F. ) ;
#34384=DIRECTION ( 'NONE',  ( -3.491481338843133750E-15, 1.000000000000000000, -0.000000000000000000 ) ) ;
#34386=CARTESIAN_POINT ( 'NONE',  ( 4.152525300728761692, -32.07686114568508629, 7.501983001166816045 ) ) ;
#34388=VERTEX_POINT ( 'NONE', #33998 ) ;
#34389=CARTESIAN_POINT ( 'NONE',  ( -1.631201490816239996, -28.89133050973324401, 7.778050822775635531 ) ) ;
#34390=CARTESIAN_POINT ( 'NONE',  ( -0.4665940226951585945, -26.82738204011747740, 7.771081512783700518 ) ) ;
#34393=EDGE_CURVE ( 'NONE', #35820, #22017, #13697, .T. ) ;
#34400=EDGE_LOOP ( 'NONE', ( #1275, #22228, #22682, #23177, #28576 ) ) ;
#34402=CARTESIAN_POINT ( 'NONE',  ( 4.672772079749174523, -27.91918934176055700, 6.887041543973315250 ) ) ;
#34405=CARTESIAN_POINT ( 'NONE',  ( 1.259933197038312302, -26.09775540055275656, 7.013842709614101167 ) ) ;
#34411=CARTESIAN_POINT ( 'NONE',  ( 3.518482029086511531, -26.59117190302356448, 7.780491323090174660 ) ) ;
#34416=B_SPLINE_CURVE_WITH_KNOTS ( 'NONE', 3,
 ( #26299, #9834, #19512, #38635, #16210, #34980, #4275, #16798, #4479, #35771 ),
 .UNSPECIFIED., .F., .F.,
 ( 4, 3, 3, 4 ),
 ( 0.0001585009270395681339, 0.0001815657551981822698, 0.0002118214035944112315, 0.0002170292169044690887 ),
 .UNSPECIFIED. ) ;
#34419=VERTEX_POINT ( 'NONE', #25121 ) ;
#34421=CARTESIAN_POINT ( 'NONE',  ( 1.057242960569753309, -26.12952878737186424, 7.686927408461905031 ) ) ;
#34423=CARTESIAN_POINT ( 'NONE',  ( 5.100237809806897005, -29.53775093374590810, 7.721096864323900633 ) ) ;
#34424=CARTESIAN_POINT ( 'NONE',  ( 4.724705146729046845, -27.80824960587721506, 7.635761828346577573 ) ) ;
#34425=DIRECTION ( 'NONE',  ( -0.6605219282605402364, 0.000000000000000000, -0.7508067542896625923 ) ) ;
#34426=VERTEX_POINT ( 'NONE', #13357 ) ;
#34439=ORIENTED_EDGE ( 'NONE', *, *, #23255, .T. ) ;
#34441=B_SPLINE_CURVE_WITH_KNOTS ( 'NONE', 3,
 ( #30419, #36791, #14149, #33527, #36189, #17629, #36592, #7969, #24230, #14965, #20521, #8369, #2225, #14747, #4696, #5298, #27530, #33104, #40082 ),
 .UNSPECIFIED., .F., .F.,
 ( 4, 3, 3, 3, 3, 3, 4 ),
 ( 0.000000000000000000, 2.546128104244709884E-05, 5.711050680483773455E-05, 8.113074941675650663E-05, 0.0001053129305727056823, 0.0001360598016347088965, 0.0001612931755702009173 ),
 .UNSPECIFIED. ) ;
#34448=CARTESIAN_POINT ( 'NONE',  ( 3.953929392453140235, -32.24611259444524336, 7.762796336881262249 ) ) ;
#34456=CARTESIAN_POINT ( 'NONE',  ( 4.739243575545716958, -31.30641337154872161, 7.638132480492516585 ) ) ;
#34457=CYLINDRICAL_SURFACE ( 'NONE', #32864, 3.399999999999999911 ) ;
#34459=CARTESIAN_POINT ( 'NONE',  ( 4.253769420360524300, -31.96372510585761262, 6.961115707816238007 ) ) ;
#34460=CARTESIAN_POINT ( 'NONE',  ( -1.582490140158303138, -30.78347898942401173, 7.640616322432099317 ) ) ;
#34468=CARTESIAN_POINT ( 'NONE',  ( -0.6339409410646490439, -32.04195642642311270, 6.997764925645181933 ) ) ;
#34475=CYLINDRICAL_SURFACE ( 'NONE', #16628, 0.09010775117053032579 ) ;
#34477=CARTESIAN_POINT ( 'NONE',  ( 1.664433243520564876, -26.17012032033359148, 7.695279973900954751 ) ) ;
#34483=CIRCLE ( 'NONE', #4204, 3.499999999999999556 ) ;
#34488=EDGE_CURVE ( 'NONE', #24849, #22624, #5303, .T. ) ;
#34489=CARTESIAN_POINT ( 'NONE',  ( 5.036121742574604099, -28.51026308303529788, 6.875780273367531059 ) ) ;
#34490=CARTESIAN_POINT ( 'NONE',  ( -1.441894026320721611, -28.27145010576420248, 6.868387053540520704 ) ) ;
#34491=CARTESIAN_POINT ( 'NONE',  ( 1.311050557978938214, -26.19229569661303358, 6.988553391373220514 ) ) ;
#34492=CARTESIAN_POINT ( 'NONE',  ( 5.026819207240812659, -30.27339969195919522, 7.761597726988851420 ) ) ;
#34500=CARTESIAN_POINT ( 'NONE',  ( -1.677331764060516095, -29.95852058763195913, 6.920489980334480151 ) ) ;
#34504=CARTESIAN_POINT ( 'NONE',  ( 4.363912183534078615, -27.45669894310492865, 6.866852738645444099 ) ) ;
#34506=CARTESIAN_POINT ( 'NONE',  ( 2.880877094127454630, -32.75841735456398851, 7.748216051605119503 ) ) ;
#34513=CARTESIAN_POINT ( 'NONE',  ( -1.593127767899503722, -28.38555688987459291, 7.635761828346575797 ) ) ;
#34515=DIRECTION ( 'NONE',  ( 0.000000000000000000, -0.6605219282605379050, 0.7508067542896647018 ) ) ;
#34516=CARTESIAN_POINT ( 'NONE',  ( 3.419202797897241908, -26.52104794612278837, 7.698786668945008849 ) ) ;
#34518=CARTESIAN_POINT ( 'NONE',  ( 3.796999183887054929, -32.24653817131153488, 6.864276522220859711 ) ) ;
#34523=EDGE_CURVE ( 'NONE', #35525, #19049, #6343, .T. ) ;
#34525=EDGE_CURVE ( 'NONE', #1708, #14526, #30322, .T. ) ;
#34529=CARTESIAN_POINT ( 'NONE',  ( 1.495091655194762614, -33.07074825365423720, 7.387053503561888057 ) ) ;
#34532=( BOUNDED_CURVE ( )  B_SPLINE_CURVE ( 3, ( #24868, #34566, #37408, #6338 ),
 .UNSPECIFIED., .F., .F. ) 
 B_SPLINE_CURVE_WITH_KNOTS ( ( 4, 4 ),
 ( 4.748221474220558846, 4.941946782021394036 ),
 .UNSPECIFIED. ) 
 CURVE ( )  GEOMETRIC_REPRESENTATION_ITEM ( )  RATIONAL_B_SPLINE_CURVE ( ( 1.000000000000000000, 0.9968749865767494445, 0.9968749865767494445, 1.000000000000000000 ) ) 
 REPRESENTATION_ITEM ( '' )  );
#34535=CARTESIAN_POINT ( 'NONE',  ( -1.653081132413799281, -30.13049306011495077, 7.782167645815905033 ) ) ;
#34536=PLANE ( 'NONE',  #22078 ) ;
#34538=EDGE_CURVE ( 'NONE', #11704, #637, #12566, .T. ) ;
#34542=EDGE_LOOP ( 'NONE', ( #33042, #28378, #15411, #1031, #16201 ) ) ;
#34547=ORIENTED_EDGE ( 'NONE', *, *, #6940, .F. ) ;
#34549=ORIENTED_EDGE ( 'NONE', *, *, #13773, .F. ) ;
#34552=B_SPLINE_CURVE_WITH_KNOTS ( 'NONE', 3,
 ( #31769, #28675, #32382, #4177, #10331, #7045, #16110, #13020, #9518, #25178, #25584, #31566, #9930, #22099, #34677, #23105, #4764, #32583, #7649 ),
 .UNSPECIFIED., .F., .F.,
 ( 4, 3, 3, 3, 3, 3, 4 ),
 ( 0.000000000000000000, 2.546128104244941632E-05, 5.711050680484522232E-05, 8.113074941676646774E-05, 0.0001053129305727113066, 0.0001360598016347110649, 0.0001612931755713681694 ),
 .UNSPECIFIED. ) ;
#34553=CARTESIAN_POINT ( 'NONE',  ( -1.348517286369409263, -27.85116208076715694, 7.695279973900954751 ) ) ;
#34566=CARTESIAN_POINT ( 'NONE',  ( 4.979517197198048528, -30.49496054528498945, 7.505001789837629111 ) ) ;
#34571=CARTESIAN_POINT ( 'NONE',  ( 4.025803068412391106, -27.08951600530382464, 7.013842709614101167 ) ) ;
#34575=ORIENTED_EDGE ( 'NONE', *, *, #18077, .T. ) ;
#34576=CYLINDRICAL_SURFACE ( 'NONE', #3690, 3.399999999999999911 ) ;
#34578=ADVANCED_FACE ( 'NONE', ( #29813 ), #329, .T. ) ;
#34579=AXIS2_PLACEMENT_3D ( 'NONE', #7603, #17862, #20757 ) ;
#34580=CARTESIAN_POINT ( 'NONE',  ( 4.077496327744512428, -27.00100707246794229, 6.895394898881669121 ) ) ;
#34581=PLANE ( 'NONE',  #8751 ) ;
#34582=DIRECTION ( 'NONE',  ( 0.3754033771448330725, -0.6502177225477903111, 0.6605219282605379050 ) ) ;
#34584=EDGE_CURVE ( 'NONE', #35289, #35977, #35305, .T. ) ;
#34590=CARTESIAN_POINT ( 'NONE',  ( -2.726063116431162392, -27.94446379774605660, 7.635761828346577573 ) ) ;
#34599=CARTESIAN_POINT ( 'NONE',  ( 5.150819523378970644, -30.15690496803471277, 7.744938106820261403 ) ) ;
#34606=VECTOR ( 'NONE', #23278, 1000.000000000000114 ) ;
#34611=CARTESIAN_POINT ( 'NONE',  ( 0.5567163972659970872, -26.27754685773958698, 7.785344483711591934 ) ) ;
#34619=CARTESIAN_POINT ( 'NONE',  ( 3.494148792721590180, -26.58186483752615814, 7.785593909369613819 ) ) ;
#34621=CARTESIAN_POINT ( 'NONE',  ( -1.146144745493847150, -27.71056485836612637, 7.013842709614101167 ) ) ;
#34630=CARTESIAN_POINT ( 'NONE',  ( 5.098439472760125213, -29.68508405565106401, 7.761597726988852308 ) ) ;
#34631=CARTESIAN_POINT ( 'NONE',  ( 0.5037982502477853508, -26.38745190989316214, 7.695279973900954751 ) ) ;
#34634=ORIENTED_EDGE ( 'NONE', *, *, #39884, .F. ) ;
#34637=CARTESIAN_POINT ( 'NONE',  ( 1.605927042630150403, -33.06148854684589367, 7.776484688137386136 ) ) ;
#34644=CARTESIAN_POINT ( 'NONE',  ( 4.960094596816839285, -28.60332449888920081, 6.929923840112064859 ) ) ;
#34645=PLANE ( 'NONE',  #24124 ) ;
#34647=B_SPLINE_CURVE_WITH_KNOTS ( 'NONE', 3,
 ( #10936, #35484, #20209, #1909, #19817, #23115, #32393, #1302, #13839, #38938 ),
 .UNSPECIFIED., .F., .F.,
 ( 4, 3, 3, 4 ),
 ( 1.964321818484475877E-18, 3.025570593002917179E-05, 6.051145698343843299E-05, 6.468151674594082310E-05 ),
 .UNSPECIFIED. ) ;
#34651=ORIENTED_EDGE ( 'NONE', *, *, #40511, .F. ) ;
#34656=ORIENTED_EDGE ( 'NONE', *, *, #24917, .T. ) ;
#34659=CARTESIAN_POINT ( 'NONE',  ( 1.700390093233090871, -29.56993018339339940, 7.800000000000000711 ) ) ;
#34664=VERTEX_POINT ( 'NONE', #2374 ) ;
#34666=CARTESIAN_POINT ( 'NONE',  ( 0.5278090279835240262, -32.86766614071753168, 7.737115613922530777 ) ) ;
#34669=CARTESIAN_POINT ( 'NONE',  ( -1.697333596569175151, -29.44509923219823122, 6.863904403958576594 ) ) ;
#34671=CARTESIAN_POINT ( 'NONE',  ( 3.011115207906999380, -26.32487479661073948, 7.754798119455333705 ) ) ;
#34673=CARTESIAN_POINT ( 'NONE',  ( -1.796417132220990531, -29.56955632736885420, 7.767581361668585593 ) ) ;
#34674=CARTESIAN_POINT ( 'NONE',  ( 1.507917389220216231, -33.06463394440479675, 6.961115707816240672 ) ) ;
#34677=CARTESIAN_POINT ( 'NONE',  ( 4.676936809477505008, -31.39751676666076463, 7.776484688137385248 ) ) ;
#34678=ORIENTED_EDGE ( 'NONE', *, *, #38521, .T. ) ;
#34679=CARTESIAN_POINT ( 'NONE',  ( 5.200390093233089317, -29.40819670640123462, 7.383456277641987420 ) ) ;
#34686=CARTESIAN_POINT ( 'NONE',  ( 6.433851184000642043, -31.40945003658912071, 7.013842709614101167 ) ) ;
#34687=CARTESIAN_POINT ( 'NONE',  ( 2.082970273350142065, -32.94833696851883786, 6.959317978105167057 ) ) ;
#34689=CARTESIAN_POINT ( 'NONE',  ( -1.490741356227917702, -28.39658077851778728, 7.775108481317161591 ) ) ;
#34694=AXIS2_PLACEMENT_3D ( 'NONE', #28976, #25883, #38422 ) ;
#34696=FACE_OUTER_BOUND ( 'NONE', #4430, .T. ) ;
#34697=CARTESIAN_POINT ( 'NONE',  ( 0.07316740502934632184, -26.58460837109326391, 6.870716933885663735 ) ) ;
#34699=CARTESIAN_POINT ( 'NONE',  ( 3.566793122297630791, -26.60908157518823458, 6.870724624169668893 ) ) ;
#34700=VECTOR ( 'NONE', #10449, 1000.000000000000114 ) ;
#34706=LINE ( 'NONE', #29705, #21267 ) ;
#34711=CARTESIAN_POINT ( 'NONE',  ( 1.700390093233090871, -29.56993018339339940, 7.800000000000000711 ) ) ;
#34714=CARTESIAN_POINT ( 'NONE',  ( -1.585676428981071862, -30.76536307146522731, 7.767720160662275219 ) ) ;
#34721=CARTESIAN_POINT ( 'NONE',  ( -0.1008889408765406975, -32.55456798792236128, 7.784725160561911217 ) ) ;
#34722=AXIS2_PLACEMENT_3D ( 'NONE', #22404, #25284, #40487 ) ;
#34723=CARTESIAN_POINT ( 'NONE',  ( 1.725082688367724160, -32.96984567890832807, 7.740055089680399014 ) ) ;
#34724=EDGE_CURVE ( 'NONE', #651, #28942, #29294, .T. ) ;
#34727=CARTESIAN_POINT ( 'NONE',  ( -1.799609906766908685, -29.56993018339339940, 7.620413589471895399 ) ) ;
#34729=CARTESIAN_POINT ( 'NONE',  ( -0.01129010125266571157, -26.63221833370405633, 7.635761828346577573 ) ) ;
#34730=B_SPLINE_CURVE_WITH_KNOTS ( 'NONE', 3,
 ( #10779, #20869, #23947, #21085, #11583, #1960, #5026, #30144, #30557, #36322, #17971, #13886, #4631, #26452, #1541, #32839, #36125, #1748, #36521, #11382, #17159, #39389, #26653, #14478, #8092, #20659, #23359, #27247, #38980, #33241, #35928 ),
 .UNSPECIFIED., .F., .F.,
 ( 4, 3, 3, 3, 3, 3, 3, 3, 3, 3, 4 ),
 ( 9.697399036122160616E-19, 2.999644130997791255E-05, 6.002588995694985201E-05, 8.960886084588235714E-05, 0.0001190604700446521423, 0.0001489538463052733738, 0.0001796139255494002673, 0.0002109707048517114425, 0.0002426195318110404252, 0.0002740640997890113882, 0.0002849778069099895153 ),
 .UNSPECIFIED. ) ;
#34742=CARTESIAN_POINT ( 'NONE',  ( 2.205779315586366973, -33.02853860453631540, 7.771081512783697853 ) ) ;
#34745=CARTESIAN_POINT ( 'NONE',  ( -2.113887949235214947, -26.01735098123354106, 6.894806418505347700 ) ) ;
#34746=AXIS2_PLACEMENT_3D ( 'NONE', #31453, #12499, #25068 ) ;
#34752=FACE_OUTER_BOUND ( 'NONE', #22117, .T. ) ;
#34762=CARTESIAN_POINT ( 'NONE',  ( -0.8221774698600063935, -27.29028943795776030, 6.863904403958576594 ) ) ;
#34766=CARTESIAN_POINT ( 'NONE',  ( 1.015685340855933649, -33.00230245371492543, 6.866770815808350470 ) ) ;
#34768=LINE ( 'NONE', #164, #18889 ) ;
#34771=DIRECTION ( 'NONE',  ( -0.3420201433256663259, -0.9396926207859092051, 0.000000000000000000 ) ) ;
#34773=ADVANCED_FACE ( 'NONE', ( #27351 ), #33754, .F. ) ;
#34774=CARTESIAN_POINT ( 'NONE',  ( 5.007490259822573009, -30.35928972640521195, 6.988553391373222290 ) ) ;
#34777=( BOUNDED_CURVE ( )  B_SPLINE_CURVE ( 3, ( #32181, #32579, #16302, #23101 ),
 .UNSPECIFIED., .F., .T. ) 
 B_SPLINE_CURVE_WITH_KNOTS ( ( 4, 4 ),
 ( 4.748221474220558846, 4.941946782021393147 ),
 .UNSPECIFIED. ) 
 CURVE ( )  GEOMETRIC_REPRESENTATION_ITEM ( )  RATIONAL_B_SPLINE_CURVE ( ( 1.000000000000000000, 0.9968749865767494445, 0.9968749865767494445, 1.000000000000000000 ) ) 
 REPRESENTATION_ITEM ( '' )  );
#34779=ORIENTED_EDGE ( 'NONE', *, *, #17, .T. ) ;
#34783=VERTEX_POINT ( 'NONE', #1496 ) ;
#34789=EDGE_CURVE ( 'NONE', #2601, #2179, #1386, .T. ) ;
#34794=CARTESIAN_POINT ( 'NONE',  ( 5.200371613545275551, -29.55750178647830850, 7.756555456908253987 ) ) ;
#34797=VERTEX_POINT ( 'NONE', #38436 ) ;
#34803=CARTESIAN_POINT ( 'NONE',  ( 5.151091795598730094, -30.15529994797888946, 7.742274884880762542 ) ) ;
#34806=CARTESIAN_POINT ( 'NONE',  ( 4.582084150952498547, -31.37432464074042215, 7.754798119455333705 ) ) ;
#34808=ORIENTED_EDGE ( 'NONE', *, *, #6574, .T. ) ;
#34811=CARTESIAN_POINT ( 'NONE',  ( 4.676599318385033399, -27.92608080218391109, 6.880147297696981745 ) ) ;
#34817=B_SPLINE_CURVE_WITH_KNOTS ( 'NONE', 3,
 ( #37922, #32334, #34673, #31157, #34875, #7196, #22308, #19756, #16643, #23057, #29228, #2973, #32527 ),
 .UNSPECIFIED., .F., .F.,
 ( 4, 3, 3, 3, 4 ),
 ( 2.475319317933450300E-05, 2.546128104244953829E-05, 5.711050680483697561E-05, 8.113074941675614072E-05, 8.388765757908052086E-05 ),
 .UNSPECIFIED. ) ;
#34829=CARTESIAN_POINT ( 'NONE',  ( 0.5551755531694614332, -32.77125548039569480, 7.748216051605118615 ) ) ;
#34832=CARTESIAN_POINT ( 'NONE',  ( 5.100168698360202590, -29.60992969820402010, 7.784838882742139532 ) ) ;
#34833=CARTESIAN_POINT ( 'NONE',  ( -1.348152954782936730, -27.85051585561017973, 7.710604733652631104 ) ) ;
#34837=CARTESIAN_POINT ( 'NONE',  ( -1.303108374136985104, -31.16335321463953534, 7.754798119455333705 ) ) ;
#34839=VERTEX_POINT ( 'NONE', #3907 ) ;
#34845=CARTESIAN_POINT ( 'NONE',  ( -0.5390219559468002464, -26.88736040713764908, 7.773839561854632763 ) ) ;
#34862=CARTESIAN_POINT ( 'NONE',  ( 2.337381470057465549, -33.01147775668546558, 7.660770905198779346 ) ) ;
#34863=CARTESIAN_POINT ( 'NONE',  ( 1.825008882942001920, -26.07214915268203725, 7.751599049952198506 ) ) ;
#34868=DIRECTION ( 'NONE',  ( 0.7126435865141269588, 0.000000000000000000, -0.7015262779114422864 ) ) ;
#34874=CARTESIAN_POINT ( 'NONE',  ( -1.422192660794930674, -31.15090360007274839, 6.951256099901591767 ) ) ;
#34875=CARTESIAN_POINT ( 'NONE',  ( -1.794043895342124495, -29.56109672522452669, 7.773839561854631874 ) ) ;
#34877=VECTOR ( 'NONE', #33268, 1000.000000000000114 ) ;
#34879=CARTESIAN_POINT ( 'NONE',  ( -0.6205797297147237490, -32.05451548273851614, 6.887945620086118659 ) ) ;
#34880=B_SPLINE_CURVE_WITH_KNOTS ( 'NONE', 3,
 ( #8778, #36191, #40282, #2652, #14751, #2231, #11659, #36795, #40085, #27321, #36595, #24233, #14349, #39883, #8580, #5504, #5713, #11863, #24021, #15170, #33725, #8164, #33530, #11250, #12072, #18047, #7972, #20524, #30639, #2447, #36999 ),
 .UNSPECIFIED., .F., .F.,
 ( 4, 3, 3, 3, 3, 3, 3, 3, 3, 3, 4 ),
 ( 1.939479807224432123E-18, 2.999644130997642855E-05, 6.002588995694698565E-05, 8.960886084587837269E-05, 0.0001190604700446467484, 0.0001489538463052699857, 0.0001796139255493966894, 0.0002109707048517059944, 0.0002426195318110339471, 0.0002740640997890056961, 0.0002849778069099870217 ),
 .UNSPECIFIED. ) ;
#34885=CARTESIAN_POINT ( 'NONE',  ( -0.9006766493021783893, -31.75956955190471120, 7.763628509615291939 ) ) ;
#34887=DIRECTION ( 'NONE',  ( 0.4999999999999927836, 0.8660254037844429265, 0.000000000000000000 ) ) ;
#34892=EDGE_LOOP ( 'NONE', ( #22780, #11489, #36889, #24111 ) ) ;
#34893=VERTEX_POINT ( 'NONE', #29191 ) ;
#34894=CARTESIAN_POINT ( 'NONE',  ( -1.510909903798922427, -30.68686900403765705, 6.894806418505348589 ) ) ;
#34895=B_SPLINE_CURVE_WITH_KNOTS ( 'NONE', 3,
 ( #37932, #35085, #31574, #9741, #10339, #32192, #25796, #16701, #38329, #3992, #3399, #35284, #19814, #15915, #28474, #7051, #16512, #29087, #13424, #22911, #7251, #32390, #4184, #1101, #26208 ),
 .UNSPECIFIED., .F., .F.,
 ( 4, 3, 3, 3, 3, 3, 3, 3, 4 ),
 ( 6.468151674593725878E-05, 9.076621574722179618E-05, 0.0001210204262067967739, 0.0001512763324577452186, 0.0001815301820994223248, 0.0002117781465860755575, 0.0002420274594459800323, 0.0002722905548971162764, 0.0002816827545175597637 ),
 .UNSPECIFIED. ) ;
#34897=EDGE_LOOP ( 'NONE', ( #6538, #2522, #6499, #17532 ) ) ;
#34898=CARTESIAN_POINT ( 'NONE',  ( -0.9174058041325571233, -27.26220320217948867, 7.780491323090171996 ) ) ;
#34901=CARTESIAN_POINT ( 'NONE',  ( 3.589445461969659856, -26.62348856653665052, 6.887547729233690852 ) ) ;
#34911=CARTESIAN_POINT ( 'NONE',  ( 4.372846383550529126, -27.30984669459420289, 7.635761828346578461 ) ) ;
#34915=CARTESIAN_POINT ( 'NONE',  ( -1.665924965603348351, -30.04734292374604010, 6.864276522220859711 ) ) ;
#34921=DIRECTION ( 'NONE',  ( 1.000000000000000000, -7.930164461608261228E-15, 0.000000000000000000 ) ) ;
#34925=DIRECTION ( 'NONE',  ( 0.9396926207859082059, 0.3420201433256695456, -0.000000000000000000 ) ) ;
#34929=CARTESIAN_POINT ( 'NONE',  ( 3.385812859895339422, -32.63741323173702824, 6.867280401193709416 ) ) ;
#34930=CARTESIAN_POINT ( 'NONE',  ( -1.004988036239387261, -31.79051028124264988, 6.887161170156904433 ) ) ;
#34931=CARTESIAN_POINT ( 'NONE',  ( 5.196299276553091318, -29.73910164073445017, 7.013842709614101167 ) ) ;
#34933=CARTESIAN_POINT ( 'NONE',  ( 0.06066625181903905623, -26.47779407321028700, 7.750000000000000888 ) ) ;
#34935=CARTESIAN_POINT ( 'NONE',  ( 1.700390093233090871, -29.56993018339339940, 7.800000000000000711 ) ) ;
#34953=EDGE_LOOP ( 'NONE', ( #9772, #15665, #997, #23936, #2695 ) ) ;
#34959=ORIENTED_EDGE ( 'NONE', *, *, #2630, .T. ) ;
#34963=CARTESIAN_POINT ( 'NONE',  ( -0.5270797881493830550, -32.26962978289218853, 7.730015791551952731 ) ) ;
#34964=CARTESIAN_POINT ( 'NONE',  ( 1.822194502883780931, -26.07228119081829476, 7.754798119455333705 ) ) ;
#34968=CARTESIAN_POINT ( 'NONE',  ( -1.799566460562916470, -29.58736926422850999, 7.749999999999998224 ) ) ;
#34969=ORIENTED_EDGE ( 'NONE', *, *, #13798, .T. ) ;
#34970=CARTESIAN_POINT ( 'NONE',  ( -1.752826142657526676, -30.14031989453273752, 6.887161170156907097 ) ) ;
#34971=CARTESIAN_POINT ( 'NONE',  ( -0.5679913539545495826, -32.21827145269413251, 7.783750581861601070 ) ) ;
#34979=ORIENTED_EDGE ( 'NONE', *, *, #24838, .T. ) ;
#34980=CARTESIAN_POINT ( 'NONE',  ( -1.576323396845137781, -30.80003141911850051, 7.710604733652623999 ) ) ;
#34988=EDGE_CURVE ( 'NONE', #17567, #7963, #26899, .T. ) ;
#34990=ORIENTED_EDGE ( 'NONE', *, *, #24548, .T. ) ;
#34993=CARTESIAN_POINT ( 'NONE',  ( -0.8954611659357714082, -31.76573441880953297, 7.635761828346577573 ) ) ;
#34994=DIRECTION ( 'NONE',  ( -0.7394003126383923430, -0.1303762246624306231, 0.6605219282605377940 ) ) ;
#34996=CARTESIAN_POINT ( 'NONE',  ( -1.654012860102806792, -29.01496998062980381, 7.703977250142846955 ) ) ;
#34997=ORIENTED_EDGE ( 'NONE', *, *, #635, .T. ) ;
#34999=AXIS2_PLACEMENT_3D ( 'NONE', #5307, #11662, #36194 ) ;
#35000=ORIENTED_EDGE ( 'NONE', *, *, #25028, .T. ) ;
#35002=ADVANCED_FACE ( 'NONE', ( #4870 ), #5282, .F. ) ;
#35004=CARTESIAN_POINT ( 'NONE',  ( -1.499157785959173594, -28.41975916621540321, 7.635761828346577573 ) ) ;
#35006=ORIENTED_EDGE ( 'NONE', *, *, #35682, .F. ) ;
#35008=CARTESIAN_POINT ( 'NONE',  ( 4.670146650652899467, -27.91446891051451118, 6.892063359921934307 ) ) ;
#35013=CARTESIAN_POINT ( 'NONE',  ( 0.6135038235497226600, -26.24384652275122676, 7.761113333117552138 ) ) ;
#35017=ORIENTED_EDGE ( 'NONE', *, *, #31399, .F. ) ;
#35021=ORIENTED_EDGE ( 'NONE', *, *, #14968, .T. ) ;
#35022=CARTESIAN_POINT ( 'NONE',  ( 1.067007105073786599, -26.12771653675251571, 7.737115613922531665 ) ) ;
#35025=ORIENTED_EDGE ( 'NONE', *, *, #31863, .F. ) ;
#35026=CARTESIAN_POINT ( 'NONE',  ( 1.700390093233090871, -29.56993018339339940, 7.750000000000000888 ) ) ;
#35031=DIRECTION ( 'NONE',  ( -0.000000000000000000, -0.000000000000000000, 1.000000000000000000 ) ) ;
#35033=EDGE_CURVE ( 'NONE', #30829, #25728, #11845, .T. ) ;
#35035=EDGE_CURVE ( 'NONE', #5035, #35820, #16104, .T. ) ;
#35038=EDGE_LOOP ( 'NONE', ( #36190, #19488, #26974, #16235 ) ) ;
#35041=CARTESIAN_POINT ( 'NONE',  ( 1.584141490162101373, -33.06716345315124528, 7.761113333117551250 ) ) ;
#35043=DIRECTION ( 'NONE',  ( 1.000000000000000000, 0.000000000000000000, 0.000000000000000000 ) ) ;
#35044=EDGE_LOOP ( 'NONE', ( #14594, #16625, #20227, #31652, #12453 ) ) ;
#35049=ORIENTED_EDGE ( 'NONE', *, *, #16724, .T. ) ;
#35052=ORIENTED_EDGE ( 'NONE', *, *, #25587, .T. ) ;
#35056=CARTESIAN_POINT ( 'NONE',  ( -1.752388709028311897, -28.99693776809384715, 7.707984471951056626 ) ) ;
#35059=CARTESIAN_POINT ( 'NONE',  ( 2.435848945842617574, -26.14806070922363901, 6.868546646838339598 ) ) ;
#35065=VECTOR ( 'NONE', #17573, 999.9999999999998863 ) ;
#35069=CARTESIAN_POINT ( 'NONE',  ( 0.5306047266319490197, -32.86865754346513313, 7.730015791551945625 ) ) ;
#35071=CARTESIAN_POINT ( 'NONE',  ( -0.2002656416234501746, -32.50890187101184381, 6.903112506833895878 ) ) ;
#35074=CARTESIAN_POINT ( 'NONE',  ( -1.699430275127282286, -29.60499886526849167, 7.711434774245209844 ) ) ;
#35084=CARTESIAN_POINT ( 'NONE',  ( 1.714820913762807653, -33.06990055655550975, 7.636816916992233750 ) ) ;
#35085=CARTESIAN_POINT ( 'NONE',  ( 3.431434570054125111, -32.49627346798381211, 7.703977250142848732 ) ) ;
#35087=B_SPLINE_CURVE_WITH_KNOTS ( 'NONE', 3,
 ( #17756, #27043, #21278, #27448, #30963, #27647, #11375, #40202, #5018, #23940 ),
 .UNSPECIFIED., .F., .F.,
 ( 4, 3, 3, 4 ),
 ( 0.0001585009270395724165, 0.0001815657551981852242, 0.0002118214035944144299, 0.0002170292169044774099 ),
 .UNSPECIFIED. ) ;
#35088=EDGE_CURVE ( 'NONE', #15576, #347, #27301, .T. ) ;
#35095=LINE ( 'NONE', #6871, #31829 ) ;
#35098=CARTESIAN_POINT ( 'NONE',  ( 1.226041064583952567, -26.20318123971300750, 7.759451378593095860 ) ) ;
#35099=CARTESIAN_POINT ( 'NONE',  ( 1.700390093233090871, -29.56993018339339940, 7.750000000000000888 ) ) ;
#35100=ORIENTED_EDGE ( 'NONE', *, *, #20916, .F. ) ;
#35103=AXIS2_PLACEMENT_3D ( 'NONE', #3816, #10364, #9550 ) ;
#35108=CARTESIAN_POINT ( 'NONE',  ( -1.662903320652827421, -30.06828107640362902, 6.866852738645443210 ) ) ;
#35111=EDGE_CURVE ( 'NONE', #35525, #3023, #15662, .T. ) ;
#35121=CARTESIAN_POINT ( 'NONE',  ( 3.922988059513587089, -26.99698279172644177, 6.894806418505345924 ) ) ;
#35126=( BOUNDED_CURVE ( )  B_SPLINE_CURVE ( 3, ( #16043, #25523, #6593, #15227 ),
 .UNSPECIFIED., .F., .F. ) 
 B_SPLINE_CURVE_WITH_KNOTS ( ( 4, 4 ),
 ( 4.708531083176467291, 4.886921905584122428 ),
 .UNSPECIFIED. ) 
 CURVE ( )  GEOMETRIC_REPRESENTATION_ITEM ( )  RATIONAL_B_SPLINE_CURVE ( ( 1.000000000000000000, 0.9973498172709135412, 0.9973498172709135412, 1.000000000000000000 ) ) 
 REPRESENTATION_ITEM ( '' )  );
#35128=CARTESIAN_POINT ( 'NONE',  ( 5.197761719230830302, -29.70585831616093841, 6.870724624169664452 ) ) ;
#35130=CARTESIAN_POINT ( 'NONE',  ( -0.5767923600352592439, -26.91202874155498037, 7.695279973900954751 ) ) ;
#35133=AXIS2_PLACEMENT_3D ( 'NONE', #3604, #38145, #28280 ) ;
#35142=AXIS2_PLACEMENT_3D ( 'NONE', #6212, #37485, #12579 ) ;
#35149=CARTESIAN_POINT ( 'NONE',  ( 2.983339616719596243, -26.32124682031997409, 7.776484688137384360 ) ) ;
#35151=ORIENTED_EDGE ( 'NONE', *, *, #34538, .T. ) ;
#35153=EDGE_LOOP ( 'NONE', ( #8150, #21251, #4399, #124, #21460 ) ) ;
#35155=B_SPLINE_CURVE_WITH_KNOTS ( 'NONE', 3,
 ( #26552, #11081, #26160, #4725, #19770, #29040, #38486, #38892, #32938, #16469 ),
 .UNSPECIFIED., .F., .F.,
 ( 4, 3, 3, 4 ),
 ( 1.939479807224432123E-18, 3.025570593003303765E-05, 6.051145698344102830E-05, 6.468151674593725878E-05 ),
 .UNSPECIFIED. ) ;
#35158=ORIENTED_EDGE ( 'NONE', *, *, #28555, .T. ) ;
#35161=CARTESIAN_POINT ( 'NONE',  ( -1.450854365928797352, -28.29334945402236556, 7.754798119455333705 ) ) ;
#35165=EDGE_LOOP ( 'NONE', ( #36325, #12106, #18754, #24640, #33866 ) ) ;
#35166=CARTESIAN_POINT ( 'NONE',  ( 0.1384972100046504007, -34.01952225562621379, 7.695279973900954751 ) ) ;
#35169=CARTESIAN_POINT ( 'NONE',  ( -0.9762178946850544881, -31.66653927404734858, 6.864276522220859711 ) ) ;
#35170=CARTESIAN_POINT ( 'NONE',  ( -0.5849894831158207742, -32.20111717317018929, 7.785593909369613819 ) ) ;
#35172=CARTESIAN_POINT ( 'NONE',  ( 4.714906974314832411, -27.79153115915092798, 7.720710062488890912 ) ) ;
#35173=CYLINDRICAL_SURFACE ( 'NONE', #31364, 0.09010775117052761962 ) ;
#35177=CARTESIAN_POINT ( 'NONE',  ( -0.8876268677054017786, -31.77496589654743531, 7.652160403243383868 ) ) ;
#35183=CARTESIAN_POINT ( 'NONE',  ( -0.3228067372202657603, -26.83740853018669625, 6.929923840112064859 ) ) ;
#35189=CARTESIAN_POINT ( 'NONE',  ( 4.246333203224189390, -31.82341053180756774, 7.778050822775633755 ) ) ;
#35196=CARTESIAN_POINT ( 'NONE',  ( 2.910139986571841586, -32.85421171754464353, 7.635761828346577573 ) ) ;
#35200=ORIENTED_EDGE ( 'NONE', *, *, #3947, .T. ) ;
#35202=VERTEX_POINT ( 'NONE', #3254 ) ;
#35207=ORIENTED_EDGE ( 'NONE', *, *, #23533, .T. ) ;
#35208=CARTESIAN_POINT ( 'NONE',  ( 4.742477098443226957, -31.30074747219525833, 7.743886751744250674 ) ) ;
#35210=CARTESIAN_POINT ( 'NONE',  ( 4.564215312071829622, -31.40257868915064066, 6.871394612369934762 ) ) ;
#35211=CARTESIAN_POINT ( 'NONE',  ( 3.964955798375757734, -32.23858942861218679, 7.643192810543823157 ) ) ;
#35215=ORIENTED_EDGE ( 'NONE', *, *, #18929, .F. ) ;
#35223=CARTESIAN_POINT ( 'NONE',  ( 0.3635682928745467835, -32.69609516209911959, 7.013842709614101167 ) ) ;
#35230=CARTESIAN_POINT ( 'NONE',  ( 5.078796878358532219, -29.18735000327637508, 6.959317978105165281 ) ) ;
#35231=ADVANCED_FACE ( 'NONE', ( #3456 ), #34536, .F. ) ;
#35233=FACE_OUTER_BOUND ( 'NONE', #15703, .T. ) ;
#35237=CARTESIAN_POINT ( 'NONE',  ( 3.343728876470205336, -32.65988526930982516, 7.754798119455333705 ) ) ;
#35242=CARTESIAN_POINT ( 'NONE',  ( 1.615255430553348415, -33.05865649385363980, 7.780491323090172884 ) ) ;
#35245=VERTEX_POINT ( 'NONE', #15568 ) ;
#35249=ORIENTED_EDGE ( 'NONE', *, *, #13798, .F. ) ;
#35253=VERTEX_POINT ( 'NONE', #31632 ) ;
#35256=CARTESIAN_POINT ( 'NONE',  ( 2.840026228868236302, -26.36660931603533697, 7.740055089680404343 ) ) ;
#35257=EDGE_LOOP ( 'NONE', ( #34056, #33358, #26540, #40090, #34190 ) ) ;
#35258=ORIENTED_EDGE ( 'NONE', *, *, #38842, .F. ) ;
#35266=CARTESIAN_POINT ( 'NONE',  ( 4.425294480038274081, -27.53648579448824307, 6.903372536218453703 ) ) ;
#35268=EDGE_CURVE ( 'NONE', #22017, #23856, #37993, .T. ) ;
#35274=CARTESIAN_POINT ( 'NONE',  ( 0.5248424762351729944, -26.37961863118246697, 7.635761828346577573 ) ) ;
#35276=CARTESIAN_POINT ( 'NONE',  ( 5.200390093233090205, -29.56993018339339940, 6.850000000000000533 ) ) ;
#35279=CARTESIAN_POINT ( 'NONE',  ( -1.543298022821887328, -28.25521066738867049, 7.750000000000000888 ) ) ;
#35280=ADVANCED_FACE ( 'NONE', ( #31028 ), #40676, .F. ) ;
#35282=LINE ( 'NONE', #7049, #28585 ) ;
#35284=CARTESIAN_POINT ( 'NONE',  ( 3.382565993577793861, -32.52465162557860623, 7.779495906702013741 ) ) ;
#35289=VERTEX_POINT ( 'NONE', #40457 ) ;
#35294=DIRECTION ( 'NONE',  ( -0.000000000000000000, -0.000000000000000000, -1.000000000000000000 ) ) ;
#35297=CARTESIAN_POINT ( 'NONE',  ( 5.048061004931336804, -28.54860354809848033, 6.989977667959443863 ) ) ;
#35298=CARTESIAN_POINT ( 'NONE',  ( 1.075872451927647244, -26.22777759477400039, 7.712764235869105534 ) ) ;
#35299=CARTESIAN_POINT ( 'NONE',  ( 1.175744690447600105, -26.10947541539887240, 6.865554069792297653 ) ) ;
#35305=B_SPLINE_CURVE_WITH_KNOTS ( 'NONE', 3,
 ( #9574, #21945, #3441, #6506, #15957, #12869, #31413, #28519, #37977, #12052, #27714, #37183, #14951, #8973, #21559, #34135, #40070, #25193, #37723, #11998, #18588, #31375, #5853, #34285, #8712, #15102, #15513, #28271, #28069, #6466, #40622 ),
 .UNSPECIFIED., .F., .F.,
 ( 4, 3, 3, 3, 3, 3, 3, 3, 3, 3, 4 ),
 ( 1.748223473168675632E-18, 2.999644130997695371E-05, 6.002588995694948609E-05, 8.960886084588150333E-05, 0.0001190604700446518306, 0.0001489538463052718831, 0.0001796139255494018936, 0.0002109707048517080001, 0.0002426195318110375249, 0.0002740640997890114424, 0.0002849778069099955869 ),
 .UNSPECIFIED. ) ;
#35310=CARTESIAN_POINT ( 'NONE',  ( -1.719074876076428948, -28.82337947204507245, 6.873192711770539809 ) ) ;
#35322=B_SPLINE_CURVE_WITH_KNOTS ( 'NONE', 3,
 ( #177, #38228, #9832, #22408, #3891, #22210, #587, #10025, #989, #12713 ),
 .UNSPECIFIED., .F., .F.,
 ( 4, 3, 3, 4 ),
 ( 0.0001585009270395791115, 0.0001815657551981845195, 0.0002118214035944147281, 0.0002170292169044849180 ),
 .UNSPECIFIED. ) ;
#35324=ORIENTED_EDGE ( 'NONE', *, *, #31070, .F. ) ;
#35327=CARTESIAN_POINT ( 'NONE',  ( -0.04364293620010380181, -32.60287272531510894, 7.762796336881260473 ) ) ;
#35329=CARTESIAN_POINT ( 'NONE',  ( -1.026852816783328626, -31.74722329408204757, 7.780491323090176436 ) ) ;
#35331=DIRECTION ( 'NONE',  ( -0.3420201433256726542, 0.9396926207859070956, -0.000000000000000000 ) ) ;
#35332=CYLINDRICAL_SURFACE ( 'NONE', #32141, 3.399999999999999911 ) ;
#35334=CARTESIAN_POINT ( 'NONE',  ( 5.198825856949740754, -29.67505948803950488, 6.863784140767622333 ) ) ;
#35346=ORIENTED_EDGE ( 'NONE', *, *, #29461, .F. ) ;
#35348=EDGE_CURVE ( 'NONE', #4130, #20764, #1815, .T. ) ;
#35349=CARTESIAN_POINT ( 'NONE',  ( 2.881058359821971226, -26.27508231979332010, 7.750000000000000000 ) ) ;
#35351=ORIENTED_EDGE ( 'NONE', *, *, #5456, .T. ) ;
#35356=B_SPLINE_CURVE_WITH_KNOTS ( 'NONE', 3,
 ( #10031, #1203, #28986, #789, #593, #38234, #26500, #29185, #22613, #35183, #10827, #13318, #32095, #3899, #38430, #22815, #7155, #19716, #32291, #4089, #13532, #26106, #38638, #10436, #39859, #5273, #27095, #30611, #11428, #17814, #24416 ),
 .UNSPECIFIED., .F., .F.,
 ( 4, 3, 3, 3, 3, 3, 3, 3, 3, 3, 4 ),
 ( 1.084202172485504434E-19, 2.999644130997704858E-05, 6.002588995694863906E-05, 8.960886084588055465E-05, 0.0001190604700446490523, 0.0001489538463052745123, 0.0001796139255493987494, 0.0002109707048517110088, 0.0002426195318110379857, 0.0002740640997890076477, 0.0002849778069099910332 ),
 .UNSPECIFIED. ) ;
#35358=CARTESIAN_POINT ( 'NONE',  ( -1.299626552915077449, -31.16989897147455935, 6.864276522220859711 ) ) ;
#35362=ADVANCED_FACE ( 'NONE', ( #10193 ), #953, .F. ) ;
#35363=CARTESIAN_POINT ( 'NONE',  ( 0.9954086067726409803, -32.99821069240157101, 6.863654226668488789 ) ) ;
#35364=CARTESIAN_POINT ( 'NONE',  ( -1.784401156299032509, -29.50863702383910336, 7.785387725071482024 ) ) ;
#35370=CARTESIAN_POINT ( 'NONE',  ( 5.200323364668523851, -29.54781842220009480, 7.743886751744250674 ) ) ;
#35373=CARTESIAN_POINT ( 'NONE',  ( -1.030507639981847356, -31.59532027377766283, 6.920489980334481039 ) ) ;
#35376=DIRECTION ( 'NONE',  ( -0.000000000000000000, -0.000000000000000000, -1.000000000000000000 ) ) ;
#35382=CARTESIAN_POINT ( 'NONE',  ( -1.641543316846993505, -30.19561467464317772, 7.691066658568947112 ) ) ;
#35384=CARTESIAN_POINT ( 'NONE',  ( 1.740389608043702241, -26.17015157826628524, 7.784838882742139532 ) ) ;
#35386=CARTESIAN_POINT ( 'NONE',  ( -1.002985311074516162, -27.34692170059995675, 7.678495282201408756 ) ) ;
#35393=ORIENTED_EDGE ( 'NONE', *, *, #38575, .T. ) ;
#35395=CARTESIAN_POINT ( 'NONE',  ( -0.4289785860461575728, -26.79218406234506844, 6.880828092187094569 ) ) ;
#35396=CARTESIAN_POINT ( 'NONE',  ( 4.358291535071521672, -27.29274773012506827, 7.695279973900954751 ) ) ;
#35397=VECTOR ( 'NONE', #21023, 1000.000000000000114 ) ;
#35400=ORIENTED_EDGE ( 'NONE', *, *, #1283, .T. ) ;
#35402=ORIENTED_EDGE ( 'NONE', *, *, #15044, .T. ) ;
#35406=EDGE_LOOP ( 'NONE', ( #166, #11697, #5946, #37925 ) ) ;
#35408=EDGE_CURVE ( 'NONE', #36238, #36741, #10323, .T. ) ;
#35410=CARTESIAN_POINT ( 'NONE',  ( 0.03050408833857739394, -32.53159980382280736, 7.712764235869104645 ) ) ;
#35411=EDGE_CURVE ( 'NONE', #4455, #40540, #33755, .T. ) ;
#35413=CARTESIAN_POINT ( 'NONE',  ( 4.536150672677811357, -31.44568654712173128, 6.929923840112063971 ) ) ;
#35415=DIRECTION ( 'NONE',  ( 0.2567910337120269948, 0.7055275666422181624, 0.6605219282605379050 ) ) ;
#35429=DIRECTION ( 'NONE',  ( 0.000000000000000000, -0.6662082868431825622, 0.7457657263118704360 ) ) ;
#35430=CARTESIAN_POINT ( 'NONE',  ( 5.073402035585432124, -29.14231025274367326, 6.876076431790004939 ) ) ;
#35434=CARTESIAN_POINT ( 'NONE',  ( 4.404045757636788849, -31.79259668886174595, 7.710604733652627552 ) ) ;
#35435=CARTESIAN_POINT ( 'NONE',  ( 3.863272490615877519, -26.94658504119581011, 7.661510568013093270 ) ) ;
#35440=ORIENTED_EDGE ( 'NONE', *, *, #8566, .T. ) ;
#35442=CARTESIAN_POINT ( 'NONE',  ( 1.578585683582428345, -33.06757917596850405, 7.754798119455333705 ) ) ;
#35448=CARTESIAN_POINT ( 'NONE',  ( 0.000000000000000000, 0.000000000000000000, 0.000000000000000000 ) ) ;
#35449=VERTEX_POINT ( 'NONE', #10220 ) ;
#35451=CARTESIAN_POINT ( 'NONE',  ( 3.799299724975022219, -32.37074764920551218, 6.961115707816239784 ) ) ;
#35455=CARTESIAN_POINT ( 'NONE',  ( -1.316098561281709767, -31.34497840729704521, 7.730015791551948290 ) ) ;
#35456=EDGE_CURVE ( 'NONE', #17660, #33469, #11115, .T. ) ;
#35459=CARTESIAN_POINT ( 'NONE',  ( 2.385094845610274295, -26.13755791307188048, 6.866770815808350470 ) ) ;
#35465=CIRCLE ( 'NONE', #22970, 3.499999999999999556 ) ;
#35469=CARTESIAN_POINT ( 'NONE',  ( -0.1485713413135285321, -32.54168751089497391, 6.865482280155369210 ) ) ;
#35471=CARTESIAN_POINT ( 'NONE',  ( -1.699558106226426890, -29.58869826779166701, 7.748216051605116839 ) ) ;
#35473=ORIENTED_EDGE ( 'NONE', *, *, #19034, .T. ) ;
#35474=FACE_OUTER_BOUND ( 'NONE', #8329, .T. ) ;
#35477=CARTESIAN_POINT ( 'NONE',  ( 1.141703107443977849, -32.92371444179612183, 7.721096864323902409 ) ) ;
#35479=CYLINDRICAL_SURFACE ( 'NONE', #16751, 0.09010775117052885475 ) ;
#35480=B_SPLINE_CURVE_WITH_KNOTS ( 'NONE', 3,
 ( #37704, #6236, #31154, #5621, #18567, #2760, #15286, #24554, #36910, #12194, #18780, #37510, #15697, #33843, #8691, #14868, #18161, #30956, #15079, #3183, #34669, #30755, #6447, #22094, #2970, #27838, #28249, #11976, #31357, #40392, #19000 ),
 .UNSPECIFIED., .F., .F.,
 ( 4, 3, 3, 3, 3, 3, 3, 3, 3, 3, 4 ),
 ( 0.000000000000000000, 2.999644130997664200E-05, 6.002588995694806986E-05, 8.960886084588066307E-05, 0.0001190604700446488490, 0.0001489538463052730486, 0.0001796139255493973128, 0.0002109707048517051541, 0.0002426195318110360071, 0.0002740640997890082440, 0.0002849778069099824680 ),
 .UNSPECIFIED. ) ;
#35484=CARTESIAN_POINT ( 'NONE',  ( -0.4696069411706714214, -32.18740172037517766, 7.643333865083952183 ) ) ;
#35485=VERTEX_POINT ( 'NONE', #580 ) ;
#35489=CARTESIAN_POINT ( 'NONE',  ( 4.713340623123058570, -27.78888299018493058, 7.686927408461905920 ) ) ;
#35491=VERTEX_POINT ( 'NONE', #38626 ) ;
#35497=CARTESIAN_POINT ( 'NONE',  ( 4.241058378038022880, -25.24127732835732374, 7.695279973900954751 ) ) ;
#35498=CARTESIAN_POINT ( 'NONE',  ( 4.402303332471854347, -31.79471440835236606, 7.670465701733749420 ) ) ;
#35500=CARTESIAN_POINT ( 'NONE',  ( 4.944606980600187107, -30.88334510993980686, 7.751599049952199394 ) ) ;
#35504=VERTEX_POINT ( 'NONE', #25677 ) ;
#35507=CARTESIAN_POINT ( 'NONE',  ( -1.731684944490798905, -28.88366151015853944, 6.865833476810890623 ) ) ;
#35515=VERTEX_POINT ( 'NONE', #31459 ) ;
#35520=CARTESIAN_POINT ( 'NONE',  ( 3.412070287718869999, -32.50764203308273181, 7.635761828346577573 ) ) ;
#35521=EDGE_CURVE ( 'NONE', #19820, #3554, #3282, .T. ) ;
#35522=CARTESIAN_POINT ( 'NONE',  ( -0.1356099412391454651, -32.54423587553223740, 7.771081512783701406 ) ) ;
#35525=VERTEX_POINT ( 'NONE', #32079 ) ;
#35527=CARTESIAN_POINT ( 'NONE',  ( -2.165713543243725780, -26.06083781805162403, 6.954324564059724878 ) ) ;
#35528=CARTESIAN_POINT ( 'NONE',  ( -1.098727649675871554, -31.67110930927854184, 6.931070083220560285 ) ) ;
#35529=CARTESIAN_POINT ( 'NONE',  ( 5.001438667734867671, -30.73314912614656436, 7.695279973900954751 ) ) ;
#35534=FACE_OUTER_BOUND ( 'NONE', #10644, .T. ) ;
#35535=CARTESIAN_POINT ( 'NONE',  ( 2.244862549643315219, -33.02733246477049533, 6.870737987065013819 ) ) ;
#35536=ORIENTED_EDGE ( 'NONE', *, *, #24723, .F. ) ;
#35537=EDGE_CURVE ( 'NONE', #16444, #22296, #27152, .T. ) ;
#35540=EDGE_CURVE ( 'NONE', #13794, #37354, #28349, .T. ) ;
#35544=EDGE_LOOP ( 'NONE', ( #40274, #21478, #14893, #12731, #29604 ) ) ;
#35546=B_SPLINE_CURVE_WITH_KNOTS ( 'NONE', 3,
 ( #39267, #23438, #20330, #1621, #30015, #11254, #39676, #14355, #4513, #26925 ),
 .UNSPECIFIED., .F., .F.,
 ( 4, 3, 3, 4 ),
 ( 0.000000000000000000, 3.025570593003334597E-05, 6.051145698344288499E-05, 6.468151674594163625E-05 ),
 .UNSPECIFIED. ) ;
#35548=CARTESIAN_POINT ( 'NONE',  ( 2.279805425825974119, -32.92020578787989393, 7.775108481317161591 ) ) ;
#35551=CARTESIAN_POINT ( 'NONE',  ( -1.751664738099543150, -28.99259367712256008, 7.665454363767880253 ) ) ;
#35553=ORIENTED_EDGE ( 'NONE', *, *, #29461, .T. ) ;
#35559=FACE_OUTER_BOUND ( 'NONE', #28385, .T. ) ;
#35560=FACE_OUTER_BOUND ( 'NONE', #17223, .T. ) ;
#35561=PLANE ( 'NONE',  #34096 ) ;
#35563=CARTESIAN_POINT ( 'NONE',  ( 3.499140961715896836, -26.68471003353787196, 7.761597726988846091 ) ) ;
#35564=ORIENTED_EDGE ( 'NONE', *, *, #12594, .T. ) ;
#35569=CARTESIAN_POINT ( 'NONE',  ( -0.6163032562860591979, -32.18389938704100217, 7.776484688137376367 ) ) ;
#35571=CARTESIAN_POINT ( 'NONE',  ( 5.141937666525170592, -28.93293880656905870, 7.660770905198778458 ) ) ;
#35572=FACE_OUTER_BOUND ( 'NONE', #39603, .T. ) ;
#35577=CARTESIAN_POINT ( 'NONE',  ( 3.924861072458515565, -26.86775624777466120, 7.720710062488897130 ) ) ;
#35579=CARTESIAN_POINT ( 'NONE',  ( 1.808121863982283584, -26.17162928199792304, 7.768425012602592439 ) ) ;
#35582=CARTESIAN_POINT ( 'NONE',  ( 4.882868366733327470, -28.37333834040810032, 7.703977250142848732 ) ) ;
#35590=CARTESIAN_POINT ( 'NONE',  ( 4.817694033729734038, -30.92728660960060338, 6.969307238440502594 ) ) ;
#35591=PLANE ( 'NONE',  #37921 ) ;
#35592=CARTESIAN_POINT ( 'NONE',  ( 4.360557156959933955, -27.29539480379102656, 7.670465701733752084 ) ) ;
#35593=ORIENTED_EDGE ( 'NONE', *, *, #35456, .F. ) ;
#35595=CARTESIAN_POINT ( 'NONE',  ( 4.907464300517769829, -30.69894525369553762, 7.703977250142849620 ) ) ;
#35598=ORIENTED_EDGE ( 'NONE', *, *, #36764, .T. ) ;
#35600=( BOUNDED_CURVE ( )  B_SPLINE_CURVE ( 3, ( #17219, #29791, #1604, #12780 ),
 .UNSPECIFIED., .F., .T. ) 
 B_SPLINE_CURVE_WITH_KNOTS ( ( 4, 4 ),
 ( 4.748221474220559735, 4.941946782021394036 ),
 .UNSPECIFIED. ) 
 CURVE ( )  GEOMETRIC_REPRESENTATION_ITEM ( )  RATIONAL_B_SPLINE_CURVE ( ( 1.000000000000000000, 0.9968749865767494445, 0.9968749865767494445, 1.000000000000000000 ) ) 
 REPRESENTATION_ITEM ( '' )  );
#35605=VECTOR ( 'NONE', #20003, 999.9999999999998863 ) ;
#35608=DIRECTION ( 'NONE',  ( -0.9848077530122092416, 0.1736481776669241694, -0.000000000000000000 ) ) ;
#35612=ORIENTED_EDGE ( 'NONE', *, *, #40257, .T. ) ;
#35613=CARTESIAN_POINT ( 'NONE',  ( 5.131276765095678982, -30.20322308033647118, 7.781480525794718162 ) ) ;
#35614=ORIENTED_EDGE ( 'NONE', *, *, #31920, .T. ) ;
#35618=EDGE_LOOP ( 'NONE', ( #9442, #40366, #14044, #29830, #18283 ) ) ;
#35619=CARTESIAN_POINT ( 'NONE',  ( 0.3455553403917285271, -32.68833086202552352, 6.929923840112063083 ) ) ;
#35630=DIRECTION ( 'NONE',  ( -0.000000000000000000, -0.000000000000000000, -1.000000000000000000 ) ) ;
#35631=CARTESIAN_POINT ( 'NONE',  ( 3.860356151429478189, -26.94418059254374143, 7.670860738520325128 ) ) ;
#35634=CARTESIAN_POINT ( 'NONE',  ( -1.641525177248355893, -30.19571155489859393, 7.703977250142848732 ) ) ;
#35641=CARTESIAN_POINT ( 'NONE',  ( -1.644222468574767726, -30.60122393950611652, 7.006908160621410531 ) ) ;
#35648=CARTESIAN_POINT ( 'NONE',  ( 3.807593891317279766, -32.36451543350154481, 6.912143950357347855 ) ) ;
#35656=CARTESIAN_POINT ( 'NONE',  ( 2.454444230655590697, -26.15211026017857421, 6.877402575842992860 ) ) ;
#35657=CARTESIAN_POINT ( 'NONE',  ( 4.442938236509021976, -27.40294606746516592, 7.771081512783700518 ) ) ;
#35660=ORIENTED_EDGE ( 'NONE', *, *, #23205, .F. ) ;
#35661=VERTEX_POINT ( 'NONE', #34671 ) ;
#35662=DIRECTION ( 'NONE',  ( -0.000000000000000000, -0.000000000000000000, -1.000000000000000000 ) ) ;
#35663=B_SPLINE_CURVE_WITH_KNOTS ( 'NONE', 3,
 ( #7926, #16035, #29555, #26076 ),
 .UNSPECIFIED., .F., .F.,
 ( 4, 4 ),
 ( 0.000000000000000000, 6.391136169993375584E-06 ),
 .UNSPECIFIED. ) ;
#35665=DIRECTION ( 'NONE',  ( -0.000000000000000000, -0.000000000000000000, -1.000000000000000000 ) ) ;
#35670=CARTESIAN_POINT ( 'NONE',  ( 2.410368835147195021, -26.24488429107400478, 7.754798119455333705 ) ) ;
#35673=CARTESIAN_POINT ( 'NONE',  ( 2.428848143534461101, -33.77897949353074836, 7.635761828346577573 ) ) ;
#35674=CARTESIAN_POINT ( 'NONE',  ( -0.5222078730473904695, -32.14287757506037480, 6.894806418505348589 ) ) ;
#35675=CARTESIAN_POINT ( 'NONE',  ( 3.922483456672745561, -26.86580350659783178, 7.686927408461905920 ) ) ;
#35678=DIRECTION ( 'NONE',  ( 1.000000000000000000, 0.000000000000000000, 0.000000000000000000 ) ) ;
#35680=CARTESIAN_POINT ( 'NONE',  ( -1.559944549550448922, -28.33713295695417145, 7.785096263473211486 ) ) ;
#35682=EDGE_CURVE ( 'NONE', #22296, #18803, #40153, .T. ) ;
#35689=CARTESIAN_POINT ( 'NONE',  ( 4.715112165605915173, -27.79188326996616709, 7.670465701733750308 ) ) ;
#35690=ORIENTED_EDGE ( 'NONE', *, *, #29069, .T. ) ;
#35694=CARTESIAN_POINT ( 'NONE',  ( 2.326171464738295835, -32.91184545387483951, 7.695279973900954751 ) ) ;
#35695=CARTESIAN_POINT ( 'NONE',  ( 3.608358685920158848, -26.63570720646865198, 6.989977667959445640 ) ) ;
#35696=CIRCLE ( 'NONE', #15963, 3.499999999999999556 ) ;
#35697=CARTESIAN_POINT ( 'NONE',  ( 4.393959771609395659, -31.80480879032751673, 7.643192810543820492 ) ) ;
#35705=CARTESIAN_POINT ( 'NONE',  ( -1.709989797022098301, -28.78296037949930408, 6.995077437911115581 ) ) ;
#35719=CARTESIAN_POINT ( 'NONE',  ( -0.9821796830226547925, -31.80934223257329663, 7.773839561854631874 ) ) ;
#35723=CARTESIAN_POINT ( 'NONE',  ( 5.126355467162643009, -30.28602164449890566, 6.864641613908471385 ) ) ;
#35725=CARTESIAN_POINT ( 'NONE',  ( 5.095244238841699413, -29.75692037041947913, 7.013842709614101167 ) ) ;
#35726=CARTESIAN_POINT ( 'NONE',  ( 5.585000075404096265, -26.15135101585522293, 7.754798119455333705 ) ) ;
#35728=CARTESIAN_POINT ( 'NONE',  ( 1.892862797245994821, -26.07522642238200561, 6.961115707816238007 ) ) ;
#35729=CARTESIAN_POINT ( 'NONE',  ( 4.337032230407563915, -31.84938093442232088, 7.785344483711591934 ) ) ;
#35732=B_SPLINE_CURVE_WITH_KNOTS ( 'NONE', 3,
 ( #37140, #21512, #30786, #34491, #6265, #21303, #18812, #21101, #39248, #11039, #11798, #18401, #37343, #23616, #36182, #21711, #5449, #2793, #8519, #33878, #17990, #30576, #2383, #34296, #27871, #34088, #40632, #40419, #12224, #14905, #6064 ),
 .UNSPECIFIED., .F., .F.,
 ( 4, 3, 3, 3, 3, 3, 3, 3, 3, 3, 4 ),
 ( 2.168404344971008868E-19, 2.999644130997720782E-05, 6.002588995694745999E-05, 8.960886084588085281E-05, 0.0001190604700446486864, 0.0001489538463052727233, 0.0001796139255493992102, 0.0002109707048517083525, 0.0002426195318110370642, 0.0002740640997890074850, 0.0002849778069099842027 ),
 .UNSPECIFIED. ) ;
#35733=VERTEX_POINT ( 'NONE', #28251 ) ;
#35736=CARTESIAN_POINT ( 'NONE',  ( 2.290977028701361107, -26.12011756940199447, 7.750000000000000888 ) ) ;
#35739=CARTESIAN_POINT ( 'NONE',  ( 2.863609035986291573, -26.26888160889163615, 7.695279973900954751 ) ) ;
#35741=CARTESIAN_POINT ( 'NONE',  ( 2.948025465462910777, -26.31577733493585569, 7.785593909369613819 ) ) ;
#35744=EDGE_LOOP ( 'NONE', ( #4729, #7593, #9095, #40580, #29820 ) ) ;
#35745=CARTESIAN_POINT ( 'NONE',  ( -1.748756095191392523, -28.97546355617463121, 7.635761828346576685 ) ) ;
#35746=AXIS2_PLACEMENT_3D ( 'NONE', #11794, #40025, #20883 ) ;
#35751=CARTESIAN_POINT ( 'NONE',  ( -1.270646089883737506, -31.22309432593480594, 6.889465824494256374 ) ) ;
#35759=ORIENTED_EDGE ( 'NONE', *, *, #10784, .F. ) ;
#35760=B_SPLINE_CURVE_WITH_KNOTS ( 'NONE', 3,
 ( #11540, #24109, #36673, #8457, #34845, #22067, #12161, #16078, #18967, #34233, #238, #13494, #9232, #9645, #37235, #34390, #6576, #34188, #6162 ),
 .UNSPECIFIED., .F., .F.,
 ( 4, 3, 3, 3, 3, 3, 4 ),
 ( 3.252606517456513302E-19, 2.546128104244800008E-05, 5.711050680483939474E-05, 8.113074941675944753E-05, 0.0001053129305727065632, 0.0001360598016347085713, 0.0001612931755702024352 ),
 .UNSPECIFIED. ) ;
#35761=DIRECTION ( 'NONE',  ( -0.1736481776669340227, 0.9848077530122074652, -0.000000000000000000 ) ) ;
#35762=ADVANCED_FACE ( 'NONE', ( #37111 ), #6848, .F. ) ;
#35767=CARTESIAN_POINT ( 'NONE',  ( -0.02174174371171335232, -26.63833058205436899, 7.652160403243381204 ) ) ;
#35768=FACE_OUTER_BOUND ( 'NONE', #3237, .T. ) ;
#35770=CARTESIAN_POINT ( 'NONE',  ( -1.488097077937502899, -30.75041718428775184, 7.748216051605120391 ) ) ;
#35771=CARTESIAN_POINT ( 'NONE',  ( -1.576062547484235354, -30.80072589882973944, 7.695279973900954751 ) ) ;
#35772=DIRECTION ( 'NONE',  ( -0.1736481776669207000, -0.9848077530122097967, -0.000000000000000000 ) ) ;
#35774=CARTESIAN_POINT ( 'NONE',  ( 4.501207559045222517, -27.47102055165149892, 6.961115707816242448 ) ) ;
#35782=CARTESIAN_POINT ( 'NONE',  ( -0.4037637910173453304, -26.77305041633264793, 6.921725064902943814 ) ) ;
#35784=CARTESIAN_POINT ( 'NONE',  ( -1.239502271792400689, -27.67071116441090695, 7.006908160621413195 ) ) ;
#35789=ORIENTED_EDGE ( 'NONE', *, *, #32551, .F. ) ;
#35790=FACE_OUTER_BOUND ( 'NONE', #24127, .T. ) ;
#35799=DIRECTION ( 'NONE',  ( 0.6427876096865481337, -0.7660444431189707970, -0.000000000000000000 ) ) ;
#35802=EDGE_CURVE ( 'NONE', #32452, #40515, #30046, .T. ) ;
#35803=CARTESIAN_POINT ( 'NONE',  ( -0.01738578663354513332, -32.50409796781847405, 7.779495906702013741 ) ) ;
#35806=CARTESIAN_POINT ( 'NONE',  ( 3.960473582032317363, -32.24238647371081612, 7.635761828346576685 ) ) ;
#35807=DIRECTION ( 'NONE',  ( -0.000000000000000000, -0.000000000000000000, -1.000000000000000000 ) ) ;
#35810=VERTEX_POINT ( 'NONE', #13414 ) ;
#35811=DIRECTION ( 'NONE',  ( -0.000000000000000000, -0.000000000000000000, -1.000000000000000000 ) ) ;
#35812=EDGE_CURVE ( 'NONE', #1652, #12108, #15066, .T. ) ;
#35816=CARTESIAN_POINT ( 'NONE',  ( 0.4503279196356648750, -32.73180316670461565, 6.866852738645443210 ) ) ;
#35819=FACE_OUTER_BOUND ( 'NONE', #437, .T. ) ;
#35820=VERTEX_POINT ( 'NONE', #35274 ) ;
#35821=B_SPLINE_CURVE_WITH_KNOTS ( 'NONE', 3,
 ( #17969, #39812, #11781, #14676, #24571, #24157, #6047, #5845, #8500, #11991 ),
 .UNSPECIFIED., .F., .F.,
 ( 4, 3, 3, 4 ),
 ( 8.673617379884035472E-19, 3.025570593003166546E-05, 6.051145698344096054E-05, 6.468151674593702839E-05 ),
 .UNSPECIFIED. ) ;
#35825=DIRECTION ( 'NONE',  ( -3.491481338843133750E-15, 1.000000000000000000, -0.000000000000000000 ) ) ;
#35828=CARTESIAN_POINT ( 'NONE',  ( 0.5713750229309363382, -32.77700439067807281, 7.693875151218753317 ) ) ;
#35830=PLANE ( 'NONE',  #3847 ) ;
#35831=CARTESIAN_POINT ( 'NONE',  ( 3.858277372750224643, -26.94247466732882756, 7.691066658568944447 ) ) ;
#35832=VECTOR ( 'NONE', #11498, 1000.000000000000000 ) ;
#35833=CARTESIAN_POINT ( 'NONE',  ( 1.669309969508061764, -33.06979218437418666, 6.894806418505347700 ) ) ;
#35838=( BOUNDED_CURVE ( )  B_SPLINE_CURVE ( 3, ( #17018, #16821, #35984, #23420 ),
 .UNSPECIFIED., .F., .T. ) 
 B_SPLINE_CURVE_WITH_KNOTS ( ( 4, 4 ),
 ( 1.381924640371169577, 1.574767692156077148 ),
 .UNSPECIFIED. ) 
 CURVE ( )  GEOMETRIC_REPRESENTATION_ITEM ( )  RATIONAL_B_SPLINE_CURVE ( ( 1.000000000000000000, 0.9969033633783033199, 0.9969033633783033199, 1.000000000000000000 ) ) 
 REPRESENTATION_ITEM ( '' )  );
#35839=CARTESIAN_POINT ( 'NONE',  ( -1.616388873120942593, -30.68750670799986224, 6.865554069792297653 ) ) ;
#35843=CARTESIAN_POINT ( 'NONE',  ( 4.916835462155118464, -28.46786787629711668, 6.880147297696980857 ) ) ;
#35851=CARTESIAN_POINT ( 'NONE',  ( -1.225953191357326277, -31.30097466021442187, 7.695279973900954751 ) ) ;
#35853=CARTESIAN_POINT ( 'NONE',  ( 2.494101229020593724, -26.16111475381571339, 6.974994249511788702 ) ) ;
#35860=EDGE_CURVE ( 'NONE', #37042, #14030, #32813, .T. ) ;
#35861=CIRCLE ( 'NONE', #23361, 0.04999999999999991257 ) ;
#35872=CARTESIAN_POINT ( 'NONE',  ( 0.7214101843820232007, -26.31391371107089228, 7.006423389747790331 ) ) ;
#35873=CARTESIAN_POINT ( 'NONE',  ( 0.006252119912152956024, -26.50725532007327701, 6.870737987065012931 ) ) ;
#35877=DIRECTION ( 'NONE',  ( -0.6427876096865430267, 0.7660444431189749048, -0.000000000000000000 ) ) ;
#35883=VERTEX_POINT ( 'NONE', #23692 ) ;
#35888=CARTESIAN_POINT ( 'NONE',  ( 5.081024546220614724, -29.99328066215961996, 7.139196562012270597 ) ) ;
#35891=CARTESIAN_POINT ( 'NONE',  ( 3.904729273020431712, -32.15854446160317082, 7.740055089680403455 ) ) ;
#35893=CARTESIAN_POINT ( 'NONE',  ( 0.9072453234131299116, -32.87612686815500496, 6.979335674598003969 ) ) ;
#35894=CARTESIAN_POINT ( 'NONE',  ( 0.3246626803113665805, -32.78821847042190996, 6.965379264086542399 ) ) ;
#35895=DIRECTION ( 'NONE',  ( 1.000000000000000000, 0.000000000000000000, 0.000000000000000000 ) ) ;
#35896=ORIENTED_EDGE ( 'NONE', *, *, #22528, .T. ) ;
#35898=CARTESIAN_POINT ( 'NONE',  ( -1.752498985642892304, -28.99760421947164701, 7.695279973900954751 ) ) ;
#35900=CARTESIAN_POINT ( 'NONE',  ( -0.02773757890651329036, -32.61354788820055006, 7.651421919295149365 ) ) ;
#35904=CARTESIAN_POINT ( 'NONE',  ( -1.723318791039416764, -28.84314446823831091, 6.866645518795387204 ) ) ;
#35907=EDGE_CURVE ( 'NONE', #14785, #7534, #33793, .T. ) ;
#35909=CYLINDRICAL_SURFACE ( 'NONE', #22111, 0.09010775117053086702 ) ;
#35923=ORIENTED_EDGE ( 'NONE', *, *, #26054, .T. ) ;
#35925=CARTESIAN_POINT ( 'NONE',  ( 3.617749134298497538, -32.38632682485276604, 7.505001789837626447 ) ) ;
#35926=CARTESIAN_POINT ( 'NONE',  ( -1.093319172033571984, -31.67829984452200875, 6.998987538705438993 ) ) ;
#35927=CARTESIAN_POINT ( 'NONE',  ( 4.995891145035052716, -30.74877403122573938, 7.643192810543820492 ) ) ;
#35928=CARTESIAN_POINT ( 'NONE',  ( 2.817328913877361618, -32.78123018042540338, 6.894806418505346812 ) ) ;
#35939=VECTOR ( 'NONE', #781, 1000.000000000000114 ) ;
#35940=CARTESIAN_POINT ( 'NONE',  ( 6.089801904741589667, -27.84269339272794852, 7.754798119455333705 ) ) ;
#35942=CARTESIAN_POINT ( 'NONE',  ( 5.053714827962103584, -30.13136871382624804, 7.661510568013096822 ) ) ;
#35944=VECTOR ( 'NONE', #36448, 1000.000000000000000 ) ;
#35948=FACE_OUTER_BOUND ( 'NONE', #2475, .T. ) ;
#35952=CARTESIAN_POINT ( 'NONE',  ( 0.9205786840771784663, -32.98195322516173178, 7.006248344249653037 ) ) ;
#35957=CARTESIAN_POINT ( 'NONE',  ( 5.200239449971241434, -29.53745742343132719, 7.670465701733749420 ) ) ;
#35960=CARTESIAN_POINT ( 'NONE',  ( 5.140791489254627145, -28.92678305073006939, 7.686927408461905031 ) ) ;
#35961=LINE ( 'NONE', #28977, #35939 ) ;
#35963=CARTESIAN_POINT ( 'NONE',  ( -1.524152690418147493, -30.64804141902853374, 7.778050822775631090 ) ) ;
#35966=FACE_OUTER_BOUND ( 'NONE', #23276, .T. ) ;
#35973=CARTESIAN_POINT ( 'NONE',  ( 4.927871323695246275, -28.50060760253348491, 7.774064877406527074 ) ) ;
#35974=CARTESIAN_POINT ( 'NONE',  ( 4.270010460102485972, -31.79637552378333964, 6.889465824494252821 ) ) ;
#35976=EDGE_CURVE ( 'NONE', #23918, #12935, #21222, .T. ) ;
#35977=VERTEX_POINT ( 'NONE', #27187 ) ;
#35980=CARTESIAN_POINT ( 'NONE',  ( -0.4140453450342095332, -26.78081456870760135, 7.009310105710483185 ) ) ;
#35981=CARTESIAN_POINT ( 'NONE',  ( -1.287707616843211778, -27.74749443005756433, 6.865554069792297653 ) ) ;
#35982=CARTESIAN_POINT ( 'NONE',  ( 2.399720784871332224, -26.14781977356483011, 7.776484688137385248 ) ) ;
#35984=CARTESIAN_POINT ( 'NONE',  ( 1.494999628127195779, -32.97077268039931397, 7.386948897581450346 ) ) ;
#35986=ORIENTED_EDGE ( 'NONE', *, *, #21712, .T. ) ;
#35988=EDGE_CURVE ( 'NONE', #33555, #22827, #20293, .T. ) ;
#35989=ORIENTED_EDGE ( 'NONE', *, *, #24683, .T. ) ;
#35992=AXIS2_PLACEMENT_3D ( 'NONE', #13417, #22905, #885 ) ;
#35995=CARTESIAN_POINT ( 'NONE',  ( -0.7754396137877683781, -27.23962715764706033, 7.006423389747792108 ) ) ;
#35996=ORIENTED_EDGE ( 'NONE', *, *, #5387, .F. ) ;
#35998=CARTESIAN_POINT ( 'NONE',  ( 0.01152222936319628917, -32.52082164920695817, 7.756377446753164762 ) ) ;
#36000=B_SPLINE_CURVE_WITH_KNOTS ( 'NONE', 3,
 ( #1956, #11780, #20865, #36715, #17967, #33457, #5226, #30348, #2154, #24361 ),
 .UNSPECIFIED., .F., .F.,
 ( 4, 3, 3, 4 ),
 ( 1.939479807224432123E-18, 3.025570593003208558E-05, 6.051145698344203796E-05, 6.468151674592953384E-05 ),
 .UNSPECIFIED. ) ;
#36003=CARTESIAN_POINT ( 'NONE',  ( -1.246815083620857134, -27.87462772991113980, 7.763628509615285722 ) ) ;
#36006=ORIENTED_EDGE ( 'NONE', *, *, #38625, .F. ) ;
#36007=DIRECTION ( 'NONE',  ( 1.000000000000000000, 6.938893903907229167E-15, 0.000000000000000000 ) ) ;
#36011=CARTESIAN_POINT ( 'NONE',  ( 1.127397677933556830, -33.02270898565480906, 7.707984471951054850 ) ) ;
#36017=ADVANCED_FACE ( 'NONE', ( #18113 ), #1483, .T. ) ;
#36030=CARTESIAN_POINT ( 'NONE',  ( -1.196375916356071212, -27.78980578152105352, 6.866852738645442322 ) ) ;
#36032=VERTEX_POINT ( 'NONE', #30084 ) ;
#36035=EDGE_CURVE ( 'NONE', #4710, #14798, #20593, .T. ) ;
#36041=CARTESIAN_POINT ( 'NONE',  ( 4.890701645444022638, -28.39438256639548896, 7.635761828346577573 ) ) ;
#36045=DIRECTION ( 'NONE',  ( 0.9848077530122080203, 0.1736481776669307198, -0.000000000000000000 ) ) ;
#36046=CARTESIAN_POINT ( 'NONE',  ( 4.777618136733515541, -27.90236538453207515, 6.863805608295729499 ) ) ;
#36047=ORIENTED_EDGE ( 'NONE', *, *, #17431, .F. ) ;
#36050=VECTOR ( 'NONE', #32394, 1000.000000000000000 ) ;
#36051=CARTESIAN_POINT ( 'NONE',  ( -1.225969928216009475, -31.30094636736736291, 7.692469944509197965 ) ) ;
#36052=ORIENTED_EDGE ( 'NONE', *, *, #18670, .F. ) ;
#36055=CARTESIAN_POINT ( 'NONE',  ( 4.416430171046111575, -31.62687967920297538, 7.139196562012270597 ) ) ;
#36059=AXIS2_PLACEMENT_3D ( 'NONE', #25434, #32238, #3442 ) ;
#36062=CARTESIAN_POINT ( 'NONE',  ( -1.261893907174904905, -27.90113615618628273, 7.692469944509197965 ) ) ;
#36063=FACE_OUTER_BOUND ( 'NONE', #2247, .T. ) ;
#36065=B_SPLINE_CURVE_WITH_KNOTS ( 'NONE', 3,
 ( #9045, #12749, #3124, #31302, #12342, #25117, #22445, #31502, #22249, #34611, #21623, #18512, #2907, #27987, #24915, #15640, #38068, #35013, #419 ),
 .UNSPECIFIED., .F., .F.,
 ( 4, 3, 3, 3, 3, 3, 4 ),
 ( 9.697399036122160616E-19, 2.546128104244831518E-05, 5.711050680484053993E-05, 8.113074941675944753E-05, 0.0001053129305727060888, 0.0001360598016347089236, 0.0001612931755701964992 ),
 .UNSPECIFIED. ) ;
#36069=LINE ( 'NONE', #8036, #535 ) ;
#36073=CARTESIAN_POINT ( 'NONE',  ( 0.1091738275826929783, -26.45254908979351782, 6.998987538705438105 ) ) ;
#36076=CARTESIAN_POINT ( 'NONE',  ( -1.699609906766909040, -29.57443106709385816, 7.625529685907138422 ) ) ;
#36077=( BOUNDED_CURVE ( )  B_SPLINE_CURVE ( 3, ( #11446, #24227, #8983, #5707 ),
 .UNSPECIFIED., .F., .T. ) 
 B_SPLINE_CURVE_WITH_KNOTS ( ( 4, 4 ),
 ( 4.748221474220559735, 4.941946782021394036 ),
 .UNSPECIFIED. ) 
 CURVE ( )  GEOMETRIC_REPRESENTATION_ITEM ( )  RATIONAL_B_SPLINE_CURVE ( ( 1.000000000000000000, 0.9968749865767494445, 0.9968749865767494445, 1.000000000000000000 ) ) 
 REPRESENTATION_ITEM ( '' )  );
#36080=EDGE_CURVE ( 'NONE', #33085, #6054, #39633, .T. ) ;
#36081=CARTESIAN_POINT ( 'NONE',  ( -2.500070672423774454, -28.79276407692314876, 7.695279973900954751 ) ) ;
#36083=ORIENTED_EDGE ( 'NONE', *, *, #5387, .T. ) ;
#36091=DIRECTION ( 'NONE',  ( 0.000000000000000000, -0.7126435865141234061, -0.7015262779114458391 ) ) ;
#36094=CARTESIAN_POINT ( 'NONE',  ( 2.319715055549975702, -32.91304797836431106, 7.661510568013096822 ) ) ;
#36095=CARTESIAN_POINT ( 'NONE',  ( 0.4392850896841424269, -32.83485164247554877, 6.869132338375689706 ) ) ;
#36102=DIRECTION ( 'NONE',  ( -0.8660254037844415942, 0.4999999999999950040, -0.000000000000000000 ) ) ;
#36106=CARTESIAN_POINT ( 'NONE',  ( -1.712868897180792382, -28.79555068392009431, 7.013024433893851217 ) ) ;
#36112=ORIENTED_EDGE ( 'NONE', *, *, #40626, .F. ) ;
#36116=CARTESIAN_POINT ( 'NONE',  ( 5.784498025276203492, -28.13289436698813972, 6.954324564059724878 ) ) ;
#36120=ORIENTED_EDGE ( 'NONE', *, *, #18644, .T. ) ;
#36123=CARTESIAN_POINT ( 'NONE',  ( -1.087582253741100846, -31.68587304350735323, 7.011627023500185629 ) ) ;
#36124=LINE ( 'NONE', #7905, #23234 ) ;
#36125=CARTESIAN_POINT ( 'NONE',  ( 2.707230893317792653, -32.81744307353336154, 6.876076431790004939 ) ) ;
#36126=CARTESIAN_POINT ( 'NONE',  ( 2.324081863996483310, -32.91946213718349412, 7.257242401810565013 ) ) ;
#36127=CARTESIAN_POINT ( 'NONE',  ( 1.885627875660562003, -26.07483424866503086, 6.989977667959444751 ) ) ;
#36136=EDGE_CURVE ( 'NONE', #6925, #579, #19650, .T. ) ;
#36137=CARTESIAN_POINT ( 'NONE',  ( 0.1827919725910926718, -26.52741295444542047, 6.979335674598004857 ) ) ;
#36140=LINE ( 'NONE', #20469, #33069 ) ;
#36143=CARTESIAN_POINT ( 'NONE',  ( 5.053090684323510828, -30.13509655968624656, 7.652160403243382980 ) ) ;
#36152=CARTESIAN_POINT ( 'NONE',  ( 4.042482038083015539, -27.10525874040772365, 6.959317978105166169 ) ) ;
#36163=CARTESIAN_POINT ( 'NONE',  ( 0.9940451555042898457, -25.35698173488204432, 7.695279973900954751 ) ) ;
#36165=CARTESIAN_POINT ( 'NONE',  ( 0.6407229928749871295, -26.23419853405188462, 6.875780273367531059 ) ) ;
#36167=CARTESIAN_POINT ( 'NONE',  ( 3.977455998898224099, -32.22793147407356429, 7.700536657684220465 ) ) ;
#36169=CARTESIAN_POINT ( 'NONE',  ( 4.169743078853456630, -31.90708568365600684, 6.988553391373226731 ) ) ;
#36172=CARTESIAN_POINT ( 'NONE',  ( 2.288810108494835571, -33.01126522079324843, 7.778495531946296282 ) ) ;
#36178=CARTESIAN_POINT ( 'NONE',  ( -1.605806591528507354, -28.77678541357339981, 6.979335674598005745 ) ) ;
#36182=CARTESIAN_POINT ( 'NONE',  ( 1.288977975861898662, -26.19490350224902642, 6.887945620086118659 ) ) ;
#36189=CARTESIAN_POINT ( 'NONE',  ( 4.731075428271440231, -27.83036318828329669, 7.773839561854632763 ) ) ;
#36190=ORIENTED_EDGE ( 'NONE', *, *, #10132, .F. ) ;
#36191=CARTESIAN_POINT ( 'NONE',  ( 3.229898424385141187, -32.60648237212752321, 7.006423389747791219 ) ) ;
#36193=DIRECTION ( 'NONE',  ( 0.000000000000000000, 0.6605219282605402364, -0.7508067542896625923 ) ) ;
#36194=DIRECTION ( 'NONE',  ( -0.7660444431189770143, 0.6427876096865404731, 0.000000000000000000 ) ) ;
#36195=DIRECTION ( 'NONE',  ( -0.3420201433256663259, 0.9396926207859092051, 0.000000000000000000 ) ) ;
#36196=ADVANCED_FACE ( 'NONE', ( #26032 ), #35909, .F. ) ;
#36199=DIRECTION ( 'NONE',  ( -0.000000000000000000, -0.000000000000000000, -1.000000000000000000 ) ) ;
#36208=CARTESIAN_POINT ( 'NONE',  ( -1.425774885472621767, -28.23310838303483550, 7.013842709614101167 ) ) ;
#36209=EDGE_CURVE ( 'NONE', #7270, #34797, #13668, .T. ) ;
#36210=CARTESIAN_POINT ( 'NONE',  ( 4.733915118986097958, -28.03444136281207832, 7.013842709614101167 ) ) ;
#36215=CARTESIAN_POINT ( 'NONE',  ( 1.700390093233090871, -29.56993018339339940, 7.750000000000000888 ) ) ;
#36217=CARTESIAN_POINT ( 'NONE',  ( 2.792826902421812196, -32.89234763507269577, 7.766640943994341129 ) ) ;
#36220=CARTESIAN_POINT ( 'NONE',  ( -1.135147046452389397, -27.69383203199361532, 6.979335674598006634 ) ) ;
#36226=CARTESIAN_POINT ( 'NONE',  ( -1.646367189487829119, -30.59424959516734432, 6.912143950357346078 ) ) ;
#36227=CARTESIAN_POINT ( 'NONE',  ( 3.411265863501067308, -26.50879084905291450, 7.255881584735163869 ) ) ;
#36229=ORIENTED_EDGE ( 'NONE', *, *, #23255, .F. ) ;
#36237=CARTESIAN_POINT ( 'NONE',  ( 4.318115897878434417, -27.40022832085480786, 7.779495906702013741 ) ) ;
#36238=VERTEX_POINT ( 'NONE', #25621 ) ;
#36243=ORIENTED_EDGE ( 'NONE', *, *, #29614, .T. ) ;
#36248=ORIENTED_EDGE ( 'NONE', *, *, #24547, .F. ) ;
#36250=CYLINDRICAL_SURFACE ( 'NONE', #29357, 3.399999999999999911 ) ;
#36251=LINE ( 'NONE', #23290, #1762 ) ;
#36254=CARTESIAN_POINT ( 'NONE',  ( 1.677877769585896628, -26.06999691478939241, 7.646866513072557048 ) ) ;
#36258=EDGE_CURVE ( 'NONE', #17469, #33252, #28794, .T. ) ;
#36259=ADVANCED_FACE ( 'NONE', ( #23731 ), #36301, .F. ) ;
#36260=CARTESIAN_POINT ( 'NONE',  ( 3.472143277054946076, -26.66805309164448801, 6.870716933885665512 ) ) ;
#36263=CARTESIAN_POINT ( 'NONE',  ( 0.5908764294676954743, -26.35605721920861555, 6.887041543973314361 ) ) ;
#36267=CYLINDRICAL_SURFACE ( 'NONE', #31916, 0.09010775117052929883 ) ;
#36268=LINE ( 'NONE', #8044, #39056 ) ;
#36274=B_SPLINE_CURVE_WITH_KNOTS ( 'NONE', 3,
 ( #22366, #3444, #26256, #10585, #38181, #13688, #15960, #28522, #35334, #38582, #4228, #35128, #6906, #29335, #23157, #25843, #10179, #19462, #332, #26051, #38790, #1154, #19257, #12872, #37981, #22768, #32432, #25436, #9984, #7103, #34931 ),
 .UNSPECIFIED., .F., .F.,
 ( 4, 3, 3, 3, 3, 3, 3, 3, 3, 3, 4 ),
 ( 4.336808689942017736E-18, 3.077658087705547918E-05, 6.152638666998892195E-05, 9.267501192706379103E-05, 0.0001241882240135189545, 0.0001556618703051619482, 0.0001866161554452189968, 0.0002167966385860955179, 0.0002463805737537769474, 0.0002758761370306513517, 0.0002847094172290125843 ),
 .UNSPECIFIED. ) ;
#36275=CARTESIAN_POINT ( 'NONE',  ( 1.217126534916886937, -26.10345411493373291, 7.750000000000000888 ) ) ;
#36280=CARTESIAN_POINT ( 'NONE',  ( 3.802248482306934463, -32.24242835236076843, 7.768425012602589774 ) ) ;
#36283=LINE ( 'NONE', #8058, #2390 ) ;
#36284=CARTESIAN_POINT ( 'NONE',  ( 1.281736550542457831, -26.09505782811984176, 6.971170733404104425 ) ) ;
#36290=CARTESIAN_POINT ( 'NONE',  ( -0.03790328338398483987, -32.60774784362404688, 7.635761828346575797 ) ) ;
#36301=PLANE ( 'NONE',  #27993 ) ;
#36305=CARTESIAN_POINT ( 'NONE',  ( 3.426543769787936622, -26.64069931422037030, 7.782167645815906809 ) ) ;
#36313=CARTESIAN_POINT ( 'NONE',  ( -2.718383313029612225, -27.92336371131444750, 7.695279973900954751 ) ) ;
#36315=CARTESIAN_POINT ( 'NONE',  ( 5.174553870628630037, -29.14543674784208704, 6.989977667959446528 ) ) ;
#36319=LINE ( 'NONE', #20062, #23563 ) ;
#36320=CARTESIAN_POINT ( 'NONE',  ( -1.040518353328913959, -31.74651596798171127, 6.863805608295729499 ) ) ;
#36321=CARTESIAN_POINT ( 'NONE',  ( 4.993907954365692348, -30.75430347691218813, 7.635761828346578461 ) ) ;
#36322=CARTESIAN_POINT ( 'NONE',  ( 2.666995777737314111, -32.82963468697713694, 6.929923840112063083 ) ) ;
#36324=CARTESIAN_POINT ( 'NONE',  ( 1.892518328694925422, -26.07520748464628468, 6.951256099901589991 ) ) ;
#36325=ORIENTED_EDGE ( 'NONE', *, *, #9059, .F. ) ;
#36333=CARTESIAN_POINT ( 'NONE',  ( 2.923652617287828992, -26.39759808583085388, 6.880147297696980857 ) ) ;
#36334=B_SPLINE_CURVE_WITH_KNOTS ( 'NONE', 3,
 ( #7922, #14296, #20677, #35551, #17178, #4249, #20079, #20471, #963, #35745 ),
 .UNSPECIFIED., .F., .F.,
 ( 4, 3, 3, 4 ),
 ( 8.673617379884034509E-19, 3.025505781527745516E-05, 6.051003801291361255E-05, 6.468145402690660616E-05 ),
 .UNSPECIFIED. ) ;
#36335=ORIENTED_EDGE ( 'NONE', *, *, #18727, .F. ) ;
#36340=EDGE_CURVE ( 'NONE', #39584, #14639, #14518, .T. ) ;
#36347=EDGE_LOOP ( 'NONE', ( #17147, #10165, #2502, #26416, #21863 ) ) ;
#36350=CARTESIAN_POINT ( 'NONE',  ( 4.002494580657026901, -27.06784897793791700, 6.871394612369936539 ) ) ;
#36351=DIRECTION ( 'NONE',  ( 0.9396926207859135349, -0.3420201433256548351, 0.000000000000000000 ) ) ;
#36360=CARTESIAN_POINT ( 'NONE',  ( 1.491082739486949471, -32.96348259045947060, 6.939395833800441338 ) ) ;
#36361=CARTESIAN_POINT ( 'NONE',  ( 2.485966948262496867, -26.26192714095899561, 6.997764925645182821 ) ) ;
#36363=CARTESIAN_POINT ( 'NONE',  ( -1.504793647276889246, -30.70430101763167841, 7.782167645815905033 ) ) ;
#36365=CARTESIAN_POINT ( 'NONE',  ( 0.6760706814591578295, -26.22317290067247342, 6.912143950357346078 ) ) ;
#36366=CARTESIAN_POINT ( 'NONE',  ( 4.411012430042179133, -27.35574694287801378, 6.880608371227947551 ) ) ;
#36368=CARTESIAN_POINT ( 'NONE',  ( 4.180051228910634187, -31.89615321790286018, 6.895222827070024429 ) ) ;
#36372=CARTESIAN_POINT ( 'NONE',  ( 3.976596914110534620, -33.75953324440050096, 6.954324564059724878 ) ) ;
#36376=CARTESIAN_POINT ( 'NONE',  ( 0.1649012726517564975, -26.53640515764040231, 7.013842709614101167 ) ) ;
#36378=VECTOR ( 'NONE', #19785, 1000.000000000000114 ) ;
#36384=CARTESIAN_POINT ( 'NONE',  ( -1.679395455362387102, -29.14213866777389228, 7.134148492716103185 ) ) ;
#36387=CARTESIAN_POINT ( 'NONE',  ( -0.7953160622768807864, -27.26092192145711124, 6.876076431790005827 ) ) ;
#36389=VECTOR ( 'NONE', #31826, 1000.000000000000000 ) ;
#36399=CARTESIAN_POINT ( 'NONE',  ( 5.022340310865588187, -30.29431027711538249, 6.865637334398153158 ) ) ;
#36403=CARTESIAN_POINT ( 'NONE',  ( 2.896889677700020371, -32.75244314399080281, 7.691066658568946224 ) ) ;
#36407=CARTESIAN_POINT ( 'NONE',  ( 5.123610338733788794, -30.29864684015847232, 7.753200566781575986 ) ) ;
#36409=CARTESIAN_POINT ( 'NONE',  ( -0.5160548967603080239, -32.28747347318100935, 7.255881584735161205 ) ) ;
#36420=CARTESIAN_POINT ( 'NONE',  ( 4.995180358529765385, -28.43394519631405970, 7.785593909369613819 ) ) ;
#36421=ORIENTED_EDGE ( 'NONE', *, *, #13628, .T. ) ;
#36430=EDGE_CURVE ( 'NONE', #5985, #12935, #32232, .T. ) ;
#36433=DIRECTION ( 'NONE',  ( 0.4826092789263634053, -0.5751513419797926741, 0.6605219282605379050 ) ) ;
#36434=ORIENTED_EDGE ( 'NONE', *, *, #19424, .F. ) ;
#36436=ORIENTED_EDGE ( 'NONE', *, *, #20437, .T. ) ;
#36438=CARTESIAN_POINT ( 'NONE',  ( 4.337010013012764453, -27.42322653021406964, 7.785868773668302545 ) ) ;
#36441=DIRECTION ( 'NONE',  ( -0.000000000000000000, -0.000000000000000000, -1.000000000000000000 ) ) ;
#36442=ORIENTED_EDGE ( 'NONE', *, *, #39719, .T. ) ;
#36444=CARTESIAN_POINT ( 'NONE',  ( 2.908949165453299734, -26.39197723079101010, 6.894806418505348589 ) ) ;
#36445=CARTESIAN_POINT ( 'NONE',  ( -1.795422484021812926, -29.39876237255725400, 7.011627023500182965 ) ) ;
#36448=DIRECTION ( 'NONE',  ( 0.8660254037844380415, 0.5000000000000009992, -0.000000000000000000 ) ) ;
#36451=ADVANCED_FACE ( 'NONE', ( #28245 ), #2966, .T. ) ;
#36463=CARTESIAN_POINT ( 'NONE',  ( 4.672147420734682477, -31.41889161793999463, 6.865482280155366546 ) ) ;
#36465=( BOUNDED_CURVE ( )  B_SPLINE_CURVE ( 3, ( #40317, #18084, #2482, #24058 ),
 .UNSPECIFIED., .F., .T. ) 
 B_SPLINE_CURVE_WITH_KNOTS ( ( 4, 4 ),
 ( 4.748221474220558846, 4.941946782021393147 ),
 .UNSPECIFIED. ) 
 CURVE ( )  GEOMETRIC_REPRESENTATION_ITEM ( )  RATIONAL_B_SPLINE_CURVE ( ( 1.000000000000000000, 0.9968749865767494445, 0.9968749865767494445, 1.000000000000000000 ) ) 
 REPRESENTATION_ITEM ( '' )  );
#36466=CARTESIAN_POINT ( 'NONE',  ( 4.310691338497240288, -31.89452001513661727, 7.771081512783700518 ) ) ;
#36467=CARTESIAN_POINT ( 'NONE',  ( 1.736346942945644400, -33.06974547922812491, 7.695279973900954751 ) ) ;
#36470=B_SPLINE_CURVE_WITH_KNOTS ( 'NONE', 3,
 ( #8943, #24815, #21528, #22143, #28507, #34104, #34506, #15747, #28299, #18210, #6281, #30801, #31003, #31606, #18830, #27885, #31403, #34308, #12241, #3228, #18613, #9152, #119, #12650, #25225 ),
 .UNSPECIFIED., .F., .F.,
 ( 4, 3, 3, 3, 3, 3, 3, 3, 4 ),
 ( 6.468151674593503617E-05, 9.076621574721972265E-05, 0.0001210204262067955813, 0.0001512763324577427520, 0.0001815301820994167140, 0.0002117781465860681307, 0.0002420274594459719550, 0.0002722905548971150838, 0.0002816827545175578664 ),
 .UNSPECIFIED. ) ;
#36475=CARTESIAN_POINT ( 'NONE',  ( -1.338463389079526777, -27.83344699523806298, 7.638132480492515697 ) ) ;
#36477=ORIENTED_EDGE ( 'NONE', *, *, #7679, .T. ) ;
#36478=AXIS2_PLACEMENT_3D ( 'NONE', #37513, #270, #9727 ) ;
#36479=DIRECTION ( 'NONE',  ( 0.6427876096865481337, -0.7660444431189706860, -0.000000000000000000 ) ) ;
#36480=CARTESIAN_POINT ( 'NONE',  ( 3.877316292843988155, -32.18164630026152651, 7.775108481317165143 ) ) ;
#36484=EDGE_CURVE ( 'NONE', #13345, #6019, #21426, .T. ) ;
#36493=CARTESIAN_POINT ( 'NONE',  ( -0.1694320636984359418, -32.40961275103795458, 6.911401339314954484 ) ) ;
#36497=CARTESIAN_POINT ( 'NONE',  ( 2.255382727820350652, -26.21553259517144951, 7.692469944509197965 ) ) ;
#36500=CARTESIAN_POINT ( 'NONE',  ( -0.9199683733837696886, -27.40342225418419631, 7.740055089680393685 ) ) ;
#36506=CARTESIAN_POINT ( 'NONE',  ( -1.773773684162445852, -29.99442361894472953, 6.989977667959445640 ) ) ;
#36513=CARTESIAN_POINT ( 'NONE',  ( 4.882868366733327470, -28.37333834040810032, 7.695279973900954751 ) ) ;
#36518=CARTESIAN_POINT ( 'NONE',  ( 1.129853303793442620, -32.92172554530420570, 7.643333865083955736 ) ) ;
#36520=CARTESIAN_POINT ( 'NONE',  ( 4.997854627175230213, -30.74328504515684912, 7.651421919295145813 ) ) ;
#36521=CARTESIAN_POINT ( 'NONE',  ( 2.725517943428533929, -32.81170637720346406, 6.868387053540520704 ) ) ;
#36522=CARTESIAN_POINT ( 'NONE',  ( 5.095993465723490878, -29.74278196016128462, 6.882085323592687764 ) ) ;
#36530=VERTEX_POINT ( 'NONE', #32371 ) ;
#36532=CARTESIAN_POINT ( 'NONE',  ( -0.6763298692248193023, -32.13921067023287037, 7.013842709614101167 ) ) ;
#36533=CARTESIAN_POINT ( 'NONE',  ( 3.058269330830037713, -26.45285399309853602, 6.959317978105167057 ) ) ;
#36535=ADVANCED_FACE ( 'NONE', ( #19398 ), #13408, .F. ) ;
#36538=ORIENTED_EDGE ( 'NONE', *, *, #18206, .T. ) ;
#36539=ADVANCED_FACE ( 'NONE', ( #9922 ), #7035, .F. ) ;
#36544=( BOUNDED_CURVE ( )  B_SPLINE_CURVE ( 3, ( #21976, #28756, #12493, #157 ),
 .UNSPECIFIED., .F., .T. ) 
 B_SPLINE_CURVE_WITH_KNOTS ( ( 4, 4 ),
 ( 1.347909859412853129, 1.534781240595298968 ),
 .UNSPECIFIED. ) 
 CURVE ( )  GEOMETRIC_REPRESENTATION_ITEM ( )  RATIONAL_B_SPLINE_CURVE ( ( 1.000000000000000000, 0.9970920404276225613, 0.9970920404276225613, 1.000000000000000000 ) ) 
 REPRESENTATION_ITEM ( '' )  );
#36551=ORIENTED_EDGE ( 'NONE', *, *, #345, .F. ) ;
#36555=CARTESIAN_POINT ( 'NONE',  ( 1.491073016268174678, -32.96348093246033528, 6.969307238440506147 ) ) ;
#36557=CARTESIAN_POINT ( 'NONE',  ( 4.906539508589050413, -30.70157509802881890, 7.670860738520331346 ) ) ;
#36560=CARTESIAN_POINT ( 'NONE',  ( 0.6790634579381706892, -26.22225927169515458, 6.989977667959444751 ) ) ;
#36562=CARTESIAN_POINT ( 'NONE',  ( 4.494975343341260476, -27.46272638530924226, 6.912143950357350519 ) ) ;
#36564=CARTESIAN_POINT ( 'NONE',  ( 4.244032359733176385, -31.82602863437616136, 6.866852738645441434 ) ) ;
#36565=ORIENTED_EDGE ( 'NONE', *, *, #7725, .T. ) ;
#36570=VECTOR ( 'NONE', #16100, 1000.000000000000000 ) ;
#36575=VECTOR ( 'NONE', #29865, 1000.000000000000227 ) ;
#36577=CARTESIAN_POINT ( 'NONE',  ( 4.984179672459081445, -25.57221830738312107, 7.695279973900954751 ) ) ;
#36578=CARTESIAN_POINT ( 'NONE',  ( -1.634384595334445578, -28.90707823045441671, 6.874555630061440326 ) ) ;
#36581=EDGE_CURVE ( 'NONE', #23038, #14737, #38920, .T. ) ;
#36587=ORIENTED_EDGE ( 'NONE', *, *, #37520, .T. ) ;
#36589=CARTESIAN_POINT ( 'NONE',  ( -1.573542698591475997, -28.33242721227279759, 6.883108633650831365 ) ) ;
#36592=CARTESIAN_POINT ( 'NONE',  ( 4.735674590641913539, -27.84972924505143510, 7.781480525794718162 ) ) ;
#36595=CARTESIAN_POINT ( 'NONE',  ( 3.220794542350093881, -32.61104474200681835, 6.920489980334479263 ) ) ;
#36597=FACE_OUTER_BOUND ( 'NONE', #29245, .T. ) ;
#36602=CARTESIAN_POINT ( 'NONE',  ( 1.826415646469069731, -26.07219983930859897, 7.750000000000000888 ) ) ;
#36605=CARTESIAN_POINT ( 'NONE',  ( 0.3442295505392951038, -32.69542910597172636, 7.386948897581449458 ) ) ;
#36606=CARTESIAN_POINT ( 'NONE',  ( 1.052472996047527642, -32.99480600882493775, 7.785096263473212375 ) ) ;
#36614=CARTESIAN_POINT ( 'NONE',  ( 1.682951012397970292, -26.06997362959739206, 7.750000000000000888 ) ) ;
#36616=CARTESIAN_POINT ( 'NONE',  ( -0.4828924690311028889, -26.96353856790022974, 7.769368695748486431 ) ) ;
#36621=ORIENTED_EDGE ( 'NONE', *, *, #20437, .F. ) ;
#36626=FACE_OUTER_BOUND ( 'NONE', #28195, .T. ) ;
#36629=ORIENTED_EDGE ( 'NONE', *, *, #40163, .T. ) ;
#36630=CARTESIAN_POINT ( 'NONE',  ( 1.513399906207050449, -32.96478432900200062, 7.013842709614101167 ) ) ;
#36638=ORIENTED_EDGE ( 'NONE', *, *, #3152, .T. ) ;
#36639=CARTESIAN_POINT ( 'NONE',  ( 4.815892087276667510, -27.97503390834088677, 6.903112506833889661 ) ) ;
#36644=CARTESIAN_POINT ( 'NONE',  ( 4.739426510580063479, -28.04537359934935736, 6.997764925645181933 ) ) ;
#36645=ORIENTED_EDGE ( 'NONE', *, *, #18112, .F. ) ;
#36646=CARTESIAN_POINT ( 'NONE',  ( -0.03065438358791758300, -26.64358689880297248, 7.695279973900954751 ) ) ;
#36648=CARTESIAN_POINT ( 'NONE',  ( -1.794351914757954303, -29.37815317404309923, 6.941203072598476354 ) ) ;
#36651=CARTESIAN_POINT ( 'NONE',  ( 0.5248424762351729944, -26.37961863118246697, 7.635761828346577573 ) ) ;
#36660=CARTESIAN_POINT ( 'NONE',  ( -89.20959394718985891, -29.55642757665872722, 7.635761828346577573 ) ) ;
#36664=CARTESIAN_POINT ( 'NONE',  ( 4.642268686586925597, -31.46607214451510615, 7.011627023500183853 ) ) ;
#36668=ORIENTED_EDGE ( 'NONE', *, *, #38624, .T. ) ;
#36673=CARTESIAN_POINT ( 'NONE',  ( -0.5531492059869442812, -26.89374777234154124, 7.762796336881263137 ) ) ;
#36674=AXIS2_PLACEMENT_3D ( 'NONE', #17959, #14267, #33228 ) ;
#36676=CARTESIAN_POINT ( 'NONE',  ( -0.5754365072339435727, -32.09591863859081684, 7.757178535559534183 ) ) ;
#36677=CARTESIAN_POINT ( 'NONE',  ( 3.855084250238081101, -32.20002288419953373, 7.784838882742139532 ) ) ;
#36685=VECTOR ( 'NONE', #35799, 999.9999999999998863 ) ;
#36692=ORIENTED_EDGE ( 'NONE', *, *, #27216, .T. ) ;
#36701=CARTESIAN_POINT ( 'NONE',  ( 3.374961858174662765, -26.61090707544855150, 7.730758795053814580 ) ) ;
#36705=ADVANCED_FACE ( 'NONE', ( #23685 ), #17288, .T. ) ;
#36709=CYLINDRICAL_SURFACE ( 'NONE', #32100, 0.09010775117052761962 ) ;
#36712=CARTESIAN_POINT ( 'NONE',  ( 0.5371711504799139281, -32.87097875789517332, 7.695279973900954751 ) ) ;
#36715=CARTESIAN_POINT ( 'NONE',  ( 3.374874343695283940, -26.61085896171689669, 7.661510568013103928 ) ) ;
#36717=LINE ( 'NONE', #24781, #37741 ) ;
#36720=CARTESIAN_POINT ( 'NONE',  ( 4.628153510667976533, -27.84128456964326759, 7.670860738520332234 ) ) ;
#36721=CARTESIAN_POINT ( 'NONE',  ( 4.932896964134850570, -28.51593809159530934, 7.761597726988850532 ) ) ;
#36722=VECTOR ( 'NONE', #14317, 1000.000000000000227 ) ;
#36723=ADVANCED_FACE ( 'NONE', ( #32969 ), #26982, .F. ) ;
#36729=EDGE_LOOP ( 'NONE', ( #26179, #11561, #5352, #7598 ) ) ;
#36730=CARTESIAN_POINT ( 'NONE',  ( -0.9836270791399484015, -27.32572798912499934, 7.762796336881262249 ) ) ;
#36732=CARTESIAN_POINT ( 'NONE',  ( -2.749201978999709084, -28.00803730016500737, 7.695279973900954751 ) ) ;
#36734=DIRECTION ( 'NONE',  ( 0.000000000000000000, 0.7541618601367546804, 0.6566885781822843215 ) ) ;
#36735=CARTESIAN_POINT ( 'NONE',  ( 2.950452266830542403, -26.40805720008219382, 6.866852738645442322 ) ) ;
#36741=VERTEX_POINT ( 'NONE', #17902 ) ;
#36753=ORIENTED_EDGE ( 'NONE', *, *, #19932, .F. ) ;
#36760=CARTESIAN_POINT ( 'NONE',  ( 4.904015517545673220, -30.70870076041410002, 7.652160403243385645 ) ) ;
#36762=CARTESIAN_POINT ( 'NONE',  ( -1.389564992689783951, -31.21326896663422090, 7.754798119455333705 ) ) ;
#36763=CARTESIAN_POINT ( 'NONE',  ( 0.6818738419495123937, -26.22140444123891356, 6.980586498568968068 ) ) ;
#36764=EDGE_CURVE ( 'NONE', #32722, #29003, #36251, .T. ) ;
#36767=EDGE_CURVE ( 'NONE', #36032, #18940, #26912, .T. ) ;
#36768=CARTESIAN_POINT ( 'NONE',  ( 3.913290293412392096, -32.15122301917286762, 7.693875151218754205 ) ) ;
#36770=CARTESIAN_POINT ( 'NONE',  ( 4.215805345278602623, -31.85745850766918252, 6.865312560952603782 ) ) ;
#36774=AXIS2_PLACEMENT_3D ( 'NONE', #37164, #28516, #5884 ) ;
#36779=( BOUNDED_CURVE ( )  B_SPLINE_CURVE ( 3, ( #29267, #36055, #19986, #39319 ),
 .UNSPECIFIED., .F., .T. ) 
 B_SPLINE_CURVE_WITH_KNOTS ( ( 4, 4 ),
 ( 1.381924640371166912, 1.574767692156074483 ),
 .UNSPECIFIED. ) 
 CURVE ( )  GEOMETRIC_REPRESENTATION_ITEM ( )  RATIONAL_B_SPLINE_CURVE ( ( 1.000000000000000000, 0.9969033633783033199, 0.9969033633783033199, 1.000000000000000000 ) ) 
 REPRESENTATION_ITEM ( '' )  );
#36783=ORIENTED_EDGE ( 'NONE', *, *, #19932, .T. ) ;
#36791=CARTESIAN_POINT ( 'NONE',  ( 4.725321061085611341, -27.80929984067426375, 7.756742906098588186 ) ) ;
#36793=EDGE_CURVE ( 'NONE', #12012, #37904, #24070, .T. ) ;
#36795=CARTESIAN_POINT ( 'NONE',  ( 3.214877922168270619, -32.61399439622474716, 6.949473656533219135 ) ) ;
#36796=CARTESIAN_POINT ( 'NONE',  ( 4.933350524036014484, -30.91084454984529373, 6.880828092187094569 ) ) ;
#36808=CARTESIAN_POINT ( 'NONE',  ( 1.104723037367069338, -33.01887311167336492, 7.756742906098588186 ) ) ;
#36815=DIRECTION ( 'NONE',  ( -0.1303762246624229071, 0.7394003126383915658, -0.6605219282605403475 ) ) ;
#36820=CARTESIAN_POINT ( 'NONE',  ( -0.4384946125261977024, -26.92698254572272631, 7.785172627573962778 ) ) ;
#36827=ORIENTED_EDGE ( 'NONE', *, *, #15484, .F. ) ;
#36837=CARTESIAN_POINT ( 'NONE',  ( 0.03162470699431464694, -32.53223031769636009, 7.695279973900954751 ) ) ;
#36838=B_SPLINE_CURVE_WITH_KNOTS ( 'NONE', 3,
 ( #7065, #4594, #10946, #36094, #26017, #32605, #38949, #32805, #7266, #35694 ),
 .UNSPECIFIED., .F., .F.,
 ( 4, 3, 3, 4 ),
 ( 9.697399036122160616E-19, 3.025570593003103526E-05, 6.051145698344126547E-05, 6.468151674593655405E-05 ),
 .UNSPECIFIED. ) ;
#36841=VERTEX_POINT ( 'NONE', #9058 ) ;
#36843=CARTESIAN_POINT ( 'NONE',  ( 5.076139281392760161, -29.16456933348392511, 7.013842709614101167 ) ) ;
#36846=AXIS2_PLACEMENT_3D ( 'NONE', #11732, #24307, #15043 ) ;
#36851=CARTESIAN_POINT ( 'NONE',  ( -1.794870900927445057, -29.38781717045270270, 6.912143950357346966 ) ) ;
#36855=CARTESIAN_POINT ( 'NONE',  ( 0.5064072726788814149, -26.38646991025836286, 7.670860738520330457 ) ) ;
#36866=PLANE ( 'NONE',  #8366 ) ;
#36868=CARTESIAN_POINT ( 'NONE',  ( 1.067812944203182068, -26.12756469803955994, 7.651421919295144924 ) ) ;
#36871=LINE ( 'NONE', #17303, #25298 ) ;
#36872=CARTESIAN_POINT ( 'NONE',  ( 4.683157593253919337, -31.40110544287195182, 6.863805608295730387 ) ) ;
#36881=CARTESIAN_POINT ( 'NONE',  ( -0.6411629333918610341, -32.17099039281331585, 7.754798119455333705 ) ) ;
#36883=B_SPLINE_CURVE_WITH_KNOTS ( 'NONE', 3,
 ( #19711, #32286, #13528, #39022, #35577, #7346, #4087, #26099, #32679, #38636 ),
 .UNSPECIFIED., .F., .F.,
 ( 4, 3, 3, 4 ),
 ( 0.0001585009270395771057, 0.0001815657551981834624, 0.0002118214035944139149, 0.0002170292169044812859 ),
 .UNSPECIFIED. ) ;
#36888=CARTESIAN_POINT ( 'NONE',  ( -1.476689534549258553, -28.35907466968827251, 6.892063359921935195 ) ) ;
#36889=ORIENTED_EDGE ( 'NONE', *, *, #34161, .T. ) ;
#36891=CARTESIAN_POINT ( 'NONE',  ( -1.650274565467498622, -28.99282850696639713, 7.635761828346577573 ) ) ;
#36894=AXIS2_PLACEMENT_3D ( 'NONE', #6104, #30823, #4921 ) ;
#36900=( BOUNDED_CURVE ( )  B_SPLINE_CURVE ( 3, ( #34513, #6290, #33900, #5674 ),
 .UNSPECIFIED., .F., .T. ) 
 B_SPLINE_CURVE_WITH_KNOTS ( ( 4, 4 ),
 ( 4.708531083176466403, 4.895802057644187855 ),
 .UNSPECIFIED. ) 
 CURVE ( )  GEOMETRIC_REPRESENTATION_ITEM ( )  RATIONAL_B_SPLINE_CURVE ( ( 1.000000000000000000, 0.9970795998553221295, 0.9970795998553221295, 1.000000000000000000 ) ) 
 REPRESENTATION_ITEM ( '' )  );
#36905=ORIENTED_EDGE ( 'NONE', *, *, #39641, .F. ) ;
#36910=CARTESIAN_POINT ( 'NONE',  ( -1.693162313832979882, -29.36062282964724446, 6.939395833800440450 ) ) ;
#36915=CARTESIAN_POINT ( 'NONE',  ( 1.564461960465584056, -33.06730180939113950, 6.870724624169668004 ) ) ;
#36917=ADVANCED_FACE ( 'NONE', ( #6750 ), #31666, .F. ) ;
#36918=ORIENTED_EDGE ( 'NONE', *, *, #13069, .T. ) ;
#36920=CARTESIAN_POINT ( 'NONE',  ( -1.697894189101925688, -29.44521499630638317, 7.082877429276022596 ) ) ;
#36921=EDGE_CURVE ( 'NONE', #11301, #12509, #14036, .T. ) ;
#36925=CARTESIAN_POINT ( 'NONE',  ( 1.142679410947742502, -32.92387906214399607, 7.670860738520326905 ) ) ;
#36927=LINE ( 'NONE', #5846, #914 ) ;
#36930=CARTESIAN_POINT ( 'NONE',  ( 4.905573833743076761, -28.43555934915513816, 7.782167645815905033 ) ) ;
#36934=ORIENTED_EDGE ( 'NONE', *, *, #3313, .F. ) ;
#36937=CARTESIAN_POINT ( 'NONE',  ( 0.1096350232455502172, -26.56499967738685442, 6.863904403958575706 ) ) ;
#36938=CARTESIAN_POINT ( 'NONE',  ( 2.970096061415592903, -26.41590945512262323, 6.864276522220859711 ) ) ;
#36943=B_SPLINE_CURVE_WITH_KNOTS ( 'NONE', 3,
 ( #29608, #13959, #10263, #10857, #29216, #1025, #26133, #23436, #36003, #4701, #11253, #30217, #24237, #39887, #20528, #11057, #26923, #2034, #23629, #27536, #40088, #5716, #18256, #23818, #39266 ),
 .UNSPECIFIED., .F., .F.,
 ( 4, 3, 3, 3, 3, 3, 3, 3, 4 ),
 ( 6.468151674593992863E-05, 9.076621574722235184E-05, 0.0001210204262068006228, 0.0001512763324577468178, 0.0001815301820994240866, 0.0002117781465860793522, 0.0002420274594459826344, 0.0002722905548971214806, 0.0002816827545175697926 ),
 .UNSPECIFIED. ) ;
#36944=CARTESIAN_POINT ( 'NONE',  ( 5.909439403370450705, -28.84147213309200808, 7.635761828346577573 ) ) ;
#36947=DIRECTION ( 'NONE',  ( 0.000000000000000000, -0.7541618601367544583, 0.6566885781822845436 ) ) ;
#36954=VERTEX_POINT ( 'NONE', #38827 ) ;
#36963=ADVANCED_FACE ( 'NONE', ( #35572 ), #29573, .F. ) ;
#36964=CARTESIAN_POINT ( 'NONE',  ( 1.506707068943643479, -32.96441568433041880, 7.006423389747790331 ) ) ;
#36969=CARTESIAN_POINT ( 'NONE',  ( -1.477562859369297987, -28.36137111117319520, 6.894806418505348589 ) ) ;
#36970=CARTESIAN_POINT ( 'NONE',  ( 5.046487440160131399, -28.96688155391847630, 7.756377446753163873 ) ) ;
#36978=CARTESIAN_POINT ( 'NONE',  ( -1.659482627397846022, -30.09084907119505914, 7.784476445165072533 ) ) ;
#36979=CARTESIAN_POINT ( 'NONE',  ( 5.401390093233090717, -28.79627056164295595, 7.013842709614101167 ) ) ;
#36982=ORIENTED_EDGE ( 'NONE', *, *, #20574, .T. ) ;
#36984=CARTESIAN_POINT ( 'NONE',  ( -0.5845629148083903992, -32.22116963437284198, 6.880608371227951992 ) ) ;
#36985=VERTEX_POINT ( 'NONE', #22605 ) ;
#36987=ORIENTED_EDGE ( 'NONE', *, *, #28391, .F. ) ;
#36991=ADVANCED_FACE ( 'NONE', ( #7542 ), #23005, .T. ) ;
#36994=AXIS2_PLACEMENT_3D ( 'NONE', #30990, #22335, #31387 ) ;
#36995=CARTESIAN_POINT ( 'NONE',  ( -1.779986342064762805, -29.14226580803136812, 7.134293011406500185 ) ) ;
#36996=ORIENTED_EDGE ( 'NONE', *, *, #39984, .T. ) ;
#36999=CARTESIAN_POINT ( 'NONE',  ( 3.357996495870312792, -32.53848892694827555, 6.894806418505347700 ) ) ;
#37000=CARTESIAN_POINT ( 'NONE',  ( 4.948068533112945921, -30.87476149476646015, 6.865482280155367434 ) ) ;
#37002=PLANE ( 'NONE',  #4726 ) ;
#37005=CARTESIAN_POINT ( 'NONE',  ( 3.939786388318850641, -26.88011527646091992, 7.635761828346575797 ) ) ;
#37006=CARTESIAN_POINT ( 'NONE',  ( -0.9595137531180226720, -31.84477669336278893, 7.720710062488890912 ) ) ;
#37007=EDGE_CURVE ( 'NONE', #9806, #908, #35961, .T. ) ;
#37008=CARTESIAN_POINT ( 'NONE',  ( 4.978066369605828712, -28.34239679187065164, 7.670465701733752972 ) ) ;
#37012=ORIENTED_EDGE ( 'NONE', *, *, #7066, .F. ) ;
#37013=DIRECTION ( 'NONE',  ( 0.8660254037844404840, -0.4999999999999968359, 0.000000000000000000 ) ) ;
#37014=B_SPLINE_CURVE_WITH_KNOTS ( 'NONE', 3,
 ( #6295, #3841, #330, #16358, #12870, #34929, #733, #13270, #25841, #16752, #17555, #33238, #1538, #38977, #14276, #23155, #29928, #13883, #20252, #7903, #7298, #14071, #23559, #11177, #17349, #29333, #8089, #29727, #17155, #10386, #13686 ),
 .UNSPECIFIED., .F., .F.,
 ( 4, 3, 3, 3, 3, 3, 3, 3, 3, 3, 4 ),
 ( 2.453269466693398698E-18, 3.077658087705472024E-05, 6.152638666998585908E-05, 9.267501192706446866E-05, 0.0001241882240135159729, 0.0001556618703051619753, 0.0001866161554452215447, 0.0002167966385860964937, 0.0002463805737537774895, 0.0002758761370306528696, 0.0002847094172290100906 ),
 .UNSPECIFIED. ) ;
#37015=CARTESIAN_POINT ( 'NONE',  ( 4.643443039977110942, -31.27241053648453928, 7.769368695748485543 ) ) ;
#37016=CARTESIAN_POINT ( 'NONE',  ( 4.085542087826527613, -27.00846887205345936, 6.998987538705435441 ) ) ;
#37018=CARTESIAN_POINT ( 'NONE',  ( 4.790345179149528398, -27.92659140015631891, 7.754798119455333705 ) ) ;
#37031=CARTESIAN_POINT ( 'NONE',  ( -1.741157480058983076, -30.20692156021776142, 7.660770905198784675 ) ) ;
#37032=ORIENTED_EDGE ( 'NONE', *, *, #29249, .F. ) ;
#37039=ORIENTED_EDGE ( 'NONE', *, *, #40073, .F. ) ;
#37042=VERTEX_POINT ( 'NONE', #13920 ) ;
#37047=CARTESIAN_POINT ( 'NONE',  ( 3.340113934647170435, -32.66206629357650115, 7.750000000000000888 ) ) ;
#37049=CARTESIAN_POINT ( 'NONE',  ( -1.799411162598936187, -29.53200968670955007, 6.887161170156905321 ) ) ;
#37052=CARTESIAN_POINT ( 'NONE',  ( 0.5038290195879405742, -26.38744034030630914, 7.692469944509198854 ) ) ;
#37054=DIRECTION ( 'NONE',  ( -0.1303762246624131926, -0.7394003126383953406, 0.6605219282605379050 ) ) ;
#37055=EDGE_LOOP ( 'NONE', ( #22449, #16456, #13548, #15953, #6988 ) ) ;
#37060=LINE ( 'NONE', #8850, #35397 ) ;
#37065=CARTESIAN_POINT ( 'NONE',  ( -0.6769021000928485687, -27.12926683874087530, 7.505001789837627335 ) ) ;
#37069=CARTESIAN_POINT ( 'NONE',  ( 4.384407265606144577, -31.81413237766177815, 7.762796336881259585 ) ) ;
#37071=ORIENTED_EDGE ( 'NONE', *, *, #16621, .T. ) ;
#37073=DIRECTION ( 'NONE',  ( 1.047444401652940007E-14, -1.000000000000000000, -0.000000000000000000 ) ) ;
#37079=CARTESIAN_POINT ( 'NONE',  ( 4.417933383020717031, -31.78637517338679075, 7.255881584735162981 ) ) ;
#37084=B_SPLINE_CURVE_WITH_KNOTS ( 'NONE', 3,
 ( #17768, #40409, #12215, #30355, #31174, #24787, #9129, #21704, #2160, #15512 ),
 .UNSPECIFIED., .F., .F.,
 ( 4, 3, 3, 4 ),
 ( 0.000000000000000000, 3.025570593003203137E-05, 6.051145698344047942E-05, 6.468151674593313881E-05 ),
 .UNSPECIFIED. ) ;
#37087=CARTESIAN_POINT ( 'NONE',  ( 5.028764603308605530, -28.48812247857538438, 7.754798119455333705 ) ) ;
#37088=ORIENTED_EDGE ( 'NONE', *, *, #30204, .T. ) ;
#37094=ADVANCED_FACE ( 'NONE', ( #35768 ), #35173, .F. ) ;
#37095=CARTESIAN_POINT ( 'NONE',  ( -0.1776591873979048719, -32.40417280263461208, 6.969307238440504371 ) ) ;
#37098=CARTESIAN_POINT ( 'NONE',  ( 2.325436196043557224, -33.01366662812485941, 7.640616322432100205 ) ) ;
#37100=DIRECTION ( 'NONE',  ( 0.7541618601367571229, 0.000000000000000000, -0.6566885781822815460 ) ) ;
#37103=VERTEX_POINT ( 'NONE', #10621 ) ;
#37104=VECTOR ( 'NONE', #16510, 1000.000000000000000 ) ;
#37107=DIRECTION ( 'NONE',  ( -0.000000000000000000, -0.000000000000000000, -1.000000000000000000 ) ) ;
#37111=FACE_OUTER_BOUND ( 'NONE', #5772, .T. ) ;
#37116=CARTESIAN_POINT ( 'NONE',  ( 5.200390093233090205, -29.56993018339339940, 7.202408869016171167 ) ) ;
#37118=CARTESIAN_POINT ( 'NONE',  ( 2.135230303526129081, -33.04281284647206007, 7.006908160621413195 ) ) ;
#37122=CARTESIAN_POINT ( 'NONE',  ( -0.08001846698760761711, -26.55660217189416272, 7.710604733652626663 ) ) ;
#37123=CARTESIAN_POINT ( 'NONE',  ( 0.4174405697466118670, -32.81861354646682827, 7.776484688137385248 ) ) ;
#37124=CARTESIAN_POINT ( 'NONE',  ( 4.221612433196463066, -25.23005020686840183, 7.635761828346577573 ) ) ;
#37125=CARTESIAN_POINT ( 'NONE',  ( 4.626733377823518012, -27.83888570657239470, 7.693875151218754205 ) ) ;
#37127=( GEOMETRIC_REPRESENTATION_CONTEXT ( 3 ) GLOBAL_UNCERTAINTY_ASSIGNED_CONTEXT ( ( #30410 ) ) GLOBAL_UNIT_ASSIGNED_CONTEXT ( ( #21229, #14228, #30712 ) ) REPRESENTATION_CONTEXT ( 'NONE', 'WORKASPACE' ) );
#37133=VECTOR ( 'NONE', #28337, 1000.000000000000114 ) ;
#37136=CYLINDRICAL_SURFACE ( 'NONE', #10121, 0.09010775117053149152 ) ;
#37137=DIRECTION ( 'NONE',  ( -0.3420201433256725987, 0.9396926207859068736, -0.000000000000000000 ) ) ;
#37138=CARTESIAN_POINT ( 'NONE',  ( -1.416918730809773042, -28.21258232695399926, 6.939395833800441338 ) ) ;
#37139=( BOUNDED_CURVE ( )  B_SPLINE_CURVE ( 3, ( #28359, #171, #22402, #10019 ),
 .UNSPECIFIED., .F., .T. ) 
 B_SPLINE_CURVE_WITH_KNOTS ( ( 4, 4 ),
 ( 1.381924640371167579, 1.574767692156076260 ),
 .UNSPECIFIED. ) 
 CURVE ( )  GEOMETRIC_REPRESENTATION_ITEM ( )  RATIONAL_B_SPLINE_CURVE ( ( 1.000000000000000000, 0.9969033633783032089, 0.9969033633783032089, 1.000000000000000000 ) ) 
 REPRESENTATION_ITEM ( '' )  );
#37140=CARTESIAN_POINT ( 'NONE',  ( 1.295029243323604806, -26.19418099523372945, 7.013842709614101167 ) ) ;
#37143=ORIENTED_EDGE ( 'NONE', *, *, #26058, .F. ) ;
#37154=LINE ( 'NONE', #40645, #15570 ) ;
#37164=CARTESIAN_POINT ( 'NONE',  ( 1.578585683582352850, -25.86893018339335981, 7.754798119455333705 ) ) ;
#37165=CARTESIAN_POINT ( 'NONE',  ( 3.419804421016331641, -26.52138713537738468, 7.710604733652623999 ) ) ;
#37167=CARTESIAN_POINT ( 'NONE',  ( 4.902191478375081068, -30.71383239352053707, 7.643333865083957512 ) ) ;
#37170=DIRECTION ( 'NONE',  ( -0.7126435865141291792, 0.000000000000000000, 0.7015262779114398439 ) ) ;
#37171=CARTESIAN_POINT ( 'NONE',  ( 5.067139036913483885, -29.09558115474426998, 7.759451378593096749 ) ) ;
#37178=CARTESIAN_POINT ( 'NONE',  ( 4.949602693582518143, -30.84314527041428278, 7.780491323090173772 ) ) ;
#37179=CARTESIAN_POINT ( 'NONE',  ( 2.193195751821546580, -33.03421897962276432, 7.761113333117550361 ) ) ;
#37183=CARTESIAN_POINT ( 'NONE',  ( -1.557289549629824466, -30.54335471976638416, 6.911401339314958925 ) ) ;
#37184=ORIENTED_EDGE ( 'NONE', *, *, #35408, .F. ) ;
#37187=CARTESIAN_POINT ( 'NONE',  ( 0.5834512725888432172, -26.35863018636138122, 6.894806418505347700 ) ) ;
#37193=CARTESIAN_POINT ( 'NONE',  ( -1.521281195261787733, -28.20213550263213165, 6.993830769476428344 ) ) ;
#37200=CARTESIAN_POINT ( 'NONE',  ( 4.920199257240864377, -30.94209232664453779, 6.980586498568960963 ) ) ;
#37206=CARTESIAN_POINT ( 'NONE',  ( 2.429106749998194648, -26.14670993789270526, 7.753200566781576875 ) ) ;
#37207=AXIS2_PLACEMENT_3D ( 'NONE', #4667, #20295, #5268 ) ;
#37210=CARTESIAN_POINT ( 'NONE',  ( 3.504784550580148483, -26.68823612567400971, 7.754798119455333705 ) ) ;
#37215=CARTESIAN_POINT ( 'NONE',  ( 2.880952512028528645, -26.27504388691242454, 7.640616322432101093 ) ) ;
#37216=CARTESIAN_POINT ( 'NONE',  ( 4.614225597785307720, -31.32194692201518293, 7.785172627573962778 ) ) ;
#37219=ORIENTED_EDGE ( 'NONE', *, *, #30549, .F. ) ;
#37226=EDGE_CURVE ( 'NONE', #14186, #32722, #9601, .T. ) ;
#37231=CARTESIAN_POINT ( 'NONE',  ( 3.481437286441587897, -32.58288071328335178, 7.695279973900954751 ) ) ;
#37235=CARTESIAN_POINT ( 'NONE',  ( -0.4715774662971216613, -26.83452162274424424, 7.776484688137385248 ) ) ;
#37236=EDGE_LOOP ( 'NONE', ( #37286, #19234, #3251, #13893 ) ) ;
#37238=EDGE_CURVE ( 'NONE', #6366, #20740, #16242, .T. ) ;
#37242=CARTESIAN_POINT ( 'NONE',  ( 2.294856720451861953, -26.12078399496891734, 7.635761828346576685 ) ) ;
#37243=ORIENTED_EDGE ( 'NONE', *, *, #21718, .T. ) ;
#37252=FACE_OUTER_BOUND ( 'NONE', #31739, .T. ) ;
#37260=CARTESIAN_POINT ( 'NONE',  ( 3.501669127342749821, -26.58529237886445173, 7.784725160561910329 ) ) ;
#37265=CARTESIAN_POINT ( 'NONE',  ( -0.9267661122611743352, -27.41167846166631961, 7.680992449362110897 ) ) ;
#37268=CARTESIAN_POINT ( 'NONE',  ( 1.079328522417935421, -26.12547340107537863, 7.635761828346579350 ) ) ;
#37270=CARTESIAN_POINT ( 'NONE',  ( 5.144118623760252085, -28.96327807028931289, 7.767720160662276108 ) ) ;
#37273=VECTOR ( 'NONE', #27260, 1000.000000000000227 ) ;
#37276=AXIS2_PLACEMENT_3D ( 'NONE', #28569, #16204, #6746 ) ;
#37280=CARTESIAN_POINT ( 'NONE',  ( 5.043330201822981529, -28.53322799357174588, 7.013842709614101167 ) ) ;
#37281=ORIENTED_EDGE ( 'NONE', *, *, #35411, .F. ) ;
#37286=ORIENTED_EDGE ( 'NONE', *, *, #3997, .F. ) ;
#37290=ORIENTED_EDGE ( 'NONE', *, *, #35035, .F. ) ;
#37297=CARTESIAN_POINT ( 'NONE',  ( -0.1776515958430064102, -32.40417910011337455, 6.939395833800439561 ) ) ;
#37298=ORIENTED_EDGE ( 'NONE', *, *, #25209, .T. ) ;
#37302=CARTESIAN_POINT ( 'NONE',  ( 0.6463980014349960390, -26.33742331249164081, 7.761597726988850532 ) ) ;
#37305=AXIS2_PLACEMENT_3D ( 'NONE', #8038, #29483, #16903 ) ;
#37306=ORIENTED_EDGE ( 'NONE', *, *, #23021, .F. ) ;
#37307=DIRECTION ( 'NONE',  ( -1.000000000000000000, 0.000000000000000000, 0.000000000000000000 ) ) ;
#37311=CARTESIAN_POINT ( 'NONE',  ( -2.293238129880355913, -32.69087815247542039, 6.954324564059724878 ) ) ;
#37319=DIRECTION ( 'NONE',  ( 0.6662082868431814520, 0.000000000000000000, 0.7457657263118715463 ) ) ;
#37325=LINE ( 'NONE', #5637, #27523 ) ;
#37328=LINE ( 'NONE', #34686, #2995 ) ;
#37330=EDGE_CURVE ( 'NONE', #15980, #26363, #29722, .T. ) ;
#37335=ORIENTED_EDGE ( 'NONE', *, *, #14362, .T. ) ;
#37336=DIRECTION ( 'NONE',  ( 0.9848077530122080203, 0.1736481776669307198, -0.000000000000000000 ) ) ;
#37339=ORIENTED_EDGE ( 'NONE', *, *, #2208, .F. ) ;
#37340=DIRECTION ( 'NONE',  ( -1.000000000000000000, -0.000000000000000000, -0.000000000000000000 ) ) ;
#37341=CARTESIAN_POINT ( 'NONE',  ( 0.04722595069169110288, -26.59889400027656592, 6.889465824494255486 ) ) ;
#37342=CARTESIAN_POINT ( 'NONE',  ( -1.420842525589276928, -28.22162052951723155, 6.911401339314954484 ) ) ;
#37343=CARTESIAN_POINT ( 'NONE',  ( 1.301827788660890217, -26.19337156708387226, 6.903372536218456368 ) ) ;
#37344=CARTESIAN_POINT ( 'NONE',  ( 5.039647113661429145, -30.20982371162487468, 7.785868773668302545 ) ) ;
#37348=VERTEX_POINT ( 'NONE', #24460 ) ;
#37349=ORIENTED_EDGE ( 'NONE', *, *, #19347, .F. ) ;
#37351=CARTESIAN_POINT ( 'NONE',  ( -1.677952523657942008, -29.95307700655620664, 6.969307238440509700 ) ) ;
#37354=VERTEX_POINT ( 'NONE', #3091 ) ;
#37356=CARTESIAN_POINT ( 'NONE',  ( 4.620198719170100610, -31.31197426661971761, 6.894806418505346812 ) ) ;
#37362=AXIS2_PLACEMENT_3D ( 'NONE', #16554, #37978, #31618 ) ;
#37365=CARTESIAN_POINT ( 'NONE',  ( 1.689233551583659620, -32.96992199003639712, 7.775108481317161591 ) ) ;
#37369=CARTESIAN_POINT ( 'NONE',  ( 3.974563734633631995, -27.04245323997484007, 7.759451378593098525 ) ) ;
#37370=CARTESIAN_POINT ( 'NONE',  ( 4.724705146729046845, -27.80824960587721506, 7.635761828346577573 ) ) ;
#37372=CARTESIAN_POINT ( 'NONE',  ( 5.060262813864030207, -29.04901129559175743, 7.784476445165073422 ) ) ;
#37374=EDGE_CURVE ( 'NONE', #5035, #2507, #22415, .T. ) ;
#37382=( BOUNDED_CURVE ( )  B_SPLINE_CURVE ( 3, ( #9672, #31921, #28408, #631 ),
 .UNSPECIFIED., .F., .F. ) 
 B_SPLINE_CURVE_WITH_KNOTS ( ( 4, 4 ),
 ( 4.708531083176467291, 4.895802057644188743 ),
 .UNSPECIFIED. ) 
 CURVE ( )  GEOMETRIC_REPRESENTATION_ITEM ( )  RATIONAL_B_SPLINE_CURVE ( ( 1.000000000000000000, 0.9970795998553221295, 0.9970795998553221295, 1.000000000000000000 ) ) 
 REPRESENTATION_ITEM ( '' )  );
#37385=CARTESIAN_POINT ( 'NONE',  ( -1.666031540912286335, -30.04659083958180688, 7.761597726988851420 ) ) ;
#37388=FACE_OUTER_BOUND ( 'NONE', #25412, .T. ) ;
#37390=ORIENTED_EDGE ( 'NONE', *, *, #25406, .T. ) ;
#37400=EDGE_LOOP ( 'NONE', ( #5172, #23813, #18604, #28210 ) ) ;
#37402=CARTESIAN_POINT ( 'NONE',  ( 0.9719320429316903320, -25.36088087325603624, 7.635761828346577573 ) ) ;
#37407=ORIENTED_EDGE ( 'NONE', *, *, #28772, .T. ) ;
#37408=CARTESIAN_POINT ( 'NONE',  ( 4.913015741384740842, -30.70456324267604131, 7.257242401810564125 ) ) ;
#37411=CARTESIAN_POINT ( 'NONE',  ( 5.009633645164218052, -30.35025518876119222, 6.903372536218457256 ) ) ;
#37414=LINE ( 'NONE', #2667, #31888 ) ;
#37415=VERTEX_POINT ( 'NONE', #28987 ) ;
#37417=CARTESIAN_POINT ( 'NONE',  ( 3.480514495105446748, -26.67316417380424554, 6.866852738645443210 ) ) ;
#37419=CARTESIAN_POINT ( 'NONE',  ( 4.014016674530351381, -26.94369103923406783, 6.865554069792297653 ) ) ;
#37424=CARTESIAN_POINT ( 'NONE',  ( 1.873241870000961873, -26.17432681090300051, 6.882085323592685100 ) ) ;
#37426=CARTESIAN_POINT ( 'NONE',  ( 4.790345179149528398, -27.92659140015631891, 7.754798119455333705 ) ) ;
#37428=ORIENTED_EDGE ( 'NONE', *, *, #6846, .T. ) ;
#37436=ORIENTED_EDGE ( 'NONE', *, *, #8216, .F. ) ;
#37438=CARTESIAN_POINT ( 'NONE',  ( -1.506684114051581647, -28.44091511309124343, 7.695279973900954751 ) ) ;
#37439=EDGE_LOOP ( 'NONE', ( #16270, #1756, #36538, #15838 ) ) ;
#37443=ORIENTED_EDGE ( 'NONE', *, *, #22707, .F. ) ;
#37445=AXIS2_PLACEMENT_3D ( 'NONE', #27138, #11477, #14370 ) ;
#37446=CARTESIAN_POINT ( 'NONE',  ( 4.749272330503722550, -31.28874288805750936, 7.698786668945012401 ) ) ;
#37451=CARTESIAN_POINT ( 'NONE',  ( 5.144146178010085890, -28.94499496390147186, 7.750000000000002665 ) ) ;
#37454=ORIENTED_EDGE ( 'NONE', *, *, #25205, .F. ) ;
#37455=EDGE_CURVE ( 'NONE', #11405, #38807, #16925, .T. ) ;
#37457=TOROIDAL_SURFACE ( 'NONE', #1986, 3.449999999999999289, 0.05000000000000000278 ) ;
#37458=CARTESIAN_POINT ( 'NONE',  ( 3.461681733142665252, -26.55548550598080482, 7.778495531946297170 ) ) ;
#37464=DIRECTION ( 'NONE',  ( 0.000000000000000000, 0.7508067542896625923, -0.6605219282605402364 ) ) ;
#37467=EDGE_CURVE ( 'NONE', #25920, #12896, #31710, .T. ) ;
#37469=CARTESIAN_POINT ( 'NONE',  ( 5.147370308016914642, -29.03863631697392833, 7.782861076432729952 ) ) ;
#37470=CARTESIAN_POINT ( 'NONE',  ( -1.348517286369409263, -27.85116208076715694, 7.695279973900954751 ) ) ;
#37471=CARTESIAN_POINT ( 'NONE',  ( 3.875507134935765041, -26.95672030760948346, 7.635761828346577573 ) ) ;
#37473=CARTESIAN_POINT ( 'NONE',  ( -1.245527615359759421, -31.26744862341078601, 7.769368695748486431 ) ) ;
#37480=B_SPLINE_CURVE_WITH_KNOTS ( 'NONE', 3,
 ( #53, #34240, #31132, #37684, #9489, #29457, #862, #38706, #13807, #16878, #29054, #16482, #22882, #19177, #23084, #32165, #13198, #35648, #16083, #25766, #1268, #4355, #35451, #6631, #38501, #7418, #9906, #13601, #13395, #25968, #12995 ),
 .UNSPECIFIED., .F., .F.,
 ( 4, 3, 3, 3, 3, 3, 3, 3, 3, 3, 4 ),
 ( 1.226634733346699349E-18, 3.077658087705221980E-05, 6.152638666998412435E-05, 9.267501192705790924E-05, 0.0001241882240135090069, 0.0001556618703051638184, 0.0001866161554452129795, 0.0002167966385860912895, 0.0002463805737537707674, 0.0002758761370306483701, 0.0002847094172289977307 ),
 .UNSPECIFIED. ) ;
#37485=DIRECTION ( 'NONE',  ( -0.1736481776669207000, -0.9848077530122097967, -0.000000000000000000 ) ) ;
#37489=ORIENTED_EDGE ( 'NONE', *, *, #24795, .F. ) ;
#37496=CARTESIAN_POINT ( 'NONE',  ( 2.357492685323943071, -26.13216693042389238, 6.878641987404677138 ) ) ;
#37509=CARTESIAN_POINT ( 'NONE',  ( 4.264666792353081881, -31.95205776465687109, 6.903112506833895878 ) ) ;
#37510=CARTESIAN_POINT ( 'NONE',  ( -1.693758227496673818, -29.37045797875395081, 6.911401339314954484 ) ) ;
#37512=CARTESIAN_POINT ( 'NONE',  ( -1.386736143452785397, -31.21906680561900771, 6.865482280155368322 ) ) ;
#37513=CARTESIAN_POINT ( 'NONE',  ( 1.700390093233090871, -29.56993018339339940, 7.800000000000000711 ) ) ;
#37518=CARTESIAN_POINT ( 'NONE',  ( 0.5270352314696233886, -32.86739471733553586, 7.651421919295140484 ) ) ;
#37520=EDGE_CURVE ( 'NONE', #4296, #15988, #3712, .T. ) ;
#37524=CARTESIAN_POINT ( 'NONE',  ( -0.9362298265465702762, -31.71663383657275048, 7.785868773668303433 ) ) ;
#37525=CARTESIAN_POINT ( 'NONE',  ( 1.700390093233090871, -29.56993018339339940, 7.800000000000000711 ) ) ;
#37526=B_SPLINE_CURVE_WITH_KNOTS ( 'NONE', 3,
 ( #27288, #18015, #39853, #40660, #11621, #17806, #34116, #14933, #2817, #20911, #30603, #5888, #21126, #24200, #27897, #21538, #2412, #30812, #33693 ),
 .UNSPECIFIED., .F., .F.,
 ( 4, 3, 3, 3, 3, 3, 4 ),
 ( 0.000000000000000000, 2.546128104244658723E-05, 5.711050680483961836E-05, 8.113074941675755018E-05, 0.0001053129305727055061, 0.0001360598016347104686, 0.0001612931755713720725 ),
 .UNSPECIFIED. ) ;
#37534=EDGE_CURVE ( 'NONE', #357, #30063, #14283, .T. ) ;
#37538=AXIS2_PLACEMENT_3D ( 'NONE', #19941, #36199, #36007 ) ;
#37539=CARTESIAN_POINT ( 'NONE',  ( 4.888269927152609995, -30.75209629908899345, 7.779495906702014629 ) ) ;
#37544=CARTESIAN_POINT ( 'NONE',  ( 3.427626883898521548, -33.95934199490189087, 7.754798119455333705 ) ) ;
#37546=AXIS2_PLACEMENT_3D ( 'NONE', #5592, #18132, #30723 ) ;
#37547=ORIENTED_EDGE ( 'NONE', *, *, #21774, .T. ) ;
#37550=CARTESIAN_POINT ( 'NONE',  ( -1.677952468049122681, -29.95308686996596492, 6.939395833800444002 ) ) ;
#37553=EDGE_CURVE ( 'NONE', #15769, #32660, #28079, .T. ) ;
#37554=CARTESIAN_POINT ( 'NONE',  ( 4.412680168184114571, -27.51969055122301100, 6.882085323592682435 ) ) ;
#37565=CARTESIAN_POINT ( 'NONE',  ( 1.626685898479098835, -32.96914518493439772, 6.874555630061442102 ) ) ;
#37569=CARTESIAN_POINT ( 'NONE',  ( -0.07139632246815744154, -26.55151886593404953, 7.651421919295142260 ) ) ;
#37570=CARTESIAN_POINT ( 'NONE',  ( 4.327908163969745203, -31.72774129374396423, 7.693875151218750652 ) ) ;
#37571=CARTESIAN_POINT ( 'NONE',  ( 3.481393211524530074, -32.58290676861527402, 7.698786668945011513 ) ) ;
#37572=CARTESIAN_POINT ( 'NONE',  ( 5.054793046568992310, -30.12489038615697012, 7.695279973900954751 ) ) ;
#37577=ORIENTED_EDGE ( 'NONE', *, *, #11562, .F. ) ;
#37580=CARTESIAN_POINT ( 'NONE',  ( -1.648452539126854077, -30.15751253820718603, 7.769368695748486431 ) ) ;
#37581=EDGE_CURVE ( 'NONE', #35253, #16534, #22734, .T. ) ;
#37589=ORIENTED_EDGE ( 'NONE', *, *, #5381, .T. ) ;
#37590=CARTESIAN_POINT ( 'NONE',  ( 4.037419903619875683, -26.96561723250201226, 7.761113333117551250 ) ) ;
#37594=CARTESIAN_POINT ( 'NONE',  ( -1.749422520758312505, -28.97934324792513294, 7.750000000000000000 ) ) ;
#37596=CARTESIAN_POINT ( 'NONE',  ( -0.8497392533635172995, -27.32118824274597202, 6.870716933885663735 ) ) ;
#37598=ORIENTED_EDGE ( 'NONE', *, *, #40257, .F. ) ;
#37600=CARTESIAN_POINT ( 'NONE',  ( -0.004744360168457827966, -26.52985000677408678, 7.785096263473211486 ) ) ;
#37606=ORIENTED_EDGE ( 'NONE', *, *, #32774, .T. ) ;
#37613=( BOUNDED_CURVE ( )  B_SPLINE_CURVE ( 3, ( #15607, #40715, #12514, #25491 ),
 .UNSPECIFIED., .F., .T. ) 
 B_SPLINE_CURVE_WITH_KNOTS ( ( 4, 4 ),
 ( 4.708531083176467291, 4.886921905584129533 ),
 .UNSPECIFIED. ) 
 CURVE ( )  GEOMETRIC_REPRESENTATION_ITEM ( )  RATIONAL_B_SPLINE_CURVE ( ( 1.000000000000000000, 0.9973498172709134302, 0.9973498172709134302, 1.000000000000000000 ) ) 
 REPRESENTATION_ITEM ( '' )  );
#37615=ORIENTED_EDGE ( 'NONE', *, *, #23927, .T. ) ;
#37618=CARTESIAN_POINT ( 'NONE',  ( 4.626733377823518012, -27.83888570657239470, 7.703977250142849620 ) ) ;
#37620=ORIENTED_EDGE ( 'NONE', *, *, #10665, .T. ) ;
#37622=CARTESIAN_POINT ( 'NONE',  ( 4.252472416081320539, -31.81647455533660107, 7.782034975670476307 ) ) ;
#37624=ORIENTED_EDGE ( 'NONE', *, *, #21679, .F. ) ;
#37629=DIRECTION ( 'NONE',  ( 0.1303762246624182997, 0.7394003126383944524, 0.6605219282605379050 ) ) ;
#37631=CARTESIAN_POINT ( 'NONE',  ( -1.627575555862121215, -28.87372634162266039, 7.768425012602595991 ) ) ;
#37634=ORIENTED_EDGE ( 'NONE', *, *, #29510, .F. ) ;
#37637=ORIENTED_EDGE ( 'NONE', *, *, #37834, .T. ) ;
#37639=CARTESIAN_POINT ( 'NONE',  ( 4.380275065937200729, -27.47751031055269166, 7.757178535559531518 ) ) ;
#37640=VERTEX_POINT ( 'NONE', #2575 ) ;
#37642=CARTESIAN_POINT ( 'NONE',  ( 4.671426276349930795, -27.91676604085201063, 6.889465824494257262 ) ) ;
#37647=CARTESIAN_POINT ( 'NONE',  ( 4.313599969017027469, -31.74504722509605159, 7.635761828346577573 ) ) ;
#37650=AXIS2_PLACEMENT_3D ( 'NONE', #10806, #25872, #7732 ) ;
#37659=ORIENTED_EDGE ( 'NONE', *, *, #22165, .T. ) ;
#37668=CARTESIAN_POINT ( 'NONE',  ( -1.241387487007608925, -31.27463350997279790, 7.763628509615286610 ) ) ;
#37671=ORIENTED_EDGE ( 'NONE', *, *, #28966, .T. ) ;
#37675=AXIS2_PLACEMENT_3D ( 'NONE', #11055, #26921, #5305 ) ;
#37677=ORIENTED_EDGE ( 'NONE', *, *, #26429, .T. ) ;
#37684=CARTESIAN_POINT ( 'NONE',  ( 3.907593953511830254, -32.28622381979772626, 6.875671892026060661 ) ) ;
#37689=CARTESIAN_POINT ( 'NONE',  ( 2.865950163328865319, -26.37595621308645022, 7.769368695748489095 ) ) ;
#37690=ADVANCED_FACE ( 'NONE', ( #28477 ), #283, .F. ) ;
#37693=CARTESIAN_POINT ( 'NONE',  ( 3.963477911421234623, -32.23984282750152630, 7.750000000000001776 ) ) ;
#37701=CARTESIAN_POINT ( 'NONE',  ( -0.8614879664499306422, -31.96464424086259370, 7.139344958878412584 ) ) ;
#37704=CARTESIAN_POINT ( 'NONE',  ( -1.694464052375517671, -29.38293999636734810, 7.013842709614101167 ) ) ;
#37706=CARTESIAN_POINT ( 'NONE',  ( -1.376837950267322030, -31.23749498225474497, 6.863805608295729499 ) ) ;
#37710=DIRECTION ( 'NONE',  ( 1.000000000000000000, 2.973811673103098158E-15, 0.000000000000000000 ) ) ;
#37712=CARTESIAN_POINT ( 'NONE',  ( 5.660191562250180830, -26.39039255756133429, 7.013842709614101167 ) ) ;
#37716=CARTESIAN_POINT ( 'NONE',  ( 1.722902416880312426, -33.06986345199739930, 7.646866513072557048 ) ) ;
#37718=DIRECTION ( 'NONE',  ( -0.8660254037844415942, 0.4999999999999950040, -0.000000000000000000 ) ) ;
#37719=CARTESIAN_POINT ( 'NONE',  ( 1.665003373911284612, -26.17011430565816710, 7.680992449362118890 ) ) ;
#37723=CARTESIAN_POINT ( 'NONE',  ( -1.541386100576979556, -30.59505803358882403, 6.868387053540521592 ) ) ;
#37724=ORIENTED_EDGE ( 'NONE', *, *, #37534, .F. ) ;
#37727=CARTESIAN_POINT ( 'NONE',  ( 4.361462012329716309, -31.84340686930758935, 6.894806418505347700 ) ) ;
#37735=CARTESIAN_POINT ( 'NONE',  ( 5.030206442791328669, -28.49176951078394993, 6.867199677474202346 ) ) ;
#37736=CARTESIAN_POINT ( 'NONE',  ( 3.549351527779726734, -26.59817285589183200, 6.865482280155369210 ) ) ;
#37737=CARTESIAN_POINT ( 'NONE',  ( 5.025435985552490159, -30.27990892530747047, 7.754798119455333705 ) ) ;
#37741=VECTOR ( 'NONE', #14884, 1000.000000000000000 ) ;
#37743=CARTESIAN_POINT ( 'NONE',  ( 0.4696423075776997580, -26.29345953671220570, 7.698786668945011513 ) ) ;
#37744=ADVANCED_FACE ( 'NONE', ( #34076 ), #8915, .F. ) ;
#37755=B_SPLINE_CURVE_WITH_KNOTS ( 'NONE', 3,
 ( #20750, #36407, #23449, #8178 ),
 .UNSPECIFIED., .F., .F.,
 ( 4, 4 ),
 ( 0.000000000000000000, 6.391136169995200940E-06 ),
 .UNSPECIFIED. ) ;
#37763=AXIS2_PLACEMENT_3D ( 'NONE', #29132, #17154, #10775 ) ;
#37768=CARTESIAN_POINT ( 'NONE',  ( 3.772447927860530736, -32.26558897670516757, 6.868387053540522480 ) ) ;
#37773=DIRECTION ( 'NONE',  ( 0.9848077530122080203, 0.1736481776669307198, -0.000000000000000000 ) ) ;
#37780=EDGE_CURVE ( 'NONE', #25105, #20784, #7253, .T. ) ;
#37790=CARTESIAN_POINT ( 'NONE',  ( -1.765215435290630408, -33.48785941387868803, 7.013842709614101167 ) ) ;
#37791=ORIENTED_EDGE ( 'NONE', *, *, #28655, .T. ) ;
#37792=CARTESIAN_POINT ( 'NONE',  ( 3.964281165953357000, -26.91534161652651491, 7.781480525794718162 ) ) ;
#37793=AXIS2_PLACEMENT_3D ( 'NONE', #7003, #29036, #13372 ) ;
#37804=CARTESIAN_POINT ( 'NONE',  ( -0.03917690187701790977, -26.53924484835505382, 7.773839561854631874 ) ) ;
#37809=ORIENTED_EDGE ( 'NONE', *, *, #5344, .F. ) ;
#37812=CARTESIAN_POINT ( 'NONE',  ( -1.030057409390036538, -31.59592535501132460, 6.988553391373222290 ) ) ;
#37815=CARTESIAN_POINT ( 'NONE',  ( 5.011198270955363299, -30.34358980514384285, 7.013842709614101167 ) ) ;
#37826=CARTESIAN_POINT ( 'NONE',  ( 1.675697498098485116, -26.17001468787846719, 7.740055089680400791 ) ) ;
#37834=EDGE_CURVE ( 'NONE', #34419, #11926, #35126, .T. ) ;
#37836=VERTEX_POINT ( 'NONE', #37647 ) ;
#37839=CARTESIAN_POINT ( 'NONE',  ( 5.200346647029098435, -29.55249110255828882, 7.749999999999999112 ) ) ;
#37841=CARTESIAN_POINT ( 'NONE',  ( -1.647457617777850825, -28.97670534922106000, 7.769368695748486431 ) ) ;
#37842=ORIENTED_EDGE ( 'NONE', *, *, #29482, .T. ) ;
#37855=( BOUNDED_CURVE ( )  B_SPLINE_CURVE ( 3, ( #10576, #9774, #19854, #29327 ),
 .UNSPECIFIED., .F., .T. ) 
 B_SPLINE_CURVE_WITH_KNOTS ( ( 4, 4 ),
 ( 1.347909859412852684, 1.534781240595297414 ),
 .UNSPECIFIED. ) 
 CURVE ( )  GEOMETRIC_REPRESENTATION_ITEM ( )  RATIONAL_B_SPLINE_CURVE ( ( 1.000000000000000000, 0.9970920404276226723, 0.9970920404276226723, 1.000000000000000000 ) ) 
 REPRESENTATION_ITEM ( '' )  );
#37856=CARTESIAN_POINT ( 'NONE',  ( 3.342564306745924974, -32.66067906797238152, 7.753200566781577763 ) ) ;
#37867=CARTESIAN_POINT ( 'NONE',  ( 3.487362763175719138, -26.57752209578763569, 7.785344483711591934 ) ) ;
#37871=ORIENTED_EDGE ( 'NONE', *, *, #37834, .F. ) ;
#37875=CARTESIAN_POINT ( 'NONE',  ( 5.140392049853408807, -28.99927055885797600, 7.783750581861601070 ) ) ;
#37876=LINE ( 'NONE', #645, #2965 ) ;
#37880=CARTESIAN_POINT ( 'NONE',  ( -1.296490702453536592, -31.17578218382766408, 7.768425012602592439 ) ) ;
#37886=DIRECTION ( 'NONE',  ( -0.000000000000000000, -0.000000000000000000, -1.000000000000000000 ) ) ;
#37894=AXIS2_PLACEMENT_3D ( 'NONE', #34102, #9149, #38316 ) ;
#37898=ORIENTED_EDGE ( 'NONE', *, *, #15940, .F. ) ;
#37902=CARTESIAN_POINT ( 'NONE',  ( -1.752498985642892304, -28.99760421947164701, 7.695279973900954751 ) ) ;
#37904=VERTEX_POINT ( 'NONE', #37451 ) ;
#37906=CARTESIAN_POINT ( 'NONE',  ( 2.343537225896454856, -33.01033157941493101, 7.686927408461905031 ) ) ;
#37907=CARTESIAN_POINT ( 'NONE',  ( 5.566493729709874216, -33.07902254873519610, 6.954324564059724878 ) ) ;
#37916=CARTESIAN_POINT ( 'NONE',  ( 4.254245903155988273, -31.96321675751186220, 6.941203072598475465 ) ) ;
#37920=CARTESIAN_POINT ( 'NONE',  ( -1.371934420958921486, -31.24648083264167298, 6.865554069792297653 ) ) ;
#37921=AXIS2_PLACEMENT_3D ( 'NONE', #30573, #32301, #36734 ) ;
#37922=CARTESIAN_POINT ( 'NONE',  ( -1.796521113867400654, -29.56993018341788826, 7.767301406056523305 ) ) ;
#37925=ORIENTED_EDGE ( 'NONE', *, *, #26045, .F. ) ;
#37926=CARTESIAN_POINT ( 'NONE',  ( -0.6300129605891890971, -32.04565666399172841, 6.903372536218456368 ) ) ;
#37930=FACE_OUTER_BOUND ( 'NONE', #17827, .T. ) ;
#37932=CARTESIAN_POINT ( 'NONE',  ( 3.431434570054124222, -32.49627346798381211, 7.695279973900954751 ) ) ;
#37935=LINE ( 'NONE', #22323, #4657 ) ;
#37936=EDGE_CURVE ( 'NONE', #4035, #13762, #36065, .T. ) ;
#37938=ORIENTED_EDGE ( 'NONE', *, *, #14619, .T. ) ;
#37943=CARTESIAN_POINT ( 'NONE',  ( 5.640181823254226678, -32.92274630468555330, 7.695279973900954751 ) ) ;
#37954=DIRECTION ( 'NONE',  ( -0.000000000000000000, -0.000000000000000000, -1.000000000000000000 ) ) ;
#37958=CARTESIAN_POINT ( 'NONE',  ( -1.482099749853996951, -30.76649125703855958, 7.692469944509198854 ) ) ;
#37962=ORIENTED_EDGE ( 'NONE', *, *, #14885, .T. ) ;
#37966=DIRECTION ( 'NONE',  ( -0.7055275666422136105, -0.2567910337120335451, -0.6605219282605402364 ) ) ;
#37972=CARTESIAN_POINT ( 'NONE',  ( 0.6198671074021896432, -26.24097615965804664, 7.753200566781576875 ) ) ;
#37974=CARTESIAN_POINT ( 'NONE',  ( 1.732569342880620367, -32.96977789996720531, 7.721096864323902409 ) ) ;
#37975=CARTESIAN_POINT ( 'NONE',  ( 3.419158195859357097, -26.52102280379090971, 7.697032948437506406 ) ) ;
#37977=CARTESIAN_POINT ( 'NONE',  ( -1.560093393064529321, -30.53390888824981531, 6.939395833800445779 ) ) ;
#37978=DIRECTION ( 'NONE',  ( 0.000000000000000000, 0.000000000000000000, -1.000000000000000000 ) ) ;
#37981=CARTESIAN_POINT ( 'NONE',  ( 5.195328097890849151, -29.75810123217307890, 6.980586498568961851 ) ) ;
#37982=CARTESIAN_POINT ( 'NONE',  ( 2.343537225896455745, -33.01033157941493101, 7.695279973900954751 ) ) ;
#37984=CIRCLE ( 'NONE', #10391, 3.499999999999999556 ) ;
#37986=CARTESIAN_POINT ( 'NONE',  ( -2.508659216904252975, -30.29838823369475520, 7.635761828346577573 ) ) ;
#37991=ORIENTED_EDGE ( 'NONE', *, *, #2825, .T. ) ;
#37993=LINE ( 'NONE', #9795, #24710 ) ;
#37997=ORIENTED_EDGE ( 'NONE', *, *, #32057, .T. ) ;
#38008=CARTESIAN_POINT ( 'NONE',  ( -1.697659286293943692, -29.45477631113573480, 7.761597726988852308 ) ) ;
#38012=EDGE_LOOP ( 'NONE', ( #30385, #20304, #18729, #28751 ) ) ;
#38014=CARTESIAN_POINT ( 'NONE',  ( 0.9853232624859283861, -32.99610581046875524, 6.864673517077424236 ) ) ;
#38021=EDGE_CURVE ( 'NONE', #20380, #18803, #14756, .T. ) ;
#38022=ORIENTED_EDGE ( 'NONE', *, *, #37226, .T. ) ;
#38023=CARTESIAN_POINT ( 'NONE',  ( -0.9401865930518452652, -31.71174127773586449, 6.887041543973311697 ) ) ;
#38026=CYLINDRICAL_SURFACE ( 'NONE', #34722, 3.499999999999999556 ) ;
#38031=EDGE_LOOP ( 'NONE', ( #1603, #34247, #15383, #35258, #15204 ) ) ;
#38033=CARTESIAN_POINT ( 'NONE',  ( -0.8954611659357714082, -31.76573441880953297, 7.635761828346577573 ) ) ;
#38037=CARTESIAN_POINT ( 'NONE',  ( -1.676686771118219177, -28.62493188826283941, 7.501983001166816933 ) ) ;
#38041=VERTEX_POINT ( 'NONE', #25070 ) ;
#38043=B_SPLINE_CURVE_WITH_KNOTS ( 'NONE', 3,
 ( #19414, #21899, #31172, #40616, #3400, #37719, #9322, #3792, #3594, #34477 ),
 .UNSPECIFIED., .F., .F.,
 ( 4, 3, 3, 4 ),
 ( 2.168404344971008868E-19, 3.025570593003157737E-05, 6.051145698344088600E-05, 6.468151674593620168E-05 ),
 .UNSPECIFIED. ) ;
#38049=CARTESIAN_POINT ( 'NONE',  ( -0.9006701161811203615, -27.22837715677322379, 7.754798119455333705 ) ) ;
#38052=CARTESIAN_POINT ( 'NONE',  ( -1.636944644631000756, -28.92016341951145719, 7.785172627573962778 ) ) ;
#38064=CARTESIAN_POINT ( 'NONE',  ( 4.744203891191327571, -28.05493923841747161, 6.959317978105162616 ) ) ;
#38065=CARTESIAN_POINT ( 'NONE',  ( 4.537656249502012962, -31.44341042241281059, 6.920489980334477487 ) ) ;
#38067=CARTESIAN_POINT ( 'NONE',  ( 3.423404917024849059, -32.61643964784510530, 6.894806418505347700 ) ) ;
#38068=CARTESIAN_POINT ( 'NONE',  ( 0.6079532840439894059, -26.24751273171437660, 7.766640943994647550 ) ) ;
#38080=VERTEX_POINT ( 'NONE', #21987 ) ;
#38081=CARTESIAN_POINT ( 'NONE',  ( 0.5091161720689987291, -32.75440289402452265, 7.782167645815905033 ) ) ;
#38084=CARTESIAN_POINT ( 'NONE',  ( 5.061235702123782154, -30.12945902767138406, 7.257242401810555243 ) ) ;
#38093=CARTESIAN_POINT ( 'NONE',  ( 1.632755592654337118, -33.05534186026571319, 7.784725160561909441 ) ) ;
#38094=VERTEX_POINT ( 'NONE', #9400 ) ;
#38097=ORIENTED_EDGE ( 'NONE', *, *, #32287, .T. ) ;
#38098=CARTESIAN_POINT ( 'NONE',  ( 5.928245814084836418, -30.19173177851781276, 7.754798119455333705 ) ) ;
#38099=DIRECTION ( 'NONE',  ( 0.000000000000000000, 0.6662082868431841165, -0.7457657263118691038 ) ) ;
#38101=( BOUNDED_CURVE ( )  B_SPLINE_CURVE ( 3, ( #19492, #16387, #13295, #34251 ),
 .UNSPECIFIED., .F., .T. ) 
 B_SPLINE_CURVE_WITH_KNOTS ( ( 4, 4 ),
 ( 1.381924640371167579, 1.396263401595456699 ),
 .UNSPECIFIED. ) 
 CURVE ( )  GEOMETRIC_REPRESENTATION_ITEM ( )  RATIONAL_B_SPLINE_CURVE ( ( 1.000000000000000000, 0.9999828667339337729, 0.9999828667339337729, 1.000000000000000000 ) ) 
 REPRESENTATION_ITEM ( '' )  );
#38112=CARTESIAN_POINT ( 'NONE',  ( -1.610418084489225299, -28.79627056164295595, 7.013842709614101167 ) ) ;
#38117=ORIENTED_EDGE ( 'NONE', *, *, #31284, .T. ) ;
#38118=EDGE_CURVE ( 'NONE', #37042, #1511, #34768, .T. ) ;
#38119=CARTESIAN_POINT ( 'NONE',  ( 1.816638696304109235, -26.07269691363555708, 7.761113333117549473 ) ) ;
#38120=EDGE_CURVE ( 'NONE', #30519, #24028, #12701, .T. ) ;
#38123=CARTESIAN_POINT ( 'NONE',  ( -0.9720661970843325062, -31.83001367219261013, 7.635761828346575797 ) ) ;
#38126=CARTESIAN_POINT ( 'NONE',  ( -1.699425784502139880, -29.60531690271519523, 7.680992449362115337 ) ) ;
#38127=CARTESIAN_POINT ( 'NONE',  ( 3.579383117828557559, -26.73631314339753473, 6.949473656533216470 ) ) ;
#38129=CARTESIAN_POINT ( 'NONE',  ( 2.829405163535267942, -26.36285597610873310, 7.695279973900954751 ) ) ;
#38132=CYLINDRICAL_SURFACE ( 'NONE', #29512, 3.399999999999999911 ) ;
#38135=CARTESIAN_POINT ( 'NONE',  ( 1.736346942945644400, -33.06974547922812491, 7.685194954629195330 ) ) ;
#38136=CARTESIAN_POINT ( 'NONE',  ( 1.735776812554923332, -32.96974606112863171, 7.680992449362117114 ) ) ;
#38137=CARTESIAN_POINT ( 'NONE',  ( 2.093592994196940449, -32.94711934045682966, 6.997764925645183709 ) ) ;
#38139=CARTESIAN_POINT ( 'NONE',  ( -1.506684114051581869, -28.44091511309124343, 7.703977250142847844 ) ) ;
#38142=FACE_OUTER_BOUND ( 'NONE', #10509, .T. ) ;
#38144=VERTEX_POINT ( 'NONE', #5718 ) ;
#38145=DIRECTION ( 'NONE',  ( -0.000000000000000000, -0.000000000000000000, -1.000000000000000000 ) ) ;
#38146=CARTESIAN_POINT ( 'NONE',  ( -1.594457770366995319, -28.38926191680453925, 7.750000000000000888 ) ) ;
#38148=CARTESIAN_POINT ( 'NONE',  ( -0.7800240848564992113, -27.24451720821412337, 7.013842709614101167 ) ) ;
#38149=PRODUCT_DEFINITION ( 'UNKNOWN', '', #33396, #23806 ) ;
#38159=CARTESIAN_POINT ( 'NONE',  ( -1.003704078136529176, -27.34779726144116552, 7.698786668945016842 ) ) ;
#38164=ADVANCED_FACE ( 'NONE', ( #6335 ), #12500, .T. ) ;
#38165=CARTESIAN_POINT ( 'NONE',  ( -1.625693567409081108, -30.65681645307677883, 7.761113333117553914 ) ) ;
#38166=B_SPLINE_CURVE_WITH_KNOTS ( 'NONE', 3,
 ( #7632, #7231, #19792, #13609, #26181, #29465, #32365, #19390, #7426, #1276 ),
 .UNSPECIFIED., .F., .F.,
 ( 4, 3, 3, 4 ),
 ( 0.0002170292169044772744, 0.0002420761345915938153, 0.0002723302478206962997, 0.0002816811360866765842 ),
 .UNSPECIFIED. ) ;
#38168=ORIENTED_EDGE ( 'NONE', *, *, #14569, .T. ) ;
#38174=ORIENTED_EDGE ( 'NONE', *, *, #27849, .T. ) ;
#38175=CARTESIAN_POINT ( 'NONE',  ( -0.04847345716399687615, -32.59792774950750527, 7.767720160662273443 ) ) ;
#38179=CARTESIAN_POINT ( 'NONE',  ( 3.725780183617367403, -32.30082791660831987, 6.920489980334481039 ) ) ;
#38181=CARTESIAN_POINT ( 'NONE',  ( 5.199813315060819896, -29.63410109264166081, 6.870737987065016483 ) ) ;
#38188=CARTESIAN_POINT ( 'NONE',  ( 5.030284764849001000, -28.49206123220129783, 7.750000000000000888 ) ) ;
#38192=EDGE_CURVE ( 'NONE', #24834, #14785, #5647, .T. ) ;
#38193=CARTESIAN_POINT ( 'NONE',  ( -0.1977194167126442581, -34.26956452006460552, 6.954324564059724878 ) ) ;
#38195=VECTOR ( 'NONE', #14669, 1000.000000000000000 ) ;
#38197=VERTEX_POINT ( 'NONE', #31255 ) ;
#38205=CARTESIAN_POINT ( 'NONE',  ( 5.043330201822981529, -28.53322799357174588, 7.013842709614101167 ) ) ;
#38208=ORIENTED_EDGE ( 'NONE', *, *, #5549, .T. ) ;
#38214=CARTESIAN_POINT ( 'NONE',  ( 2.875937710231030398, -32.76024173560432473, 7.635761828346577573 ) ) ;
#38220=CARTESIAN_POINT ( 'NONE',  ( -1.024433710227528715, -31.60349360017290010, 7.006423389747791219 ) ) ;
#38224=DIRECTION ( 'NONE',  ( 0.5751513419797864568, 0.4826092789263677907, -0.6605219282605402364 ) ) ;
#38228=CARTESIAN_POINT ( 'NONE',  ( -0.5662622401650002635, -26.90303891564647643, 7.743886751744256003 ) ) ;
#38232=ORIENTED_EDGE ( 'NONE', *, *, #20166, .F. ) ;
#38233=CARTESIAN_POINT ( 'NONE',  ( 1.780896029553550974, -26.17087081469721710, 7.782034975670476307 ) ) ;
#38234=CARTESIAN_POINT ( 'NONE',  ( -0.3205960974507152672, -26.83577306605956281, 6.969307238440506147 ) ) ;
#38235=CARTESIAN_POINT ( 'NONE',  ( 4.655111535418318347, -27.88775428304872861, 7.779495906702015517 ) ) ;
#38240=CARTESIAN_POINT ( 'NONE',  ( 4.224974933773748553, -31.84731275619759927, 7.754798119455333705 ) ) ;
#38244=CARTESIAN_POINT ( 'NONE',  ( -0.4167251375549447245, -26.78284871713423954, 6.895394898881664680 ) ) ;
#38247=VERTEX_POINT ( 'NONE', #18237 ) ;
#38261=CARTESIAN_POINT ( 'NONE',  ( 4.685711905533233690, -27.94270749518966568, 6.870716933885665512 ) ) ;
#38275=CARTESIAN_POINT ( 'NONE',  ( 4.044183932535696080, -26.97057787552901331, 7.751599049952198506 ) ) ;
#38288=CARTESIAN_POINT ( 'NONE',  ( 1.713892699967726196, -25.86893018339335271, 7.635761828346577573 ) ) ;
#38293=CARTESIAN_POINT ( 'NONE',  ( -1.555370887017037518, -28.56597033754369619, 7.139196562012273262 ) ) ;
#38299=CARTESIAN_POINT ( 'NONE',  ( 4.929393269055085902, -28.50520041390408110, 6.864651958020304257 ) ) ;
#38306=CYLINDRICAL_SURFACE ( 'NONE', #5781, 0.09010775117052928496 ) ;
#38307=CARTESIAN_POINT ( 'NONE',  ( 2.891664014397211435, -26.38545747276229037, 7.782167645815905921 ) ) ;
#38316=DIRECTION ( 'NONE',  ( -0.6427876096865502431, -0.7660444431189689096, 0.000000000000000000 ) ) ;
#38321=CARTESIAN_POINT ( 'NONE',  ( 2.320588003725592152, -26.22697422319578919, 7.782167645815905033 ) ) ;
#38322=CARTESIAN_POINT ( 'NONE',  ( 3.565367263018084376, -26.72706101894873854, 7.006423389747789443 ) ) ;
#38324=DIRECTION ( 'NONE',  ( 0.2567910337120318243, -0.7055275666422164971, 0.6605219282605376829 ) ) ;
#38328=CARTESIAN_POINT ( 'NONE',  ( -0.8958908980039607117, -31.76523428969960960, 7.756377446753169203 ) ) ;
#38329=CARTESIAN_POINT ( 'NONE',  ( 3.405093419812497135, -32.51170776363409232, 7.763628509615287498 ) ) ;
#38330=CARTESIAN_POINT ( 'NONE',  ( 2.088980497471658371, -32.94765204068701081, 6.920489980334479263 ) ) ;
#38331=EDGE_CURVE ( 'NONE', #22060, #21747, #8510, .T. ) ;
#38333=CARTESIAN_POINT ( 'NONE',  ( -1.459351274368037465, -28.31449385892586079, 7.774064877406528851 ) ) ;
#38334=ADVANCED_FACE ( 'NONE', ( #37388 ), #19477, .F. ) ;
#38336=ORIENTED_EDGE ( 'NONE', *, *, #39830, .F. ) ;
#38337=( BOUNDED_CURVE ( )  B_SPLINE_CURVE ( 3, ( #10957, #38558, #14053, #29114 ),
 .UNSPECIFIED., .F., .T. ) 
 B_SPLINE_CURVE_WITH_KNOTS ( ( 4, 4 ),
 ( 4.708531083176466403, 4.895802057644187855 ),
 .UNSPECIFIED. ) 
 CURVE ( )  GEOMETRIC_REPRESENTATION_ITEM ( )  RATIONAL_B_SPLINE_CURVE ( ( 1.000000000000000000, 0.9970795998553221295, 0.9970795998553221295, 1.000000000000000000 ) ) 
 REPRESENTATION_ITEM ( '' )  );
#38343=CARTESIAN_POINT ( 'NONE',  ( -2.707143391484601924, -27.16588715693004730, 7.754798119455333705 ) ) ;
#38347=CARTESIAN_POINT ( 'NONE',  ( 0.4868412872024892035, -26.28704995000200029, 7.640616322432099317 ) ) ;
#38348=CARTESIAN_POINT ( 'NONE',  ( -1.468618840926277036, -28.33807089344026764, 6.874555630061441214 ) ) ;
#38351=EDGE_LOOP ( 'NONE', ( #30886, #25194, #19101, #1993, #8775 ) ) ;
#38357=ORIENTED_EDGE ( 'NONE', *, *, #22298, .F. ) ;
#38367=CARTESIAN_POINT ( 'NONE',  ( 4.336009428051142756, -27.42202173051807890, 6.894806418505345924 ) ) ;
#38368=ORIENTED_EDGE ( 'NONE', *, *, #6940, .T. ) ;
#38372=CARTESIAN_POINT ( 'NONE',  ( -0.9900718542488416984, -31.79106902588718597, 7.781480525794717273 ) ) ;
#38375=CARTESIAN_POINT ( 'NONE',  ( 3.738435213701987614, -32.29140130045581714, 6.895222827070023541 ) ) ;
#38377=CARTESIAN_POINT ( 'NONE',  ( -2.227706725756020578, -32.93668375692303130, 7.695279973900954751 ) ) ;
#38386=ORIENTED_EDGE ( 'NONE', *, *, #1916, .T. ) ;
#38394=CARTESIAN_POINT ( 'NONE',  ( -0.6250228819461873808, -32.05034436148299193, 7.013842709614101167 ) ) ;
#38398=CARTESIAN_POINT ( 'NONE',  ( 2.221308981034764152, -32.92980290402432786, 7.784476445165072533 ) ) ;
#38403=EDGE_LOOP ( 'NONE', ( #27907, #24082, #1517, #36006 ) ) ;
#38408=VERTEX_POINT ( 'NONE', #39402 ) ;
#38409=ORIENTED_EDGE ( 'NONE', *, *, #29195, .F. ) ;
#38411=CIRCLE ( 'NONE', #7503, 3.499999999999999556 ) ;
#38413=CARTESIAN_POINT ( 'NONE',  ( 0.9047207686989762188, -32.97828907382665165, 6.945385021654666424 ) ) ;
#38418=CARTESIAN_POINT ( 'NONE',  ( 5.200346560046187783, -29.55237849334843503, 7.640616322432100205 ) ) ;
#38419=CARTESIAN_POINT ( 'NONE',  ( -1.027896628602648299, -31.59884209547612954, 6.911401339314958037 ) ) ;
#38422=DIRECTION ( 'NONE',  ( 0.6834397476448822450, 0.000000000000000000, 0.7300069255418744074 ) ) ;
#38423=CARTESIAN_POINT ( 'NONE',  ( 1.700390093233090871, -29.56993018339339940, 7.800000000000000711 ) ) ;
#38430=CARTESIAN_POINT ( 'NONE',  ( -0.3434165924072999365, -26.85277739775768779, 6.887945620086119547 ) ) ;
#38431=CARTESIAN_POINT ( 'NONE',  ( 4.664684489921304689, -27.90468147679489164, 7.784838882742139532 ) ) ;
#38436=CARTESIAN_POINT ( 'NONE',  ( -0.4545477510665002496, -26.81228124332190532, 7.754798119455333705 ) ) ;
#38440=ORIENTED_EDGE ( 'NONE', *, *, #6540, .T. ) ;
#38442=CARTESIAN_POINT ( 'NONE',  ( 4.818630077464289840, -30.92514033129047490, 6.979335674598001305 ) ) ;
#38447=ORIENTED_EDGE ( 'NONE', *, *, #30165, .F. ) ;
#38455=ORIENTED_EDGE ( 'NONE', *, *, #28206, .F. ) ;
#38466=ORIENTED_EDGE ( 'NONE', *, *, #22423, .T. ) ;
#38470=CARTESIAN_POINT ( 'NONE',  ( 1.111671518581322848, -33.02006264939198132, 7.747520101777646495 ) ) ;
#38473=VERTEX_POINT ( 'NONE', #32649 ) ;
#38474=VECTOR ( 'NONE', #24215, 1000.000000000000000 ) ;
#38475=CARTESIAN_POINT ( 'NONE',  ( 0.4368679818768612111, -32.72644202797246749, 7.768425012602594215 ) ) ;
#38477=CARTESIAN_POINT ( 'NONE',  ( 5.885943586549580608, -28.70822073431874344, 7.754798119455333705 ) ) ;
#38481=CARTESIAN_POINT ( 'NONE',  ( 0.5712820523693047381, -32.77697165990360162, 7.691066658568947112 ) ) ;
#38484=VERTEX_POINT ( 'NONE', #11392 ) ;
#38485=CARTESIAN_POINT ( 'NONE',  ( 3.858641814960187766, -26.94277397789914730, 7.680992449362115337 ) ) ;
#38486=CARTESIAN_POINT ( 'NONE',  ( 3.431349736501141390, -32.49632364862963385, 7.691066658568946224 ) ) ;
#38490=ORIENTED_EDGE ( 'NONE', *, *, #9203, .F. ) ;
#38493=CARTESIAN_POINT ( 'NONE',  ( 3.015109609237833332, -26.32624206733842698, 7.750000000000000888 ) ) ;
#38501=CARTESIAN_POINT ( 'NONE',  ( 3.802745552976189991, -32.36816203956407634, 6.980586498568969844 ) ) ;
#38506=EDGE_CURVE ( 'NONE', #19029, #30413, #11595, .T. ) ;
#38507=CARTESIAN_POINT ( 'NONE',  ( -1.233968097352797555, -31.28736617508928575, 7.643333865083958401 ) ) ;
#38511=CARTESIAN_POINT ( 'NONE',  ( 4.448805861693501562, -27.40704168211281910, 7.766640943994347346 ) ) ;
#38515=CARTESIAN_POINT ( 'NONE',  ( 4.337561542305367723, -27.42392627274044514, 6.892063359921933419 ) ) ;
#38516=CARTESIAN_POINT ( 'NONE',  ( 1.768024593811872380, -26.08451850652108206, 7.784725160561909441 ) ) ;
#38519=CARTESIAN_POINT ( 'NONE',  ( -0.1886652755034646245, -32.51637180025015539, 6.887547729233694405 ) ) ;
#38521=EDGE_CURVE ( 'NONE', #28243, #614, #29708, .T. ) ;
#38523=CARTESIAN_POINT ( 'NONE',  ( -1.699484971103116582, -29.59922004846627885, 7.730758795053803922 ) ) ;
#38529=CARTESIAN_POINT ( 'NONE',  ( -1.461284153450459922, -28.05286529242975035, 7.501983001166816933 ) ) ;
#38531=CARTESIAN_POINT ( 'NONE',  ( 1.115330424693315559, -32.91922472814544420, 7.763628509615286610 ) ) ;
#38532=CARTESIAN_POINT ( 'NONE',  ( -0.6250228819461873808, -32.05034436148299193, 7.013842709614101167 ) ) ;
#38533=FACE_OUTER_BOUND ( 'NONE', #1503, .T. ) ;
#38534=CARTESIAN_POINT ( 'NONE',  ( 2.177802833585739339, -32.93624524222983752, 6.864276522220859711 ) ) ;
#38536=DIRECTION ( 'NONE',  ( 0.7541618601367590102, 0.000000000000000000, 0.6566885781822794366 ) ) ;
#38538=EDGE_LOOP ( 'NONE', ( #20936, #36243, #14445, #30894, #34979 ) ) ;
#38540=CARTESIAN_POINT ( 'NONE',  ( -1.237321756456247979, -31.28161037787917209, 7.635761828346577573 ) ) ;
#38543=ORIENTED_EDGE ( 'NONE', *, *, #35033, .F. ) ;
#38545=CARTESIAN_POINT ( 'NONE',  ( -1.600658481268679267, -28.40671124064021669, 7.695279973900954751 ) ) ;
#38548=CARTESIAN_POINT ( 'NONE',  ( 1.149416566283971264, -26.21485601168476265, 7.784838882742139532 ) ) ;
#38550=EDGE_LOOP ( 'NONE', ( #471, #25311, #39439, #19036 ) ) ;
#38552=CARTESIAN_POINT ( 'NONE',  ( -1.740577464315611778, -30.21005312756170014, 7.720710062488897130 ) ) ;
#38554=CARTESIAN_POINT ( 'NONE',  ( 0.4825641552805304269, -26.28863138271496069, 7.743886751744252450 ) ) ;
#38558=CARTESIAN_POINT ( 'NONE',  ( 5.060299201773582389, -28.56549731252922442, 7.387053503561886281 ) ) ;
#38564=EDGE_CURVE ( 'NONE', #12896, #35515, #19597, .T. ) ;
#38566=DIRECTION ( 'NONE',  ( -0.6427876096865430267, 0.7660444431189749048, -0.000000000000000000 ) ) ;
#38575=EDGE_CURVE ( 'NONE', #37640, #10191, #38799, .T. ) ;
#38579=CARTESIAN_POINT ( 'NONE',  ( 3.364053381479577443, -33.98248085747043490, 7.695279973900954751 ) ) ;
#38581=CARTESIAN_POINT ( 'NONE',  ( 5.108578917255564456, -30.36632773413393593, 6.961115707816237119 ) ) ;
#38582=CARTESIAN_POINT ( 'NONE',  ( 5.198488150005315944, -29.68529909257772204, 6.865482280155367434 ) ) ;
#38583=CARTESIAN_POINT ( 'NONE',  ( 5.012114302463782423, -30.72325263940121332, 7.255881584735163869 ) ) ;
#38590=CARTESIAN_POINT ( 'NONE',  ( 2.262617859748651483, -33.02448960739329920, 6.880608371227950215 ) ) ;
#38592=ORIENTED_EDGE ( 'NONE', *, *, #21724, .T. ) ;
#38594=CIRCLE ( 'NONE', #23503, 3.499999999999999556 ) ;
#38598=CARTESIAN_POINT ( 'NONE',  ( -1.423139387634945630, -28.22694525714970837, 7.006423389747790331 ) ) ;
#38602=CARTESIAN_POINT ( 'NONE',  ( 3.011115207906999380, -26.32487479661073948, 7.754798119455333705 ) ) ;
#38618=VECTOR ( 'NONE', #32831, 1000.000000000000227 ) ;
#38619=DIRECTION ( 'NONE',  ( 1.000000000000000000, 0.000000000000000000, 0.000000000000000000 ) ) ;
#38624=EDGE_CURVE ( 'NONE', #14639, #26823, #36838, .T. ) ;
#38625=EDGE_CURVE ( 'NONE', #23856, #38408, #22134, .T. ) ;
#38626=CARTESIAN_POINT ( 'NONE',  ( 1.826415646469069731, -26.07219983930859897, 7.750000000000000888 ) ) ;
#38627=CARTESIAN_POINT ( 'NONE',  ( -0.5359795030213230227, -32.26226207767182785, 7.750000000000001776 ) ) ;
#38630=DIRECTION ( 'NONE',  ( -0.000000000000000000, -0.000000000000000000, -1.000000000000000000 ) ) ;
#38635=CARTESIAN_POINT ( 'NONE',  ( -1.578505209958239064, -30.79420367845479234, 7.730015791551944737 ) ) ;
#38636=CARTESIAN_POINT ( 'NONE',  ( 3.922483456672744673, -26.86580350659783178, 7.695279973900954751 ) ) ;
#38638=CARTESIAN_POINT ( 'NONE',  ( -0.4045127432807891776, -26.89981875494305896, 6.864651958020304257 ) ) ;
#38639=CARTESIAN_POINT ( 'NONE',  ( 4.884195952716768652, -28.37687517664920023, 7.721096864323903297 ) ) ;
#38640=CARTESIAN_POINT ( 'NONE',  ( -1.654432145176447877, -28.54863573104451291, 7.139344958878412584 ) ) ;
#38645=CARTESIAN_POINT ( 'NONE',  ( 4.821622712055471105, -30.91823983726953529, 6.911401339314952708 ) ) ;
#38646=CARTESIAN_POINT ( 'NONE',  ( -1.231427077925708824, -27.65826548145907893, 6.931070083220557621 ) ) ;
#38648=B_SPLINE_CURVE_WITH_KNOTS ( 'NONE', 3,
 ( #10350, #35489, #38943, #35689, #7865, #19824, #26608, #23120, #16919, #17118 ),
 .UNSPECIFIED., .F., .F.,
 ( 4, 3, 3, 4 ),
 ( 0.0002170292169044793886, 0.0002420761345915981521, 0.0002723302478207042686, 0.0002816811360866789153 ),
 .UNSPECIFIED. ) ;
#38651=CARTESIAN_POINT ( 'NONE',  ( 4.976842733950423536, -28.33913446795707358, 7.695279973900954751 ) ) ;
#38653=CARTESIAN_POINT ( 'NONE',  ( -89.20959394718985891, -30.27593629695115496, 6.954324564059724878 ) ) ;
#38661=VECTOR ( 'NONE', #11565, 1000.000000000000114 ) ;
#38662=CARTESIAN_POINT ( 'NONE',  ( 4.617590328857891002, -31.31634092226461163, 6.889465824494259927 ) ) ;
#38667=ORIENTED_EDGE ( 'NONE', *, *, #12594, .F. ) ;
#38669=VERTEX_POINT ( 'NONE', #14041 ) ;
#38683=CARTESIAN_POINT ( 'NONE',  ( 5.078860115546572018, -29.18790842463809199, 6.949473656533217358 ) ) ;
#38688=CARTESIAN_POINT ( 'NONE',  ( 4.077110055691020918, -27.00064969655394620, 7.013842709614101167 ) ) ;
#38695=( BOUNDED_CURVE ( )  B_SPLINE_CURVE ( 3, ( #8286, #8083, #26446, #1740 ),
 .UNSPECIFIED., .F., .T. ) 
 B_SPLINE_CURVE_WITH_KNOTS ( ( 4, 4 ),
 ( 1.347909859412853795, 1.396263401595456477 ),
 .UNSPECIFIED. ) 
 CURVE ( )  GEOMETRIC_REPRESENTATION_ITEM ( )  RATIONAL_B_SPLINE_CURVE ( ( 1.000000000000000000, 0.9998051707368829089, 0.9998051707368829089, 1.000000000000000000 ) ) 
 REPRESENTATION_ITEM ( '' )  );
#38696=CARTESIAN_POINT ( 'NONE',  ( -1.648992718206064190, -30.58562869017961816, 6.971170733404099096 ) ) ;
#38697=EDGE_CURVE ( 'NONE', #31392, #11306, #29489, .T. ) ;
#38701=ORIENTED_EDGE ( 'NONE', *, *, #18864, .F. ) ;
#38704=VERTEX_POINT ( 'NONE', #26816 ) ;
#38706=CARTESIAN_POINT ( 'NONE',  ( 3.876975877821416283, -32.31083862995539135, 6.863805608295730387 ) ) ;
#38715=CARTESIAN_POINT ( 'NONE',  ( 2.477620004848760882, -26.15731123158247939, 6.898188844117810525 ) ) ;
#38719=CARTESIAN_POINT ( 'NONE',  ( -2.259411375784011078, -32.74946780922542899, 7.013842709614101167 ) ) ;
#38723=CARTESIAN_POINT ( 'NONE',  ( 1.666174409104983711, -26.07009584004536862, 7.674970859709602244 ) ) ;
#38724=B_SPLINE_CURVE_WITH_KNOTS ( 'NONE', 3,
 ( #13702, #4640, #17173, #26268, #38803, #10196, #22781, #23172, #29742, #35739 ),
 .UNSPECIFIED., .F., .F.,
 ( 4, 3, 3, 4 ),
 ( 0.0001585009270395723623, 0.0001815657551981830558, 0.0002118214035944115297, 0.0002170292169044746994 ),
 .UNSPECIFIED. ) ;
#38728=CARTESIAN_POINT ( 'NONE',  ( 2.293614927405436266, -26.22208247238246059, 7.769368695748487319 ) ) ;
#38729=CARTESIAN_POINT ( 'NONE',  ( -2.503969810797764151, -28.81487718949574983, 7.635761828346577573 ) ) ;
#38730=CYLINDRICAL_SURFACE ( 'NONE', #12356, 3.399999999999999911 ) ;
#38731=CARTESIAN_POINT ( 'NONE',  ( 0.6752622430376749030, -26.32815398958332409, 6.868387053540520704 ) ) ;
#38734=LINE ( 'NONE', #32388, #20684 ) ;
#38735=CARTESIAN_POINT ( 'NONE',  ( 4.715819433959782536, -31.34677736058242559, 6.894806418505347700 ) ) ;
#38742=CARTESIAN_POINT ( 'NONE',  ( 6.126843302897349020, -31.19539656904077418, 7.635761828346577573 ) ) ;
#38746=DIRECTION ( 'NONE',  ( -0.2567910337120223874, -0.7055275666422197167, 0.6605219282605379050 ) ) ;
#38749=ORIENTED_EDGE ( 'NONE', *, *, #21406, .F. ) ;
#38754=CARTESIAN_POINT ( 'NONE',  ( 0.9044146924870181126, -32.87544423742601651, 6.959317978105164393 ) ) ;
#38757=CARTESIAN_POINT ( 'NONE',  ( 0.3289290232599537123, -32.79003885831642862, 6.984548363133216142 ) ) ;
#38759=ORIENTED_EDGE ( 'NONE', *, *, #40073, .T. ) ;
#38762=CARTESIAN_POINT ( 'NONE',  ( -1.740020712282138948, -30.21302698773406803, 7.698786668945015954 ) ) ;
#38764=DIRECTION ( 'NONE',  ( -0.6427876096865430267, 0.7660444431189749048, -0.000000000000000000 ) ) ;
#38765=ORIENTED_EDGE ( 'NONE', *, *, #7347, .T. ) ;
#38768=CARTESIAN_POINT ( 'NONE',  ( -1.733656465401150149, -28.89360903037850292, 6.868650645600655302 ) ) ;
#38781=B_SPLINE_CURVE_WITH_KNOTS ( 'NONE', 3,
 ( #28985, #13317, #13738, #19514, #1202, #37826, #28580, #9631, #25490, #16015, #19308, #25689, #19714, #35384, #389, #6560, #22412, #38233, #19105, #23013, #35579, #22214, #31674, #31880, #3490 ),
 .UNSPECIFIED., .F., .F.,
 ( 4, 3, 3, 3, 3, 3, 3, 3, 4 ),
 ( 6.468151674593620168E-05, 9.076621574722080685E-05, 0.0001210204262067971669, 0.0001512763324577431315, 0.0001815301820994211592, 0.0002117781465860709496, 0.0002420274594459750450, 0.0002722905548971160054, 0.0002816827545175581917 ),
 .UNSPECIFIED. ) ;
#38789=CARTESIAN_POINT ( 'NONE',  ( 5.115234526135282067, -30.33731918955309936, 6.887547729233687299 ) ) ;
#38790=CARTESIAN_POINT ( 'NONE',  ( 5.195132101224134047, -29.76170719274372090, 6.941203072598468360 ) ) ;
#38792=CARTESIAN_POINT ( 'NONE',  ( 2.242723711017451382, -32.92639770848892766, 6.894806418505347700 ) ) ;
#38793=CARTESIAN_POINT ( 'NONE',  ( 1.755573734986932033, -26.07036524390695220, 6.875671892026062437 ) ) ;
#38794=CARTESIAN_POINT ( 'NONE',  ( 4.342461014271223441, -31.84348076181812814, 7.785096263473212375 ) ) ;
#38799=B_SPLINE_CURVE_WITH_KNOTS ( 'NONE', 3,
 ( #2589, #15111, #28697, #9137, #9332, #32000, #21913, #22125, #18598, #12837, #37735, #31183, #34489, #18810, #3209, #9544, #12633, #25203, #28899, #13650, #10143, #20419, #1507, #904, #23526, #35297, #10355, #25807, #23324, #22733, #20222 ),
 .UNSPECIFIED., .F., .F.,
 ( 4, 3, 3, 3, 3, 3, 3, 3, 3, 3, 4 ),
 ( 8.673617379884035472E-19, 3.077658087705402906E-05, 6.152638666999016878E-05, 9.267501192706322183E-05, 0.0001241882240135154308, 0.0001556618703051673150, 0.0001866161554452174247, 0.0002167966385860936747, 0.0002463805737537735322, 0.0002758761370306494001, 0.0002847094172290008749 ),
 .UNSPECIFIED. ) ;
#38803=CARTESIAN_POINT ( 'NONE',  ( 2.866511140812421754, -26.26990339287398868, 7.720710062488891801 ) ) ;
#38807=VERTEX_POINT ( 'NONE', #3916 ) ;
#38810=ORIENTED_EDGE ( 'NONE', *, *, #10784, .T. ) ;
#38815=CARTESIAN_POINT ( 'NONE',  ( -1.318642678379643218, -31.13375132202764561, 6.871394612369934762 ) ) ;
#38818=CARTESIAN_POINT ( 'NONE',  ( 0.9128126353795650294, -32.98017209969670205, 6.993830769476427456 ) ) ;
#38819=FACE_OUTER_BOUND ( 'NONE', #35257, .T. ) ;
#38821=CARTESIAN_POINT ( 'NONE',  ( 3.461027628862304084, -26.66127814943644125, 7.784476445165070757 ) ) ;
#38822=CARTESIAN_POINT ( 'NONE',  ( 2.495473842921097418, -33.76723158512031375, 7.695279973900954751 ) ) ;
#38826=CARTESIAN_POINT ( 'NONE',  ( -1.614537886288068158, -25.59834652758622653, 7.635761828346577573 ) ) ;
#38827=CARTESIAN_POINT ( 'NONE',  ( 5.200346647029098435, -29.55249110255828882, 7.749999999999999112 ) ) ;
#38829=CARTESIAN_POINT ( 'NONE',  ( -2.527465627618633803, -28.94812858826901802, 7.754798119455333705 ) ) ;
#38830=CARTESIAN_POINT ( 'NONE',  ( 3.894409106313954538, -26.97255664000370246, 7.775108481317160702 ) ) ;
#38831=CARTESIAN_POINT ( 'NONE',  ( -1.339380734913657500, -27.83505459351727396, 7.750000000000002665 ) ) ;
#38832=CYLINDRICAL_SURFACE ( 'NONE', #39669, 0.09010775117052974292 ) ;
#38833=ADVANCED_FACE ( 'NONE', ( #19325 ), #19531, .F. ) ;
#38834=CARTESIAN_POINT ( 'NONE',  ( 4.491609779761556176, -27.45826272268804047, 6.903112506833895878 ) ) ;
#38835=AXIS2_PLACEMENT_3D ( 'NONE', #19407, #6040, #37319 ) ;
#38838=DIRECTION ( 'NONE',  ( -0.000000000000000000, -0.000000000000000000, -1.000000000000000000 ) ) ;
#38839=CARTESIAN_POINT ( 'NONE',  ( 2.910139986571841586, -32.85421171754464353, 7.635761828346577573 ) ) ;
#38842=EDGE_CURVE ( 'NONE', #2595, #20836, #13338, .T. ) ;
#38847=CARTESIAN_POINT ( 'NONE',  ( -0.5201900046161557212, -26.86455205392092083, 6.887161170156907986 ) ) ;
#38848=CARTESIAN_POINT ( 'NONE',  ( -1.282377406787723384, -27.73875492391482211, 6.863805608295729499 ) ) ;
#38849=CARTESIAN_POINT ( 'NONE',  ( 2.390042335280297969, -26.14898894374510974, 7.780491323090172884 ) ) ;
#38855=ORIENTED_EDGE ( 'NONE', *, *, #7945, .F. ) ;
#38857=EDGE_CURVE ( 'NONE', #26935, #10351, #26716, .T. ) ;
#38863=EDGE_LOOP ( 'NONE', ( #37443, #34003, #26969, #23164 ) ) ;
#38872=ORIENTED_EDGE ( 'NONE', *, *, #3127, .T. ) ;
#38879=B_SPLINE_CURVE_WITH_KNOTS ( 'NONE', 3,
 ( #9572, #25030, #15339, #34114, #18621, #37165, #25432, #34516, #37975, #5676 ),
 .UNSPECIFIED., .F., .F.,
 ( 4, 3, 3, 4 ),
 ( 0.0001585009270395705192, 0.0001815657551981863355, 0.0002118214035944168423, 0.0002170292169044748620 ),
 .UNSPECIFIED. ) ;
#38881=CARTESIAN_POINT ( 'NONE',  ( -1.489952004402606667, -30.76578679454389587, 7.257242401810563237 ) ) ;
#38882=EDGE_LOOP ( 'NONE', ( #7188, #3115, #18706, #24923, #34808 ) ) ;
#38887=CARTESIAN_POINT ( 'NONE',  ( 5.155307176249795731, -29.05665538096915412, 7.776484688137381696 ) ) ;
#38891=CARTESIAN_POINT ( 'NONE',  ( 3.866188828012731893, -26.94898948837244035, 7.652160403243380316 ) ) ;
#38892=CARTESIAN_POINT ( 'NONE',  ( 3.431406277207060818, -32.49629020484249509, 7.692469944509197077 ) ) ;
#38893=AXIS2_PLACEMENT_3D ( 'NONE', #32319, #35807, #16631 ) ;
#38896=VERTEX_POINT ( 'NONE', #10648 ) ;
#38902=VERTEX_POINT ( 'NONE', #7964 ) ;
#38903=EDGE_CURVE ( 'NONE', #35504, #25345, #17222, .T. ) ;
#38912=ORIENTED_EDGE ( 'NONE', *, *, #35537, .F. ) ;
#38913=CARTESIAN_POINT ( 'NONE',  ( 2.487967551086643692, -26.15968826709010031, 6.993830769476427456 ) ) ;
#38918=ORIENTED_EDGE ( 'NONE', *, *, #11255, .F. ) ;
#38920=LINE ( 'NONE', #6644, #36570 ) ;
#38922=CARTESIAN_POINT ( 'NONE',  ( -0.4954141421830357550, -26.97407892422453202, 7.635761828346577573 ) ) ;
#38925=CARTESIAN_POINT ( 'NONE',  ( -0.2136480384828472467, -32.50019606712385212, 6.961115707816242448 ) ) ;
#38927=CARTESIAN_POINT ( 'NONE',  ( 4.372846383550529126, -27.30984669459420289, 7.635761828346578461 ) ) ;
#38930=CARTESIAN_POINT ( 'NONE',  ( 6.112940767310136359, -27.90626689514689218, 7.695279973900954751 ) ) ;
#38931=CARTESIAN_POINT ( 'NONE',  ( 4.932354078450567059, -25.52873147056503811, 7.754798119455333705 ) ) ;
#38934=DIRECTION ( 'NONE',  ( -0.1736481776669240584, -0.9848077530122092416, 0.000000000000000000 ) ) ;
#38935=( BOUNDED_CURVE ( )  B_SPLINE_CURVE ( 3, ( #17315, #7464, #20021, #19631 ),
 .UNSPECIFIED., .F., .T. ) 
 B_SPLINE_CURVE_WITH_KNOTS ( ( 4, 4 ),
 ( 1.347909859412853351, 1.534781240595298302 ),
 .UNSPECIFIED. ) 
 CURVE ( )  GEOMETRIC_REPRESENTATION_ITEM ( )  RATIONAL_B_SPLINE_CURVE ( ( 1.000000000000000000, 0.9970920404276226723, 0.9970920404276226723, 1.000000000000000000 ) ) 
 REPRESENTATION_ITEM ( '' )  );
#38936=LINE ( 'NONE', #1300, #32567 ) ;
#38937=CARTESIAN_POINT ( 'NONE',  ( -1.546934178659356451, -28.27117655838526389, 7.766640943994350010 ) ) ;
#38938=CARTESIAN_POINT ( 'NONE',  ( -0.4574210171174859507, -32.19744825413003753, 7.695279973900954751 ) ) ;
#38939=EDGE_LOOP ( 'NONE', ( #25129, #18877, #25550, #27201, #8193, #37298, #36436 ) ) ;
#38943=CARTESIAN_POINT ( 'NONE',  ( 4.713943603702952068, -27.78990194465062302, 7.678495282201405203 ) ) ;
#38944=ORIENTED_EDGE ( 'NONE', *, *, #20897, .T. ) ;
#38945=CARTESIAN_POINT ( 'NONE',  ( -0.9720661970843325062, -31.83001367219261013, 7.635761828346575797 ) ) ;
#38946=CARTESIAN_POINT ( 'NONE',  ( 3.823592214863587913, -32.22550894298759516, 7.782034975670475418 ) ) ;
#38947=EDGE_CURVE ( 'NONE', #31847, #38807, #30423, .T. ) ;
#38949=CARTESIAN_POINT ( 'NONE',  ( 2.326074584482883179, -32.91186359347347690, 7.691066658568947112 ) ) ;
#38950=CARTESIAN_POINT ( 'NONE',  ( 3.598121943223039576, -26.62907708263870887, 7.009310105710485850 ) ) ;
#38952=CARTESIAN_POINT ( 'NONE',  ( 4.403765497540709895, -31.79293866618682785, 7.678495282201404315 ) ) ;
#38957=ORIENTED_EDGE ( 'NONE', *, *, #8404, .T. ) ;
#38960=CARTESIAN_POINT ( 'NONE',  ( -0.9352292415849461360, -31.71783863626873767, 6.894806418505345924 ) ) ;
#38963=DIRECTION ( 'NONE',  ( -0.8660254037844415942, 0.4999999999999950040, -0.000000000000000000 ) ) ;
#38967=ADVANCED_FACE ( 'NONE', ( #35790 ), #7568, .F. ) ;
#38972=LINE ( 'NONE', #10771, #16266 ) ;
#38974=ORIENTED_EDGE ( 'NONE', *, *, #22628, .T. ) ;
#38977=CARTESIAN_POINT ( 'NONE',  ( 3.315058325667250116, -32.67523709003925347, 6.880828092187092793 ) ) ;
#38978=CARTESIAN_POINT ( 'NONE',  ( -1.088725521452697409, -31.68436562166070658, 7.009310105710489402 ) ) ;
#38980=CARTESIAN_POINT ( 'NONE',  ( 2.812523938828905834, -32.78289859174327603, 6.889465824494257262 ) ) ;
#38984=CARTESIAN_POINT ( 'NONE',  ( 1.871557904069252487, -26.07411760613849694, 7.011627023500182965 ) ) ;
#38985=ORIENTED_EDGE ( 'NONE', *, *, #21544, .F. ) ;
#38995=CARTESIAN_POINT ( 'NONE',  ( 2.324907734538560256, -32.91208277201279486, 7.712764235869103757 ) ) ;
#38997=CARTESIAN_POINT ( 'NONE',  ( 2.645388388363652865, -26.19285331904208647, 7.501983001166817822 ) ) ;
#38998=VECTOR ( 'NONE', #9197, 1000.000000000000000 ) ;
#39000=ORIENTED_EDGE ( 'NONE', *, *, #21764, .T. ) ;
#39004=CARTESIAN_POINT ( 'NONE',  ( 0.5751845763345247997, -26.36150267606116060, 7.784838882742139532 ) ) ;
#39007=CARTESIAN_POINT ( 'NONE',  ( 3.558396595903837056, -26.60381962644626697, 7.750000000000000888 ) ) ;
#39010=ORIENTED_EDGE ( 'NONE', *, *, #16965, .F. ) ;
#39012=VECTOR ( 'NONE', #25000, 1000.000000000000000 ) ;
#39013=VECTOR ( 'NONE', #36102, 1000.000000000000000 ) ;
#39015=CARTESIAN_POINT ( 'NONE',  ( -0.03065438358791858567, -26.64358689880297248, 7.693875151218752428 ) ) ;
#39018=CARTESIAN_POINT ( 'NONE',  ( -1.511438080339128076, -30.68539464244183179, 7.785868773668302545 ) ) ;
#39019=B_SPLINE_CURVE_WITH_KNOTS ( 'NONE', 3,
 ( #38146, #20022, #31789, #6872, #22331, #10353, #4195, #29303, #19224, #38545 ),
 .UNSPECIFIED., .F., .F.,
 ( 4, 3, 3, 4 ),
 ( 0.0001585009270395740699, 0.0001815657551981801556, 0.0002118214035944104455, 0.0002170292169044772744 ),
 .UNSPECIFIED. ) ;
#39022=CARTESIAN_POINT ( 'NONE',  ( 3.927859974615581340, -26.87023058389461738, 7.730015791551953619 ) ) ;
#39028=CARTESIAN_POINT ( 'NONE',  ( 4.496857463589675419, -27.46522619576845869, 6.989977667959448304 ) ) ;
#39030=CARTESIAN_POINT ( 'NONE',  ( 5.055212331642637835, -30.59122463574226103, 7.139344958878412584 ) ) ;
#39031=CARTESIAN_POINT ( 'NONE',  ( 4.236974709687405749, -31.83396407781120274, 6.864651958020303368 ) ) ;
#39039=CARTESIAN_POINT ( 'NONE',  ( 1.530267914844154253, -26.16714112483892762, 7.139196562012272373 ) ) ;
#39041=CARTESIAN_POINT ( 'NONE',  ( 2.372232459882097189, -26.14921434934317901, 7.784725160561909441 ) ) ;
#39055=LINE ( 'NONE', #20131, #36685 ) ;
#39056=VECTOR ( 'NONE', #27195, 1000.000000000000114 ) ;
#39058=CARTESIAN_POINT ( 'NONE',  ( 5.049922047023196470, -28.94623841263004138, 7.257242401810563237 ) ) ;
#39062=CARTESIAN_POINT ( 'NONE',  ( 3.926249267005272436, -32.27095793936597090, 6.894806418505347700 ) ) ;
#39068=EDGE_CURVE ( 'NONE', #36841, #19982, #23071, .T. ) ;
#39071=CARTESIAN_POINT ( 'NONE',  ( 0.3574051669894162675, -32.69345966426144656, 7.006423389747790331 ) ) ;
#39081=CARTESIAN_POINT ( 'NONE',  ( 5.150390093233091271, -29.56993018339339940, 6.850000000000000533 ) ) ;
#39085=CARTESIAN_POINT ( 'NONE',  ( -1.765272865745179498, -30.05733663009887024, 7.754798119455333705 ) ) ;
#39086=CARTESIAN_POINT ( 'NONE',  ( -0.5125101069461960313, -26.98863734761392053, 7.703977250142846955 ) ) ;
#39091=CARTESIAN_POINT ( 'NONE',  ( -1.179709461578283269, -27.76296156357867417, 6.863904403958576594 ) ) ;
#39095=CARTESIAN_POINT ( 'NONE',  ( 2.118382188679144296, -33.04488093583253061, 6.941203072598475465 ) ) ;
#39096=CARTESIAN_POINT ( 'NONE',  ( -0.5243941317258925539, -32.27184342263215200, 7.670465701733752972 ) ) ;
#39110=CIRCLE ( 'NONE', #31918, 3.499999999999999556 ) ;
#39112=VERTEX_POINT ( 'NONE', #6320 ) ;
#39113=VECTOR ( 'NONE', #4436, 1000.000000000000000 ) ;
#39114=CARTESIAN_POINT ( 'NONE',  ( 0.1069670619869697303, -26.56643171602332032, 7.754798119455333705 ) ) ;
#39128=CARTESIAN_POINT ( 'NONE',  ( -0.4475183596422435683, -26.93431084857535751, 6.894806418505348589 ) ) ;
#39131=FACE_OUTER_BOUND ( 'NONE', #21035, .T. ) ;
#39132=CARTESIAN_POINT ( 'NONE',  ( -0.5240671274847170658, -32.14127148892561792, 6.892063359921933419 ) ) ;
#39136=CARTESIAN_POINT ( 'NONE',  ( -1.713032059046489142, -28.79627056164295595, 7.013842709614101167 ) ) ;
#39146=CARTESIAN_POINT ( 'NONE',  ( -1.343227611574053348, -27.84180251125378902, 7.651421919295147589 ) ) ;
#39150=CARTESIAN_POINT ( 'NONE',  ( 3.340113934647170435, -32.66206629357650115, 7.750000000000000888 ) ) ;
#39152=CARTESIAN_POINT ( 'NONE',  ( 0.4689551980386493235, -32.84614736048875017, 6.888594555015729703 ) ) ;
#39153=CARTESIAN_POINT ( 'NONE',  ( 1.283089764802823218, -26.09489629076599115, 6.961115707816241560 ) ) ;
#39154=ORIENTED_EDGE ( 'NONE', *, *, #7628, .T. ) ;
#39159=ORIENTED_EDGE ( 'NONE', *, *, #19993, .F. ) ;
#39162=CARTESIAN_POINT ( 'NONE',  ( -1.737164628395478694, -28.91167429922809973, 6.877267274870244584 ) ) ;
#39166=DIRECTION ( 'NONE',  ( -0.3754033771448320178, 0.6502177225477884237, -0.6605219282605403475 ) ) ;
#39169=( BOUNDED_CURVE ( )  B_SPLINE_CURVE ( 3, ( #4633, #29732, #14281, #1159 ),
 .UNSPECIFIED., .F., .T. ) 
 B_SPLINE_CURVE_WITH_KNOTS ( ( 4, 4 ),
 ( 1.381924640371168245, 1.574767692156076038 ),
 .UNSPECIFIED. ) 
 CURVE ( )  GEOMETRIC_REPRESENTATION_ITEM ( )  RATIONAL_B_SPLINE_CURVE ( ( 1.000000000000000000, 0.9969033633783033199, 0.9969033633783033199, 1.000000000000000000 ) ) 
 REPRESENTATION_ITEM ( '' )  );
#39174=ORIENTED_EDGE ( 'NONE', *, *, #14815, .T. ) ;
#39179=ORIENTED_EDGE ( 'NONE', *, *, #24723, .T. ) ;
#39180=CARTESIAN_POINT ( 'NONE',  ( 5.171756705836403789, -29.12309438737783651, 6.887547729233691740 ) ) ;
#39184=CARTESIAN_POINT ( 'NONE',  ( 5.112950570154877639, -30.34738380003949487, 7.009310105710484962 ) ) ;
#39185=B_SPLINE_CURVE_WITH_KNOTS ( 'NONE', 3,
 ( #14196, #19781, #13803, #17269, #32552, #10497, #39306, #32950, #26370, #20368 ),
 .UNSPECIFIED., .F., .F.,
 ( 4, 3, 3, 4 ),
 ( 0.0001585009270395684592, 0.0001815657551981856850, 0.0002118214035944121260, 0.0002170292169044726936 ),
 .UNSPECIFIED. ) ;
#39189=CARTESIAN_POINT ( 'NONE',  ( 1.870087168943759703, -26.07404647501646622, 6.895394898881668233 ) ) ;
#39199=CARTESIAN_POINT ( 'NONE',  ( -1.015649984579921172, -27.51298068758381277, 7.139196562012270597 ) ) ;
#39203=AXIS2_PLACEMENT_3D ( 'NONE', #26390, #32575, #3775 ) ;
#39214=CARTESIAN_POINT ( 'NONE',  ( 0.3883083225179605469, -32.81460370194803744, 7.753200566781576875 ) ) ;
#39215=CARTESIAN_POINT ( 'NONE',  ( 4.025803068412391106, -27.08951600530382464, 7.013842709614101167 ) ) ;
#39216=FACE_OUTER_BOUND ( 'NONE', #37439, .T. ) ;
#39222=AXIS2_PLACEMENT_3D ( 'NONE', #28776, #38630, #13122 ) ;
#39224=EDGE_CURVE ( 'NONE', #39701, #38197, #36334, .T. ) ;
#39225=CARTESIAN_POINT ( 'NONE',  ( 1.493817720656384518, -32.96364906610717327, 6.929923840112063971 ) ) ;
#39229=LINE ( 'NONE', #29576, #13469 ) ;
#39232=VECTOR ( 'NONE', #25232, 1000.000000000000000 ) ;
#39234=CARTESIAN_POINT ( 'NONE',  ( 3.975236603202493946, -32.22983402974450229, 7.720710062488896241 ) ) ;
#39236=CARTESIAN_POINT ( 'NONE',  ( 4.196096248743072188, -31.87893844532966980, 6.876076431790008492 ) ) ;
#39239=EDGE_CURVE ( 'NONE', #30063, #9233, #25043, .T. ) ;
#39240=CARTESIAN_POINT ( 'NONE',  ( 0.9419643339933850834, -26.24837854292180950, 7.139196562012272373 ) ) ;
#39244=CARTESIAN_POINT ( 'NONE',  ( 5.198120437317888864, -29.69595573662939358, 7.750000000000000888 ) ) ;
#39248=CARTESIAN_POINT ( 'NONE',  ( 1.317233406660536232, -26.19158762211118585, 6.939395833800440450 ) ) ;
#39254=CARTESIAN_POINT ( 'NONE',  ( 4.993907954365692348, -30.75430347691218813, 7.635761828346578461 ) ) ;
#39255=EDGE_CURVE ( 'NONE', #33383, #2110, #31140, .T. ) ;
#39262=EDGE_CURVE ( 'NONE', #12173, #11301, #15368, .T. ) ;
#39266=CARTESIAN_POINT ( 'NONE',  ( -1.181303964486304814, -27.76553572604635534, 7.754798119455333705 ) ) ;
#39267=CARTESIAN_POINT ( 'NONE',  ( 4.651604549657131216, -31.25822317698004227, 7.635761828346577573 ) ) ;
#39270=CARTESIAN_POINT ( 'NONE',  ( 5.121331332881381648, -30.25958242544057342, 7.780491323090173772 ) ) ;
#39273=B_SPLINE_CURVE_WITH_KNOTS ( 'NONE', 3,
 ( #1022, #4508, #7180, #10260, #10854, #32714, #13555, #1229, #32316, #1423, #16629, #23627, #23433 ),
 .UNSPECIFIED., .F., .F.,
 ( 4, 3, 3, 3, 4 ),
 ( 0.0002076538946377561555, 0.0002109707048517078375, 0.0002426195318110312908, 0.0002740640997890035277, 0.0002849778069099851785 ),
 .UNSPECIFIED. ) ;
#39278=CARTESIAN_POINT ( 'NONE',  ( 1.028547726584102762, -32.99064601744363046, 7.784725160561909441 ) ) ;
#39281=CARTESIAN_POINT ( 'NONE',  ( 5.986119168300054305, -26.95491573082899706, 7.754798119455333705 ) ) ;
#39285=PLANE ( 'NONE',  #655 ) ;
#39291=DIRECTION ( 'NONE',  ( 0.000000000000000000, 0.6834397476448857978, 0.7300069255418710767 ) ) ;
#39292=ORIENTED_EDGE ( 'NONE', *, *, #811, .F. ) ;
#39297=ORIENTED_EDGE ( 'NONE', *, *, #3152, .F. ) ;
#39306=CARTESIAN_POINT ( 'NONE',  ( 5.140819687086514378, -28.92693390833609612, 7.700536657684214248 ) ) ;
#39307=( LENGTH_UNIT ( ) NAMED_UNIT ( * ) SI_UNIT ( .MILLI., .METRE. ) );
#39309=CARTESIAN_POINT ( 'NONE',  ( 4.763064956553218821, -27.87579221007247199, 6.870737987065014707 ) ) ;
#39317=CARTESIAN_POINT ( 'NONE',  ( 0.1010915821888478394, -26.56955616128021092, 7.761597726988854085 ) ) ;
#39319=CARTESIAN_POINT ( 'NONE',  ( 4.651604549657131216, -31.25822317698004227, 7.635761828346577573 ) ) ;
#39328=CARTESIAN_POINT ( 'NONE',  ( 4.281682929012584182, -27.35702998321412593, 7.695279973900954751 ) ) ;
#39329=CARTESIAN_POINT ( 'NONE',  ( 1.685959272703401401, -26.06995981023128905, 7.636816916992233750 ) ) ;
#39333=CARTESIAN_POINT ( 'NONE',  ( 4.659413201177963870, -31.24450194833492489, 7.730758795053803034 ) ) ;
#39336=CARTESIAN_POINT ( 'NONE',  ( -0.02262473055865150268, -26.52342071894167574, 6.894806418505347700 ) ) ;
#39339=CARTESIAN_POINT ( 'NONE',  ( 4.976842733950424424, -28.33913446795707358, 7.697032948437508182 ) ) ;
#39340=CARTESIAN_POINT ( 'NONE',  ( -1.181303964486304814, -27.76553572604635534, 7.754798119455333705 ) ) ;
#39348=CARTESIAN_POINT ( 'NONE',  ( -1.340340806711404209, -27.83673787031249347, 7.643192810543823157 ) ) ;
#39350=CARTESIAN_POINT ( 'NONE',  ( -0.5008017999313679747, -32.16123271495482072, 7.779495906702011077 ) ) ;
#39351=EDGE_CURVE ( 'NONE', #9389, #19164, #6967, .T. ) ;
#39352=CARTESIAN_POINT ( 'NONE',  ( 3.796401147549515631, -32.24700651031859877, 7.761597726988847867 ) ) ;
#39353=CARTESIAN_POINT ( 'NONE',  ( 4.269670580072574495, -31.94665014585129725, 7.013842709614101167 ) ) ;
#39355=CARTESIAN_POINT ( 'NONE',  ( 0.3325954124718418226, -32.79160147188828489, 6.993830769476427456 ) ) ;
#39358=EDGE_CURVE ( 'NONE', #21657, #25871, #26468, .T. ) ;
#39359=CARTESIAN_POINT ( 'NONE',  ( -1.740011302788441183, -30.21307731605675073, 7.695279973900954751 ) ) ;
#39363=CARTESIAN_POINT ( 'NONE',  ( -0.01837800939314764015, -32.61883756299590686, 7.686927408461906808 ) ) ;
#39364=ORIENTED_EDGE ( 'NONE', *, *, #30745, .T. ) ;
#39370=ORIENTED_EDGE ( 'NONE', *, *, #7217, .F. ) ;
#39371=CARTESIAN_POINT ( 'NONE',  ( -0.8782802225456025624, -27.35395321429220061, 7.784838882742138644 ) ) ;
#39378=CARTESIAN_POINT ( 'NONE',  ( 5.200390093233090205, -29.56993018339339940, 7.800000000000000711 ) ) ;
#39380=DIRECTION ( 'NONE',  ( 0.7394003126383904556, 0.1303762246624302623, -0.6605219282605401254 ) ) ;
#39381=CARTESIAN_POINT ( 'NONE',  ( 5.175262448506648738, -29.15127664070277547, 6.971170733404104425 ) ) ;
#39384=CARTESIAN_POINT ( 'NONE',  ( 3.465471057152984091, -32.59226193070500699, 7.750000000000000000 ) ) ;
#39385=B_SPLINE_CURVE_WITH_KNOTS ( 'NONE', 3,
 ( #26294, #35960, #1388, #19705, #35571, #26490, #4080, #16996, #23004, #13310 ),
 .UNSPECIFIED., .F., .F.,
 ( 4, 3, 3, 4 ),
 ( 0.0002170292169044726936, 0.0002420761345915969052, 0.0002723302478206978718, 0.0002816811360866732774 ),
 .UNSPECIFIED. ) ;
#39386=CARTESIAN_POINT ( 'NONE',  ( 3.432076046773545386, -32.50414549462902158, 7.257242401810562349 ) ) ;
#39387=CARTESIAN_POINT ( 'NONE',  ( -1.099610869996748841, -31.66993096438462629, 6.971170733404106201 ) ) ;
#39388=FACE_OUTER_BOUND ( 'NONE', #15020, .T. ) ;
#39389=CARTESIAN_POINT ( 'NONE',  ( 2.755104336738883219, -32.80220150006005753, 6.864276522220859711 ) ) ;
#39390=CARTESIAN_POINT ( 'NONE',  ( 5.094108975946863183, -29.77650255597014350, 6.929923840112069300 ) ) ;
#39391=CARTESIAN_POINT ( 'NONE',  ( 1.774512685358780928, -26.07070055451856305, 6.867280401193708528 ) ) ;
#39394=VERTEX_POINT ( 'NONE', #6069 ) ;
#39401=CARTESIAN_POINT ( 'NONE',  ( 0.1848793752431239501, -26.52637391292726932, 6.939395833800441338 ) ) ;
#39402=CARTESIAN_POINT ( 'NONE',  ( 0.4906401998943609177, -26.28564864924214461, 7.635761828346577573 ) ) ;
#39404=LINE ( 'NONE', #17992, #17259 ) ;
#39405=DIRECTION ( 'NONE',  ( -0.000000000000000000, -0.000000000000000000, -1.000000000000000000 ) ) ;
#39408=CARTESIAN_POINT ( 'NONE',  ( 3.055030623276686619, -26.34271016697629619, 7.013842709614101167 ) ) ;
#39412=( BOUNDED_CURVE ( )  B_SPLINE_CURVE ( 3, ( #10086, #7006, #10486, #13584 ),
 .UNSPECIFIED., .F., .T. ) 
 B_SPLINE_CURVE_WITH_KNOTS ( ( 4, 4 ),
 ( 4.748221474220560623, 4.941946782021394924 ),
 .UNSPECIFIED. ) 
 CURVE ( )  GEOMETRIC_REPRESENTATION_ITEM ( )  RATIONAL_B_SPLINE_CURVE ( ( 1.000000000000000000, 0.9968749865767494445, 0.9968749865767494445, 1.000000000000000000 ) ) 
 REPRESENTATION_ITEM ( '' )  );
#39415=CARTESIAN_POINT ( 'NONE',  ( 0.6039493587051372181, -26.35155809456087184, 7.784476445165072533 ) ) ;
#39418=CARTESIAN_POINT ( 'NONE',  ( 4.026613127742574960, -27.09026904771587851, 6.895222827070023541 ) ) ;
#39419=CARTESIAN_POINT ( 'NONE',  ( 3.262282976461500894, -25.12033811116058502, 7.695279973900954751 ) ) ;
#39430=CARTESIAN_POINT ( 'NONE',  ( -0.07526459735246904259, -26.55379720668586430, 7.660770905198777569 ) ) ;
#39433=CARTESIAN_POINT ( 'NONE',  ( 4.494099358499767938, -27.46156052226480071, 6.998987538705438993 ) ) ;
#39435=CARTESIAN_POINT ( 'NONE',  ( 4.209064950534304295, -31.86482679551882313, 6.868387053540522480 ) ) ;
#39439=ORIENTED_EDGE ( 'NONE', *, *, #12924, .T. ) ;
#39440=ADVANCED_FACE ( 'NONE', ( #9142 ), #24591, .F. ) ;
#39445=CARTESIAN_POINT ( 'NONE',  ( 4.877469721015450510, -30.78078569709849788, 6.892063359921935195 ) ) ;
#39447=CARTESIAN_POINT ( 'NONE',  ( 2.290977028701361107, -26.12011756940199447, 7.750000000000000888 ) ) ;
#39448=ORIENTED_EDGE ( 'NONE', *, *, #32993, .F. ) ;
#39449=CARTESIAN_POINT ( 'NONE',  ( -0.6716104971371780197, -32.14357770917872870, 6.887547729233689964 ) ) ;
#39451=CARTESIAN_POINT ( 'NONE',  ( -1.722611958414476563, -28.83982133125606495, 7.751599049952172749 ) ) ;
#39459=VERTEX_POINT ( 'NONE', #5868 ) ;
#39467=CYLINDRICAL_SURFACE ( 'NONE', #34999, 0.09010775117052832739 ) ;
#39471=CARTESIAN_POINT ( 'NONE',  ( 5.200390093233090205, -29.62634814563647012, 7.139253571461096293 ) ) ;
#39472=ORIENTED_EDGE ( 'NONE', *, *, #10415, .F. ) ;
#39480=ORIENTED_EDGE ( 'NONE', *, *, #37007, .F. ) ;
#39482=CARTESIAN_POINT ( 'NONE',  ( -2.508659216904252975, -30.29838823369475520, 7.635761828346577573 ) ) ;
#39489=ORIENTED_EDGE ( 'NONE', *, *, #7818, .F. ) ;
#39492=CIRCLE ( 'NONE', #4043, 3.449999999999999734 ) ;
#39493=ADVANCED_FACE ( 'NONE', ( #18816 ), #9758, .T. ) ;
#39494=CARTESIAN_POINT ( 'NONE',  ( -1.145543808814603937, -27.70963634121479657, 6.895222827070022653 ) ) ;
#39495=VERTEX_POINT ( 'NONE', #304 ) ;
#39503=CARTESIAN_POINT ( 'NONE',  ( -1.740229416237445648, -30.21191358056005782, 7.678495282201406980 ) ) ;
#39504=ORIENTED_EDGE ( 'NONE', *, *, #40102, .T. ) ;
#39508=ADVANCED_FACE ( 'NONE', ( #25411 ), #19230, .F. ) ;
#39512=ORIENTED_EDGE ( 'NONE', *, *, #25209, .F. ) ;
#39515=ORIENTED_EDGE ( 'NONE', *, *, #8165, .F. ) ;
#39522=CARTESIAN_POINT ( 'NONE',  ( -1.797366426793039151, -29.44420554634202247, 6.867199677474203234 ) ) ;
#39529=CARTESIAN_POINT ( 'NONE',  ( 0.3856705772283747780, -32.81361829944838604, 7.750000000000000888 ) ) ;
#39536=CARTESIAN_POINT ( 'NONE',  ( 1.700390093233090871, -29.56993018339339940, 7.800000000000000711 ) ) ;
#39537=CARTESIAN_POINT ( 'NONE',  ( 0.6255804977955936597, -26.34427047815355749, 6.866852738645443210 ) ) ;
#39538=CARTESIAN_POINT ( 'NONE',  ( 0.1191028511967372472, -26.44750632012536329, 6.941203072598479018 ) ) ;
#39541=CARTESIAN_POINT ( 'NONE',  ( 4.703888560603170177, -27.97650715214728123, 7.754798119455333705 ) ) ;
#39542=CARTESIAN_POINT ( 'NONE',  ( 5.187224694358618216, -29.60529023175765673, 7.783750581861599294 ) ) ;
#39546=CARTESIAN_POINT ( 'NONE',  ( 4.354978660100002230, -31.83382125611363378, 7.781480525794719050 ) ) ;
#39553=CARTESIAN_POINT ( 'NONE',  ( -1.749609906766908640, -29.56993018339339940, 6.800000000000000711 ) ) ;
#39555=CYLINDRICAL_SURFACE ( 'NONE', #18692, 3.399999999999999911 ) ;
#39556=CARTESIAN_POINT ( 'NONE',  ( 3.900211856183038783, -32.16237771637295140, 7.748216051605122168 ) ) ;
#39559=CARTESIAN_POINT ( 'NONE',  ( -1.477562859369297987, -28.36137111117319520, 6.894806418505348589 ) ) ;
#39560=CARTESIAN_POINT ( 'NONE',  ( 0.3325276087138285264, -32.79156831072005218, 6.916197352289366052 ) ) ;
#39561=CARTESIAN_POINT ( 'NONE',  ( 1.265549882940071313, -26.09704752031474229, 7.006908160621415860 ) ) ;
#39562=ORIENTED_EDGE ( 'NONE', *, *, #20377, .T. ) ;
#39563=B_SPLINE_CURVE_WITH_KNOTS ( 'NONE', 3,
 ( #28910, #7080, #26027, #10368, #26234, #39162, #13664, #38768, #35507, #7882, #13865, #26628, #35904, #20038, #35310, #7481, #32414, #4209, #13455, #25823, #1131, #10156, #716, #26433, #10564, #23138, #3822, #32217, #35705, #32619, #32014, #4414, #36106, #16339 ),
 .UNSPECIFIED., .F., .F.,
 ( 4, 3, 3, 3, 3, 3, 3, 3, 3, 3, 3, 4 ),
 ( 0.0002070713223507422327, 0.0002134813625843692516, 0.0002436920583247462343, 0.0002744103412181350156, 0.0003056492822488889884, 0.0003371912505268163376, 0.0003686006886010369916, 0.0003994157908200238020, 0.0004294560467902368219, 0.0004589785222107595208, 0.0004885217042653181626, 0.0004917893847005023198 ),
 .UNSPECIFIED. ) ;
#39575=AXIS2_PLACEMENT_3D ( 'NONE', #1499, #4981, #32797 ) ;
#39576=CARTESIAN_POINT ( 'NONE',  ( -0.9124018737164114601, -27.39430309170973388, 7.756377446753158544 ) ) ;
#39579=CARTESIAN_POINT ( 'NONE',  ( 4.333310421813720836, -31.87597283208960874, 6.867280401193706751 ) ) ;
#39583=CARTESIAN_POINT ( 'NONE',  ( 4.331203346590854153, -31.73491918113357357, 7.257242401810562349 ) ) ;
#39584=VERTEX_POINT ( 'NONE', #106 ) ;
#39588=CARTESIAN_POINT ( 'NONE',  ( 0.7753597313414962722, -32.84905728735835595, 7.505001789837629111 ) ) ;
#39589=DIRECTION ( 'NONE',  ( -3.491481338843133750E-15, 1.000000000000000000, -0.000000000000000000 ) ) ;
#39590=CARTESIAN_POINT ( 'NONE',  ( 5.156371316636622737, -29.01658238726313854, 6.875671892026062437 ) ) ;
#39594=CARTESIAN_POINT ( 'NONE',  ( 3.343728876470205336, -32.65988526930982516, 7.754798119455333705 ) ) ;
#39598=DIRECTION ( 'NONE',  ( 0.6427876096865284827, 0.7660444431189872283, 0.000000000000000000 ) ) ;
#39599=CARTESIAN_POINT ( 'NONE',  ( 4.630071603208546271, -27.84454145904519251, 7.661510568013100375 ) ) ;
#39603=EDGE_LOOP ( 'NONE', ( #3280, #4687, #38749, #7996, #8318 ) ) ;
#39610=VERTEX_POINT ( 'NONE', #10148 ) ;
#39611=CARTESIAN_POINT ( 'NONE',  ( -0.8650427792287253004, -27.18905761710760416, 7.006908160621412307 ) ) ;
#39619=ORIENTED_EDGE ( 'NONE', *, *, #38506, .F. ) ;
#39621=B_SPLINE_CURVE_WITH_KNOTS ( 'NONE', 3,
 ( #11917, #9042, #25323, #24492, #12543, #12339, #8833, #24703, #12746, #28185 ),
 .UNSPECIFIED., .F., .F.,
 ( 4, 3, 3, 4 ),
 ( 8.673617379884035472E-19, 3.025570593003056093E-05, 6.051145698344016094E-05, 6.468151674593633721E-05 ),
 .UNSPECIFIED. ) ;
#39626=CARTESIAN_POINT ( 'NONE',  ( 3.941824067710134383, -27.01335656366605420, 6.874555630061442102 ) ) ;
#39633=B_SPLINE_CURVE_WITH_KNOTS ( 'NONE', 3,
 ( #16541, #1333, #524, #4611 ),
 .UNSPECIFIED., .F., .F.,
 ( 4, 4 ),
 ( 0.000000000000000000, 6.391136169994592770E-06 ),
 .UNSPECIFIED. ) ;
#39635=CARTESIAN_POINT ( 'NONE',  ( 2.341155903240350167, -26.23085468064335046, 6.892063359921932530 ) ) ;
#39639=CARTESIAN_POINT ( 'NONE',  ( 0.6494831848250305351, -26.23141567014731734, 6.880828092187096345 ) ) ;
#39640=ADVANCED_FACE ( 'NONE', ( #515 ), #22739, .F. ) ;
#39641=EDGE_CURVE ( 'NONE', #32059, #30749, #15930, .T. ) ;
#39642=VECTOR ( 'NONE', #21286, 1000.000000000000000 ) ;
#39646=CARTESIAN_POINT ( 'NONE',  ( 5.097523595859303924, -28.69978428133380888, 7.501983001166817822 ) ) ;
#39650=B_SPLINE_CURVE_WITH_KNOTS ( 'NONE', 3,
 ( #38735, #23111, #20008, #32588, #4385, #16910, #39753, #36872, #8855, #36463, #12149, #30498, #20601, #21030, #30713, #34014, #2724, #30096, #8653, #8238, #20808, #11941, #14618, #18120, #27801, #5788, #11530, #27394, #18326, #36664, #33603 ),
 .UNSPECIFIED., .F., .F.,
 ( 4, 3, 3, 3, 3, 3, 3, 3, 3, 3, 4 ),
 ( 8.182674270850422113E-18, 3.077658087705610260E-05, 6.152638666999237784E-05, 9.267501192706366906E-05, 0.0001241882240135212313, 0.0001556618703051610537, 0.0001866161554452267488, 0.0002167966385861010473, 0.0002463805737537807963, 0.0002758761370306577485, 0.0002847094172290174090 ),
 .UNSPECIFIED. ) ;
#39651=CARTESIAN_POINT ( 'NONE',  ( 0.7302373594189235373, -26.30393590818857064, 7.386948897581449458 ) ) ;
#39653=CARTESIAN_POINT ( 'NONE',  ( 4.862263076544310003, -30.81999235699081652, 6.866852738645444099 ) ) ;
#39654=( BOUNDED_CURVE ( )  B_SPLINE_CURVE ( 3, ( #15713, #28684, #9526, #494 ),
 .UNSPECIFIED., .F., .T. ) 
 B_SPLINE_CURVE_WITH_KNOTS ( ( 4, 4 ),
 ( 4.708531083176467291, 4.895802057644188743 ),
 .UNSPECIFIED. ) 
 CURVE ( )  GEOMETRIC_REPRESENTATION_ITEM ( )  RATIONAL_B_SPLINE_CURVE ( ( 1.000000000000000000, 0.9970795998553221295, 0.9970795998553221295, 1.000000000000000000 ) ) 
 REPRESENTATION_ITEM ( '' )  );
#39658=CARTESIAN_POINT ( 'NONE',  ( -0.6132364880641560934, -32.19616932755274519, 6.865554069792297653 ) ) ;
#39663=DIRECTION ( 'NONE',  ( -0.5751513419797977811, 0.4826092789263575211, 0.6605219282605377940 ) ) ;
#39669=AXIS2_PLACEMENT_3D ( 'NONE', #23201, #35772, #17204 ) ;
#39676=CARTESIAN_POINT ( 'NONE',  ( 4.662641849846992592, -31.23878144412272206, 7.691066658568944447 ) ) ;
#39678=ORIENTED_EDGE ( 'NONE', *, *, #3107, .T. ) ;
#39681=CARTESIAN_POINT ( 'NONE',  ( -0.9620374312546590145, -31.84181919407372163, 7.730015791551947402 ) ) ;
#39683=CARTESIAN_POINT ( 'NONE',  ( 4.983270326624491098, -28.35638137736280484, 7.640616322432102869 ) ) ;
#39688=DIRECTION ( 'NONE',  ( -1.000000000000000000, 0.000000000000000000, 0.000000000000000000 ) ) ;
#39689=CARTESIAN_POINT ( 'NONE',  ( 5.200252094213874798, -29.60101030711846448, 6.894806418505347700 ) ) ;
#39693=PLANE ( 'NONE',  #29290 ) ;
#39700=CARTESIAN_POINT ( 'NONE',  ( 5.028764603308605530, -28.48812247857538438, 7.754798119455333705 ) ) ;
#39701=VERTEX_POINT ( 'NONE', #35898 ) ;
#39712=ORIENTED_EDGE ( 'NONE', *, *, #21963, .T. ) ;
#39714=CARTESIAN_POINT ( 'NONE',  ( 0.01787935223071997204, -32.52445247686870289, 7.643333865083955736 ) ) ;
#39719=EDGE_CURVE ( 'NONE', #34893, #15830, #12260, .T. ) ;
#39720=CARTESIAN_POINT ( 'NONE',  ( 4.813436497423070115, -27.97025956726023566, 7.011627023500182077 ) ) ;
#39722=VERTEX_POINT ( 'NONE', #1717 ) ;
#39727=CARTESIAN_POINT ( 'NONE',  ( 0.07058059489397008890, -26.58600545297078099, 7.782034975670478083 ) ) ;
#39739=CARTESIAN_POINT ( 'NONE',  ( -1.260542631132519853, -27.89873549449913170, 7.670860738520326905 ) ) ;
#39740=CARTESIAN_POINT ( 'NONE',  ( 6.149982165465896600, -31.13182306662183052, 7.695279973900954751 ) ) ;
#39746=AXIS2_PLACEMENT_3D ( 'NONE', #25795, #279, #25391 ) ;
#39747=CARTESIAN_POINT ( 'NONE',  ( -0.9271071152667473836, -27.41209366881661325, 7.692469944509192636 ) ) ;
#39750=EDGE_CURVE ( 'NONE', #17262, #23554, #22053, .T. ) ;
#39752=CARTESIAN_POINT ( 'NONE',  ( -0.5145088012743496142, -26.98099630600513876, 7.257242401810563237 ) ) ;
#39753=CARTESIAN_POINT ( 'NONE',  ( 4.688487803309406843, -31.39236593672921316, 6.865554069792297653 ) ) ;
#39759=CARTESIAN_POINT ( 'NONE',  ( 1.215732341648462000, -26.10364848027380447, 7.751599049952174525 ) ) ;
#39761=CARTESIAN_POINT ( 'NONE',  ( 4.301450302647315205, -31.91148321001355370, 7.754798119455333705 ) ) ;
#39766=AXIS2_PLACEMENT_3D ( 'NONE', #13735, #4478, #23399 ) ;
#39767=FACE_OUTER_BOUND ( 'NONE', #7205, .T. ) ;
#39770=CARTESIAN_POINT ( 'NONE',  ( 1.062037487868057184, -32.90946697031814949, 6.894806418505346812 ) ) ;
#39773=CARTESIAN_POINT ( 'NONE',  ( -1.699406134149164416, -29.53190947434445235, 7.784295182778427247 ) ) ;
#39783=( BOUNDED_CURVE ( )  B_SPLINE_CURVE ( 3, ( #19406, #6852, #16308, #685 ),
 .UNSPECIFIED., .F., .T. ) 
 B_SPLINE_CURVE_WITH_KNOTS ( ( 4, 4 ),
 ( 4.708531083176469068, 4.895802057644189631 ),
 .UNSPECIFIED. ) 
 CURVE ( )  GEOMETRIC_REPRESENTATION_ITEM ( )  RATIONAL_B_SPLINE_CURVE ( ( 1.000000000000000000, 0.9970795998553221295, 0.9970795998553221295, 1.000000000000000000 ) ) 
 REPRESENTATION_ITEM ( '' )  );
#39787=EDGE_CURVE ( 'NONE', #6937, #28759, #4013, .T. ) ;
#39792=DIRECTION ( 'NONE',  ( 0.000000000000000000, 0.7126435865141285131, 0.7015262779114406211 ) ) ;
#39795=DIRECTION ( 'NONE',  ( 0.000000000000000000, 0.000000000000000000, 1.000000000000000000 ) ) ;
#39799=CARTESIAN_POINT ( 'NONE',  ( 5.042305363714541855, -28.94414881188822619, 7.695279973900954751 ) ) ;
#39801=CARTESIAN_POINT ( 'NONE',  ( 1.595260788587017586, -33.06836594711004551, 6.863784140767622333 ) ) ;
#39805=CARTESIAN_POINT ( 'NONE',  ( 3.973866779147308570, -26.90885826429679284, 6.894806418505347700 ) ) ;
#39807=CARTESIAN_POINT ( 'NONE',  ( 5.174907696227332821, -29.14835287555633769, 6.980586498568971621 ) ) ;
#39810=CARTESIAN_POINT ( 'NONE',  ( 3.378579686077430644, -32.62731885087992367, 7.782861076432731728 ) ) ;
#39811=CARTESIAN_POINT ( 'NONE',  ( 1.135223716940237937, -32.92263077448382091, 7.652160403243382980 ) ) ;
#39812=CARTESIAN_POINT ( 'NONE',  ( 5.045182535701832727, -28.95967786423770818, 7.643333865083955736 ) ) ;
#39816=CARTESIAN_POINT ( 'NONE',  ( 5.100005351453509306, -29.62113694480887105, 6.892063359921934307 ) ) ;
#39818=CARTESIAN_POINT ( 'NONE',  ( 4.878343045835490166, -30.77848925561357873, 6.894806418505348589 ) ) ;
#39819=CARTESIAN_POINT ( 'NONE',  ( -1.583891440918162585, -30.77968007673214146, 7.635761828346579350 ) ) ;
#39826=CARTESIAN_POINT ( 'NONE',  ( -0.9919418010453353585, -27.33356058713898307, 7.750000000000000888 ) ) ;
#39830=EDGE_CURVE ( 'NONE', #3023, #15769, #29406, .T. ) ;
#39831=CARTESIAN_POINT ( 'NONE',  ( 2.177050749421512332, -32.93635181753877816, 7.761597726988850532 ) ) ;
#39832=ORIENTED_EDGE ( 'NONE', *, *, #34488, .T. ) ;
#39847=ORIENTED_EDGE ( 'NONE', *, *, #18065, .T. ) ;
#39851=CARTESIAN_POINT ( 'NONE',  ( 1.585995385899496846, -32.96800520477448515, 6.864276522220859711 ) ) ;
#39852=CARTESIAN_POINT ( 'NONE',  ( 2.474049714983522108, -26.25912200567108457, 7.013842709614101167 ) ) ;
#39853=CARTESIAN_POINT ( 'NONE',  ( -1.744021509508924206, -30.18346125941860336, 7.762796336881262249 ) ) ;
#39856=LINE ( 'NONE', #40251, #29980 ) ;
#39857=CARTESIAN_POINT ( 'NONE',  ( -0.03790328338398483987, -32.60774784362404688, 7.635761828346575797 ) ) ;
#39859=CARTESIAN_POINT ( 'NONE',  ( -0.4205071184425808739, -26.91252637186863339, 6.870716933885664623 ) ) ;
#39860=CARTESIAN_POINT ( 'NONE',  ( 4.165461883494793405, -31.91160235871856443, 6.939395833800444890 ) ) ;
#39861=VERTEX_POINT ( 'NONE', #29450 ) ;
#39865=AXIS2_PLACEMENT_3D ( 'NONE', #7640, #21011, #1476 ) ;
#39868=CARTESIAN_POINT ( 'NONE',  ( -1.637662370169622461, -28.92386071996777375, 6.887041543973312585 ) ) ;
#39870=CARTESIAN_POINT ( 'NONE',  ( -0.6653948319370099895, -32.14929951971039657, 6.880828092187096345 ) ) ;
#39878=CARTESIAN_POINT ( 'NONE',  ( -0.7642813497525950961, -27.22783823854348384, 6.959317978105167946 ) ) ;
#39879=ORIENTED_EDGE ( 'NONE', *, *, #33298, .T. ) ;
#39883=CARTESIAN_POINT ( 'NONE',  ( 3.234894228808482985, -32.60395886024767265, 6.895222827070022653 ) ) ;
#39884=EDGE_CURVE ( 'NONE', #38896, #6366, #7204, .T. ) ;
#39885=DIRECTION ( 'NONE',  ( 0.3420201433256790380, -0.9396926207859046531, -0.000000000000000000 ) ) ;
#39887=CARTESIAN_POINT ( 'NONE',  ( -1.223904788644516239, -27.83540028486481788, 7.784838882742139532 ) ) ;
#39888=VECTOR ( 'NONE', #23534, 1000.000000000000000 ) ;
#39890=AXIS2_PLACEMENT_3D ( 'NONE', #17487, #29474, #30080 ) ;
#39892=ORIENTED_EDGE ( 'NONE', *, *, #30189, .T. ) ;
#39893=CARTESIAN_POINT ( 'NONE',  ( 5.200390093233090205, -29.56993018339339940, 7.202408869016171167 ) ) ;
#39895=CARTESIAN_POINT ( 'NONE',  ( 3.462070670749302970, -32.59424523688933562, 7.635761828346575797 ) ) ;
#39896=CARTESIAN_POINT ( 'NONE',  ( 1.010737851185899761, -32.99087142304168907, 7.780491323090171107 ) ) ;
#39901=CARTESIAN_POINT ( 'NONE',  ( 0.1833252022694565608, -32.73160443007695619, 7.501983001166818710 ) ) ;
#39902=FACE_OUTER_BOUND ( 'NONE', #20125, .T. ) ;
#39905=FACE_OUTER_BOUND ( 'NONE', #34897, .T. ) ;
#39909=CARTESIAN_POINT ( 'NONE',  ( -2.712160580843945734, -31.23359347163986399, 7.695279973900954751 ) ) ;
#39918=VECTOR ( 'NONE', #9730, 1000.000000000000114 ) ;
#39922=CARTESIAN_POINT ( 'NONE',  ( -0.4513664592218429861, -26.80950562565463358, 7.750000000000000888 ) ) ;
#39937=ORIENTED_EDGE ( 'NONE', *, *, #18126, .F. ) ;
#39939=DIRECTION ( 'NONE',  ( -0.1736481776669340227, 0.9848077530122073542, -0.000000000000000000 ) ) ;
#39940=CARTESIAN_POINT ( 'NONE',  ( -1.794470407209020513, -29.38028857357967283, 6.931070083220557621 ) ) ;
#39946=CARTESIAN_POINT ( 'NONE',  ( -1.653996770750948642, -29.01487273886056784, 7.691066658568944447 ) ) ;
#39954=CARTESIAN_POINT ( 'NONE',  ( -0.9205506017878787306, -27.40413144861377148, 7.652160403243376763 ) ) ;
#39955=DIRECTION ( 'NONE',  ( -0.4999999999999918954, -0.8660254037844432595, -0.000000000000000000 ) ) ;
#39956=CARTESIAN_POINT ( 'NONE',  ( -1.645585159361036220, -30.17362680341680203, 7.635761828346577573 ) ) ;
#39959=CARTESIAN_POINT ( 'NONE',  ( 5.185009940666303940, -29.62933811247615168, 7.785593909369614707 ) ) ;
#39960=LINE ( 'NONE', #1907, #3996 ) ;
#39962=CARTESIAN_POINT ( 'NONE',  ( 0.5371711504799139281, -32.87097875789517332, 7.695279973900954751 ) ) ;
#39971=EDGE_LOOP ( 'NONE', ( #11079, #21626, #24498, #27916, #32601, #36827 ) ) ;
#39972=CARTESIAN_POINT ( 'NONE',  ( 4.550595850147784560, -31.61296642115005895, 7.501983001166816933 ) ) ;
#39979=ORIENTED_EDGE ( 'NONE', *, *, #13933, .F. ) ;
#39984=EDGE_CURVE ( 'NONE', #7963, #33743, #10211, .T. ) ;
#39988=CARTESIAN_POINT ( 'NONE',  ( 2.255350295996689347, -26.21552723005750352, 7.695279973900954751 ) ) ;
#39992=CARTESIAN_POINT ( 'NONE',  ( -0.8336107809199673202, -27.30301714566001792, 7.768425012602596880 ) ) ;
#39996=CARTESIAN_POINT ( 'NONE',  ( 1.664433243520564876, -26.17012032033359148, 7.695279973900954751 ) ) ;
#40000=CARTESIAN_POINT ( 'NONE',  ( -1.315039247493585250, -27.79308300620435901, 6.894806418505347700 ) ) ;
#40003=ORIENTED_EDGE ( 'NONE', *, *, #31587, .F. ) ;
#40004=CARTESIAN_POINT ( 'NONE',  ( -0.4171441595639596156, -26.78316706317107787, 7.013842709614101167 ) ) ;
#40005=CARTESIAN_POINT ( 'NONE',  ( 5.168232458229329751, -29.09648105291681475, 6.870724624169668893 ) ) ;
#40008=CARTESIAN_POINT ( 'NONE',  ( 3.348332484698080425, -32.65674733949929731, 7.761113333117551250 ) ) ;
#40009=FACE_BOUND ( 'NONE', #23568, .T. ) ;
#40013=CARTESIAN_POINT ( 'NONE',  ( 4.933620711012202342, -28.51815776361375754, 7.759451378593094972 ) ) ;
#40017=ORIENTED_EDGE ( 'NONE', *, *, #25714, .T. ) ;
#40022=VERTEX_POINT ( 'NONE', #18288 ) ;
#40025=DIRECTION ( 'NONE',  ( -0.4826092789263618510, 0.5751513419797912308, -0.6605219282605402364 ) ) ;
#40026=CARTESIAN_POINT ( 'NONE',  ( 3.043375019476788346, -26.44640070252536290, 7.006423389747791219 ) ) ;
#40027=( BOUNDED_CURVE ( )  B_SPLINE_CURVE ( 3, ( #19160, #3345, #4137, #18956 ),
 .UNSPECIFIED., .F., .T. ) 
 B_SPLINE_CURVE_WITH_KNOTS ( ( 4, 4 ),
 ( 4.708531083176468179, 4.895802057644189631 ),
 .UNSPECIFIED. ) 
 CURVE ( )  GEOMETRIC_REPRESENTATION_ITEM ( )  RATIONAL_B_SPLINE_CURVE ( ( 1.000000000000000000, 0.9970795998553221295, 0.9970795998553221295, 1.000000000000000000 ) ) 
 REPRESENTATION_ITEM ( '' )  );
#40030=CARTESIAN_POINT ( 'NONE',  ( 2.211347688137016210, -32.93132991176759106, 7.782034975670476307 ) ) ;
#40039=ORIENTED_EDGE ( 'NONE', *, *, #34058, .T. ) ;
#40047=CARTESIAN_POINT ( 'NONE',  ( -1.320963929511134394, -31.33668423227719302, 7.643192810543818716 ) ) ;
#40049=TOROIDAL_SURFACE ( 'NONE', #26883, 3.449999999999999289, 0.05000000000000000278 ) ;
#40054=CARTESIAN_POINT ( 'NONE',  ( 3.090657818664316103, -26.35045347725774434, 7.387053503561885393 ) ) ;
#40056=CARTESIAN_POINT ( 'NONE',  ( -0.5730865926811068434, -32.23100210249002373, 6.894806418505347700 ) ) ;
#40063=CYLINDRICAL_SURFACE ( 'NONE', #19150, 0.09010775117052784167 ) ;
#40064=EDGE_CURVE ( 'NONE', #25477, #28596, #21397, .T. ) ;
#40069=CARTESIAN_POINT ( 'NONE',  ( 4.828954996240010900, -30.90115017889735682, 6.887945620086116882 ) ) ;
#40070=CARTESIAN_POINT ( 'NONE',  ( -1.547122796906874598, -30.57677098347808098, 6.876076431790006716 ) ) ;
#40071=ORIENTED_EDGE ( 'NONE', *, *, #21724, .F. ) ;
#40073=EDGE_CURVE ( 'NONE', #14142, #35485, #1931, .T. ) ;
#40075=CARTESIAN_POINT ( 'NONE',  ( -0.6847619013603313265, -32.13139149473335721, 6.998987538705432776 ) ) ;
#40076=VERTEX_POINT ( 'NONE', #19320 ) ;
#40080=CARTESIAN_POINT ( 'NONE',  ( -1.525418950806410212, -28.21191307850770258, 6.898188844117813190 ) ) ;
#40082=CARTESIAN_POINT ( 'NONE',  ( 4.790345179149528398, -27.92659140015631891, 7.754798119455333705 ) ) ;
#40085=CARTESIAN_POINT ( 'NONE',  ( 3.215900811223072697, -32.61348645385951528, 6.939395833800443114 ) ) ;
#40086=CARTESIAN_POINT ( 'NONE',  ( 4.976157933844921999, -30.80256632143474604, 6.887161170156908874 ) ) ;
#40087=CARTESIAN_POINT ( 'NONE',  ( -1.225953191357326277, -31.30097466021442187, 7.695279973900954751 ) ) ;
#40088=CARTESIAN_POINT ( 'NONE',  ( -1.188758931704360089, -27.77748128243219483, 7.768425012602592439 ) ) ;
#40090=ORIENTED_EDGE ( 'NONE', *, *, #8165, .T. ) ;
#40091=CARTESIAN_POINT ( 'NONE',  ( 5.016239155254060833, -30.32173691802341509, 6.876076431790006716 ) ) ;
#40094=CARTESIAN_POINT ( 'NONE',  ( -0.9639628759317209195, -31.83956276478470926, 7.737115613922529000 ) ) ;
#40095=CARTESIAN_POINT ( 'NONE',  ( 4.983950756172366603, -28.35822323759031605, 7.638132480492517473 ) ) ;
#40099=VERTEX_POINT ( 'NONE', #38049 ) ;
#40101=DIRECTION ( 'NONE',  ( -0.7660444431189726844, -0.6427876096865458022, -0.000000000000000000 ) ) ;
#40102=EDGE_CURVE ( 'NONE', #20830, #28641, #28799, .T. ) ;
#40104=ADVANCED_FACE ( 'NONE', ( #22015 ), #9426, .F. ) ;
#40109=CARTESIAN_POINT ( 'NONE',  ( 1.894073117522566463, -26.17544468245638356, 7.006423389747790331 ) ) ;
#40121=ORIENTED_EDGE ( 'NONE', *, *, #15727, .F. ) ;
#40122=CARTESIAN_POINT ( 'NONE',  ( -1.740011302788441183, -30.21307731605675073, 7.695279973900954751 ) ) ;
#40124=VERTEX_POINT ( 'NONE', #10046 ) ;
#40135=ORIENTED_EDGE ( 'NONE', *, *, #29249, .T. ) ;
#40138=CARTESIAN_POINT ( 'NONE',  ( -1.795240888762144937, -29.39510444811675072, 7.006908160621414972 ) ) ;
#40146=ORIENTED_EDGE ( 'NONE', *, *, #17743, .F. ) ;
#40149=CARTESIAN_POINT ( 'NONE',  ( 5.140436678832947415, -30.21500869279741508, 6.887161170156907097 ) ) ;
#40151=CARTESIAN_POINT ( 'NONE',  ( 3.555970037240517190, -26.60239115476207772, 7.753200566781577763 ) ) ;
#40153=B_SPLINE_CURVE_WITH_KNOTS ( 'NONE', 3,
 ( #12196, #2763, #34264, #12407, #6650, #19200, #37920, #37706, #9111, #37512, #5831, #9726, #15491, #22096, #31562, #22307, #3580, #15288, #77, #40394, #2972, #34874, #24767, #481, #18782, #8897, #9307, #19002, #31766, #25175, #6238 ),
 .UNSPECIFIED., .F., .F.,
 ( 4, 3, 3, 3, 3, 3, 3, 3, 3, 3, 4 ),
 ( 8.055264624169107152E-18, 3.077658087705768824E-05, 6.152638666999025010E-05, 9.267501192706735535E-05, 0.0001241882240135194423, 0.0001556618703051683992, 0.0001866161554452216802, 0.0002167966385861003697, 0.0002463805737537802000, 0.0002758761370306561764, 0.0002847094172290048322 ),
 .UNSPECIFIED. ) ;
#40154=CARTESIAN_POINT ( 'NONE',  ( 1.058406696066443331, -26.12931067392286266, 7.678495282201404315 ) ) ;
#40157=CARTESIAN_POINT ( 'NONE',  ( 5.189124044873195452, -29.59783471987984171, 7.781480525794717273 ) ) ;
#40161=CARTESIAN_POINT ( 'NONE',  ( 1.736346942945644400, -33.06974547922812491, 7.701614758090453705 ) ) ;
#40163=EDGE_CURVE ( 'NONE', #36954, #17549, #25469, .T. ) ;
#40173=CARTESIAN_POINT ( 'NONE',  ( -1.346119371218626792, -31.29294500718514271, 6.894806418505347700 ) ) ;
#40176=ORIENTED_EDGE ( 'NONE', *, *, #23793, .T. ) ;
#40181=CARTESIAN_POINT ( 'NONE',  ( -2.707143391484601924, -27.16588715693004730, 7.754798119455333705 ) ) ;
#40184=CARTESIAN_POINT ( 'NONE',  ( 3.883994185819156453, -32.28945568252876086, 7.782861076432730840 ) ) ;
#40186=CARTESIAN_POINT ( 'NONE',  ( 5.118969260771242702, -33.45454016556441701, 7.754798119455333705 ) ) ;
#40192=AXIS2_PLACEMENT_3D ( 'NONE', #13630, #38324, #7246 ) ;
#40195=CYLINDRICAL_SURFACE ( 'NONE', #32799, 3.399999999999999911 ) ;
#40196=FACE_OUTER_BOUND ( 'NONE', #5127, .T. ) ;
#40198=CARTESIAN_POINT ( 'NONE',  ( -1.773855778497440250, -29.99374101709560492, 6.921725064902953584 ) ) ;
#40202=CARTESIAN_POINT ( 'NONE',  ( 5.001421652434105525, -30.73319741649938308, 7.698786668945012401 ) ) ;
#40203=LINE ( 'NONE', #15706, #27580 ) ;
#40204=CARTESIAN_POINT ( 'NONE',  ( 5.149536281657578485, -30.16439681061213918, 7.635761828346576685 ) ) ;
#40208=CARTESIAN_POINT ( 'NONE',  ( -0.08065709997538077214, -26.55697965350343281, 7.695279973900954751 ) ) ;
#40209=CARTESIAN_POINT ( 'NONE',  ( 0.4745948466847342839, -32.83438907916249150, 7.783750581861599294 ) ) ;
#40210=DIRECTION ( 'NONE',  ( 0.5000000000000101030, -0.8660254037844328234, -0.000000000000000000 ) ) ;
#40211=CARTESIAN_POINT ( 'NONE',  ( 5.098465114614175064, -29.68432489072703717, 6.864276522220859711 ) ) ;
#40215=EDGE_CURVE ( 'NONE', #320, #32452, #17133, .T. ) ;
#40220=ORIENTED_EDGE ( 'NONE', *, *, #27893, .F. ) ;
#40221=FACE_OUTER_BOUND ( 'NONE', #34542, .T. ) ;
#40227=CARTESIAN_POINT ( 'NONE',  ( 5.037724831097187383, -30.21969694727531675, 7.785172627573962778 ) ) ;
#40228=ORIENTED_EDGE ( 'NONE', *, *, #1083, .F. ) ;
#40231=B_SPLINE_CURVE_WITH_KNOTS ( 'NONE', 3,
 ( #12497, #19288, #31854, #9815, #37804, #9196, #25066, #24648, #37600, #6330, #28140, #22394, #31046, #15586, #21984, #9609, #40692, #31450, #18460 ),
 .UNSPECIFIED., .F., .F.,
 ( 4, 3, 3, 3, 3, 3, 4 ),
 ( 1.143643797815609544E-18, 2.546128104244724791E-05, 5.711050680483827665E-05, 8.113074941675742821E-05, 0.0001053129305727045710, 0.0001360598016347049663, 0.0001612931755713734548 ),
 .UNSPECIFIED. ) ;
#40232=ORIENTED_EDGE ( 'NONE', *, *, #29699, .T. ) ;
#40239=CARTESIAN_POINT ( 'NONE',  ( 4.667247927850000977, -31.42674373642585195, 7.751599049952172749 ) ) ;
#40243=DIRECTION ( 'NONE',  ( -0.9848077530122091305, 0.1736481776669241417, -0.000000000000000000 ) ) ;
#40248=CARTESIAN_POINT ( 'NONE',  ( 1.062037487868057184, -32.90946697031814949, 6.894806418505346812 ) ) ;
#40251=CARTESIAN_POINT ( 'NONE',  ( -2.253834945959114489, -26.23431501015891243, 7.635761828346577573 ) ) ;
#40257=EDGE_CURVE ( 'NONE', #20340, #5658, #40694, .T. ) ;
#40258=VERTEX_POINT ( 'NONE', #13940 ) ;
#40259=( BOUNDED_CURVE ( )  B_SPLINE_CURVE ( 3, ( #15912, #6858, #31571, #3591 ),
 .UNSPECIFIED., .F., .T. ) 
 B_SPLINE_CURVE_WITH_KNOTS ( ( 4, 4 ),
 ( 1.347909859412854683, 1.534781240595299634 ),
 .UNSPECIFIED. ) 
 CURVE ( )  GEOMETRIC_REPRESENTATION_ITEM ( )  RATIONAL_B_SPLINE_CURVE ( ( 1.000000000000000000, 0.9970920404276226723, 0.9970920404276226723, 1.000000000000000000 ) ) 
 REPRESENTATION_ITEM ( '' )  );
#40262=CARTESIAN_POINT ( 'NONE',  ( 4.986072540958928379, -30.76641830744928896, 7.767720160662274331 ) ) ;
#40263=CARTESIAN_POINT ( 'NONE',  ( 2.495473842921097418, -33.76723158512031375, 7.695279973900954751 ) ) ;
#40267=ORIENTED_EDGE ( 'NONE', *, *, #23146, .F. ) ;
#40270=EDGE_CURVE ( 'NONE', #14835, #29836, #18487, .T. ) ;
#40274=ORIENTED_EDGE ( 'NONE', *, *, #14347, .T. ) ;
#40275=VERTEX_POINT ( 'NONE', #3912 ) ;
#40277=CARTESIAN_POINT ( 'NONE',  ( -1.541782405220441410, -28.25144320491839878, 6.868546646838340486 ) ) ;
#40279=CARTESIAN_POINT ( 'NONE',  ( -0.8692302736362943483, -27.34348484300344850, 6.889465824494254598 ) ) ;
#40282=CARTESIAN_POINT ( 'NONE',  ( 3.224946677277165552, -32.60896660074035225, 6.997764925645181933 ) ) ;
#40284=CYLINDRICAL_SURFACE ( 'NONE', #3274, 3.399999999999999911 ) ;
#40291=CARTESIAN_POINT ( 'NONE',  ( 2.431875535358183793, -26.14722233025152676, 7.750000000000000888 ) ) ;
#40294=CARTESIAN_POINT ( 'NONE',  ( 3.865379090973303011, -26.93911693003565944, 7.257242401810562349 ) ) ;
#40297=CARTESIAN_POINT ( 'NONE',  ( 2.272716057154847924, -26.11704110451741556, 7.695279973900954751 ) ) ;
#40298=ORIENTED_EDGE ( 'NONE', *, *, #21774, .F. ) ;
#40300=CARTESIAN_POINT ( 'NONE',  ( 4.629620962406147733, -31.29608385994819741, 7.782167645815905033 ) ) ;
#40303=CARTESIAN_POINT ( 'NONE',  ( 1.700390093233090871, -29.56993018339339940, 7.750000000000000888 ) ) ;
#40306=CARTESIAN_POINT ( 'NONE',  ( -0.4306752572297538606, -26.92065449774550601, 7.784476445165073422 ) ) ;
#40309=CARTESIAN_POINT ( 'NONE',  ( 4.327908163969745203, -31.72774129374396423, 7.703977250142846955 ) ) ;
#40317=CARTESIAN_POINT ( 'NONE',  ( 4.851634552394991751, -30.84651091276440482, 7.754798119455333705 ) ) ;
#40333=DIRECTION ( 'NONE',  ( 1.000000000000000000, 0.000000000000000000, 0.000000000000000000 ) ) ;
#40343=VERTEX_POINT ( 'NONE', #2432 ) ;
#40347=CARTESIAN_POINT ( 'NONE',  ( 2.736589650407802665, -32.91302612543738348, 6.895394898881668233 ) ) ;
#40351=CARTESIAN_POINT ( 'NONE',  ( 5.144801695975108835, -28.95639910736822031, 7.762796336881262249 ) ) ;
#40352=CARTESIAN_POINT ( 'NONE',  ( 5.197623362990931639, -29.68617878646442421, 7.761113333117554802 ) ) ;
#40353=B_SPLINE_CURVE_WITH_KNOTS ( 'NONE', 3,
 ( #17916, #31722, #27800, #9466, #22265, #9066, #25543, #3141, #34013, #34423, #3341, #6608, #16062, #2723, #22052, #21642, #34222, #8854, #5787, #34832, #21845, #19155, #24936, #36, #3536, #9265, #6197, #34630, #12148, #25133, #18742 ),
 .UNSPECIFIED., .F., .F.,
 ( 4, 3, 3, 3, 3, 3, 3, 3, 3, 3, 4 ),
 ( 0.000000000000000000, 3.025570593002915146E-05, 6.051145698343717938E-05, 9.076621574721707990E-05, 0.0001210204262067937246, 0.0001512763324577387405, 0.0001815301820994196414, 0.0002117781465860642275, 0.0002420274594459682145, 0.0002722905548971127528, 0.0002816827545175567822 ),
 .UNSPECIFIED. ) ;
#40356=CARTESIAN_POINT ( 'NONE',  ( 5.200390093233090205, -29.56993018339339940, 7.620413589471895399 ) ) ;
#40358=CARTESIAN_POINT ( 'NONE',  ( -2.664219611515487696, -32.04831937761618832, 7.695279973900954751 ) ) ;
#40363=ORIENTED_EDGE ( 'NONE', *, *, #38192, .F. ) ;
#40366=ORIENTED_EDGE ( 'NONE', *, *, #5532, .T. ) ;
#40369=ORIENTED_EDGE ( 'NONE', *, *, #17357, .F. ) ;
#40377=CARTESIAN_POINT ( 'NONE',  ( 2.323504162460518163, -33.01401688474696527, 7.638132480492516585 ) ) ;
#40384=EDGE_CURVE ( 'NONE', #30829, #4710, #7308, .T. ) ;
#40385=AXIS2_PLACEMENT_3D ( 'NONE', #4581, #7451, #35678 ) ;
#40389=CARTESIAN_POINT ( 'NONE',  ( 3.628592791061993061, -26.64078201953907410, 7.387053503561886281 ) ) ;
#40392=CARTESIAN_POINT ( 'NONE',  ( -1.699225164987326675, -29.51872342197794907, 6.892063359921933419 ) ) ;
#40394=CARTESIAN_POINT ( 'NONE',  ( -1.421068687739435177, -31.15312598190119431, 6.931070083220557621 ) ) ;
#40396=CARTESIAN_POINT ( 'NONE',  ( 1.531218635892081847, -33.06583936671340496, 7.013842709614101167 ) ) ;
#40398=CARTESIAN_POINT ( 'NONE',  ( 0.9267304714826859469, -32.88073836111571779, 7.013842709614101167 ) ) ;
#40399=CYLINDRICAL_SURFACE ( 'NONE', #27675, 0.09010775117053086702 ) ;
#40404=CARTESIAN_POINT ( 'NONE',  ( 1.145332648700278844, -32.92431704737744269, 7.691066658568946224 ) ) ;
#40409=CARTESIAN_POINT ( 'NONE',  ( 2.844292303360262064, -26.36812879825141920, 7.643333865083958401 ) ) ;
#40413=ORIENTED_EDGE ( 'NONE', *, *, #28450, .F. ) ;
#40419=CARTESIAN_POINT ( 'NONE',  ( 1.165815618567649148, -26.21221814525847904, 6.887041543973316138 ) ) ;
#40420=EDGE_LOOP ( 'NONE', ( #11283, #4516, #38985, #4353, #6078 ) ) ;
#40425=CARTESIAN_POINT ( 'NONE',  ( -0.9974217071671265256, -27.34017228433088320, 7.737115613922534330 ) ) ;
#40434=ORIENTED_EDGE ( 'NONE', *, *, #4070, .F. ) ;
#40438=LINE ( 'NONE', #14928, #12949 ) ;
#40439=CARTESIAN_POINT ( 'NONE',  ( 1.736346942945643512, -32.96974004645320377, 7.695279973900954751 ) ) ;
#40446=FACE_OUTER_BOUND ( 'NONE', #37400, .T. ) ;
#40457=CARTESIAN_POINT ( 'NONE',  ( -1.553683706606911130, -30.55532538593644176, 7.013842709614101167 ) ) ;
#40462=ORIENTED_EDGE ( 'NONE', *, *, #32792, .F. ) ;
#40469=ORIENTED_EDGE ( 'NONE', *, *, #20769, .F. ) ;
#40473=CARTESIAN_POINT ( 'NONE',  ( -1.330386342644613640, -31.11085822340198703, 6.887945620086118659 ) ) ;
#40474=EDGE_LOOP ( 'NONE', ( #22073, #30929, #15987, #37039 ) ) ;
#40475=DIRECTION ( 'NONE',  ( 0.6427876096865369204, 0.7660444431189800119, 0.000000000000000000 ) ) ;
#40480=CYLINDRICAL_SURFACE ( 'NONE', #22879, 0.09010775117052932659 ) ;
#40487=DIRECTION ( 'NONE',  ( -1.000000000000000000, 0.000000000000000000, 0.000000000000000000 ) ) ;
#40500=FACE_OUTER_BOUND ( 'NONE', #26087, .T. ) ;
#40501=CARTESIAN_POINT ( 'NONE',  ( 1.783834813784320295, -26.17095431136780803, 6.870716933885665512 ) ) ;
#40504=CARTESIAN_POINT ( 'NONE',  ( 4.303098841883999270, -31.75760181544790584, 7.769368695748487319 ) ) ;
#40511=EDGE_CURVE ( 'NONE', #5237, #3514, #38724, .T. ) ;
#40514=DIRECTION ( 'NONE',  ( 0.9396926207859082059, 0.3420201433256695456, -0.000000000000000000 ) ) ;
#40515=VERTEX_POINT ( 'NONE', #20467 ) ;
#40517=CARTESIAN_POINT ( 'NONE',  ( -1.653394165169625118, -29.01124319760426573, 7.721096864323898856 ) ) ;
#40522=CARTESIAN_POINT ( 'NONE',  ( -1.506651383277110012, -28.44082214252960839, 7.691066658568946224 ) ) ;
#40529=CARTESIAN_POINT ( 'NONE',  ( 4.743946363699223845, -28.05441946540344489, 6.939395833800440450 ) ) ;
#40540=VERTEX_POINT ( 'NONE', #14088 ) ;
#40541=DIRECTION ( 'NONE',  ( 1.000000000000000000, 0.000000000000000000, 0.000000000000000000 ) ) ;
#40545=CARTESIAN_POINT ( 'NONE',  ( 2.714783994791350352, -32.91970706126133450, 6.961115707816238007 ) ) ;
#40548=CARTESIAN_POINT ( 'NONE',  ( -1.699609906766908818, -29.56993018339339940, 6.949309202340325342 ) ) ;
#40553=FACE_OUTER_BOUND ( 'NONE', #772, .T. ) ;
#40564=VERTEX_POINT ( 'NONE', #1975 ) ;
#40572=ORIENTED_EDGE ( 'NONE', *, *, #25016, .T. ) ;
#40575=EDGE_LOOP ( 'NONE', ( #3231, #2403, #35200, #3144 ) ) ;
#40579=CARTESIAN_POINT ( 'NONE',  ( -0.1155882611554212708, -32.44435575052494869, 6.865312560952602894 ) ) ;
#40580=ORIENTED_EDGE ( 'NONE', *, *, #15663, .T. ) ;
#40585=DIRECTION ( 'NONE',  ( -1.000000000000000000, 0.000000000000000000, 0.000000000000000000 ) ) ;
#40598=CARTESIAN_POINT ( 'NONE',  ( -1.578260247530195670, -30.79486269434816492, 7.660770905198775793 ) ) ;
#40605=EDGE_CURVE ( 'NONE', #3561, #24059, #20887, .T. ) ;
#40613=CARTESIAN_POINT ( 'NONE',  ( -0.8809027425463861194, -31.78283038357269419, 7.703977250142849620 ) ) ;
#40615=CARTESIAN_POINT ( 'NONE',  ( 2.183653651549320340, -33.03640625185305879, 7.750000000000000888 ) ) ;
#40616=CARTESIAN_POINT ( 'NONE',  ( 1.671000381532037560, -26.17005720858299966, 7.661510568013097711 ) ) ;
#40622=CARTESIAN_POINT ( 'NONE',  ( -1.510909903798922427, -30.68686900403765705, 6.894806418505348589 ) ) ;
#40624=CYLINDRICAL_SURFACE ( 'NONE', #27174, 0.09010775117052870209 ) ;
#40626=EDGE_CURVE ( 'NONE', #579, #28636, #26462, .T. ) ;
#40628=DIRECTION ( 'NONE',  ( 0.3420201433256536139, 0.9396926207859139790, 0.000000000000000000 ) ) ;
#40630=DIRECTION ( 'NONE',  ( -0.6427876096865179356, -0.7660444431189958880, 0.000000000000000000 ) ) ;
#40631=CARTESIAN_POINT ( 'NONE',  ( -1.438163258879938455, -28.26242175678535418, 6.871394612369935651 ) ) ;
#40632=CARTESIAN_POINT ( 'NONE',  ( 1.173600465780690438, -26.21097873563609326, 6.880147297696982633 ) ) ;
#40641=CARTESIAN_POINT ( 'NONE',  ( -1.003736583562488072, -27.34783681995375915, 7.697032948437509070 ) ) ;
#40645=CARTESIAN_POINT ( 'NONE',  ( 6.040270069758088667, -32.09115252335679003, 7.635761828346577573 ) ) ;
#40648=CARTESIAN_POINT ( 'NONE',  ( -0.7800240848564992113, -27.24451720821412337, 7.013842709614101167 ) ) ;
#40650=CARTESIAN_POINT ( 'NONE',  ( 4.041943119853272037, -26.96886997397920638, 7.754798119455333705 ) ) ;
#40658=CARTESIAN_POINT ( 'NONE',  ( 1.607140144109659108, -32.96866533745306072, 6.866852738645442322 ) ) ;
#40660=CARTESIAN_POINT ( 'NONE',  ( -1.743338437294067456, -30.17658229649751078, 7.767720160662275219 ) ) ;
#40663=CARTESIAN_POINT ( 'NONE',  ( 4.198225232297463805, -33.92331276665304785, 7.635761828346577573 ) ) ;
#40664=CARTESIAN_POINT ( 'NONE',  ( 3.478789117475594495, -32.58444706447512118, 7.720710062488893577 ) ) ;
#40665=CARTESIAN_POINT ( 'NONE',  ( 3.977572546501454642, -32.22783162523180067, 7.695279973900954751 ) ) ;
#40668=VECTOR ( 'NONE', #32022, 1000.000000000000000 ) ;
#40673=( BOUNDED_CURVE ( )  B_SPLINE_CURVE ( 3, ( #37356, #12856, #8736, #18415 ),
 .UNSPECIFIED., .F., .T. ) 
 B_SPLINE_CURVE_WITH_KNOTS ( ( 4, 4 ),
 ( 1.381924640371169133, 1.574767692156077148 ),
 .UNSPECIFIED. ) 
 CURVE ( )  GEOMETRIC_REPRESENTATION_ITEM ( )  RATIONAL_B_SPLINE_CURVE ( ( 1.000000000000000000, 0.9969033633783032089, 0.9969033633783032089, 1.000000000000000000 ) ) 
 REPRESENTATION_ITEM ( '' )  );
#40674=CARTESIAN_POINT ( 'NONE',  ( -1.651477885001130241, -30.14008421266758120, 7.779495906702013741 ) ) ;
#40675=EDGE_CURVE ( 'NONE', #20764, #18601, #12231, .T. ) ;
#40676=CYLINDRICAL_SURFACE ( 'NONE', #12213, 0.09010775117052992333 ) ;
#40679=EDGE_LOOP ( 'NONE', ( #17164, #25454, #9873, #39979 ) ) ;
#40685=VERTEX_POINT ( 'NONE', #15878 ) ;
#40690=CARTESIAN_POINT ( 'NONE',  ( -0.8291548937095295502, -27.29805823298918455, 6.864276522220859711 ) ) ;
#40692=CARTESIAN_POINT ( 'NONE',  ( 0.04761811793521757152, -26.48768737936845596, 7.766640943994350010 ) ) ;
#40694=B_SPLINE_CURVE_WITH_KNOTS ( 'NONE', 3,
 ( #17216, #32492, #32895, #1215, #29196, #7562, #35981, #38848, #1008, #19728, #1407, #6969, #4682, #26313, #16818, #32695, #10247, #7167, #7762, #38646, #13750, #22826, #13542, #10642, #23219, #26115, #14134, #35784, #4495, #29593, #17015 ),
 .UNSPECIFIED., .F., .F.,
 ( 4, 3, 3, 3, 3, 3, 3, 3, 3, 3, 4 ),
 ( 1.084202172485504434E-18, 3.077658087705639398E-05, 6.152638666998869155E-05, 9.267501192706414340E-05, 0.0001241882240135153224, 0.0001556618703051647400, 0.0001866161554452207315, 0.0002167966385860965208, 0.0002463805737537760258, 0.0002758761370306513517, 0.0002847094172290016881 ),
 .UNSPECIFIED. ) ;
#40695=CARTESIAN_POINT ( 'NONE',  ( 4.951888024848370762, -30.86525491651966746, 6.863784140767622333 ) ) ;
#40697=FACE_OUTER_BOUND ( 'NONE', #38863, .T. ) ;
#40704=DIRECTION ( 'NONE',  ( 0.3420201433256790380, -0.9396926207859046531, -0.000000000000000000 ) ) ;
#40709=DIRECTION ( 'NONE',  ( 0.1303762246624128318, 0.7394003126383930091, -0.6605219282605405695 ) ) ;
#40712=ORIENTED_EDGE ( 'NONE', *, *, #19347, .T. ) ;
#40715=CARTESIAN_POINT ( 'NONE',  ( -1.781046303933295549, -29.98589987418001357, 7.398879060202668612 ) ) ;
#40716=CARTESIAN_POINT ( 'NONE',  ( -1.722317759908783996, -28.83844474126830804, 7.750000000000000888 ) ) ;
#40719=CARTESIAN_POINT ( 'NONE',  ( 4.259121667494660812, -31.80890180388914956, 7.784476445165073422 ) ) ;
#40760=COLOUR_RGB('Black',0.12,0.14,0.17);
#40761=FILL_AREA_STYLE_COLOUR('',#40760);
#40762=FILL_AREA_STYLE('',(#40761));
#40763=SURFACE_STYLE_FILL_AREA(#40762);
#40764=SURFACE_SIDE_STYLE('',(#40763));
#40765=SURFACE_STYLE_USAGE(.BOTH.,#40764);
#40766=PRESENTATION_STYLE_ASSIGNMENT((#40765));
ENDSEC;
END-ISO-10303-21;
